ISO-10303-21;
HEADER;
/* Generated by software containing ST-Developer
 * from STEP Tools, Inc. (www.steptools.com) 
 */

FILE_DESCRIPTION(
/* description */ (
'Independent keyed-quill tailstock, native coupled50mm slider andM16x2
 feed screw, conical dead center, bronze sleeves/thrust washers, cross
-pinned handwheel and bolted guide key. Custom center taper; no standa
rd taper compatibility, machine-bed compatibility or load rating assig
ned.'),
/* implementation_level */ '2;1');

FILE_NAME(
/* name */ 'Socket head cap screw M4x12.step',
/* time_stamp */ '2026-11-14T07:17:36-08:00',
/* author */ (''),
/* organization */ (''),
/* preprocessor_version */ 'ST-DEVELOPER v20.2',
/* originating_system */ 'Autodesk Translation Framework v15.17.0.0',
/* authorisation */ '');

FILE_SCHEMA (('AUTOMOTIVE_DESIGN { 1 0 10303 214 3 1 1 }'));
ENDSEC;

DATA;
#10=MECHANICAL_DESIGN_GEOMETRIC_PRESENTATION_REPRESENTATION('',(#169),#289387);
#118=CONICAL_SURFACE('',#17849,1.5,0.785398163397449);
#135=SHAPE_REPRESENTATION_RELATIONSHIP('SRR','None',#289470,#152);
#152=ADVANCED_BREP_SHAPE_REPRESENTATION('',(#186),#289386);
#169=STYLED_ITEM('',(#289553),#186);
#186=MANIFOLD_SOLID_BREP('Body1',#16857);
#271=FACE_BOUND('',#1804,.T.);
#272=FACE_BOUND('',#1807,.T.);
#301=B_SPLINE_SURFACE_WITH_KNOTS('',3,3,((#288259,#288260,#288261,#288262,
#288263,#288264,#288265,#288266,#288267,#288268,#288269,#288270,#288271,
#288272,#288273,#288274,#288275,#288276,#288277,#288278,#288279,#288280,
#288281,#288282,#288283,#288284,#288285,#288286,#288287,#288288,#288289,
#288290,#288291,#288292,#288293,#288294,#288295,#288296,#288297,#288298,
#288299,#288300,#288301,#288302,#288303,#288304,#288305,#288306,#288307,
#288308,#288309,#288310,#288311,#288312,#288313,#288314,#288315,#288316,
#288317,#288318,#288319,#288320,#288321,#288322,#288323,#288324,#288325,
#288326,#288327,#288328,#288329,#288330,#288331,#288332,#288333,#288334,
#288335,#288336,#288337,#288338,#288339,#288340,#288341,#288342,#288343,
#288344,#288345,#288346,#288347,#288348,#288349,#288350,#288351,#288352,
#288353,#288354,#288355,#288356,#288357,#288358,#288359,#288360,#288361,
#288362,#288363,#288364),(#288365,#288366,#288367,#288368,#288369,#288370,
#288371,#288372,#288373,#288374,#288375,#288376,#288377,#288378,#288379,
#288380,#288381,#288382,#288383,#288384,#288385,#288386,#288387,#288388,
#288389,#288390,#288391,#288392,#288393,#288394,#288395,#288396,#288397,
#288398,#288399,#288400,#288401,#288402,#288403,#288404,#288405,#288406,
#288407,#288408,#288409,#288410,#288411,#288412,#288413,#288414,#288415,
#288416,#288417,#288418,#288419,#288420,#288421,#288422,#288423,#288424,
#288425,#288426,#288427,#288428,#288429,#288430,#288431,#288432,#288433,
#288434,#288435,#288436,#288437,#288438,#288439,#288440,#288441,#288442,
#288443,#288444,#288445,#288446,#288447,#288448,#288449,#288450,#288451,
#288452,#288453,#288454,#288455,#288456,#288457,#288458,#288459,#288460,
#288461,#288462,#288463,#288464,#288465,#288466,#288467,#288468,#288469,
#288470),(#288471,#288472,#288473,#288474,#288475,#288476,#288477,#288478,
#288479,#288480,#288481,#288482,#288483,#288484,#288485,#288486,#288487,
#288488,#288489,#288490,#288491,#288492,#288493,#288494,#288495,#288496,
#288497,#288498,#288499,#288500,#288501,#288502,#288503,#288504,#288505,
#288506,#288507,#288508,#288509,#288510,#288511,#288512,#288513,#288514,
#288515,#288516,#288517,#288518,#288519,#288520,#288521,#288522,#288523,
#288524,#288525,#288526,#288527,#288528,#288529,#288530,#288531,#288532,
#288533,#288534,#288535,#288536,#288537,#288538,#288539,#288540,#288541,
#288542,#288543,#288544,#288545,#288546,#288547,#288548,#288549,#288550,
#288551,#288552,#288553,#288554,#288555,#288556,#288557,#288558,#288559,
#288560,#288561,#288562,#288563,#288564,#288565,#288566,#288567,#288568,
#288569,#288570,#288571,#288572,#288573,#288574,#288575,#288576),(#288577,
#288578,#288579,#288580,#288581,#288582,#288583,#288584,#288585,#288586,
#288587,#288588,#288589,#288590,#288591,#288592,#288593,#288594,#288595,
#288596,#288597,#288598,#288599,#288600,#288601,#288602,#288603,#288604,
#288605,#288606,#288607,#288608,#288609,#288610,#288611,#288612,#288613,
#288614,#288615,#288616,#288617,#288618,#288619,#288620,#288621,#288622,
#288623,#288624,#288625,#288626,#288627,#288628,#288629,#288630,#288631,
#288632,#288633,#288634,#288635,#288636,#288637,#288638,#288639,#288640,
#288641,#288642,#288643,#288644,#288645,#288646,#288647,#288648,#288649,
#288650,#288651,#288652,#288653,#288654,#288655,#288656,#288657,#288658,
#288659,#288660,#288661,#288662,#288663,#288664,#288665,#288666,#288667,
#288668,#288669,#288670,#288671,#288672,#288673,#288674,#288675,#288676,
#288677,#288678,#288679,#288680,#288681,#288682)),.UNSPECIFIED.,.F.,.F.,
 .F.,(4,4),(4,1,1,1,1,1,1,1,1,1,1,1,1,1,1,1,1,1,1,1,1,1,1,1,1,1,1,1,1,1,
1,1,1,1,1,1,1,1,1,1,1,1,1,1,1,1,1,1,1,1,1,1,1,1,1,1,1,1,1,1,1,1,1,1,1,1,
1,1,1,1,1,1,1,1,1,1,1,1,1,1,1,1,1,1,1,1,1,1,1,1,1,1,1,1,1,1,1,1,1,1,1,1,
1,4),(-0.000292638147730025,0.0463354487950187),(11.6151020518147,12.6127573616628,
13.610093204215,14.6074290467673,15.6047648893195,16.6021007318718,17.599436574424,
18.5967724169762,19.5941082595285,20.5914441020807,21.588779944633,22.5861157871852,
23.5834516297375,24.5807874722897,25.5781233148419,26.5754591573942,27.5727949999464,
28.5701308424987,29.5674666850509,30.5648025276032,31.5621383701554,32.5594742127077,
33.5568100552599,34.5541458978121,35.5514817403644,36.5488175829166,37.5461534254689,
38.5434892680211,39.5408251105734,40.5381609531256,41.5354967956779,42.5328326382301,
43.5301684807823,44.5275043233346,45.5248401658868,46.5221760084391,47.5195118509913,
48.5168476935436,49.5141835360958,50.5115193786481,51.5088552212003,52.5061910637525,
53.5035269063048,54.500862748857,55.4981985914093,56.4955344339615,57.4928702765138,
58.490206119066,59.4875419616182,60.4848778041705,61.4822136467227,62.479549489275,
63.4768853318272,64.4742211743795,65.4715570169317,66.468892859484,67.4662287020362,
68.4635645445884,69.4609003871407,70.4582362296929,71.4555720722452,72.4529079147974,
73.4502437573497,74.4475795999019,75.4449154424541,76.4422512850064,77.4395871275586,
78.4369229701109,79.4342588126631,80.4315946552154,81.4289304977676,82.4262663403199,
83.4236021828721,84.4209380254243,85.4182738679766,86.4156097105288,87.4129455530811,
88.4102813956333,89.4076172381856,90.4049530807378,91.4022889232901,92.3996247658423,
93.3969606083945,94.3942964509468,95.391632293499,96.3889681360513,97.3863039786035,
98.3836398211558,99.380975663708,100.37831150626,101.375647348812,102.372983191365,
103.370319033917,104.367654876469,105.364990719021,106.362326561574,107.359662404126,
108.356998246678,109.35433408923,110.351669931783,111.349005774335,112.346341616887,
113.343677459439,114.341333934333),.UNSPECIFIED.);
#302=B_SPLINE_SURFACE_WITH_KNOTS('',3,3,((#288765,#288766,#288767,#288768,
#288769,#288770,#288771,#288772,#288773,#288774,#288775,#288776,#288777,
#288778,#288779,#288780,#288781,#288782,#288783,#288784,#288785,#288786,
#288787,#288788,#288789,#288790,#288791,#288792,#288793,#288794,#288795,
#288796,#288797,#288798,#288799,#288800,#288801,#288802,#288803,#288804,
#288805,#288806,#288807,#288808,#288809,#288810,#288811,#288812,#288813,
#288814,#288815,#288816,#288817,#288818,#288819,#288820,#288821,#288822,
#288823,#288824,#288825,#288826,#288827,#288828,#288829,#288830,#288831,
#288832,#288833,#288834,#288835,#288836,#288837,#288838,#288839,#288840,
#288841,#288842,#288843,#288844,#288845,#288846,#288847,#288848,#288849,
#288850,#288851,#288852,#288853,#288854,#288855,#288856,#288857,#288858,
#288859,#288860,#288861,#288862,#288863,#288864,#288865,#288866,#288867,
#288868,#288869,#288870,#288871,#288872),(#288873,#288874,#288875,#288876,
#288877,#288878,#288879,#288880,#288881,#288882,#288883,#288884,#288885,
#288886,#288887,#288888,#288889,#288890,#288891,#288892,#288893,#288894,
#288895,#288896,#288897,#288898,#288899,#288900,#288901,#288902,#288903,
#288904,#288905,#288906,#288907,#288908,#288909,#288910,#288911,#288912,
#288913,#288914,#288915,#288916,#288917,#288918,#288919,#288920,#288921,
#288922,#288923,#288924,#288925,#288926,#288927,#288928,#288929,#288930,
#288931,#288932,#288933,#288934,#288935,#288936,#288937,#288938,#288939,
#288940,#288941,#288942,#288943,#288944,#288945,#288946,#288947,#288948,
#288949,#288950,#288951,#288952,#288953,#288954,#288955,#288956,#288957,
#288958,#288959,#288960,#288961,#288962,#288963,#288964,#288965,#288966,
#288967,#288968,#288969,#288970,#288971,#288972,#288973,#288974,#288975,
#288976,#288977,#288978,#288979,#288980),(#288981,#288982,#288983,#288984,
#288985,#288986,#288987,#288988,#288989,#288990,#288991,#288992,#288993,
#288994,#288995,#288996,#288997,#288998,#288999,#289000,#289001,#289002,
#289003,#289004,#289005,#289006,#289007,#289008,#289009,#289010,#289011,
#289012,#289013,#289014,#289015,#289016,#289017,#289018,#289019,#289020,
#289021,#289022,#289023,#289024,#289025,#289026,#289027,#289028,#289029,
#289030,#289031,#289032,#289033,#289034,#289035,#289036,#289037,#289038,
#289039,#289040,#289041,#289042,#289043,#289044,#289045,#289046,#289047,
#289048,#289049,#289050,#289051,#289052,#289053,#289054,#289055,#289056,
#289057,#289058,#289059,#289060,#289061,#289062,#289063,#289064,#289065,
#289066,#289067,#289068,#289069,#289070,#289071,#289072,#289073,#289074,
#289075,#289076,#289077,#289078,#289079,#289080,#289081,#289082,#289083,
#289084,#289085,#289086,#289087,#289088),(#289089,#289090,#289091,#289092,
#289093,#289094,#289095,#289096,#289097,#289098,#289099,#289100,#289101,
#289102,#289103,#289104,#289105,#289106,#289107,#289108,#289109,#289110,
#289111,#289112,#289113,#289114,#289115,#289116,#289117,#289118,#289119,
#289120,#289121,#289122,#289123,#289124,#289125,#289126,#289127,#289128,
#289129,#289130,#289131,#289132,#289133,#289134,#289135,#289136,#289137,
#289138,#289139,#289140,#289141,#289142,#289143,#289144,#289145,#289146,
#289147,#289148,#289149,#289150,#289151,#289152,#289153,#289154,#289155,
#289156,#289157,#289158,#289159,#289160,#289161,#289162,#289163,#289164,
#289165,#289166,#289167,#289168,#289169,#289170,#289171,#289172,#289173,
#289174,#289175,#289176,#289177,#289178,#289179,#289180,#289181,#289182,
#289183,#289184,#289185,#289186,#289187,#289188,#289189,#289190,#289191,
#289192,#289193,#289194,#289195,#289196)),.UNSPECIFIED.,.F.,.F.,.F.,(4,
4),(4,1,1,1,1,1,1,1,1,1,1,1,1,1,1,1,1,1,1,1,1,1,1,1,1,1,1,1,1,1,1,1,1,1,
1,1,1,1,1,1,1,1,1,1,1,1,1,1,1,1,1,1,1,1,1,1,1,1,1,1,1,1,1,1,1,1,1,1,1,1,
1,1,1,1,1,1,1,1,1,1,1,1,1,1,1,1,1,1,1,1,1,1,1,1,1,1,1,1,1,1,1,1,1,1,1,4),
(-0.000320373313366601,0.0463083434471542),(8.31044130225981,9.30859389336977,
10.3066008639999,11.30460783463,12.30261480526,13.3006217758901,14.2986287465202,
15.2966357171503,16.2946426877804,17.2926496584105,18.2906566290406,19.2886635996707,
20.2866705703008,21.2846775409308,22.2826845115609,23.280691482191,24.2786984528211,
25.2767054234512,26.2747123940813,27.2727193647114,28.2707263353415,29.2687333059716,
30.2667402766016,31.2647472472317,32.2627542178618,33.2607611884919,34.258768159122,
35.2567751297521,36.2547821003822,37.2527890710123,38.2507960416424,39.2488030122724,
40.2468099829025,41.2448169535326,42.2428239241627,43.2408308947928,44.2388378654229,
45.236844836053,46.2348518066831,47.2328587773132,48.2308657479432,49.2288727185733,
50.2268796892034,51.2248866598335,52.2228936304636,53.2209006010937,54.2189075717238,
55.2169145423539,56.214921512984,57.212928483614,58.2109354542441,59.2089424248742,
60.2069493955043,61.2049563661344,62.2029633367645,63.2009703073946,64.1989772780247,
65.1969842486548,66.1949912192848,67.1929981899149,68.191005160545,69.1890121311751,
70.1870191018052,71.1850260724353,72.1830330430654,73.1810400136955,74.1790469843256,
75.1770539549557,76.1750609255857,77.1730678962158,78.1710748668459,79.169081837476,
80.1670888081061,81.1650957787362,82.1631027493663,83.1611097199964,84.1591166906264,
85.1571236612565,86.1551306318866,87.1531376025167,88.1511445731468,89.1491515437769,
90.147158514407,91.1451654850371,92.1431724556672,93.1411794262973,94.1391863969273,
95.1371933675574,96.1352003381875,97.1332073088176,98.1312142794477,99.1292212500778,
100.127228220708,101.125235191338,102.123242161968,103.121249132598,104.119256103228,
105.117263073858,106.115270044488,107.113277015118,108.111283985749,109.109290956379,
110.107297927009,111.105304897639,112.103311868269,113.101639212212),
 .UNSPECIFIED.);
#413=PLANE('',#17851);
#414=PLANE('',#17852);
#415=PLANE('',#17853);
#416=PLANE('',#17854);
#417=PLANE('',#17855);
#418=PLANE('',#17856);
#419=PLANE('',#17857);
#420=PLANE('',#17858);
#421=PLANE('',#17862);
#422=PLANE('',#17863);
#1057=FACE_OUTER_BOUND('',#1791,.T.);
#1058=FACE_OUTER_BOUND('',#1792,.T.);
#1059=FACE_OUTER_BOUND('',#1793,.T.);
#1060=FACE_OUTER_BOUND('',#1794,.T.);
#1061=FACE_OUTER_BOUND('',#1795,.T.);
#1062=FACE_OUTER_BOUND('',#1796,.T.);
#1063=FACE_OUTER_BOUND('',#1797,.T.);
#1064=FACE_OUTER_BOUND('',#1798,.T.);
#1065=FACE_OUTER_BOUND('',#1799,.T.);
#1066=FACE_OUTER_BOUND('',#1800,.T.);
#1067=FACE_OUTER_BOUND('',#1801,.T.);
#1068=FACE_OUTER_BOUND('',#1802,.T.);
#1069=FACE_OUTER_BOUND('',#1803,.T.);
#1070=FACE_OUTER_BOUND('',#1805,.T.);
#1071=FACE_OUTER_BOUND('',#1806,.T.);
#1072=FACE_OUTER_BOUND('',#1808,.T.);
#1791=EDGE_LOOP('',(#15523,#15524,#15525,#15526,#15527,#15528,#15529,#15530,
#15531,#15532,#15533,#15534,#15535,#15536,#15537,#15538,#15539,#15540,#15541,
#15542,#15543,#15544,#15545,#15546,#15547,#15548,#15549,#15550,#15551,#15552,
#15553,#15554,#15555,#15556,#15557,#15558));
#1792=EDGE_LOOP('',(#15559,#15560,#15561,#15562,#15563,#15564,#15565,#15566,
#15567,#15568,#15569,#15570,#15571,#15572,#15573,#15574,#15575,#15576,#15577,
#15578,#15579,#15580,#15581));
#1793=EDGE_LOOP('',(#15582,#15583,#15584,#15585,#15586,#15587,#15588,#15589,
#15590));
#1794=EDGE_LOOP('',(#15591,#15592,#15593,#15594,#15595,#15596,#15597,#15598,
#15599,#15600,#15601,#15602,#15603,#15604,#15605,#15606,#15607,#15608,#15609,
#15610,#15611,#15612,#15613,#15614,#15615,#15616,#15617,#15618,#15619));
#1795=EDGE_LOOP('',(#15620,#15621,#15622,#15623,#15624,#15625,#15626,#15627,
#15628,#15629,#15630,#15631,#15632,#15633,#15634,#15635,#15636,#15637,#15638,
#15639,#15640,#15641,#15642,#15643,#15644,#15645,#15646,#15647,#15648,#15649,
#15650,#15651));
#1796=EDGE_LOOP('',(#15652,#15653,#15654,#15655));
#1797=EDGE_LOOP('',(#15656,#15657,#15658,#15659));
#1798=EDGE_LOOP('',(#15660,#15661,#15662,#15663));
#1799=EDGE_LOOP('',(#15664,#15665,#15666,#15667));
#1800=EDGE_LOOP('',(#15668,#15669,#15670,#15671));
#1801=EDGE_LOOP('',(#15672,#15673,#15674,#15675));
#1802=EDGE_LOOP('',(#15676,#15677,#15678,#15679,#15680,#15681));
#1803=EDGE_LOOP('',(#15682));
#1804=EDGE_LOOP('',(#15683,#15684,#15685,#15686));
#1805=EDGE_LOOP('',(#15687,#15688,#15689,#15690));
#1806=EDGE_LOOP('',(#15691));
#1807=EDGE_LOOP('',(#15692,#15693,#15694,#15695,#15696,#15697));
#1808=EDGE_LOOP('',(#15698));
#1982=CIRCLE('',#17844,1.954);
#1983=CIRCLE('',#17845,1.954);
#1984=CIRCLE('',#17847,1.5555);
#1985=CIRCLE('',#17848,1.5555);
#1986=CIRCLE('',#17850,1.);
#1987=CIRCLE('',#17859,3.5);
#1988=CIRCLE('',#17861,3.5);
#3880=B_SPLINE_CURVE_WITH_KNOTS('',3,(#279133,#279134,#279135,#279136,#279137,
#279138,#279139,#279140,#279141,#279142,#279143,#279144,#279145,#279146,
#279147,#279148,#279149,#279150,#279151,#279152,#279153,#279154,#279155,
#279156,#279157,#279158,#279159,#279160,#279161,#279162,#279163,#279164,
#279165,#279166,#279167,#279168,#279169,#279170,#279171,#279172,#279173,
#279174,#279175,#279176,#279177,#279178,#279179,#279180,#279181,#279182,
#279183,#279184,#279185,#279186,#279187,#279188,#279189,#279190,#279191,
#279192,#279193),.UNSPECIFIED.,.F.,.F.,(4,3,3,3,3,3,3,3,3,3,3,3,3,3,3,3,
3,3,3,3,4),(-4.09254174883833,-3.98934337020898,-3.88363221779152,-3.77808060077488,
-3.67265482016529,-3.56729632526176,-3.46196930491298,-3.35663799380962,
-3.25119893725734,-3.14569903290218,-3.04002256345967,-2.99200752765673,
-2.88747169635222,-2.78311107345422,-2.6788481173541,-2.57464534892016,
-2.470465371017,-2.3662011665343,-2.26189731347916,-2.15741074042207,-2.06549299936852),
 .UNSPECIFIED.);
#3881=B_SPLINE_CURVE_WITH_KNOTS('',3,(#279197,#279198,#279199,#279200,#279201,
#279202,#279203,#279204,#279205,#279206,#279207,#279208,#279209,#279210,
#279211,#279212,#279213,#279214,#279215,#279216,#279217,#279218,#279219,
#279220,#279221,#279222,#279223,#279224,#279225,#279226,#279227,#279228,
#279229,#279230),.UNSPECIFIED.,.F.,.F.,(4,3,3,3,3,3,3,3,3,3,3,4),(0.,0.107973995962156,
0.219228117795647,0.327124364615333,0.435023022759881,0.542953260606805,
0.650944276415295,0.759103142526299,0.867360126689599,0.97581640543646,
0.998006970630082,1.11419103802948),.UNSPECIFIED.);
#3882=B_SPLINE_CURVE_WITH_KNOTS('',3,(#279232,#279233,#279234,#279235,#279236,
#279237,#279238,#279239,#279240,#279241,#279242,#279243,#279244,#279245,
#279246,#279247,#279248,#279249,#279250,#279251,#279252,#279253,#279254,
#279255,#279256,#279257,#279258,#279259,#279260,#279261,#279262,#279263,
#279264,#279265,#279266,#279267,#279268,#279269,#279270,#279271,#279272,
#279273,#279274,#279275,#279276,#279277,#279278,#279279,#279280,#279281,
#279282,#279283,#279284,#279285,#279286,#279287,#279288,#279289,#279290,
#279291,#279292,#279293,#279294,#279295,#279296,#279297,#279298,#279299,
#279300,#279301,#279302,#279303,#279304,#279305,#279306,#279307,#279308,
#279309,#279310,#279311,#279312,#279313,#279314,#279315,#279316,#279317,
#279318,#279319,#279320,#279321,#279322,#279323,#279324,#279325,#279326,
#279327,#279328,#279329,#279330,#279331,#279332,#279333,#279334,#279335,
#279336,#279337,#279338,#279339,#279340,#279341,#279342,#279343,#279344,
#279345,#279346,#279347,#279348,#279349,#279350,#279351,#279352,#279353,
#279354,#279355,#279356,#279357,#279358,#279359,#279360,#279361,#279362,
#279363,#279364,#279365,#279366,#279367,#279368,#279369,#279370,#279371,
#279372,#279373,#279374,#279375,#279376,#279377,#279378,#279379,#279380,
#279381,#279382,#279383,#279384,#279385,#279386,#279387,#279388,#279389,
#279390,#279391,#279392,#279393,#279394,#279395,#279396,#279397,#279398,
#279399,#279400,#279401,#279402,#279403,#279404,#279405,#279406,#279407,
#279408,#279409,#279410,#279411,#279412,#279413,#279414,#279415,#279416,
#279417,#279418,#279419,#279420,#279421),.UNSPECIFIED.,.F.,.F.,(4,3,3,3,
3,3,3,3,3,3,3,3,3,3,3,3,3,3,3,3,3,3,3,3,3,3,3,3,3,3,3,3,3,3,3,3,3,3,3,3,
3,3,3,3,3,3,3,3,3,3,3,3,3,3,3,3,3,3,3,3,3,3,3,4),(1.11419103844308,1.21719187770655,
1.32003209885005,1.42278427700502,1.52548718566634,1.6281795105233,1.73096939481268,
1.83381185890053,1.93683560088162,1.99601394126018,2.10167359162095,2.20717435751719,
2.31255046470255,2.41786002560773,2.5231389034132,2.62842291627881,2.73381640871969,
2.83927155151866,2.94490541042443,2.99402091189026,3.09970332166566,3.20523066244488,
3.31063889552096,3.41598401676772,3.52130184505124,3.62662815778746,3.73206875948818,
3.83757382877443,3.94326146232322,3.99202788252035,4.09738133007778,4.20257357461044,
4.30763927886319,4.41263745687271,4.51760445552907,4.62257657593037,4.72766031671474,
4.83280647814355,4.93813581606208,4.99003485315045,5.0955641079553,5.20093443441008,
5.30618072088195,5.41136093238526,5.51651114356894,5.62166738469945,5.72693536855835,
5.83226611849798,5.93777863534395,5.98804182378054,6.0935615968424,6.19892280124285,
6.30416054776096,6.40933258652753,6.51447500595197,6.61962385045829,6.72488509082588,
6.83020946041486,6.93571622877576,6.98604879441062,7.10224037718433,7.21807745680911,
7.33333553933627,7.39737593502646),.UNSPECIFIED.);
#3883=B_SPLINE_CURVE_WITH_KNOTS('',3,(#279423,#279424,#279425,#279426,#279427,
#279428,#279429,#279430,#279431,#279432),.UNSPECIFIED.,.F.,.F.,(4,1,1,1,
1,1,1,4),(7.39737634520907,7.98405576504071,8.9820627356708,9.98006970630089,
10.978076676931,11.9760836475611,12.9740906181912,13.6805616523887),
 .UNSPECIFIED.);
#3884=B_SPLINE_CURVE_WITH_KNOTS('',3,(#279434,#279435,#279436,#279437,#279438,
#279439,#279440,#279441,#279442,#279443,#279444,#279445,#279446,#279447,
#279448,#279449,#279450,#279451,#279452,#279453,#279454,#279455,#279456,
#279457,#279458,#279459,#279460,#279461,#279462,#279463,#279464,#279465,
#279466,#279467,#279468,#279469,#279470,#279471,#279472,#279473,#279474,
#279475,#279476,#279477,#279478,#279479,#279480,#279481,#279482,#279483,
#279484,#279485,#279486,#279487,#279488,#279489,#279490,#279491,#279492,
#279493,#279494,#279495,#279496,#279497,#279498,#279499,#279500,#279501,
#279502,#279503,#279504,#279505,#279506,#279507,#279508,#279509,#279510,
#279511,#279512,#279513,#279514,#279515,#279516,#279517,#279518,#279519,
#279520,#279521,#279522,#279523,#279524,#279525,#279526,#279527,#279528,
#279529,#279530,#279531,#279532,#279533,#279534,#279535,#279536,#279537,
#279538,#279539,#279540,#279541,#279542,#279543,#279544,#279545,#279546,
#279547,#279548,#279549,#279550,#279551,#279552,#279553,#279554,#279555,
#279556,#279557,#279558,#279559,#279560,#279561,#279562,#279563,#279564,
#279565,#279566,#279567,#279568,#279569,#279570,#279571,#279572,#279573,
#279574,#279575,#279576,#279577,#279578,#279579,#279580,#279581,#279582,
#279583,#279584,#279585,#279586,#279587,#279588,#279589,#279590,#279591,
#279592,#279593,#279594,#279595,#279596,#279597,#279598,#279599,#279600,
#279601,#279602,#279603,#279604,#279605,#279606,#279607,#279608,#279609,
#279610,#279611,#279612,#279613,#279614,#279615,#279616,#279617,#279618,
#279619,#279620,#279621,#279622,#279623,#279624,#279625,#279626),
 .UNSPECIFIED.,.F.,.F.,(4,3,3,3,3,3,3,3,3,3,3,3,3,3,3,3,3,3,3,3,3,3,3,3,
3,3,3,3,3,3,3,3,3,3,3,3,3,3,3,3,3,3,3,3,3,3,3,3,3,3,3,3,3,3,3,3,3,3,3,3,
3,3,3,3,4),(13.6805618160026,13.8082883325048,13.9379733142516,13.9720975888212,
14.077595545405,14.1829344247124,14.2881492016154,14.3932978838084,14.4984165948394,
14.6035414138825,14.7087783117543,14.8140781221029,14.919560253473,14.9701045594513,
15.0756023545526,15.1809410711868,15.2861556844645,15.391304202538,15.4964227492074,
15.6015474038986,15.7067841385673,15.8120837861284,15.9175657570756,15.9681115300814,
16.0736092504098,16.1789478903724,16.2841624245375,16.3893108620278,16.4944293267638,
16.5995538982904,16.7047905484922,16.8100901107186,16.9155719958822,16.9661185007115,
17.0716163081709,17.1769550366742,17.2821696610324,17.3873181896896,17.4924367464281,
17.5975614106554,17.7027981539825,17.8080978097136,17.9135797879851,17.9641254713416,
18.0696232498215,18.1749619490664,18.280176543899,18.3853250428819,18.4904435698429,
18.5955682042347,18.7008049178441,18.8061045438807,18.9115864928076,18.9621324419717,
19.0676302129107,19.1729689043845,19.2781834911422,19.3833319818661,19.4884505003964,
19.593575126198,19.6988118310328,19.8041114481769,19.9095933881216,19.9601394126018,
19.9637469595682),.UNSPECIFIED.);
#3885=B_SPLINE_CURVE_WITH_KNOTS('',3,(#279628,#279629,#279630,#279631,#279632,
#279633,#279634,#279635,#279636,#279637,#279638,#279639,#279640,#279641,
#279642,#279643,#279644,#279645,#279646,#279647,#279648,#279649,#279650,
#279651,#279652,#279653,#279654,#279655,#279656,#279657,#279658,#279659,
#279660,#279661,#279662,#279663,#279664,#279665,#279666,#279667,#279668,
#279669,#279670,#279671,#279672,#279673,#279674,#279675,#279676,#279677,
#279678,#279679,#279680,#279681,#279682,#279683,#279684,#279685,#279686,
#279687,#279688,#279689,#279690,#279691,#279692,#279693,#279694,#279695,
#279696,#279697,#279698,#279699,#279700,#279701,#279702,#279703,#279704,
#279705,#279706,#279707,#279708,#279709,#279710,#279711,#279712,#279713,
#279714,#279715,#279716,#279717,#279718,#279719,#279720,#279721,#279722,
#279723,#279724,#279725,#279726,#279727,#279728,#279729,#279730,#279731,
#279732,#279733,#279734,#279735,#279736,#279737,#279738,#279739,#279740,
#279741,#279742,#279743,#279744,#279745,#279746,#279747,#279748,#279749,
#279750,#279751,#279752,#279753,#279754,#279755,#279756,#279757,#279758,
#279759,#279760,#279761,#279762,#279763,#279764,#279765,#279766,#279767,
#279768,#279769,#279770,#279771,#279772,#279773,#279774,#279775,#279776,
#279777,#279778,#279779,#279780,#279781,#279782,#279783,#279784,#279785,
#279786,#279787,#279788,#279789,#279790,#279791,#279792,#279793,#279794,
#279795,#279796,#279797,#279798,#279799,#279800,#279801,#279802,#279803,
#279804,#279805,#279806,#279807,#279808,#279809,#279810,#279811,#279812,
#279813,#279814,#279815,#279816,#279817),.UNSPECIFIED.,.F.,.F.,(4,3,3,3,
3,3,3,3,3,3,3,3,3,3,3,3,3,3,3,3,3,3,3,3,3,3,3,3,3,3,3,3,3,3,3,3,3,3,3,3,
3,3,3,3,3,3,3,3,3,3,3,3,3,3,3,3,3,3,3,3,3,3,3,4),(19.9637469599589,20.0691762496,
20.1744465389314,20.2795930074112,20.3846736705057,20.4897247569757,20.5947824515381,
20.6999523658092,20.8051858417855,20.9106005879211,20.9581463832319,21.0636441615438,
21.1689828605436,21.2741974550174,21.3793459535709,21.4844644800325,21.5895891138554,
21.6948258267937,21.8001254520998,21.9056074002119,21.956153353862,22.0616511315823,
22.1669898299647,22.2722044237851,22.3773529216633,22.4824714474289,22.5875960805357,
22.6928327927324,22.7981324172816,22.9036143646201,22.954160324492,23.0596581039059,
23.1649968040116,23.2702113995914,23.3753598992505,23.4804784268152,23.5856030617377,
23.6908397757618,23.7961394021476,23.9016213513182,23.9521672951221,24.057665073735,
24.1630037730298,24.2682183677881,24.3733668666195,24.4784853933521,24.5836100274381,
24.6888467406263,24.7941463661753,24.8996283145162,24.9501742657522,25.0556720443539,
25.1610107436346,25.2662253383753,25.3713738371867,25.4764923638964,25.5816169979577,
25.6868537111176,25.7921533366363,25.8976352849442,25.9481812363823,26.0768101553301,
26.2036580691034,26.2469320881093),.UNSPECIFIED.);
#3886=B_SPLINE_CURVE_WITH_KNOTS('',3,(#279819,#279820,#279821,#279822,#279823,
#279824,#279825,#279826,#279827,#279828),.UNSPECIFIED.,.F.,.F.,(4,1,1,1,
1,1,1,4),(26.2469322667478,26.9461882070124,27.9441951776425,28.9422021482726,
29.9402091189027,30.9382160895327,31.9362230601628,32.5301175739274),
 .UNSPECIFIED.);
#3887=B_SPLINE_CURVE_WITH_KNOTS('',3,(#279830,#279831,#279832,#279833,#279834,
#279835,#279836,#279837,#279838,#279839,#279840,#279841,#279842,#279843,
#279844,#279845,#279846,#279847,#279848,#279849,#279850,#279851,#279852,
#279853,#279854,#279855,#279856,#279857,#279858,#279859,#279860,#279861,
#279862,#279863,#279864,#279865,#279866,#279867,#279868,#279869,#279870,
#279871,#279872,#279873,#279874,#279875,#279876,#279877,#279878,#279879,
#279880,#279881,#279882,#279883,#279884,#279885,#279886,#279887,#279888,
#279889,#279890,#279891,#279892,#279893,#279894,#279895,#279896,#279897,
#279898,#279899,#279900,#279901,#279902,#279903,#279904,#279905,#279906,
#279907,#279908,#279909,#279910,#279911,#279912,#279913,#279914,#279915,
#279916,#279917,#279918,#279919,#279920,#279921,#279922,#279923,#279924,
#279925,#279926,#279927,#279928,#279929,#279930,#279931,#279932,#279933,
#279934,#279935,#279936,#279937,#279938,#279939,#279940,#279941,#279942,
#279943,#279944,#279945,#279946,#279947,#279948,#279949,#279950,#279951,
#279952,#279953,#279954,#279955,#279956,#279957,#279958,#279959,#279960,
#279961,#279962,#279963,#279964,#279965,#279966,#279967,#279968,#279969,
#279970,#279971,#279972,#279973,#279974,#279975,#279976,#279977,#279978,
#279979,#279980,#279981,#279982,#279983,#279984,#279985,#279986,#279987,
#279988,#279989,#279990,#279991,#279992,#279993,#279994,#279995,#279996,
#279997,#279998,#279999,#280000,#280001,#280002,#280003,#280004,#280005,
#280006,#280007,#280008,#280009,#280010,#280011,#280012,#280013,#280014,
#280015,#280016,#280017,#280018,#280019),.UNSPECIFIED.,.F.,.F.,(4,3,3,3,
3,3,3,3,3,3,3,3,3,3,3,3,3,3,3,3,3,3,3,3,3,3,3,3,3,3,3,3,3,3,3,3,3,3,3,3,
3,3,3,3,3,3,3,3,3,3,3,3,3,3,3,3,3,3,3,3,3,3,3,4),(32.530118003655,32.64600712011,
32.762304561712,32.879155677441,32.9342300307929,33.0397278095187,33.1450665089264,
33.2502811037972,33.3554296027407,33.4605481295847,33.5656727637819,33.670909477079,
33.7762091027359,33.8816910511823,33.932237001423,34.0377347801494,34.1430734795579,
34.2482880744293,34.3534365733734,34.458555100218,34.5636797344156,34.6689164477134,
34.7742160733709,34.8796980218179,34.9302439720531,35.03574175078,35.1410804501888,
35.2462950450607,35.3514435440053,35.4565620708504,35.5616867050485,35.6669234183467,
35.7722230440048,35.8777049924522,35.9282509426832,36.0337487214096,36.1390874208181,
36.2443020156895,36.3494505146337,36.4545690414783,36.5596936756759,36.6649303889737,
36.7702300146313,36.8757119630783,36.9262579133133,37.0317556920399,37.1370943914484,
37.2423089863199,37.3474574852643,37.452576012109,37.5577006463068,37.6629373596046,
37.7682369852624,37.8737189337095,37.9242648839434,38.0283818027737,38.1323195313251,
38.2361576431265,38.3399340926199,38.4436867444814,38.5475137381468,38.6513807199573,
38.7554057475333,38.813302881107),.UNSPECIFIED.);
#3888=B_SPLINE_CURVE_WITH_KNOTS('',3,(#280021,#280022,#280023,#280024,#280025,
#280026,#280027,#280028,#280029,#280030,#280031),.UNSPECIFIED.,.F.,.F.,
(4,1,1,1,1,1,1,1,4),(38.813302881107,38.9222718545735,39.9202788252036,
40.9182857958337,41.9162927664637,42.9142997370938,43.9123067077239,44.910313678354,
45.0964881882866),.UNSPECIFIED.);
#3889=B_SPLINE_CURVE_WITH_KNOTS('',3,(#280033,#280034,#280035,#280036,#280037,
#280038,#280039,#280040,#280041,#280042),.UNSPECIFIED.,.F.,.F.,(4,1,1,1,
1,1,1,4),(45.0964881882866,45.9083206489841,46.9063276196142,47.9043345902443,
48.9023415608744,49.9003485315045,50.8983555021345,51.3796721305015),
 .UNSPECIFIED.);
#3890=B_SPLINE_CURVE_WITH_KNOTS('',3,(#280044,#280045,#280046,#280047,#280048,
#280049,#280050,#280051,#280052,#280053,#280054,#280055,#280056,#280057,
#280058,#280059,#280060,#280061,#280062,#280063,#280064,#280065,#280066,
#280067,#280068,#280069,#280070,#280071,#280072,#280073,#280074,#280075,
#280076,#280077,#280078,#280079,#280080,#280081,#280082,#280083,#280084,
#280085,#280086,#280087,#280088,#280089,#280090,#280091,#280092,#280093,
#280094,#280095,#280096,#280097,#280098,#280099,#280100,#280101,#280102,
#280103,#280104,#280105,#280106,#280107,#280108,#280109,#280110,#280111,
#280112,#280113,#280114,#280115,#280116,#280117,#280118,#280119,#280120,
#280121,#280122,#280123,#280124,#280125,#280126,#280127,#280128,#280129,
#280130,#280131,#280132,#280133,#280134,#280135,#280136,#280137,#280138,
#280139,#280140,#280141,#280142,#280143,#280144,#280145,#280146,#280147,
#280148,#280149,#280150,#280151,#280152,#280153,#280154,#280155,#280156,
#280157,#280158,#280159,#280160,#280161,#280162,#280163,#280164,#280165,
#280166,#280167,#280168,#280169,#280170,#280171,#280172,#280173,#280174,
#280175,#280176,#280177,#280178,#280179,#280180,#280181,#280182,#280183,
#280184,#280185,#280186,#280187,#280188,#280189,#280190,#280191,#280192,
#280193,#280194,#280195,#280196,#280197,#280198,#280199,#280200,#280201,
#280202,#280203,#280204,#280205,#280206,#280207,#280208,#280209,#280210,
#280211,#280212,#280213,#280214,#280215,#280216,#280217,#280218,#280219,
#280220,#280221,#280222,#280223,#280224,#280225,#280226,#280227,#280228,
#280229,#280230,#280231,#280232,#280233),.UNSPECIFIED.,.F.,.F.,(4,3,3,3,
3,3,3,3,3,3,3,3,3,3,3,3,3,3,3,3,3,3,3,3,3,3,3,3,3,3,3,3,3,3,3,3,3,3,3,3,
3,3,3,3,3,3,3,3,3,3,3,3,3,3,3,3,3,3,3,3,3,3,3,4),(51.3796734954662,51.4890034742577,
51.5986022051298,51.70834049393,51.8183684296074,51.8963624727646,52.0018602514911,
52.1071989508998,52.2124135457714,52.3175620447157,52.4226805715604,52.5278052057581,
52.6330419190561,52.7383415447139,52.843823493161,52.8943694433947,52.9998672221213,
53.1052059215298,53.2104205164014,53.3155690153457,53.4206875421904,53.5258121763882,
53.6310488896862,53.7363485153438,53.8418304637909,53.8923764140248,53.9978741927513,
54.1032128921599,54.2084274870315,54.3135759859757,54.4186945128204,54.5238191470182,
54.6290558603161,54.734355485974,54.839837434421,54.8903833846549,54.9958811633815,
55.10121986279,55.2064344576615,55.3115829566059,55.4167014834508,55.5218261176487,
55.6270628309466,55.7323624566042,55.8378444050512,55.888390355285,55.9938881340116,
56.0992268334203,56.2044414282919,56.3095899272362,56.414708454081,56.5198330882791,
56.625069801577,56.7303694272347,56.835851375682,56.8863973259151,56.9904386065909,
57.0943385322742,57.1981352595082,57.3018667940288,57.405608533537,57.5093549662644,
57.6132006623058,57.6628588026458),.UNSPECIFIED.);
#3891=B_SPLINE_CURVE_WITH_KNOTS('',3,(#280235,#280236,#280237,#280238,#280239,
#280240,#280241,#280242,#280243,#280244,#280245),.UNSPECIFIED.,.F.,.F.,
(4,1,1,1,1,1,1,1,4),(57.6628588026458,57.8844042965452,58.8824112671752,
59.8804182378054,60.8784252084354,61.8764321790655,62.8744391496956,63.8724461203257,
63.9460441098254),.UNSPECIFIED.);
#3892=B_SPLINE_CURVE_WITH_KNOTS('',3,(#280247,#280248,#280249,#280250,#280251,
#280252,#280253,#280254,#280255,#280256),.UNSPECIFIED.,.F.,.F.,(4,1,1,1,
1,1,1,4),(63.9460441098254,64.8704530909558,65.8684600615859,66.866467032216,
67.8644740028461,68.8624809734761,69.8604879441062,70.2292218444269),
 .UNSPECIFIED.);
#3893=B_SPLINE_CURVE_WITH_KNOTS('',3,(#280258,#280259,#280260,#280261,#280262,
#280263,#280264,#280265,#280266,#280267,#280268,#280269,#280270,#280271,
#280272,#280273,#280274,#280275,#280276,#280277,#280278,#280279,#280280,
#280281,#280282,#280283,#280284,#280285,#280286,#280287,#280288,#280289,
#280290,#280291,#280292,#280293,#280294,#280295,#280296,#280297,#280298,
#280299,#280300,#280301,#280302,#280303,#280304,#280305,#280306,#280307,
#280308,#280309,#280310,#280311,#280312,#280313,#280314,#280315,#280316,
#280317,#280318,#280319,#280320,#280321,#280322,#280323,#280324,#280325,
#280326,#280327,#280328,#280329,#280330,#280331,#280332,#280333,#280334,
#280335,#280336,#280337,#280338,#280339,#280340,#280341,#280342,#280343,
#280344,#280345,#280346,#280347,#280348,#280349,#280350,#280351,#280352,
#280353,#280354,#280355,#280356,#280357,#280358,#280359,#280360,#280361,
#280362,#280363,#280364,#280365,#280366,#280367,#280368,#280369,#280370,
#280371,#280372,#280373,#280374,#280375,#280376,#280377,#280378,#280379,
#280380,#280381,#280382,#280383,#280384,#280385,#280386,#280387,#280388,
#280389,#280390,#280391,#280392,#280393,#280394,#280395,#280396,#280397,
#280398,#280399,#280400,#280401,#280402,#280403,#280404,#280405,#280406,
#280407,#280408,#280409,#280410,#280411,#280412,#280413,#280414,#280415,
#280416,#280417,#280418,#280419,#280420,#280421,#280422,#280423,#280424,
#280425,#280426,#280427,#280428,#280429,#280430,#280431,#280432,#280433,
#280434,#280435,#280436,#280437,#280438,#280439,#280440,#280441,#280442,
#280443,#280444,#280445,#280446,#280447),.UNSPECIFIED.,.F.,.F.,(4,3,3,3,
3,3,3,3,3,3,3,3,3,3,3,3,3,3,3,3,3,3,3,3,3,3,3,3,3,3,3,3,3,3,3,3,3,3,3,3,
3,3,3,3,3,3,3,3,3,3,3,3,3,3,3,3,3,3,3,3,3,3,3,4),(70.229229417005,70.335009033057,
70.4407990188872,70.5467185962429,70.6527015297735,70.7589032664553,70.8584949147363,
70.9639926934621,71.0693313928698,71.1745459877406,71.2796944866842,71.3848130135281,
71.4899376477252,71.5951743610223,71.7004739866793,71.8059559351256,71.8565018853664,
71.9619996640953,72.0673383635062,72.17255295838,72.2777014573267,72.3828199841735,
72.4879446183735,72.5931813316736,72.6984809573335,72.8039629057828,72.8545088559965,
72.9600066347213,73.065345334128,73.1705599289978,73.2757084279404,73.3808269547834,
73.4859515889798,73.5911883022759,73.696487927932,73.8019698763775,73.8525158266266,
73.9580136053487,74.0633523047526,74.1685668996196,74.2737153985593,74.3788339253994,
74.4839585595926,74.589195272886,74.6944948985394,74.799976846982,74.8505227972567,
74.9560205759993,75.0613592754235,75.1665738703108,75.271722369271,75.3768408961317,
75.4819655303449,75.5872022436584,75.6925018693315,75.7979838177936,75.8485297678868,
75.9539872943584,76.0592890581743,76.1644713975019,76.2695756454254,76.3746355093251,
76.4797099416953,76.5124147241846),.UNSPECIFIED.);
#3894=B_SPLINE_CURVE_WITH_KNOTS('',3,(#280449,#280450,#280451,#280452,#280453,
#280454,#280455,#280456,#280457,#280458),.UNSPECIFIED.,.F.,.F.,(4,1,1,1,
1,1,1,4),(76.5124219319248,76.8465367385169,77.8445437091469,78.842550679777,
79.8405576504071,80.8385646210372,81.8365715916673,82.7955949071842),
 .UNSPECIFIED.);
#3895=B_SPLINE_CURVE_WITH_KNOTS('',3,(#280460,#280461,#280462,#280463,#280464,
#280465,#280466,#280467,#280468,#280469,#280470,#280471,#280472,#280473,
#280474,#280475,#280476,#280477,#280478,#280479,#280480,#280481,#280482,
#280483,#280484,#280485,#280486,#280487,#280488,#280489,#280490,#280491,
#280492,#280493,#280494,#280495,#280496,#280497,#280498,#280499,#280500,
#280501,#280502,#280503,#280504,#280505,#280506,#280507,#280508,#280509,
#280510,#280511,#280512,#280513,#280514,#280515,#280516,#280517,#280518,
#280519,#280520,#280521,#280522,#280523,#280524,#280525,#280526,#280527,
#280528,#280529,#280530,#280531,#280532,#280533,#280534,#280535,#280536,
#280537,#280538,#280539,#280540,#280541,#280542,#280543,#280544,#280545,
#280546,#280547,#280548,#280549,#280550,#280551,#280552,#280553,#280554,
#280555,#280556,#280557,#280558,#280559,#280560,#280561,#280562,#280563,
#280564,#280565,#280566,#280567,#280568,#280569,#280570,#280571,#280572,
#280573,#280574,#280575,#280576,#280577,#280578,#280579,#280580,#280581,
#280582,#280583,#280584,#280585,#280586,#280587,#280588,#280589,#280590,
#280591,#280592,#280593,#280594,#280595,#280596,#280597,#280598,#280599,
#280600,#280601,#280602,#280603,#280604,#280605,#280606,#280607,#280608,
#280609,#280610,#280611,#280612,#280613,#280614,#280615,#280616,#280617,
#280618,#280619,#280620,#280621,#280622,#280623,#280624,#280625,#280626,
#280627,#280628,#280629,#280630,#280631,#280632,#280633,#280634,#280635,
#280636,#280637,#280638,#280639,#280640,#280641,#280642,#280643,#280644,
#280645,#280646,#280647,#280648,#280649),.UNSPECIFIED.,.F.,.F.,(4,3,3,3,
3,3,3,3,3,3,3,3,3,3,3,3,3,3,3,3,3,3,3,3,3,3,3,3,3,3,3,3,3,3,3,3,3,3,3,3,
3,3,3,3,3,3,3,3,3,3,3,3,3,3,3,3,3,3,3,3,3,3,3,4),(82.7956000313642,82.8345785622974,
82.9400763406927,83.0454150397571,83.1506296342673,83.2557781328398,83.360896659303,
83.4660212931101,83.5712580060064,83.6765576312558,83.7820395792885,83.8325855329275,
83.9380833163443,84.0434220204612,84.1486366200449,84.253785123701,84.3589036552502,
84.4640282941382,84.5692650120724,84.6745646423428,84.7800465953174,84.8305925035576,
84.9360902738077,85.0414289647494,85.1466435512085,85.2517920417788,85.3569105603002,
85.4620351862373,85.567271891425,85.6725715090463,85.7780534496546,85.8285994741877,
85.9340972534072,86.0394359532236,86.1446505483768,86.2497990475246,86.354917574495,
86.4600422087412,86.5652789219716,86.6705785474958,86.7760604957101,86.8266064448178,
86.9321042532473,87.0374429824998,87.1426576072785,87.2478061361519,87.3529246929027,
87.4580493569388,87.5632860997688,87.6685857548277,87.7740677321644,87.8246134154479,
87.9301111310943,88.0354497674402,88.140664299576,88.2458127360226,88.3509312006986,
88.4560557731484,88.5612924257495,88.6665919912204,88.772073880896,88.822620386078,
88.9578209224006,89.0787851943848),.UNSPECIFIED.);
#3896=B_SPLINE_CURVE_WITH_KNOTS('',3,(#280651,#280652,#280653,#280654,#280655,
#280656,#280657,#280658,#280659,#280660),.UNSPECIFIED.,.F.,.F.,(4,1,1,1,
1,1,1,4),(89.0787853385438,89.820627356708,90.8186343273381,91.8166412979682,
92.8146482685983,93.8126552392284,94.8106622098585,95.3619706457233),
 .UNSPECIFIED.);
#3897=B_SPLINE_CURVE_WITH_KNOTS('',3,(#280662,#280663,#280664,#280665,#280666,
#280667,#280668,#280669),.UNSPECIFIED.,.F.,.F.,(4,1,1,1,1,4),(95.3619706457233,
95.8086691804886,96.8066761511186,97.8046831217487,98.8026900923788,99.1486641472938),
 .UNSPECIFIED.);
#3898=B_SPLINE_CURVE_WITH_KNOTS('',3,(#280673,#280674,#280675,#280676,#280677,
#280678,#280679,#280680,#280681,#280682,#280683,#280684,#280685,#280686,
#280687,#280688,#280689,#280690,#280691,#280692,#280693,#280694,#280695,
#280696,#280697,#280698,#280699,#280700,#280701,#280702,#280703,#280704,
#280705,#280706,#280707,#280708,#280709,#280710,#280711,#280712,#280713,
#280714,#280715,#280716,#280717,#280718,#280719,#280720,#280721,#280722,
#280723,#280724,#280725,#280726,#280727,#280728,#280729,#280730,#280731,
#280732,#280733,#280734,#280735,#280736,#280737,#280738,#280739,#280740,
#280741,#280742,#280743,#280744,#280745,#280746,#280747,#280748,#280749,
#280750,#280751,#280752,#280753,#280754,#280755,#280756,#280757,#280758,
#280759,#280760),.UNSPECIFIED.,.F.,.F.,(4,3,3,3,3,3,3,3,3,3,3,3,3,3,3,3,
3,3,3,3,3,3,3,3,3,3,3,3,3,4),(-101.213781757955,-101.103717934714,-100.993312031664,
-100.882718756788,-100.77180592249,-100.730920097777,-100.625250669449,
-100.519739902776,-100.414353549507,-100.309033583812,-100.203744159594,
-100.098449475631,-99.9930453966476,-99.8875795787119,-99.7819355250837,
-99.7335842552244,-99.6278935405064,-99.522357699021,-99.4169407542712,
-99.3115867820018,-99.2062599780791,-99.1009245796907,-98.9954749913784,
-98.8899608557558,-98.7842646387928,-98.7362484126722,-98.6191022761829,
-98.5023548078507,-98.3862549016326,-98.3403218112339),.UNSPECIFIED.);
#3899=B_SPLINE_CURVE_WITH_KNOTS('',3,(#280762,#280763,#280764,#280765,#280766,
#280767,#280768,#280769,#280770,#280771),.UNSPECIFIED.,.F.,.F.,(4,1,1,1,
1,1,1,4),(-98.3403213565322,-97.7389125701199,-96.7415767275677,-95.7442408850154,
-94.7469050424632,-93.7495691999109,-92.7522333573587,-92.0571360493526),
 .UNSPECIFIED.);
#3900=B_SPLINE_CURVE_WITH_KNOTS('',3,(#280773,#280774,#280775,#280776,#280777,
#280778,#280779,#280780,#280781,#280782,#280783,#280784,#280785,#280786,
#280787,#280788,#280789,#280790,#280791,#280792,#280793,#280794,#280795,
#280796,#280797,#280798,#280799,#280800,#280801,#280802,#280803,#280804,
#280805,#280806,#280807,#280808,#280809,#280810,#280811,#280812,#280813,
#280814,#280815,#280816,#280817,#280818,#280819,#280820,#280821,#280822,
#280823,#280824,#280825,#280826,#280827,#280828,#280829,#280830,#280831,
#280832,#280833,#280834,#280835,#280836,#280837,#280838,#280839,#280840,
#280841,#280842,#280843,#280844,#280845,#280846,#280847,#280848,#280849,
#280850,#280851,#280852,#280853,#280854,#280855,#280856,#280857,#280858,
#280859,#280860,#280861,#280862,#280863,#280864,#280865,#280866,#280867,
#280868,#280869,#280870,#280871,#280872,#280873,#280874,#280875,#280876,
#280877,#280878,#280879,#280880,#280881,#280882,#280883,#280884,#280885,
#280886,#280887,#280888,#280889,#280890,#280891,#280892,#280893,#280894,
#280895,#280896,#280897,#280898,#280899,#280900,#280901,#280902,#280903,
#280904,#280905,#280906,#280907,#280908,#280909,#280910,#280911,#280912,
#280913,#280914,#280915,#280916,#280917,#280918,#280919,#280920,#280921,
#280922,#280923,#280924,#280925,#280926,#280927,#280928,#280929,#280930,
#280931,#280932,#280933,#280934,#280935,#280936,#280937,#280938,#280939,
#280940,#280941,#280942,#280943,#280944,#280945,#280946,#280947,#280948,
#280949,#280950,#280951,#280952,#280953,#280954,#280955,#280956,#280957,
#280958,#280959,#280960,#280961,#280962),.UNSPECIFIED.,.F.,.F.,(4,3,3,3,
3,3,3,3,3,3,3,3,3,3,3,3,3,3,3,3,3,3,3,3,3,3,3,3,3,3,3,3,3,3,3,3,3,3,3,3,
3,3,3,3,3,3,3,3,3,3,3,3,3,3,3,3,3,3,3,3,3,3,3,4),(-92.0571358644987,-91.9309798648606,
-91.8030898888977,-91.7548975148065,-91.6493896706802,-91.5440406918723,
-91.4388155855705,-91.333656423695,-91.2285270990573,-91.1233915487001,
-91.0181440166959,-90.9128334881802,-90.8073411349775,-90.7575616722542,
-90.6520546685707,-90.546706533492,-90.4414822715455,-90.3363239539049,
-90.2311954720731,-90.126060761783,-90.0208140598827,-89.9155043569929,
-89.8100128137758,-89.760225829702,-89.6547194791003,-89.54937201196,-89.444148436697,
-89.3389908169854,-89.2338630432782,-89.1287290502691,-89.0234830746453,
-88.9181741042341,-88.8126832954185,-88.7628899871497,-88.6573830323899,
-88.552034951717,-88.4468107520647,-88.3416525015875,-88.2365240916977,
-88.1313894580427,-88.0261428393948,-87.9208332236598,-87.8153417727399,
-87.7655541445975,-87.6600473539947,-87.5546994387229,-87.4494754054875,
-87.3443173219588,-87.2391890792919,-87.1340546128773,-87.0288081603432,
-86.9234987103214,-86.818007422749,-86.7682183020452,-86.6627698224436,
-86.5574801750676,-86.4523142026813,-86.3472139535958,-86.242143229031,
-86.13706587418,-86.0318764403095,-85.9266234721262,-85.8211895798944,-85.7739507426258),
 .UNSPECIFIED.);
#3901=B_SPLINE_CURVE_WITH_KNOTS('',3,(#280964,#280965,#280966,#280967,#280968,
#280969,#280970,#280971,#280972,#280973,#280974,#280975,#280976,#280977,
#280978,#280979,#280980,#280981,#280982,#280983,#280984,#280985,#280986,
#280987,#280988,#280989,#280990,#280991,#280992,#280993,#280994,#280995,
#280996,#280997,#280998,#280999,#281000,#281001,#281002,#281003,#281004,
#281005,#281006,#281007,#281008,#281009,#281010,#281011,#281012,#281013,
#281014,#281015,#281016,#281017,#281018,#281019,#281020,#281021,#281022,
#281023,#281024,#281025,#281026,#281027,#281028,#281029,#281030,#281031,
#281032,#281033,#281034,#281035,#281036,#281037,#281038,#281039,#281040,
#281041,#281042,#281043,#281044,#281045,#281046,#281047,#281048,#281049,
#281050,#281051,#281052,#281053,#281054,#281055,#281056,#281057,#281058,
#281059,#281060,#281061,#281062,#281063,#281064,#281065,#281066,#281067,
#281068,#281069,#281070,#281071,#281072,#281073,#281074,#281075,#281076,
#281077,#281078,#281079,#281080,#281081,#281082,#281083,#281084,#281085,
#281086,#281087,#281088,#281089,#281090,#281091,#281092,#281093,#281094,
#281095,#281096,#281097,#281098,#281099,#281100,#281101,#281102,#281103,
#281104,#281105,#281106,#281107,#281108,#281109,#281110,#281111,#281112,
#281113,#281114,#281115,#281116,#281117,#281118,#281119,#281120,#281121,
#281122,#281123,#281124,#281125,#281126,#281127,#281128,#281129,#281130,
#281131,#281132,#281133,#281134,#281135,#281136,#281137,#281138,#281139,
#281140,#281141,#281142,#281143,#281144,#281145,#281146,#281147,#281148,
#281149,#281150,#281151,#281152,#281153,#281154,#281155,#281156),
 .UNSPECIFIED.,.F.,.F.,(4,3,3,3,3,3,3,3,3,3,3,3,3,3,3,3,3,3,3,3,3,3,3,3,
3,3,3,3,3,3,3,3,3,3,3,3,3,3,3,3,3,3,3,3,3,3,3,3,3,3,3,3,3,3,3,3,3,3,3,3,
3,3,3,3,4),(-85.773950742173,-85.770882459493,-85.6653756550451,-85.5600277263926,
-85.4548036805353,-85.3496455848643,-85.2445173305549,-85.1393828530184,
-85.0341363902315,-84.9288269304384,-84.8233356339455,-84.7735466169407,
-84.6680398418928,-84.5626919429278,-84.4574679270362,-84.3523098614858,
-84.2471816374057,-84.142047190161,-84.0368007575523,-83.9314913279168,
-83.8260000612317,-83.7762107743885,-83.6707040065865,-83.5653561150936,
-83.4601321069731,-83.3549740493751,-83.2498458334168,-83.1447113944518,
-83.0394649703059,-82.9341555492503,-82.8286642912366,-82.7788749318363,
-82.6733681517915,-82.5680202478474,-82.4627962270287,-82.3576381565863,
-82.2525099276572,-82.147375475614,-82.042129038317,-81.9368196040492,-81.8313283328676,
-81.781539089284,-81.6760323142181,-81.5706844153093,-81.4654603995842,
-81.3603023342687,-81.2551741104917,-81.1500396636184,-81.0447932314822,
-80.9394838023778,-80.8339925363091,-80.7842032467318,-80.6786964722063,
-80.5733485738632,-80.4681245587387,-80.3629664940452,-80.2578382709107,
-80.1527038246994,-80.0474573932505,-79.9421479648487,-79.8366566994992,
-79.7868674041795,-79.6578860557949,-79.5307260217994,-79.4907656077684),
 .UNSPECIFIED.);
#3902=B_SPLINE_CURVE_WITH_KNOTS('',3,(#281158,#281159,#281160,#281161,#281162,
#281163,#281164,#281165,#281166,#281167),.UNSPECIFIED.,.F.,.F.,(4,1,1,1,
1,1,1,4),(-79.4907654349934,-78.7895315616273,-77.792195719075,-76.7948598765228,
-75.7975240339705,-74.8001881914183,-73.802852348866,-73.2075801278138),
 .UNSPECIFIED.);
#3903=B_SPLINE_CURVE_WITH_KNOTS('',3,(#281169,#281170,#281171,#281172,#281173,
#281174,#281175,#281176,#281177,#281178,#281179,#281180,#281181,#281182,
#281183,#281184,#281185,#281186,#281187,#281188,#281189,#281190,#281191,
#281192,#281193,#281194,#281195,#281196,#281197,#281198,#281199,#281200,
#281201,#281202,#281203,#281204,#281205,#281206,#281207,#281208,#281209,
#281210,#281211,#281212,#281213,#281214,#281215,#281216,#281217,#281218,
#281219,#281220,#281221,#281222,#281223,#281224,#281225,#281226,#281227,
#281228,#281229,#281230,#281231,#281232,#281233,#281234,#281235,#281236,
#281237,#281238,#281239,#281240,#281241,#281242,#281243,#281244,#281245,
#281246,#281247,#281248,#281249,#281250,#281251,#281252,#281253,#281254,
#281255,#281256,#281257,#281258,#281259,#281260,#281261,#281262,#281263,
#281264,#281265,#281266,#281267,#281268,#281269,#281270,#281271,#281272,
#281273,#281274,#281275,#281276,#281277,#281278,#281279,#281280,#281281,
#281282,#281283,#281284,#281285,#281286,#281287,#281288,#281289,#281290,
#281291,#281292,#281293,#281294,#281295,#281296,#281297,#281298,#281299,
#281300,#281301,#281302,#281303,#281304,#281305,#281306,#281307,#281308,
#281309,#281310,#281311,#281312,#281313,#281314,#281315,#281316,#281317,
#281318,#281319,#281320,#281321,#281322,#281323,#281324,#281325,#281326,
#281327,#281328,#281329,#281330,#281331,#281332,#281333,#281334,#281335,
#281336,#281337,#281338,#281339,#281340,#281341,#281342,#281343,#281344,
#281345,#281346,#281347,#281348,#281349,#281350,#281351,#281352,#281353,
#281354,#281355,#281356,#281357,#281358),.UNSPECIFIED.,.F.,.F.,(4,3,3,3,
3,3,3,3,3,3,3,3,3,3,3,3,3,3,3,3,3,3,3,3,3,3,3,3,3,3,3,3,3,3,3,3,3,3,3,3,
3,3,3,3,3,3,3,3,3,3,3,3,3,3,3,3,3,3,3,3,3,3,3,4),(-73.2075796958044,-73.0915613768673,
-72.9751283017546,-72.8581383239148,-72.8055165063138,-72.700009730801,
-72.5946618314507,-72.4894378152941,-72.3842797495539,-72.2791515253595,
-72.1740170780766,-72.068770645546,-71.9634612160551,-71.8579699496164,
-71.8081806637616,-71.7026738882456,-71.5973259888921,-71.4921019727325,
-71.3869439069892,-71.2818156827917,-71.1766812355058,-71.0714348029722,
-70.9661253734783,-70.8606341070367,-70.8108448212093,-70.7053380456898,
-70.5999901463325,-70.4947661301691,-70.389608064422,-70.2844798402206,
-70.1793453929309,-70.0740989603933,-69.9687895308954,-69.8632982644497,
-69.8135089786571,-69.7080022031405,-69.6026543037862,-69.4974302876257,
-69.3922722218816,-69.2871439976833,-69.1820095503966,-69.0767631178621,
-68.9714536883672,-68.8659624219246,-68.8161731361048,-68.7106663605875,
-68.6053184612326,-68.5000944450716,-68.3949363793268,-68.2898081551279,
-68.1846737078405,-68.0794272753054,-67.9741178458099,-67.8686265793667,
-67.8188372935526,-67.7146690912171,-67.610679764849,-67.5067899220888,
-67.4029616617978,-67.2991571716489,-67.1952770554739,-67.0913570786103,
-66.9872756614915,-66.9243948210848),.UNSPECIFIED.);
#3904=B_SPLINE_CURVE_WITH_KNOTS('',3,(#281360,#281361,#281362,#281363,#281364,
#281365,#281366,#281367,#281368,#281369,#281370,#281371,#281372,#281373,
#281374,#281375,#281376,#281377,#281378,#281379,#281380,#281381,#281382,
#281383,#281384,#281385,#281386,#281387,#281388,#281389,#281390,#281391,
#281392,#281393,#281394,#281395,#281396,#281397,#281398,#281399,#281400,
#281401,#281402,#281403,#281404,#281405,#281406,#281407,#281408,#281409,
#281410,#281411,#281412,#281413,#281414,#281415,#281416,#281417,#281418,
#281419,#281420,#281421,#281422,#281423,#281424,#281425,#281426,#281427,
#281428,#281429,#281430,#281431,#281432,#281433,#281434,#281435,#281436,
#281437,#281438,#281439,#281440,#281441,#281442,#281443,#281444,#281445,
#281446,#281447,#281448,#281449,#281450,#281451,#281452,#281453,#281454,
#281455,#281456,#281457,#281458,#281459,#281460,#281461,#281462,#281463,
#281464,#281465,#281466,#281467,#281468,#281469,#281470,#281471,#281472,
#281473,#281474,#281475,#281476,#281477,#281478,#281479,#281480,#281481,
#281482,#281483,#281484,#281485,#281486,#281487,#281488,#281489,#281490,
#281491,#281492,#281493,#281494,#281495,#281496,#281497,#281498,#281499,
#281500,#281501,#281502,#281503,#281504,#281505,#281506,#281507,#281508,
#281509,#281510,#281511,#281512,#281513,#281514,#281515,#281516,#281517,
#281518,#281519,#281520,#281521,#281522,#281523,#281524,#281525,#281526,
#281527,#281528,#281529,#281530,#281531,#281532,#281533,#281534,#281535,
#281536,#281537,#281538,#281539,#281540,#281541,#281542,#281543,#281544,
#281545,#281546,#281547,#281548,#281549),.UNSPECIFIED.,.F.,.F.,(4,3,3,3,
3,3,3,3,3,3,3,3,3,3,3,3,3,3,3,3,3,3,3,3,3,3,3,3,3,3,3,3,3,3,3,3,3,3,3,3,
3,3,3,3,3,3,3,3,3,3,3,3,3,3,3,3,3,3,3,3,3,3,3,4),(-66.9243948206342,-66.8215014510004,
-66.7159946754828,-66.6106467761274,-66.5054227599659,-66.4002646942207,
-66.2951364700213,-66.1900020227335,-66.0847555901979,-65.979446160702,
-65.8739548942583,-65.8241656084481,-65.7186588329308,-65.6133109335758,
-65.5080869174147,-65.4029288516699,-65.2978006274709,-65.1926661801835,
-65.0874197476483,-64.9821103181527,-64.8766190517094,-64.8268297658959,
-64.7213229903785,-64.6159750910234,-64.5107510748621,-64.4055930091172,
-64.3004647849181,-64.1953303376305,-64.0900839050952,-63.9847744755996,
-63.8792832091562,-63.8294939233436,-63.7239871478262,-63.6186392484711,
-63.5134152323099,-63.4082571665649,-63.3031289423658,-63.1979944950782,
-63.0927480625429,-62.9874386330473,-62.8819473666039,-62.8321580807914,
-62.726651305274,-62.6213034059189,-62.5160793897577,-62.4109213240128,
-62.3057930998137,-62.2006586525262,-62.0954122199908,-61.9901027904952,
-61.8846115240518,-61.8348222382391,-61.7293154627217,-61.6239675633666,
-61.5187435472054,-61.4135854814605,-61.3084572572614,-61.203322809974,
-61.0980763774386,-60.992766947943,-60.8872756814996,-60.8374863956869,
-60.6852066800683,-60.6412095134546),.UNSPECIFIED.);
#3905=B_SPLINE_CURVE_WITH_KNOTS('',3,(#281551,#281552,#281553,#281554,#281555,
#281556,#281557,#281558,#281559,#281560),.UNSPECIFIED.,.F.,.F.,(4,1,1,1,
1,1,1,4),(-60.6412060868095,-59.8401505531347,-58.8428147105824,-57.8454788680302,
-56.8481430254779,-55.8508071829257,-54.8534713403734,-54.3580242062751),
 .UNSPECIFIED.);
#3906=B_SPLINE_CURVE_WITH_KNOTS('',3,(#281562,#281563,#281564,#281565,#281566,
#281567,#281568,#281569,#281570,#281571),.UNSPECIFIED.,.F.,.F.,(4,1,1,1,
1,1,1,4),(-54.3580242062751,-53.8561354978212,-52.8587996552689,-51.8614638127167,
-50.8641279701645,-49.8667921276122,-48.86945628506,-48.0748417259287),
 .UNSPECIFIED.);
#3907=B_SPLINE_CURVE_WITH_KNOTS('',3,(#281573,#281574,#281575,#281576,#281577,
#281578,#281579,#281580,#281581,#281582,#281583,#281584,#281585,#281586,
#281587,#281588,#281589,#281590,#281591,#281592,#281593,#281594,#281595,
#281596,#281597,#281598,#281599,#281600,#281601,#281602,#281603,#281604,
#281605,#281606,#281607,#281608,#281609,#281610,#281611,#281612,#281613,
#281614,#281615,#281616,#281617,#281618,#281619,#281620,#281621,#281622,
#281623,#281624,#281625,#281626,#281627,#281628,#281629,#281630,#281631,
#281632,#281633,#281634,#281635,#281636,#281637,#281638,#281639,#281640,
#281641,#281642,#281643,#281644,#281645,#281646,#281647,#281648,#281649,
#281650,#281651,#281652,#281653,#281654,#281655,#281656,#281657,#281658,
#281659,#281660,#281661,#281662,#281663,#281664,#281665,#281666,#281667,
#281668,#281669,#281670,#281671,#281672,#281673,#281674,#281675,#281676,
#281677,#281678,#281679,#281680,#281681,#281682,#281683,#281684,#281685,
#281686,#281687,#281688,#281689,#281690,#281691,#281692,#281693,#281694,
#281695,#281696,#281697,#281698,#281699,#281700,#281701,#281702,#281703,
#281704,#281705,#281706,#281707,#281708,#281709,#281710,#281711,#281712,
#281713,#281714,#281715,#281716,#281717,#281718,#281719,#281720,#281721,
#281722,#281723,#281724,#281725,#281726,#281727,#281728,#281729,#281730,
#281731,#281732,#281733,#281734,#281735,#281736,#281737,#281738,#281739,
#281740,#281741,#281742,#281743,#281744,#281745,#281746,#281747,#281748,
#281749,#281750,#281751,#281752,#281753,#281754,#281755,#281756,#281757,
#281758,#281759,#281760,#281761,#281762),.UNSPECIFIED.,.F.,.F.,(4,3,3,3,
3,3,3,3,3,3,3,3,3,3,3,3,3,3,3,3,3,3,3,3,3,3,3,3,3,3,3,3,3,3,3,3,3,3,3,3,
3,3,3,3,3,3,3,3,3,3,3,3,3,3,3,3,3,3,3,3,3,3,3,4),(-48.0748388990955,-47.9250099117185,
-47.8721204425077,-47.7666136669904,-47.6612657676354,-47.5560417514743,
-47.4508836857296,-47.3457554615306,-47.2406210142432,-47.135374581708,
-47.0300651522125,-46.9245738857692,-46.8747845999555,-46.769277824438,
-46.6639299250828,-46.5587059089216,-46.4535478431766,-46.3484196189775,
-46.2432851716899,-46.1380387391545,-46.0327293096589,-45.9272380432155,
-45.8774487574032,-45.7719419818858,-45.6665940825307,-45.5613700663695,
-45.4562120006246,-45.3510837764254,-45.2459493291379,-45.1407028966025,
-45.0353934671069,-44.9299022006635,-44.880112914851,-44.7746061393336,
-44.6692582399785,-44.5640342238173,-44.4588761580724,-44.3537479338733,
-44.2486134865857,-44.1433670540504,-44.0380576245548,-43.9325663581114,
-43.8827770722987,-43.7772702967813,-43.6719223974262,-43.566698381265,
-43.46154031552,-43.3564120913209,-43.2512776440333,-43.146031211498,-43.0407217820023,
-42.9352305155589,-42.8854412297465,-42.779934454229,-42.674586554874,-42.5693625387129,
-42.4642044729679,-42.3590762487688,-42.2539418014812,-42.1486953689459,
-42.0433859394503,-41.9378946730069,-41.8881053871943,-41.7916535919159),
 .UNSPECIFIED.);
#3908=B_SPLINE_CURVE_WITH_KNOTS('',3,(#281764,#281765,#281766,#281767,#281768,
#281769,#281770,#281771,#281772,#281773),.UNSPECIFIED.,.F.,.F.,(4,1,1,1,
1,1,1,4),(-41.7916448313401,-40.890769544642,-39.8934337020898,-38.8960978595375,
-37.8987620169853,-36.901426174433,-35.9040903318808,-35.5084682847363),
 .UNSPECIFIED.);
#3909=B_SPLINE_CURVE_WITH_KNOTS('',3,(#281775,#281776,#281777,#281778,#281779,
#281780,#281781,#281782,#281783,#281784),.UNSPECIFIED.,.F.,.F.,(4,1,1,1,
1,1,1,4),(-35.5084682847363,-34.9067544893285,-33.9094186467763,-32.9120828042241,
-31.9147469616718,-30.9174111191196,-29.9200752765673,-29.2252829775567),
 .UNSPECIFIED.);
#3910=B_SPLINE_CURVE_WITH_KNOTS('',3,(#281786,#281787,#281788,#281789,#281790,
#281791,#281792,#281793,#281794,#281795,#281796,#281797,#281798,#281799,
#281800,#281801,#281802,#281803,#281804,#281805,#281806,#281807,#281808,
#281809,#281810,#281811,#281812,#281813,#281814,#281815,#281816,#281817,
#281818,#281819,#281820,#281821,#281822,#281823,#281824,#281825,#281826,
#281827,#281828,#281829,#281830,#281831,#281832,#281833,#281834,#281835,
#281836,#281837,#281838,#281839,#281840,#281841,#281842,#281843,#281844,
#281845,#281846,#281847,#281848,#281849,#281850,#281851,#281852,#281853,
#281854,#281855,#281856,#281857,#281858,#281859,#281860,#281861,#281862,
#281863,#281864,#281865,#281866,#281867,#281868,#281869,#281870,#281871,
#281872,#281873,#281874,#281875,#281876,#281877,#281878,#281879,#281880,
#281881,#281882,#281883,#281884,#281885,#281886,#281887,#281888,#281889,
#281890,#281891,#281892,#281893,#281894,#281895,#281896,#281897,#281898,
#281899,#281900,#281901,#281902,#281903,#281904,#281905,#281906,#281907,
#281908,#281909,#281910,#281911,#281912,#281913,#281914,#281915,#281916,
#281917,#281918,#281919,#281920,#281921,#281922,#281923,#281924,#281925,
#281926,#281927,#281928,#281929,#281930,#281931,#281932,#281933,#281934,
#281935,#281936,#281937,#281938,#281939,#281940,#281941,#281942,#281943,
#281944,#281945,#281946,#281947,#281948,#281949,#281950,#281951,#281952,
#281953,#281954,#281955,#281956,#281957,#281958,#281959,#281960,#281961,
#281962,#281963,#281964,#281965,#281966,#281967,#281968,#281969,#281970,
#281971,#281972,#281973,#281974,#281975),.UNSPECIFIED.,.F.,.F.,(4,3,3,3,
3,3,3,3,3,3,3,3,3,3,3,3,3,3,3,3,3,3,3,3,3,3,3,3,3,3,3,3,3,3,3,3,3,3,3,3,
3,3,3,3,3,3,3,3,3,3,3,3,3,3,3,3,3,3,3,3,3,3,3,4),(-29.2252827921887,-29.0991630781067,
-28.9713146182254,-28.9227394340151,-28.8172326585138,-28.7118847591747,
-28.6066607430293,-28.5015026773,-28.3963744531164,-28.291240005844,-28.1859935733236,
-28.0806841438427,-27.9751928774136,-27.9254035914628,-27.8198968159696,
-27.7145489166391,-27.6093249005027,-27.5041668347828,-27.3990386106088,
-27.2939041633464,-27.1886577308362,-27.0833483013658,-26.9778570349473,
-26.9280677489106,-26.8225609732847,-26.717213073821,-26.6119890575513,
-26.506830991698,-26.4017027673908,-26.2965683199958,-26.1913218873543,
-26.0860124577533,-25.9805211912066,-25.9307319063583,-25.825225130977,
-25.7198772317575,-25.6146532157305,-25.5094951501189,-25.404366926052,
-25.2992324788953,-25.193986046488,-25.088676617119,-24.9831853507987,-24.9333960638061,
-24.8278892884005,-24.7225413891591,-24.6173173731139,-24.5121593074863,
-24.4070310834057,-24.3018966362376,-24.1966502038223,-24.0913407744472,
-23.9858495081238,-23.9360602212539,-23.8306174073625,-23.7253334200811,
-23.6201730861378,-23.5150784524654,-23.4100133116324,-23.3049415001546,
-23.1997576017589,-23.0945101162213,-22.9890817997621,-22.942097670868),
 .UNSPECIFIED.);
#3911=B_SPLINE_CURVE_WITH_KNOTS('',3,(#281977,#281978,#281979,#281980,#281981,
#281982,#281983,#281984,#281985,#281986,#281987,#281988,#281989,#281990,
#281991,#281992,#281993,#281994,#281995,#281996,#281997,#281998,#281999,
#282000,#282001,#282002,#282003,#282004,#282005,#282006,#282007,#282008,
#282009,#282010,#282011,#282012,#282013,#282014,#282015,#282016,#282017,
#282018,#282019,#282020,#282021,#282022,#282023,#282024,#282025,#282026,
#282027,#282028,#282029,#282030,#282031,#282032,#282033,#282034,#282035,
#282036,#282037,#282038,#282039,#282040,#282041,#282042,#282043,#282044,
#282045,#282046,#282047,#282048,#282049,#282050,#282051,#282052,#282053,
#282054,#282055,#282056,#282057,#282058,#282059,#282060,#282061,#282062,
#282063,#282064,#282065,#282066,#282067,#282068,#282069,#282070,#282071,
#282072,#282073,#282074,#282075,#282076,#282077,#282078,#282079,#282080,
#282081,#282082,#282083,#282084,#282085,#282086,#282087,#282088,#282089,
#282090,#282091,#282092,#282093,#282094,#282095,#282096,#282097,#282098,
#282099,#282100,#282101,#282102,#282103,#282104,#282105,#282106,#282107,
#282108,#282109,#282110,#282111,#282112,#282113,#282114,#282115,#282116,
#282117,#282118,#282119,#282120,#282121,#282122,#282123,#282124,#282125,
#282126,#282127,#282128,#282129,#282130,#282131,#282132,#282133,#282134,
#282135,#282136,#282137,#282138,#282139,#282140,#282141,#282142,#282143,
#282144,#282145,#282146,#282147,#282148,#282149,#282150,#282151,#282152,
#282153,#282154,#282155,#282156,#282157,#282158,#282159,#282160,#282161,
#282162,#282163,#282164,#282165,#282166,#282167,#282168,#282169),
 .UNSPECIFIED.,.F.,.F.,(4,3,3,3,3,3,3,3,3,3,3,3,3,3,3,3,3,3,3,3,3,3,3,3,
3,3,3,3,3,3,3,3,3,3,3,3,3,3,3,3,3,3,3,3,3,3,3,3,3,3,3,3,3,3,3,3,3,3,3,3,
3,3,3,3,4),(-22.9420976703771,-22.9387243787016,-22.8332176042749,-22.7278697060081,
-22.6226456909265,-22.517487626255,-22.4123594031217,-22.3072249568909,
-22.2019785253912,-22.0966690969209,-21.9911778314761,-21.9413885361494,
-21.8358817610032,-21.7305338620323,-21.6253098462723,-21.5201517809389,
-21.4150235571609,-21.3098891103034,-21.2046426782084,-21.0993332491597,
-20.9938419831684,-20.9440526935971,-20.8385459133601,-20.7331980092675,
-20.6279739883655,-20.5228159178805,-20.417687688949,-20.3125532369439,
-20.2073067997456,-20.1019973656113,-19.9965060946152,-19.9467168510449,
-19.8412100839312,-19.7358621929697,-19.6306381851473,-19.5254801277023,
-19.4203519117524,-19.3152174726511,-19.2099710481519,-19.1046616266188,
-18.9991703679413,-18.9493810084926,-18.8438742327198,-18.7385263331949,
-18.6333023169894,-18.5281442512778,-18.4230160271889,-18.3178815800877,
-18.212635147851,-18.1073257187186,-18.0018344527325,-17.9520451659404,
-17.8465383604957,-17.741190431073,-17.635966384784,-17.5308082888913,-17.4256800345698,
-17.3205455572306,-17.2152990949553,-17.1099896358541,-17.0044983403225,
-16.9547093233881,-16.8256794531442,-16.6984772039481,-16.6589125353486),
 .UNSPECIFIED.);
#3912=B_SPLINE_CURVE_WITH_KNOTS('',3,(#282171,#282172,#282173,#282174,#282175,
#282176,#282177,#282178,#282179,#282180),.UNSPECIFIED.,.F.,.F.,(4,1,1,1,
1,1,1,4),(-16.6589123631975,-15.9573734808359,-14.9600376382837,-13.9627017957314,
-12.9653659531792,-11.9680301106269,-10.9706942680747,-10.3757270560179),
 .UNSPECIFIED.);
#3913=B_SPLINE_CURVE_WITH_KNOTS('',3,(#282181,#282182,#282183,#282184,#282185,
#282186,#282187,#282188,#282189,#282190),.UNSPECIFIED.,.F.,.F.,(4,1,1,1,
1,1,1,4),(-10.3757270560179,-9.97335842552244,-8.9760225829702,-7.97868674041795,
-6.9813508978657,-5.98401505531347,-4.98667921276122,-4.09255056054366),
 .UNSPECIFIED.);
#3914=B_SPLINE_CURVE_WITH_KNOTS('',3,(#282194,#282195,#282196,#282197,#282198,
#282199,#282200,#282201,#282202,#282203,#282204,#282205,#282206,#282207,
#282208,#282209,#282210,#282211,#282212,#282213,#282214,#282215,#282216,
#282217,#282218,#282219,#282220,#282221,#282222,#282223,#282224,#282225,
#282226,#282227,#282228,#282229,#282230,#282231,#282232,#282233,#282234,
#282235,#282236,#282237,#282238,#282239,#282240,#282241,#282242,#282243,
#282244,#282245,#282246,#282247,#282248,#282249,#282250,#282251,#282252,
#282253,#282254,#282255,#282256,#282257,#282258,#282259,#282260,#282261,
#282262,#282263,#282264,#282265,#282266,#282267,#282268,#282269,#282270,
#282271,#282272,#282273,#282274,#282275,#282276,#282277,#282278,#282279,
#282280,#282281,#282282,#282283,#282284,#282285,#282286,#282287,#282288,
#282289,#282290,#282291,#282292,#282293,#282294,#282295,#282296,#282297,
#282298,#282299,#282300,#282301,#282302,#282303,#282304,#282305,#282306,
#282307,#282308,#282309,#282310,#282311,#282312,#282313,#282314),
 .UNSPECIFIED.,.F.,.F.,(4,3,3,3,3,3,3,3,3,3,3,3,3,3,3,3,3,3,3,3,3,3,3,3,
3,3,3,3,3,3,3,3,3,3,3,3,3,3,3,3,4),(109.955742876009,110.078760970684,110.202268469162,
110.326390822107,110.351669931783,110.463583938193,110.575297619248,110.686899193039,
110.798431239825,110.909936241335,111.021537194555,111.133181961873,111.245037630442,
111.349005774335,111.460864169076,111.572528019857,111.68408329714,111.795572614607,
111.907038491634,112.018606201699,112.130220888686,112.242052138939,112.346341616887,
112.456818232952,112.567675636263,112.677845964136,112.787951966345,112.898038209298,
113.009448021833,113.119706546789,113.231692003114,113.343677459439,113.458507052372,
113.573089536432,113.687526101063,113.801851673508,113.916101021905,114.030343155428,
114.144573216633,114.258887551681,114.341013301992),.UNSPECIFIED.);
#3915=B_SPLINE_CURVE_WITH_KNOTS('',3,(#282318,#282319,#282320,#282321,#282322,
#282323,#282324,#282325,#282326,#282327,#282328,#282329,#282330,#282331,
#282332,#282333,#282334,#282335,#282336,#282337,#282338,#282339,#282340,
#282341,#282342,#282343,#282344,#282345,#282346,#282347,#282348,#282349,
#282350,#282351,#282352,#282353,#282354,#282355,#282356,#282357,#282358,
#282359,#282360,#282361,#282362,#282363,#282364,#282365,#282366,#282367,
#282368,#282369,#282370,#282371,#282372,#282373,#282374,#282375,#282376,
#282377,#282378,#282379,#282380,#282381,#282382,#282383,#282384,#282385,
#282386,#282387,#282388,#282389,#282390,#282391,#282392,#282393,#282394,
#282395,#282396,#282397,#282398,#282399,#282400,#282401,#282402),
 .UNSPECIFIED.,.F.,.F.,(4,3,3,3,3,3,3,3,3,3,3,3,3,3,3,3,3,3,3,3,3,3,3,3,
3,3,3,3,4),(109.955742875643,110.107297927009,110.219145865768,110.330798976391,
110.442343339323,110.553821588649,110.665276263946,110.776832873734,110.888436368332,
111.000257029606,111.105304897639,111.215771188973,111.326713773885,111.436873242123,
111.546968257781,111.657043400247,111.768610517253,111.878858070651,111.99108496946,
112.103311868269,112.218136295745,112.332713184882,112.447143914003,112.561463435156,
112.675706541026,112.789942338138,112.904165931924,113.018474048525,113.101318838899),
 .UNSPECIFIED.);
#3916=B_SPLINE_CURVE_WITH_KNOTS('',3,(#282404,#282405,#282406,#282407,#282408,
#282409,#282410,#282411,#282412,#282413,#282414,#282415,#282416,#282417,
#282418,#282419,#282420,#282421,#282422,#282423,#282424,#282425,#282426,
#282427,#282428,#282429,#282430,#282431,#282432,#282433,#282434,#282435,
#282436,#282437,#282438,#282439,#282440,#282441,#282442,#282443,#282444,
#282445,#282446,#282447,#282448,#282449,#282450,#282451,#282452,#282453,
#282454,#282455,#282456,#282457,#282458,#282459,#282460,#282461,#282462,
#282463,#282464,#282465,#282466,#282467,#282468,#282469,#282470,#282471,
#282472,#282473,#282474,#282475,#282476,#282477,#282478,#282479,#282480,
#282481,#282482,#282483,#282484,#282485,#282486,#282487,#282488,#282489,
#282490,#282491,#282492,#282493,#282494,#282495,#282496,#282497,#282498,
#282499,#282500,#282501,#282502,#282503,#282504,#282505,#282506,#282507,
#282508,#282509,#282510,#282511,#282512,#282513,#282514,#282515,#282516,
#282517,#282518,#282519,#282520,#282521,#282522,#282523,#282524,#282525,
#282526,#282527,#282528,#282529,#282530,#282531,#282532,#282533,#282534,
#282535,#282536,#282537,#282538,#282539,#282540,#282541,#282542,#282543,
#282544,#282545,#282546,#282547,#282548,#282549,#282550,#282551,#282552,
#282553,#282554,#282555,#282556,#282557,#282558,#282559,#282560,#282561,
#282562,#282563,#282564,#282565,#282566,#282567,#282568,#282569,#282570,
#282571,#282572,#282573,#282574,#282575,#282576,#282577,#282578,#282579,
#282580,#282581,#282582,#282583,#282584,#282585,#282586,#282587,#282588,
#282589,#282590,#282591,#282592,#282593,#282594,#282595,#282596,#282597,
#282598,#282599,#282600,#282601,#282602,#282603,#282604,#282605,#282606,
#282607,#282608,#282609,#282610,#282611,#282612,#282613,#282614,#282615,
#282616,#282617,#282618,#282619,#282620,#282621,#282622,#282623,#282624,
#282625,#282626,#282627,#282628,#282629,#282630,#282631,#282632,#282633,
#282634,#282635,#282636,#282637,#282638,#282639,#282640,#282641,#282642,
#282643,#282644,#282645,#282646,#282647,#282648,#282649,#282650,#282651,
#282652,#282653,#282654,#282655,#282656,#282657,#282658,#282659,#282660,
#282661,#282662,#282663,#282664,#282665,#282666,#282667,#282668,#282669,
#282670,#282671,#282672,#282673,#282674,#282675,#282676,#282677,#282678,
#282679,#282680,#282681,#282682,#282683,#282684,#282685,#282686,#282687,
#282688,#282689,#282690,#282691,#282692,#282693,#282694,#282695,#282696,
#282697,#282698,#282699,#282700,#282701,#282702,#282703,#282704,#282705,
#282706,#282707,#282708,#282709,#282710,#282711,#282712,#282713,#282714,
#282715,#282716,#282717,#282718,#282719,#282720,#282721,#282722,#282723,
#282724,#282725,#282726,#282727,#282728,#282729,#282730,#282731,#282732,
#282733,#282734,#282735,#282736,#282737,#282738,#282739,#282740,#282741,
#282742,#282743,#282744,#282745,#282746,#282747,#282748,#282749,#282750,
#282751,#282752,#282753,#282754,#282755,#282756,#282757,#282758,#282759,
#282760,#282761,#282762,#282763,#282764,#282765,#282766,#282767,#282768,
#282769,#282770,#282771,#282772,#282773,#282774,#282775,#282776,#282777,
#282778,#282779,#282780,#282781,#282782,#282783,#282784,#282785,#282786,
#282787,#282788,#282789,#282790,#282791,#282792,#282793,#282794,#282795,
#282796,#282797,#282798,#282799,#282800,#282801,#282802,#282803,#282804,
#282805,#282806,#282807,#282808,#282809,#282810,#282811,#282812,#282813,
#282814,#282815,#282816,#282817,#282818,#282819,#282820,#282821,#282822,
#282823,#282824,#282825,#282826,#282827,#282828,#282829,#282830,#282831,
#282832,#282833,#282834,#282835,#282836,#282837,#282838,#282839,#282840,
#282841,#282842,#282843,#282844,#282845,#282846,#282847,#282848,#282849,
#282850,#282851,#282852,#282853,#282854,#282855,#282856,#282857,#282858,
#282859),.UNSPECIFIED.,.F.,.F.,(4,2,2,2,2,2,2,2,2,2,2,2,2,2,2,2,2,2,2,2,
2,2,2,2,2,2,2,2,2,2,2,2,2,2,2,2,2,2,2,2,2,2,2,2,2,2,2,2,2,2,2,2,2,2,2,2,
2,2,2,2,2,2,2,2,2,2,2,2,2,2,2,2,2,2,2,2,2,2,2,2,2,2,2,2,2,2,2,2,2,2,2,2,
2,2,2,2,2,2,2,2,2,2,2,2,2,2,2,2,2,2,2,2,2,2,2,2,2,2,2,2,2,2,2,2,2,2,2,2,
2,2,2,2,2,2,2,2,2,2,2,2,2,2,2,2,2,2,2,2,2,2,2,2,2,2,2,2,2,2,2,2,2,2,2,2,
2,2,2,2,2,2,2,2,2,2,2,2,2,2,2,2,2,2,2,2,2,2,2,2,2,2,2,2,2,2,2,2,2,2,2,2,
2,2,2,2,2,2,2,2,2,2,2,2,2,2,2,2,2,2,2,2,2,2,2,2,2,2,2,4),(-1.96134596005299,
-1.92320411814298,-1.91683960670163,-1.91154752211252,-1.90834736782571,
-1.90543887769198,-1.9017168444316,-1.8955077480057,-1.86854562523828,-1.84488691487139,
-1.83762076146846,-1.83266440438021,-1.8305683353551,-1.83054834816283,
-1.8305282948152,-1.83050816978186,-1.83048796743229,-1.83047723424409,
-1.83046617358847,-1.83045476969429,-1.83044300574037,-1.83043086377228,
-1.83041832460025,-1.83040536769386,-1.8303919710629,-1.83037811111419,
-1.8303637625119,-1.83034889800978,-1.83033348826399,-1.83031750162281,
-1.83030090390035,-1.83028365811244,-1.83026572417907,-1.83024705859217,
-1.83022761404223,-1.83020733898793,-1.83018617716757,-1.8301640670428,
-1.83014094116354,-1.83011672543508,-1.8300913382757,-1.83006468964201,
-1.8284526754288,-1.8264457735443,-1.82235816897249,-1.79077011051556,-1.76553775262294,
-1.7573219564942,-1.7535727113588,-1.75069959681956,-1.7475469720678,-1.74235672037468,
-1.72233557364014,-1.69064080275324,-1.68234815384251,-1.67680439251776,
-1.67454359080352,-1.672913372592,-1.67108432296876,-1.66789420722315,-1.65411530591151,
-1.62545396231887,-1.60438173959295,-1.59923069395448,-1.59606587313137,
-1.59315723073407,-1.58938973360294,-1.58096195077707,-1.54495366279498,
-1.52530106324672,-1.52081365134075,-1.51871775183872,-1.51724866878963,
-1.51536381669079,-1.51201245900382,-1.49263831275019,-1.48758275217834,
-1.46794352165621,-1.45518117515106,-1.44622697242567,-1.4423342171477,
-1.43942190336144,-1.43629335230179,-1.43129169887772,-1.41443617471032,
-1.38513100777365,-1.37323544586131,-1.3683748068879,-1.36465257411225,
-1.3627117363032,-1.36109385065202,-1.35900075764574,-1.35465118897059,
-1.32723765149952,-1.30478008218077,-1.29178536072229,-1.28733172389266,
-1.28432061417718,-1.28138232148989,-1.27714935568482,-1.26672976101249,
-1.23273668958479,-1.2137184958182,-1.2093041504301,-1.20722865585897,-1.20576671583297,
-1.20387967849958,-1.20051222910936,-1.17868971868284,-1.17659051577337,
-1.14186610322758,-1.13409856059281,-1.13041214099272,-1.12752713146479,
-1.12429928864984,-1.11883185221412,-1.09220395502573,-1.06667295278604,
-1.05914007867478,-1.05396336572059,-1.05175042698459,-1.05011892086801,
-1.04825318713209,-1.04498085825219,-1.02898871799472,-0.996616895159001,
-0.980943092646712,-0.976205412111835,-0.973133641184649,-0.970197213592707,
-0.966149980218765,-0.956214815899105,-0.941425004060726,-0.923686718167545,
-0.900710994671843,-0.897327138519964,-0.895436764250386,-0.893974657300571,
-0.891902557989352,-0.887512298108303,-0.868735901791538,-0.835412908052433,
-0.824331509882609,-0.820005022489831,-0.8173158869,-0.814366000101075,
-0.8102403063064,-0.799773677160084,-0.783812236608273,-0.772087606614392,
-0.74671145522867,-0.742226637015615,-0.7401369405901,-0.738518476175967,
-0.736573031478298,-0.732829523300687,-0.727933229471062,-0.715900061524462,
-0.67691320999565,-0.667876299797195,-0.664259528026053,-0.661573746803908,
-0.658619895335551,-0.654474104214096,-0.643870446319955,-0.627598025377892,
-0.593054935535115,-0.587229332565578,-0.584849714896073,-0.583209210877953,
-0.581426327958067,-0.57844639534849,-0.566334662512619,-0.543561334604584,
-0.515213800786896,-0.509759190580938,-0.506535156382603,-0.503651296299562,
-0.499963285314192,-0.492180791509951,-0.463448410858983,-0.435129406120473,
-0.431168188777623,-0.429155087072102,-0.427512559855908,-0.425734241837209,
-0.422775021685134,-0.410950629736337,-0.387947923476124,-0.359499752004406,
-0.35404536501043,-0.350821380343177,-0.347937515683542,-0.344249432177406,
-0.336466524525731,-0.307509024143815,-0.279457032055029,-0.275095941456518,
-0.273021642336195,-0.271401699031108,-0.269470904834471,-0.26579869581264,
-0.241155611606478,-0.205636410784264,-0.199760925546063,-0.196104923614451,
-0.193224380626739,-0.18998134330574,-0.184437572184014,-0.17767642811731,
-0.162955529927346,-0.136600262176787,-0.121814639214398,-0.118576745758897,
-0.11673775303086,-0.115100380215487,-0.112839316114304,-0.107683100981236,
-0.0953527260318766,-0.065440740316503,-0.0473873156799378,-0.0422936227695306,
-0.0391465356797224,-0.0362428866832389,-0.0334015628955676,-0.029664141270674,
-0.0204810725935979,-0.000463005431037473),.UNSPECIFIED.);
#3917=B_SPLINE_CURVE_WITH_KNOTS('',3,(#282861,#282862,#282863,#282864,#282865,
#282866,#282867,#282868,#282869,#282870,#282871,#282872,#282873,#282874,
#282875,#282876,#282877,#282878,#282879,#282880,#282881,#282882,#282883,
#282884,#282885,#282886,#282887,#282888,#282889,#282890,#282891,#282892,
#282893,#282894,#282895,#282896,#282897,#282898,#282899,#282900,#282901,
#282902,#282903,#282904,#282905,#282906,#282907,#282908,#282909,#282910,
#282911,#282912,#282913,#282914,#282915,#282916,#282917,#282918,#282919,
#282920,#282921,#282922,#282923,#282924,#282925,#282926,#282927,#282928,
#282929,#282930,#282931,#282932,#282933,#282934,#282935,#282936,#282937,
#282938,#282939,#282940,#282941,#282942,#282943,#282944,#282945,#282946,
#282947,#282948,#282949,#282950,#282951,#282952,#282953,#282954,#282955,
#282956,#282957,#282958,#282959,#282960,#282961,#282962,#282963,#282964,
#282965,#282966,#282967,#282968,#282969,#282970,#282971,#282972,#282973,
#282974,#282975,#282976,#282977,#282978,#282979,#282980,#282981,#282982,
#282983,#282984,#282985,#282986,#282987,#282988,#282989,#282990,#282991,
#282992,#282993,#282994,#282995,#282996,#282997,#282998,#282999,#283000,
#283001,#283002,#283003,#283004,#283005,#283006,#283007,#283008,#283009,
#283010,#283011,#283012,#283013,#283014,#283015,#283016,#283017,#283018,
#283019,#283020,#283021,#283022,#283023,#283024,#283025,#283026,#283027,
#283028,#283029,#283030,#283031,#283032,#283033,#283034,#283035,#283036,
#283037,#283038,#283039,#283040,#283041,#283042,#283043,#283044,#283045,
#283046,#283047,#283048,#283049,#283050,#283051,#283052,#283053,#283054,
#283055,#283056,#283057,#283058,#283059,#283060,#283061,#283062,#283063,
#283064,#283065,#283066,#283067,#283068,#283069,#283070,#283071,#283072,
#283073,#283074,#283075,#283076,#283077,#283078,#283079,#283080,#283081,
#283082,#283083,#283084,#283085,#283086,#283087,#283088,#283089,#283090,
#283091,#283092,#283093,#283094,#283095,#283096,#283097,#283098,#283099,
#283100,#283101,#283102,#283103,#283104,#283105,#283106,#283107,#283108,
#283109,#283110,#283111,#283112,#283113,#283114,#283115,#283116,#283117,
#283118,#283119,#283120,#283121,#283122,#283123,#283124,#283125,#283126,
#283127,#283128,#283129,#283130,#283131,#283132,#283133,#283134,#283135,
#283136,#283137,#283138,#283139,#283140,#283141,#283142,#283143,#283144,
#283145,#283146,#283147,#283148,#283149,#283150,#283151,#283152,#283153,
#283154,#283155,#283156,#283157,#283158,#283159,#283160,#283161,#283162,
#283163,#283164,#283165,#283166,#283167,#283168,#283169,#283170,#283171,
#283172,#283173,#283174,#283175,#283176,#283177,#283178,#283179,#283180,
#283181,#283182,#283183,#283184,#283185,#283186,#283187,#283188,#283189,
#283190,#283191,#283192,#283193,#283194,#283195,#283196,#283197,#283198,
#283199,#283200,#283201,#283202,#283203,#283204,#283205,#283206,#283207,
#283208,#283209,#283210,#283211,#283212,#283213,#283214,#283215,#283216,
#283217,#283218,#283219,#283220,#283221,#283222,#283223,#283224,#283225,
#283226,#283227,#283228,#283229,#283230,#283231,#283232,#283233,#283234,
#283235,#283236,#283237,#283238,#283239,#283240,#283241,#283242,#283243,
#283244,#283245,#283246,#283247,#283248,#283249,#283250,#283251,#283252,
#283253,#283254,#283255,#283256,#283257,#283258,#283259,#283260,#283261,
#283262,#283263,#283264,#283265,#283266,#283267,#283268,#283269,#283270),
 .UNSPECIFIED.,.F.,.F.,(4,2,2,2,2,2,2,2,2,2,2,2,2,2,2,2,2,2,2,2,2,2,2,2,
2,2,2,2,2,2,2,2,2,2,2,2,2,2,2,2,2,2,2,2,2,2,2,2,2,2,2,2,2,2,2,2,2,2,2,2,
2,2,2,2,2,2,2,2,2,2,2,2,2,2,2,2,2,2,2,2,2,2,2,2,2,2,2,2,2,2,2,2,2,2,2,2,
2,2,2,2,2,2,2,2,2,2,2,2,2,2,2,2,2,2,2,2,2,2,2,2,2,2,2,2,2,2,2,2,2,2,2,2,
2,2,2,2,2,2,2,2,2,2,2,2,2,2,2,2,2,2,2,2,2,2,2,2,2,2,2,2,2,2,2,2,2,2,2,2,
2,2,2,2,2,2,2,2,2,2,2,2,2,2,2,2,2,2,2,2,2,2,2,2,2,2,2,2,2,2,2,2,2,2,2,2,
4),(-1.96120734884475,-1.9329238431295,-1.92667649358171,-1.92437579718932,
-1.92229554106251,-1.9208322559288,-1.91894674504486,-1.91558579958792,
-1.89528526779122,-1.87075070958967,-1.858404189914,-1.84972955769284,-1.84639177994775,
-1.84626159504513,-1.84330472034741,-1.84062121064667,-1.83633017915434,
-1.82548973911512,-1.79188859446564,-1.77303102016817,-1.76863157585871,
-1.76655737062743,-1.76509469171669,-1.76320480983605,-1.75982450482497,
-1.73702634591811,-1.7206009200413,-1.70491571735483,-1.69457053622545,
-1.69046174975455,-1.68751414035074,-1.6848204109009,-1.68117215023371,
-1.67194460135601,-1.6367915999586,-1.61738290890347,-1.61292578684856,
-1.61084073384937,-1.60937677950044,-1.60749420773741,-1.60414694482114,
-1.58488300835589,-1.57970580741659,-1.56010318720656,-1.5472847507949,
-1.53830134796716,-1.53440425422268,-1.53149184037439,-1.52836618116202,
-1.52337576495278,-1.50662913013879,-1.47727856090541,-1.46536708414599,
-1.46050209442759,-1.45677709057786,-1.45483513064317,-1.45321573506028,
-1.45111997344099,-1.44676426747682,-1.41940490170312,-1.38976620635212,
-1.38198121136441,-1.37829205976953,-1.37540729993235,-1.37218224883767,
-1.36672592128419,-1.34027543909824,-1.31453990499003,-1.30697708430465,
-1.30178545639366,-1.29957059756044,-1.29793924070412,-1.29607523132558,
-1.29281081948795,-1.27696416726496,-1.24444733640245,-1.23396687477194,
-1.22621395142566,-1.22253070620007,-1.21964663969088,-1.21641829728009,
-1.21094630695213,-1.18311210488112,-1.16224886602917,-1.15260080918932,
-1.14641719771057,-1.14404695780121,-1.14239155104824,-1.14059925148802,
-1.13757750717473,-1.12633829925246,-1.10054391131459,-1.07425651506294,
-1.06887963822924,-1.06567162317512,-1.06278356410061,-1.05906428590169,
-1.05297115287619,-1.02111195357638,-1.0013550692677,-0.994760077100172,
-0.99006839098625,-0.987940449308012,-0.98631864991227,-0.98440053068455,
-0.980893014534244,-0.97632415142728,-0.96551627018509,-0.945661041918234,
-0.918736154539604,-0.913242132500549,-0.910009144249384,-0.907125986544771,
-0.903450860705764,-0.895742150169642,-0.871074096063297,-0.841490466330516,
-0.83514536694182,-0.832681400236937,-0.831025145846189,-0.829270101650238,
-0.826418642658594,-0.815961227994418,-0.793624806352471,-0.765301062795747,
-0.759142627897215,-0.75544464476572,-0.752551466028968,-0.749364887114753,
-0.74408873931067,-0.720431312819312,-0.704612959536957,-0.683027746355497,
-0.678507793107124,-0.676433296073625,-0.67481299648718,-0.672881537754907,
-0.669207363183667,-0.644521082435461,-0.60904438395258,-0.603161725466596,
-0.599503219248634,-0.596621883103081,-0.593379192026751,-0.587839148554125,
-0.581084255662564,-0.566386363253881,-0.548560040894815,-0.525525655533315,
-0.522139797522101,-0.520248673530019,-0.51878614718332,-0.516713646364208,
-0.512323367469958,-0.493553197717968,-0.46025074687675,-0.449140509524315,
-0.444808905899923,-0.442118252962409,-0.439168014203132,-0.435044290600442,
-0.424596762445513,-0.408680132398467,-0.395862891421224,-0.371586283713681,
-0.367044232170259,-0.364965811513034,-0.363345303031543,-0.361417090005063,
-0.357758227958913,-0.333559770008304,-0.297465914562447,-0.291641819487452,
-0.28800049790867,-0.285121041270967,-0.281868162201887,-0.276279389102895,
-0.269448017855639,-0.254489214986801,-0.243075181732033,-0.21564181305878,
-0.211289441117452,-0.209194544093134,-0.207575456175351,-0.205633407976656,
-0.201907048880401,-0.197040053874561,-0.185119963380706,-0.147163725848762,
-0.137243040984035,-0.13309388499212,-0.130168654657908,-0.127300833839552,
-0.123054100396915,-0.118101053692855,-0.108902262384983,-0.0841889471967438,
-0.0600742653719997,-0.0555597355545908,-0.053464273600083,-0.0518452179885775,
-0.0499037740630693,-0.0461800909815272,-0.0413175708434384,-0.000460996019999361),
 .UNSPECIFIED.);
#3918=B_SPLINE_CURVE_WITH_KNOTS('',3,(#283272,#283273,#283274,#283275,#283276,
#283277,#283278,#283279,#283280,#283281),.UNSPECIFIED.,.F.,.F.,(4,1,1,1,
1,1,1,4),(78.5398163397448,79.169081837476,80.1670888081061,81.1650957787362,
82.1631027493663,83.1611097199964,84.1591166906264,84.8230016469244),
 .UNSPECIFIED.);
#3919=B_SPLINE_CURVE_WITH_KNOTS('',3,(#283283,#283284,#283285,#283286,#283287,
#283288,#283289,#283290,#283291,#283292,#283293,#283294,#283295,#283296,
#283297,#283298,#283299,#283300,#283301,#283302,#283303,#283304,#283305,
#283306,#283307,#283308,#283309,#283310,#283311,#283312,#283313,#283314,
#283315,#283316,#283317,#283318,#283319,#283320,#283321,#283322,#283323,
#283324,#283325,#283326,#283327,#283328,#283329,#283330,#283331,#283332,
#283333,#283334,#283335,#283336,#283337,#283338,#283339,#283340,#283341,
#283342,#283343,#283344,#283345,#283346,#283347,#283348,#283349,#283350,
#283351,#283352,#283353,#283354,#283355,#283356,#283357,#283358,#283359,
#283360,#283361,#283362,#283363,#283364,#283365,#283366,#283367,#283368,
#283369,#283370,#283371,#283372,#283373,#283374,#283375,#283376,#283377,
#283378,#283379,#283380,#283381,#283382,#283383,#283384,#283385,#283386,
#283387,#283388,#283389,#283390,#283391,#283392,#283393,#283394,#283395,
#283396,#283397,#283398,#283399,#283400,#283401,#283402,#283403,#283404,
#283405,#283406,#283407,#283408,#283409,#283410,#283411,#283412,#283413,
#283414,#283415,#283416,#283417,#283418,#283419,#283420,#283421,#283422,
#283423,#283424,#283425,#283426,#283427,#283428,#283429,#283430,#283431,
#283432,#283433,#283434,#283435,#283436,#283437,#283438,#283439,#283440,
#283441,#283442,#283443,#283444,#283445,#283446,#283447,#283448,#283449,
#283450,#283451,#283452,#283453,#283454,#283455,#283456,#283457,#283458,
#283459,#283460,#283461,#283462,#283463,#283464,#283465,#283466,#283467,
#283468,#283469,#283470,#283471,#283472,#283473,#283474,#283475,#283476,
#283477,#283478,#283479,#283480,#283481,#283482,#283483,#283484,#283485,
#283486,#283487,#283488,#283489,#283490,#283491,#283492,#283493,#283494,
#283495,#283496,#283497,#283498,#283499,#283500,#283501,#283502,#283503,
#283504,#283505,#283506,#283507,#283508,#283509,#283510,#283511,#283512,
#283513,#283514,#283515,#283516,#283517,#283518,#283519,#283520,#283521,
#283522,#283523,#283524,#283525,#283526,#283527,#283528,#283529,#283530,
#283531,#283532,#283533,#283534,#283535,#283536,#283537,#283538,#283539,
#283540,#283541,#283542,#283543,#283544,#283545,#283546,#283547,#283548,
#283549,#283550,#283551,#283552,#283553,#283554,#283555,#283556,#283557,
#283558,#283559,#283560,#283561,#283562,#283563,#283564,#283565,#283566,
#283567,#283568,#283569,#283570,#283571,#283572,#283573,#283574,#283575,
#283576,#283577,#283578,#283579,#283580,#283581,#283582,#283583,#283584,
#283585,#283586,#283587,#283588,#283589,#283590,#283591,#283592,#283593,
#283594,#283595,#283596,#283597,#283598,#283599,#283600,#283601,#283602,
#283603,#283604,#283605,#283606,#283607,#283608,#283609,#283610,#283611,
#283612,#283613,#283614,#283615,#283616,#283617,#283618,#283619,#283620,
#283621,#283622,#283623,#283624,#283625,#283626,#283627,#283628,#283629,
#283630,#283631,#283632,#283633,#283634,#283635,#283636,#283637,#283638,
#283639,#283640,#283641,#283642,#283643,#283644,#283645,#283646,#283647,
#283648,#283649,#283650,#283651,#283652,#283653,#283654,#283655,#283656,
#283657,#283658,#283659,#283660,#283661,#283662,#283663,#283664,#283665,
#283666,#283667,#283668,#283669,#283670,#283671,#283672,#283673,#283674,
#283675,#283676,#283677,#283678,#283679,#283680),.UNSPECIFIED.,.F.,.F.,
(4,2,2,2,2,2,2,2,2,2,2,2,2,2,2,2,2,2,2,2,2,2,2,2,2,2,2,2,2,2,2,2,2,2,2,
2,2,2,2,2,2,2,2,2,2,2,2,2,2,2,2,2,2,2,2,2,2,2,2,2,2,2,2,2,2,2,2,2,2,2,2,
2,2,2,2,2,2,2,2,2,2,2,2,2,2,2,2,2,2,2,2,2,2,2,2,2,2,2,2,2,2,2,2,2,2,2,2,
2,2,2,2,2,2,2,2,2,2,2,2,2,2,2,2,2,2,2,2,2,2,2,2,2,2,2,2,2,2,2,2,2,2,2,2,
2,2,2,2,2,2,2,2,2,2,2,2,2,2,2,2,2,2,2,2,2,2,2,2,2,2,2,2,2,2,2,2,2,2,2,2,
2,2,2,2,2,2,2,2,2,2,2,2,2,2,2,2,2,2,2,4),(-1.96053344110796,-1.92968691991721,
-1.91055048298032,-1.9061233569176,-1.90404479251844,-1.90258244773755,
-1.90069779644516,-1.8973375922818,-1.87680523446693,-1.87327167107956,
-1.85418214867251,-1.8408864322038,-1.8345579053475,-1.82939170057257,-1.82629969095901,
-1.82342075636068,-1.81977005791869,-1.81390988454385,-1.77835081058486,
-1.75371236266834,-1.75004111098677,-1.74811099150082,-1.74649168130467,
-1.7444183129971,-1.74005959929675,-1.71204237086999,-1.68310623896729,
-1.67532824260053,-1.67164188121702,-1.66875908154425,-1.66553599262994,
-1.66008241713623,-1.63162998100072,-1.60878814014973,-1.59681474923814,
-1.59384532603972,-1.59206517123355,-1.59042440456851,-1.58841699201733,
-1.58447736675957,-1.55601993420657,-1.52378918607622,-1.51822077307732,
-1.51497326955132,-1.512094696404,-1.50844925016096,-1.50260754357464,-1.46671018031895,
-1.44235617054664,-1.43869350815066,-1.43676508763112,-1.43514548593234,
-1.43306960517091,-1.42853813690989,-1.40440840912775,-1.39146520843914,
-1.3755724574329,-1.36513622663663,-1.36101542405418,-1.35806675013848,
-1.35537715315105,-1.35104647533156,-1.33993434429303,-1.30662967220022,
-1.28785849459179,-1.28346924633632,-1.28139750231834,-1.27993563376905,
-1.27804549422379,-1.27466177658614,-1.25166553042387,-1.23388155478177,
-1.21917685810568,-1.21242086750445,-1.20688018125452,-1.20363825483928,
-1.20075827178417,-1.19710240314383,-1.19122585714207,-1.15568935744395,
-1.13104368380562,-1.12737159440556,-1.12544105418401,-1.12382140297389,
-1.12174761293088,-1.11722867233391,-1.09558589047466,-1.07889449441558,
-1.05615242282734,-1.05092141569482,-1.04774530483463,-1.04485088081463,
-1.04113644247854,-1.03491660320841,-0.992881609056747,-0.980516681571756,
-0.973322320459725,-0.97073603936278,-0.969207064900069,-0.967521704837486,
-0.964993002647571,-0.957635423444112,-0.945193217524613,-0.902400787269249,
-0.896676202592614,-0.893064449631609,-0.890188322231025,-0.886917760668263,
-0.881243057487627,-0.849897868629513,-0.820575568563779,-0.816285649517556,
-0.814232451991065,-0.812615816908899,-0.810640167180081,-0.806746982981803,
-0.801593809440625,-0.788549094180412,-0.769688744013373,-0.745032078909484,
-0.739621408125712,-0.736406787311403,-0.73352115535427,-0.729816700180218,
-0.72194340273459,-0.692826781674622,-0.665061920254774,-0.660709072641957,
-0.658614266361268,-0.656995406923766,-0.655053823780055,-0.651328869454544,
-0.646464040368877,-0.634551228080059,-0.605242686934453,-0.588513660487068,
-0.583526109240286,-0.580401688567089,-0.57749004337316,-0.57359339637715,
-0.564608479708384,-0.551783716664436,-0.532176321192252,-0.527005388685896,
-0.50772942322851,-0.504382406394867,-0.502500226444007,-0.501036709486796,
-0.498952495664981,-0.494497897133751,-0.47510710521946,-0.439988492359812,
-0.430762670675787,-0.427115327223792,-0.424422323470096,-0.421475552260034,
-0.41736805191031,-0.407027134631118,-0.391347383462544,-0.374784108578653,
-0.352087157175161,-0.348709627024167,-0.346820662192318,-0.345358274082086,
-0.343283979781338,-0.338882359007789,-0.319998818633091,-0.286364937514228,
-0.275616144597339,-0.271337275188286,-0.268656345957405,-0.265698234391899,
-0.261528094469031,-0.250751902030441,-0.23408236340897,-0.197916109022278,
-0.193971042477316,-0.191961934443897,-0.190320371532765,-0.188540085133019,
-0.185571875607219,-0.173623607312659,-0.150780945848837,-0.122315025128356,
-0.116860965390557,-0.113637054324961,-0.11075318059271,-0.107064979995398,
-0.0994980728488588,-0.0794121500077125,-0.0578724433652814,-0.0405361975418842,
-0.0372412699647678,-0.035370758717511,-0.0337414912643039,-0.0321250789126551,
-0.0299549206399665,-0.0263828312756159,-0.000460541927694245),
 .UNSPECIFIED.);
#3920=B_SPLINE_CURVE_WITH_KNOTS('',3,(#283682,#283683,#283684,#283685,#283686,
#283687,#283688,#283689,#283690,#283691),.UNSPECIFIED.,.F.,.F.,(4,1,1,1,
1,1,1,4),(59.690260418206,60.2069493955043,61.2049563661344,62.2029633367645,
63.2009703073946,64.1989772780247,65.1969842486548,65.9734446845719),
 .UNSPECIFIED.);
#3921=B_SPLINE_CURVE_WITH_KNOTS('',3,(#283693,#283694,#283695,#283696,#283697,
#283698,#283699,#283700,#283701,#283702,#283703,#283704,#283705,#283706,
#283707,#283708,#283709,#283710,#283711,#283712,#283713,#283714,#283715,
#283716,#283717,#283718,#283719,#283720,#283721,#283722,#283723,#283724,
#283725,#283726,#283727,#283728,#283729,#283730,#283731,#283732,#283733,
#283734,#283735,#283736,#283737,#283738,#283739,#283740,#283741,#283742,
#283743,#283744,#283745,#283746,#283747,#283748,#283749,#283750,#283751,
#283752,#283753,#283754,#283755,#283756,#283757,#283758,#283759,#283760,
#283761,#283762,#283763,#283764,#283765,#283766,#283767,#283768,#283769,
#283770,#283771,#283772,#283773,#283774,#283775,#283776,#283777,#283778,
#283779,#283780,#283781,#283782,#283783,#283784,#283785,#283786,#283787,
#283788,#283789,#283790,#283791,#283792,#283793,#283794,#283795,#283796,
#283797,#283798,#283799,#283800,#283801,#283802,#283803,#283804,#283805,
#283806,#283807,#283808,#283809,#283810,#283811,#283812,#283813,#283814,
#283815,#283816,#283817,#283818,#283819,#283820,#283821,#283822,#283823,
#283824,#283825,#283826,#283827,#283828,#283829,#283830,#283831,#283832,
#283833,#283834,#283835,#283836,#283837,#283838,#283839,#283840,#283841,
#283842,#283843,#283844,#283845,#283846,#283847,#283848,#283849,#283850,
#283851,#283852,#283853,#283854,#283855,#283856,#283857,#283858,#283859,
#283860,#283861,#283862,#283863,#283864,#283865,#283866,#283867,#283868,
#283869,#283870,#283871,#283872,#283873,#283874,#283875,#283876,#283877,
#283878,#283879,#283880,#283881,#283882,#283883,#283884,#283885,#283886,
#283887,#283888,#283889,#283890,#283891,#283892,#283893,#283894,#283895,
#283896,#283897,#283898,#283899,#283900,#283901,#283902,#283903,#283904,
#283905,#283906,#283907,#283908,#283909,#283910,#283911,#283912,#283913,
#283914,#283915,#283916,#283917,#283918,#283919,#283920,#283921,#283922,
#283923,#283924,#283925,#283926,#283927,#283928,#283929,#283930,#283931,
#283932,#283933,#283934,#283935,#283936,#283937,#283938,#283939,#283940,
#283941,#283942,#283943,#283944,#283945,#283946,#283947,#283948,#283949,
#283950,#283951,#283952,#283953,#283954,#283955,#283956,#283957,#283958,
#283959,#283960,#283961,#283962,#283963,#283964,#283965,#283966,#283967,
#283968,#283969,#283970,#283971,#283972,#283973,#283974,#283975,#283976,
#283977,#283978,#283979,#283980,#283981,#283982,#283983,#283984,#283985,
#283986,#283987,#283988,#283989,#283990,#283991,#283992,#283993,#283994,
#283995,#283996,#283997,#283998,#283999,#284000,#284001,#284002,#284003,
#284004,#284005,#284006,#284007,#284008,#284009,#284010,#284011,#284012,
#284013,#284014,#284015,#284016,#284017,#284018,#284019,#284020,#284021,
#284022,#284023,#284024,#284025,#284026,#284027,#284028,#284029,#284030,
#284031,#284032,#284033,#284034,#284035,#284036,#284037,#284038,#284039,
#284040,#284041,#284042,#284043,#284044,#284045,#284046,#284047,#284048,
#284049,#284050,#284051,#284052,#284053,#284054,#284055,#284056,#284057,
#284058,#284059,#284060,#284061,#284062,#284063,#284064,#284065,#284066,
#284067,#284068,#284069,#284070,#284071,#284072,#284073,#284074,#284075,
#284076,#284077,#284078,#284079,#284080,#284081,#284082,#284083,#284084,
#284085,#284086,#284087,#284088,#284089,#284090,#284091,#284092,#284093,
#284094,#284095,#284096,#284097,#284098,#284099,#284100,#284101,#284102,
#284103,#284104),.UNSPECIFIED.,.F.,.F.,(4,2,2,2,2,2,2,2,2,2,2,2,2,2,2,2,
2,2,2,2,2,2,2,2,2,2,2,2,2,2,2,2,2,2,2,2,2,2,2,2,2,2,2,2,2,2,2,2,2,2,2,2,
2,2,2,2,2,2,2,2,2,2,2,2,2,2,2,2,2,2,2,2,2,2,2,2,2,2,2,2,2,2,2,2,2,2,2,2,
2,2,2,2,2,2,2,2,2,2,2,2,2,2,2,2,2,2,2,2,2,2,2,2,2,2,2,2,2,2,2,2,2,2,2,2,
2,2,2,2,2,2,2,2,2,2,2,2,2,2,2,2,2,2,2,2,2,2,2,2,2,2,2,2,2,2,2,2,2,2,2,2,
2,2,2,2,2,2,2,2,2,2,2,2,2,2,2,2,2,2,2,2,2,2,2,2,2,2,2,2,2,2,2,2,2,2,2,2,
2,2,2,2,2,2,2,2,2,4),(-1.96074350940351,-1.95917447291995,-1.95671350899246,
-1.94917971597731,-1.9123925266757,-1.89311953730399,-1.88867772530256,
-1.88659617447291,-1.88513325318232,-1.88325000330616,-1.87989707818968,
-1.86021508902107,-1.85565788050471,-1.83417429114077,-1.81640260314938,
-1.81148585030099,-1.80858850085177,-1.80580320003331,-1.80218623979858,
-1.79619319774473,-1.7546613312234,-1.74169159403833,-1.73655724866933,
-1.73267538131483,-1.73070211953118,-1.72908554107684,-1.72703002277448,
-1.72272726540563,-1.68625913422958,-1.6697436318915,-1.65903354735689,
-1.65487311476724,-1.65191702120589,-1.64923465828054,-1.6449464184678,
-1.63411842085676,-1.60053701930469,-1.58166875780566,-1.57726901045711,
-1.57519517584489,-1.57373296221407,-1.57184397045185,-1.56846590006631,
-1.54572604942813,-1.52924529754197,-1.51357087721261,-1.50323167493191,
-1.49912466078596,-1.49617813313554,-1.49348526375511,-1.48983797129163,
-1.48061177479173,-1.44547268545429,-1.42607126636259,-1.42161574201211,
-1.41953142090873,-1.41806797352049,-1.41618604331374,-1.41283990395091,
-1.39358117315324,-1.38840933545866,-1.36882032484893,-1.35600105900136,
-1.34701811294616,-1.34312192484604,-1.34021044547451,-1.33708603224572,
-1.33209813922853,-1.31536587757116,-1.28602072579389,-1.27410972418891,
-1.26924546000267,-1.26552117884254,-1.26357977143758,-1.26196094169405,
-1.25986604720019,-1.25551257973577,-1.22777146655256,-1.19866775938329,
-1.19079681751974,-1.18709282121814,-1.18420725129045,-1.18099239425393,
-1.17558060751334,-1.15091073900901,-1.1320361621118,-1.11898345585879,
-1.1138282941744,-1.10993429807784,-1.1079584888374,-1.10634185863982,-1.10428885071513,
-1.09999991071284,-1.07069075437743,-1.03955247366408,-1.03377503037985,
-1.03048274832177,-1.02760910375651,-1.02402883787984,-1.01841144528615,
-0.980410374922927,-0.957312790550657,-0.95392592017682,-0.952034821866809,
-0.950572677672377,-0.948501188441025,-0.944114828961308,-0.925376622040968,
-0.892161204092339,-0.880969872546063,-0.876626824199373,-0.873934579839489,
-0.870986969423271,-0.866875158207545,-0.856505359834304,-0.840761372636222,
-0.824980595245874,-0.803373863511543,-0.798854607160077,-0.796758439663589,
-0.79513953068634,-0.793199096555113,-0.789479583626837,-0.784623950701396,
-0.772746093684703,-0.743482809889265,-0.72667254251809,-0.72167751879759,
-0.718551566518469,-0.715640624324773,-0.711748156980437,-0.702788166667672,
-0.690012843158084,-0.670343170482305,-0.665134576215712,-0.64587485113954,
-0.642528239631406,-0.640646182212771,-0.639182694857536,-0.637098437638912,
-0.63264341572802,-0.613247852626881,-0.57811438205515,-0.568904083926527,
-0.565259279867758,-0.562566942292256,-0.559619729492917,-0.555509412826898,
-0.545148782655604,-0.529424840992287,-0.513393198679142,-0.490255315052111,
-0.486867578267891,-0.484976369989036,-0.483514369737414,-0.48144338148785,
-0.477059204685858,-0.458339913499957,-0.425177129599025,-0.413933848114941,
-0.409583321247437,-0.406889895550808,-0.403943722547694,-0.399839046094038,
-0.389516617206656,-0.373877735092742,-0.356901291671155,-0.334545045826474,
-0.331173114948465,-0.329285447512543,-0.327822933834425,-0.325746992975945,
-0.321336291244035,-0.302365482093407,-0.268478462984107,-0.258005506977063,
-0.253761583633471,-0.250819395282126,-0.247807269615527,-0.243357640616498,
-0.230416660739951,-0.208119895793539,-0.180453673722901,-0.176105372189886,
-0.174011572819604,-0.172392906147713,-0.170450847870261,-0.166723085733385,
-0.161853363487741,-0.149921257428941,-0.120589127597403,-0.103909377824713,
-0.0989267546882721,-0.0958035579980236,-0.0928917903425926,-0.0889930553048363,
-0.0799942084884878,-0.0416492524753233,-0.0266198591389201,-0.0210409164424102,
-0.0189262818004382,-0.0174077763562326,-0.0158946722602569,-0.0142038132499826,
-0.0118325809587982,-0.000460124348572881),.UNSPECIFIED.);
#3922=B_SPLINE_CURVE_WITH_KNOTS('',3,(#284106,#284107,#284108,#284109,#284110,
#284111,#284112,#284113,#284114,#284115),.UNSPECIFIED.,.F.,.F.,(4,1,1,1,
1,1,1,4),(40.840710987977,41.2448169535326,42.2428239241627,43.2408308947928,
44.2388378654229,45.236844836053,46.2348518066831,47.123880997786),
 .UNSPECIFIED.);
#3923=B_SPLINE_CURVE_WITH_KNOTS('',3,(#284117,#284118,#284119,#284120,#284121,
#284122,#284123,#284124,#284125,#284126,#284127,#284128,#284129,#284130,
#284131,#284132,#284133,#284134,#284135,#284136,#284137,#284138,#284139,
#284140,#284141,#284142,#284143,#284144,#284145,#284146,#284147,#284148,
#284149,#284150,#284151,#284152,#284153,#284154,#284155,#284156,#284157,
#284158,#284159,#284160,#284161,#284162,#284163,#284164,#284165,#284166,
#284167,#284168,#284169,#284170,#284171,#284172,#284173,#284174,#284175,
#284176,#284177,#284178,#284179,#284180,#284181,#284182,#284183,#284184,
#284185,#284186,#284187,#284188,#284189,#284190,#284191,#284192,#284193,
#284194,#284195,#284196,#284197,#284198,#284199,#284200,#284201,#284202,
#284203,#284204,#284205,#284206,#284207,#284208,#284209,#284210,#284211,
#284212,#284213,#284214,#284215,#284216,#284217,#284218,#284219,#284220,
#284221,#284222,#284223,#284224,#284225,#284226,#284227,#284228,#284229,
#284230,#284231,#284232,#284233,#284234,#284235,#284236,#284237,#284238,
#284239,#284240,#284241,#284242,#284243,#284244,#284245,#284246,#284247,
#284248,#284249,#284250,#284251,#284252,#284253,#284254,#284255,#284256,
#284257,#284258,#284259,#284260,#284261,#284262,#284263,#284264,#284265,
#284266,#284267,#284268,#284269,#284270,#284271,#284272,#284273,#284274,
#284275,#284276,#284277,#284278,#284279,#284280,#284281,#284282,#284283,
#284284,#284285,#284286,#284287,#284288,#284289,#284290,#284291,#284292,
#284293,#284294,#284295,#284296,#284297,#284298,#284299,#284300,#284301,
#284302,#284303,#284304,#284305,#284306,#284307,#284308,#284309,#284310,
#284311,#284312,#284313,#284314,#284315,#284316,#284317,#284318,#284319,
#284320,#284321,#284322,#284323,#284324,#284325,#284326,#284327,#284328,
#284329,#284330,#284331,#284332,#284333,#284334,#284335,#284336,#284337,
#284338,#284339,#284340,#284341,#284342,#284343,#284344,#284345,#284346,
#284347,#284348,#284349,#284350,#284351,#284352,#284353,#284354,#284355,
#284356,#284357,#284358,#284359,#284360,#284361,#284362,#284363,#284364,
#284365,#284366,#284367,#284368,#284369,#284370,#284371,#284372,#284373,
#284374,#284375,#284376,#284377,#284378,#284379,#284380,#284381,#284382,
#284383,#284384,#284385,#284386,#284387,#284388,#284389,#284390,#284391,
#284392,#284393,#284394,#284395,#284396,#284397,#284398,#284399,#284400,
#284401,#284402,#284403,#284404,#284405,#284406,#284407,#284408,#284409,
#284410,#284411,#284412,#284413,#284414,#284415,#284416,#284417,#284418,
#284419,#284420,#284421,#284422,#284423,#284424,#284425,#284426,#284427,
#284428,#284429,#284430,#284431,#284432,#284433,#284434,#284435,#284436,
#284437,#284438,#284439,#284440,#284441,#284442,#284443,#284444,#284445,
#284446,#284447,#284448,#284449,#284450,#284451,#284452,#284453,#284454,
#284455,#284456,#284457,#284458,#284459,#284460,#284461,#284462,#284463,
#284464,#284465,#284466,#284467,#284468,#284469,#284470,#284471,#284472,
#284473,#284474,#284475,#284476,#284477,#284478,#284479,#284480,#284481,
#284482,#284483,#284484,#284485,#284486,#284487,#284488,#284489,#284490,
#284491,#284492,#284493,#284494,#284495,#284496,#284497,#284498,#284499,
#284500,#284501,#284502,#284503,#284504,#284505,#284506,#284507,#284508,
#284509,#284510,#284511,#284512,#284513,#284514,#284515,#284516),
 .UNSPECIFIED.,.F.,.F.,(4,2,2,2,2,2,2,2,2,2,2,2,2,2,2,2,2,2,2,2,2,2,2,2,
2,2,2,2,2,2,2,2,2,2,2,2,2,2,2,2,2,2,2,2,2,2,2,2,2,2,2,2,2,2,2,2,2,2,2,2,
2,2,2,2,2,2,2,2,2,2,2,2,2,2,2,2,2,2,2,2,2,2,2,2,2,2,2,2,2,2,2,2,2,2,2,2,
2,2,2,2,2,2,2,2,2,2,2,2,2,2,2,2,2,2,2,2,2,2,2,2,2,2,2,2,2,2,2,2,2,2,2,2,
2,2,2,2,2,2,2,2,2,2,2,2,2,2,2,2,2,2,2,2,2,2,2,2,2,2,2,2,2,2,2,2,2,2,2,2,
2,2,2,2,2,2,2,2,2,2,2,2,2,2,2,2,2,2,2,2,2,2,2,2,2,2,2,2,2,2,2,4),(-1.96114492875287,
-1.95576637931755,-1.951446667606,-1.94859517363792,-1.94585143044094,-1.94276410837109,
-1.9379495198647,-1.92281222802353,-1.88465513711007,-1.87331458819503,
-1.87039192502045,-1.86862177611939,-1.86697537751122,-1.86494592768585,
-1.85993562537325,-1.82447838504788,-1.80810053210915,-1.80086596391414,
-1.79502215970159,-1.791716072214,-1.78884401621589,-1.78528343446254,-1.77840693998898,
-1.73645498864894,-1.72409870341728,-1.71911919823099,-1.71532731999055,
-1.71337213245214,-1.71175438919187,-1.70967696337979,-1.70525855594959,
-1.67731788893727,-1.6482944280941,-1.64051386731501,-1.6368263425757,-1.63394265505342,
-1.6307185961465,-1.62526343551025,-1.59679206125115,-1.57377161344205,
-1.56195398927882,-1.55899521813389,-1.55721704813573,-1.55557453285952,
-1.55356135137965,-1.54959968013638,-1.5213215942493,-1.48888205576646,
-1.48333688606303,-1.48009368368249,-1.47721337573702,-1.47355819496577,
-1.46768506809618,-1.43209496645531,-1.40748343083231,-1.40381192755028,
-1.40188132415746,-1.40026139409704,-1.39818696584068,-1.39382513231902,
-1.36582171508401,-1.33685320431929,-1.32907229375153,-1.32538456546125,
-1.32250070285318,-1.31927643174753,-1.31382087133583,-1.28547685527371,
-1.26358336900253,-1.25487522569929,-1.2491257421775,-1.24682130216123,
-1.24517732415398,-1.24335868660361,-1.2402146781448,-1.22726782871177,
-1.19877173364137,-1.18415455952539,-1.1774239576004,-1.17189926825107,
-1.16866032612286,-1.16577915526009,-1.1621165413588,-1.15447243614956,
-1.11344222345047,-1.10118064399329,-1.0938944888935,-1.09137459204419,
-1.08969092287681,-1.08794796168932,-1.08515058871851,-1.07619994376864,
-1.04874212885248,-1.02583026248366,-1.01778211819715,-1.01404603414751,
-1.01115643917933,-1.0079583798575,-1.00262633575032,-0.98059470178565,
-0.962883134199216,-0.939927174853375,-0.93654369270583,-0.934653275069281,
-0.933190914222677,-0.931118153664723,-0.926725454114284,-0.907928894359782,
-0.874547548067435,-0.863526966763021,-0.859209166816556,-0.856521238649713,
-0.853569323279406,-0.84943442056772,-0.838906930815121,-0.822808525685492,
-0.815371028106317,-0.785592192781932,-0.781322318143366,-0.779272790867857,
-0.77765609569484,-0.775676750952046,-0.77176584949165,-0.748215461411428,
-0.711841966187339,-0.706046985070254,-0.702414392950313,-0.699536070341747,
-0.696278350409146,-0.690665552776482,-0.683796221854088,-0.668706226018213,
-0.652879142178664,-0.64772108714329,-0.628438091395846,-0.625090850788478,
-0.623208588213808,-0.621745033890179,-0.619660801883373,-0.615206299946208,
-0.595817127539822,-0.560703990336907,-0.551471645088069,-0.547823203248531,
-0.545129881120517,-0.542183238132664,-0.538076811672501,-0.527743720521503,
-0.51208162060548,-0.495324141169928,-0.472786241970681,-0.469411448480073,
-0.467523061485594,-0.466060534274226,-0.463985280773575,-0.459578728328218,
-0.440649022367267,-0.406882453994987,-0.396280551626905,-0.39201759083044,
-0.389339354643281,-0.386378316820212,-0.38219268427536,-0.37130690677469,
-0.354382117308863,-0.338437650744959,-0.317077049919405,-0.313712093493294,
-0.311825926109864,-0.31036308928403,-0.308284758038825,-0.303861600876152,
-0.284773076728942,-0.250544894129886,-0.240403038206404,-0.236219404864892,
-0.233288255850289,-0.230261606925782,-0.225740734411683,-0.212180161046693,
-0.187987983707784,-0.163159749288675,-0.158749051252414,-0.156657932775563,
-0.155083789341134,-0.153558565098084,-0.150580277503387,-0.138489547329619,
-0.115708015956755,-0.0873474679874398,-0.0818930642097595,-0.0786691829708695,
-0.0757854784153475,-0.0720976912152042,-0.0643157561470027,-0.0355731630768982,
-0.00695792209858334,-0.00294883740074442,-0.0013212046580614,-0.000460615870580507),
 .UNSPECIFIED.);
#3924=B_SPLINE_CURVE_WITH_KNOTS('',3,(#284518,#284519,#284520,#284521,#284522,
#284523,#284524,#284525,#284526,#284527,#284528,#284529,#284530,#284531,
#284532,#284533,#284534,#284535,#284536,#284537,#284538,#284539,#284540,
#284541,#284542,#284543,#284544,#284545,#284546,#284547,#284548,#284549,
#284550,#284551,#284552,#284553,#284554,#284555,#284556,#284557,#284558,
#284559,#284560,#284561,#284562,#284563,#284564,#284565,#284566,#284567,
#284568,#284569,#284570,#284571,#284572,#284573,#284574,#284575,#284576,
#284577,#284578,#284579,#284580,#284581,#284582,#284583,#284584,#284585,
#284586,#284587,#284588,#284589,#284590,#284591,#284592,#284593,#284594,
#284595,#284596,#284597,#284598,#284599,#284600,#284601,#284602,#284603,
#284604,#284605,#284606,#284607,#284608,#284609,#284610,#284611,#284612,
#284613,#284614,#284615,#284616,#284617,#284618,#284619,#284620,#284621,
#284622,#284623,#284624,#284625,#284626,#284627,#284628,#284629,#284630,
#284631,#284632,#284633,#284634,#284635,#284636,#284637,#284638,#284639,
#284640,#284641,#284642,#284643,#284644,#284645,#284646,#284647,#284648,
#284649,#284650,#284651,#284652,#284653,#284654,#284655,#284656,#284657,
#284658,#284659,#284660,#284661,#284662,#284663,#284664,#284665,#284666,
#284667,#284668,#284669,#284670,#284671,#284672,#284673,#284674,#284675,
#284676,#284677,#284678,#284679,#284680,#284681,#284682,#284683,#284684,
#284685,#284686,#284687,#284688,#284689,#284690,#284691,#284692,#284693,
#284694,#284695,#284696,#284697,#284698,#284699,#284700,#284701,#284702,
#284703,#284704,#284705,#284706,#284707,#284708,#284709,#284710,#284711,
#284712,#284713,#284714,#284715,#284716,#284717,#284718,#284719,#284720,
#284721,#284722,#284723,#284724,#284725,#284726,#284727,#284728,#284729,
#284730,#284731,#284732,#284733,#284734,#284735,#284736,#284737,#284738,
#284739,#284740,#284741,#284742,#284743,#284744,#284745,#284746,#284747,
#284748,#284749,#284750,#284751,#284752,#284753,#284754,#284755,#284756,
#284757,#284758,#284759,#284760,#284761,#284762,#284763,#284764,#284765,
#284766,#284767,#284768,#284769,#284770,#284771,#284772,#284773,#284774,
#284775,#284776,#284777,#284778,#284779,#284780,#284781,#284782,#284783,
#284784,#284785,#284786,#284787,#284788,#284789,#284790,#284791,#284792,
#284793,#284794,#284795,#284796,#284797,#284798,#284799,#284800,#284801,
#284802,#284803,#284804,#284805,#284806,#284807,#284808,#284809,#284810,
#284811,#284812,#284813,#284814,#284815,#284816,#284817,#284818,#284819,
#284820,#284821,#284822,#284823,#284824,#284825,#284826,#284827,#284828,
#284829,#284830,#284831,#284832,#284833,#284834,#284835,#284836,#284837,
#284838,#284839,#284840,#284841,#284842,#284843,#284844,#284845,#284846,
#284847,#284848,#284849,#284850,#284851,#284852,#284853,#284854,#284855,
#284856,#284857,#284858,#284859,#284860,#284861,#284862,#284863,#284864,
#284865,#284866,#284867,#284868,#284869,#284870,#284871,#284872,#284873,
#284874,#284875,#284876,#284877,#284878,#284879,#284880,#284881,#284882,
#284883,#284884,#284885,#284886,#284887,#284888,#284889,#284890,#284891,
#284892,#284893,#284894,#284895,#284896,#284897,#284898,#284899,#284900,
#284901,#284902,#284903,#284904,#284905,#284906,#284907,#284908,#284909,
#284910,#284911,#284912,#284913,#284914,#284915,#284916,#284917,#284918,
#284919,#284920,#284921),.UNSPECIFIED.,.F.,.F.,(4,2,2,2,2,2,2,2,2,2,2,2,
2,2,2,2,2,2,2,2,2,2,2,2,2,2,2,2,2,2,2,2,2,2,2,2,2,2,2,2,2,2,2,2,2,2,2,2,
2,2,2,2,2,2,2,2,2,2,2,2,2,2,2,2,2,2,2,2,2,2,2,2,2,2,2,2,2,2,2,2,2,2,2,2,
2,2,2,2,2,2,2,2,2,2,2,2,2,2,2,2,2,2,2,2,2,2,2,2,2,2,2,2,2,2,2,2,2,2,2,2,
2,2,2,2,2,2,2,2,2,2,2,2,2,2,2,2,2,2,2,2,2,2,2,2,2,2,2,2,2,2,2,2,2,2,2,2,
2,2,2,2,2,2,2,2,2,2,2,2,2,2,2,2,2,2,2,2,2,2,2,2,2,2,2,2,2,2,2,2,2,2,2,2,
2,2,2,2,2,2,2,2,2,4),(-1.96091714897476,-1.96012176149206,-1.95853632991965,
-1.95589451949815,-1.94783216974802,-1.91599294862312,-1.89990466072315,
-1.889382634788,-1.88525002517998,-1.88229974712249,-1.87925530128157,-1.87464317266051,
-1.86144809406078,-1.83007205183936,-1.81665269911615,-1.81140810041174,
-1.80746293509928,-1.80584886682636,-1.80424933478267,-1.80243842795593,
-1.79930307591602,-1.78530696648465,-1.75728332091529,-1.74309652020047,
-1.73344602498232,-1.72944403832998,-1.72651658680164,-1.72343270313497,
-1.7186317963624,-1.70366916045486,-1.65916461975297,-1.65284700413774,
-1.65045825566845,-1.64880030465387,-1.64701656914454,-1.64403080122351,
-1.63311742963153,-1.6071034191073,-1.58069257613081,-1.57531452639657,
-1.5721075323954,-1.56922146069732,-1.56550623998223,-1.55942301733818,
-1.52739066094712,-1.49992001098603,-1.49607476229571,-1.49410907304509,
-1.49249241497452,-1.49042880364124,-1.48608219537813,-1.45747245891014,
-1.42531570969157,-1.41977354037265,-1.41653156477214,-1.41365202960026,
-1.40999739874575,-1.40412425055969,-1.36856280642021,-1.34394349558166,
-1.34027258699271,-1.33834244194475,-1.33672298659296,-1.33464927925256,
-1.33012989701472,-1.30641106214823,-1.29300260817071,-1.27713152139155,
-1.26670484578545,-1.26258537776457,-1.25963689736741,-1.25694696281351,
-1.25331085272942,-1.24415211231845,-1.20530222643581,-1.19328098941709,
-1.1883882012856,-1.18464725250626,-1.18270258520751,-1.18108424782528,
-1.1789941143488,-1.17450669996355,-1.14919099192974,-1.12535429698282,
-1.11190645969541,-1.10739861832612,-1.1043748023704,-1.10144198627579,
-1.09724825939276,-1.08705011963588,-1.05285953462524,-1.03378071468631,
-1.02935879814419,-1.02728078838383,-1.02581810497575,-1.02393200334928,
-1.02056688454017,-0.99897141682679,-0.981022705305819,-0.957963970394677,
-0.952592240250594,-0.949386103802839,-0.946498996581501,-0.942779907884808,
-0.934824403505638,-0.889199588072917,-0.875961978038965,-0.872806647417739,
-0.87098552021877,-0.869342338301719,-0.867043291751737,-0.861328698054324,
-0.852695494375835,-0.830726800221035,-0.802367518306779,-0.796912384311203,
-0.793688093273761,-0.790804036773963,-0.787115820424476,-0.779333061128802,
-0.750618457623808,-0.72227669246232,-0.718317574034866,-0.71630487548091,
-0.714662292538344,-0.712883288773786,-0.709921948799899,-0.698073593073806,
-0.675077084283756,-0.646652065543619,-0.641196958451298,-0.637972491717449,
-0.635088151163068,-0.63139938707036,-0.623614709106851,-0.594286155940436,
-0.56657749700128,-0.562231776161498,-0.560138207955578,-0.558519333960722,
-0.556576637631852,-0.552846101138243,-0.547971801951243,-0.536022951709776,
-0.506667681393957,-0.490014266208289,-0.485033834752996,-0.481910980576953,
-0.478998844899453,-0.47509858552568,-0.466091454910691,-0.453222589429769,
-0.433669463304257,-0.428526104767491,-0.409235119807618,-0.405887751585524,
-0.404005523095146,-0.402542026521058,-0.400457984958688,-0.396004507592167,
-0.37662678566424,-0.341553828636569,-0.332270038940211,-0.328613303778719,
-0.325917761991184,-0.322972460004503,-0.318874966112368,-0.308604459956545,
-0.293081550063853,-0.275258394187928,-0.253549671587606,-0.250182485170955,
-0.248295490452269,-0.246831733204854,-0.244751850883159,-0.240325664785076,
-0.2212196154148,-0.186927436357936,-0.176869659195013,-0.172699251924792,
-0.169769296366712,-0.166736997289291,-0.162194189588239,-0.156952378014564,
-0.146945432940435,-0.121122024362682,-0.0996479943551831,-0.095131156120863,
-0.0930351662220358,-0.0914167907493631,-0.0894780981363024,-0.0857612175790483,
-0.08090898033239,-0.0690404703623535,-0.0368923994444007,-0.0224030075793857,
-0.0176574110021688,-0.0145861917680512,-0.0118506224603147,-0.00899193696603837,
-0.00510495444921737,-0.000462804239319024),.UNSPECIFIED.);
#3925=B_SPLINE_CURVE_WITH_KNOTS('',3,(#284923,#284924,#284925,#284926,#284927,
#284928,#284929,#284930,#284931,#284932,#284933,#284934,#284935,#284936,
#284937,#284938,#284939,#284940,#284941,#284942,#284943,#284944,#284945,
#284946,#284947,#284948,#284949,#284950,#284951,#284952,#284953,#284954,
#284955,#284956,#284957,#284958,#284959,#284960,#284961,#284962,#284963,
#284964,#284965,#284966,#284967,#284968,#284969,#284970,#284971,#284972,
#284973,#284974,#284975,#284976,#284977,#284978,#284979,#284980,#284981,
#284982,#284983,#284984,#284985,#284986,#284987,#284988,#284989,#284990,
#284991,#284992,#284993,#284994,#284995,#284996,#284997,#284998,#284999,
#285000,#285001,#285002,#285003,#285004,#285005,#285006,#285007,#285008,
#285009,#285010,#285011,#285012,#285013,#285014,#285015,#285016,#285017,
#285018,#285019,#285020,#285021,#285022,#285023,#285024,#285025,#285026,
#285027,#285028,#285029,#285030,#285031,#285032,#285033,#285034,#285035,
#285036,#285037,#285038,#285039,#285040,#285041,#285042,#285043,#285044,
#285045,#285046,#285047,#285048,#285049,#285050,#285051,#285052,#285053,
#285054,#285055,#285056,#285057,#285058,#285059,#285060,#285061,#285062,
#285063,#285064,#285065,#285066,#285067,#285068,#285069,#285070),
 .UNSPECIFIED.,.F.,.F.,(4,3,3,3,3,3,3,3,3,3,3,3,3,3,3,3,3,3,3,3,3,3,3,3,
3,3,3,3,3,3,3,3,3,3,3,3,3,3,3,3,3,3,3,3,3,3,3,3,3,4),(10.376098452114,10.4921621249285,
10.6026274765781,10.7129932812893,10.8233039758027,10.9336039089491,11.0440096347695,
11.154477276847,11.2651345766751,11.30460783463,11.4164914118551,11.5281823562147,
11.6397658689834,11.7512845347586,11.8627808451948,11.9743807417522,12.0860284953431,
12.1978945566487,12.30261480526,12.4141501176243,12.5254833531454,12.6367036629042,
12.7478542641654,12.8589782743019,12.9702021872946,13.0814713211549,13.1929592520497,
13.3006217758901,13.4123432114113,13.5238659124788,13.6352775951744,13.7466211513991,
13.8579393757764,13.9693579342981,14.0808222795534,14.1925038146001,14.2986287465202,
14.4103401439347,14.5218534506597,14.6332561369876,14.7445911107436,14.8559011829471,
14.9673123393611,15.0787696795503,15.1904449850493,15.2966357171503,15.4196451177831,
15.5422562405462,15.6642417287656,15.7079632676177),.UNSPECIFIED.);
#3926=B_SPLINE_CURVE_WITH_KNOTS('',3,(#285074,#285075,#285076,#285077,#285078,
#285079,#285080,#285081,#285082,#285083,#285084,#285085,#285086,#285087,
#285088,#285089,#285090,#285091,#285092,#285093,#285094,#285095,#285096,
#285097,#285098,#285099,#285100,#285101,#285102,#285103,#285104,#285105,
#285106,#285107,#285108,#285109,#285110,#285111,#285112,#285113,#285114,
#285115,#285116,#285117,#285118,#285119,#285120,#285121,#285122,#285123,
#285124,#285125,#285126,#285127,#285128,#285129,#285130,#285131,#285132,
#285133,#285134,#285135,#285136,#285137,#285138,#285139,#285140,#285141,
#285142,#285143,#285144,#285145,#285146,#285147,#285148,#285149,#285150,
#285151,#285152,#285153,#285154,#285155,#285156,#285157,#285158,#285159,
#285160,#285161,#285162,#285163,#285164,#285165,#285166,#285167,#285168,
#285169,#285170,#285171,#285172,#285173,#285174,#285175,#285176,#285177,
#285178,#285179,#285180,#285181,#285182,#285183,#285184,#285185),
 .UNSPECIFIED.,.F.,.F.,(4,3,3,3,3,3,3,3,3,3,3,3,3,3,3,3,3,3,3,3,3,3,3,3,
3,3,3,3,3,3,3,3,3,3,3,3,3,4),(11.6154215191105,11.7297374029347,11.8439982074357,
11.9582309631743,12.0724702603026,12.1867506876971,12.3012039081309,12.4157458296163,
12.5305312494344,12.6127573616628,12.7233077204432,12.8341559059147,12.9443566479614,
13.0544767872351,13.1645609189115,13.2759439902374,13.3861606467071,13.4981269254611,
13.610093204215,13.7219630382752,13.8336341156697,13.945194057846,14.0566854855328,
14.1681509220921,14.2797142005244,14.3913222669152,14.50314328189,14.6074290467673,
14.7193214162471,14.8310214301151,14.9426141838145,15.0541422442932,15.1656480857482,
15.2772574285571,15.3889147272786,15.5007897623193,15.6047648893195,15.7079632679489),
 .UNSPECIFIED.);
#3927=B_SPLINE_CURVE_WITH_KNOTS('',3,(#285187,#285188,#285189,#285190,#285191,
#285192,#285193,#285194,#285195,#285196,#285197,#285198,#285199,#285200,
#285201,#285202,#285203,#285204,#285205,#285206,#285207,#285208,#285209,
#285210,#285211,#285212,#285213,#285214,#285215,#285216,#285217,#285218,
#285219,#285220,#285221,#285222,#285223,#285224,#285225,#285226,#285227,
#285228,#285229,#285230,#285231,#285232,#285233,#285234,#285235,#285236,
#285237,#285238,#285239,#285240,#285241,#285242,#285243,#285244,#285245,
#285246,#285247,#285248,#285249,#285250,#285251,#285252,#285253,#285254,
#285255,#285256,#285257,#285258,#285259,#285260,#285261,#285262,#285263,
#285264,#285265,#285266,#285267,#285268,#285269,#285270,#285271,#285272,
#285273,#285274,#285275,#285276,#285277,#285278,#285279,#285280,#285281,
#285282,#285283,#285284,#285285,#285286,#285287,#285288,#285289,#285290,
#285291,#285292,#285293,#285294,#285295,#285296,#285297,#285298,#285299,
#285300,#285301,#285302,#285303,#285304,#285305,#285306,#285307,#285308,
#285309,#285310,#285311,#285312,#285313,#285314,#285315,#285316,#285317,
#285318,#285319,#285320,#285321,#285322,#285323,#285324,#285325,#285326,
#285327,#285328,#285329,#285330,#285331,#285332,#285333,#285334,#285335,
#285336,#285337,#285338,#285339,#285340,#285341,#285342,#285343,#285344,
#285345,#285346,#285347,#285348,#285349,#285350,#285351,#285352,#285353,
#285354,#285355,#285356,#285357,#285358,#285359,#285360,#285361,#285362,
#285363,#285364,#285365,#285366,#285367,#285368,#285369,#285370,#285371,
#285372,#285373,#285374,#285375,#285376,#285377,#285378,#285379,#285380,
#285381,#285382,#285383,#285384,#285385,#285386,#285387,#285388,#285389,
#285390,#285391,#285392,#285393,#285394,#285395,#285396,#285397,#285398,
#285399,#285400,#285401,#285402,#285403,#285404,#285405,#285406,#285407,
#285408,#285409,#285410,#285411,#285412,#285413,#285414,#285415,#285416,
#285417,#285418,#285419,#285420,#285421,#285422,#285423,#285424,#285425,
#285426,#285427,#285428,#285429,#285430,#285431,#285432,#285433,#285434,
#285435,#285436,#285437,#285438,#285439,#285440,#285441,#285442,#285443,
#285444,#285445,#285446,#285447,#285448,#285449,#285450,#285451,#285452,
#285453,#285454,#285455,#285456,#285457,#285458,#285459,#285460,#285461,
#285462,#285463,#285464,#285465,#285466,#285467,#285468,#285469,#285470,
#285471,#285472,#285473,#285474,#285475,#285476,#285477,#285478,#285479,
#285480,#285481,#285482,#285483,#285484,#285485,#285486,#285487,#285488,
#285489,#285490,#285491,#285492,#285493,#285494,#285495,#285496,#285497,
#285498,#285499,#285500,#285501,#285502,#285503,#285504,#285505,#285506,
#285507,#285508,#285509,#285510,#285511,#285512,#285513,#285514,#285515,
#285516,#285517,#285518,#285519,#285520,#285521,#285522,#285523,#285524,
#285525,#285526,#285527,#285528,#285529,#285530,#285531,#285532,#285533,
#285534,#285535,#285536,#285537,#285538,#285539,#285540,#285541,#285542,
#285543,#285544,#285545,#285546,#285547,#285548,#285549,#285550,#285551,
#285552,#285553,#285554,#285555,#285556,#285557,#285558,#285559,#285560,
#285561,#285562,#285563,#285564,#285565,#285566,#285567,#285568,#285569,
#285570,#285571,#285572,#285573,#285574,#285575,#285576),.UNSPECIFIED.,
 .F.,.F.,(4,2,2,2,2,2,2,2,2,2,2,2,2,2,2,2,2,2,2,2,2,2,2,2,2,2,2,2,2,2,2,
2,2,2,2,2,2,2,2,2,2,2,2,2,2,2,2,2,2,2,2,2,2,2,2,2,2,2,2,2,2,2,2,2,2,2,2,
2,2,2,2,2,2,2,2,2,2,2,2,2,2,2,2,2,2,2,2,2,2,2,2,2,2,2,2,2,2,2,2,2,2,2,2,
2,2,2,2,2,2,2,2,2,2,2,2,2,2,2,2,2,2,2,2,2,2,2,2,2,2,2,2,2,2,2,2,2,2,2,2,
2,2,2,2,2,2,2,2,2,2,2,2,2,2,2,2,2,2,2,2,2,2,2,2,2,2,2,2,2,2,2,2,2,2,2,2,
2,2,2,2,2,2,2,2,2,2,2,2,2,2,2,2,2,2,2,4),(-1.96144530502008,-1.93247498786435,
-1.91353558129345,-1.90557328408703,-1.90182194876998,-1.89889613009993,
-1.89563200041529,-1.89012366035219,-1.86261338290726,-1.84264468269137,
-1.83216927446595,-1.82767811113443,-1.82430001539754,-1.82237289087038,
-1.82082090019645,-1.81872457774149,-1.81434669450849,-1.78595816191742,
-1.7537602948305,-1.74811046476254,-1.74479536679182,-1.74184270487633,
-1.73808167351323,-1.73200108902136,-1.69917281564604,-1.67313250773391,
-1.6690879797367,-1.66705142660046,-1.66539435404016,-1.66329526210157,
-1.65890993199517,-1.63043197928439,-1.59852931736083,-1.59284828791651,
-1.58953124807139,-1.58658687059593,-1.58285039631289,-1.57684079942884,
-1.53528197559511,-1.51783681667502,-1.51355509819816,-1.51147782211423,
-1.50982714553679,-1.50778674946864,-1.50368981762125,-1.47177856473146,
-1.44250534297963,-1.43698592484077,-1.43370620427395,-1.43076015798068,
-1.42697344117612,-1.4207795001759,-1.38286523394912,-1.36262264413497,
-1.35804564303371,-1.35591372739082,-1.35441879885597,-1.35249424633418,
-1.34906601330943,-1.32612150426807,-1.3082800418873,-1.29369488981543,
-1.28381811580387,-1.27972772286298,-1.2767341744703,-1.27395606328977,
-1.26937051250131,-1.25687158620433,-1.22496623208017,-1.21144558112075,
-1.20614906989429,-1.20215779290578,-1.20013631520272,-1.19848311131509,
-1.19637945333172,-1.19196253696438,-1.16372710123389,-1.13144587809553,
-1.12583799623071,-1.12253713375895,-1.11959112085485,-1.11583064342519,
-1.10973564157068,-1.07682633189008,-1.05796765044349,-1.05151358654305,
-1.04687936656118,-1.0447355883856,-1.04323863195804,-1.04132084366624,
-1.03792162817364,-1.01809572876024,-1.01346319719988,-0.99359381973634,
-0.981074719714654,-0.972210814068069,-0.968327584034351,-0.965357311172369,
-0.962151405066845,-0.956988488027418,-0.936667115455978,-0.909213691381452,
-0.893795707589246,-0.890510301564211,-0.888618055148226,-0.886947644724336,
-0.884655408636248,-0.879164407762766,-0.871040434269514,-0.848283721645345,
-0.820067810080994,-0.814545586142895,-0.811262674084308,-0.808312716223862,
-0.804519381157505,-0.796418838484311,-0.773829466566902,-0.746794905214226,
-0.737367105864967,-0.734483056363565,-0.73269683439966,-0.730978172698518,
-0.728410409780187,-0.721002315962728,-0.708504887994237,-0.666064793484975,
-0.660258479143926,-0.656581926771106,-0.653643863351469,-0.6502900313723,
-0.644431501800792,-0.63720951206192,-0.621003572707466,-0.590348181346645,
-0.581577449643865,-0.578765184137104,-0.576994817128898,-0.575264558817581,
-0.572639435079613,-0.564762791862318,-0.551034646653108,-0.518394711258836,
-0.506682389390157,-0.50220819684779,-0.499450981840181,-0.496443732344158,
-0.492267801069473,-0.48181766182671,-0.465976954076878,-0.435842357682096,
-0.426161628119392,-0.423251765222197,-0.421460063523569,-0.41974541873305,
-0.417197526769793,-0.409944655860342,-0.397839016948237,-0.358079290939424,
-0.349557291243556,-0.345731404748461,-0.342769270729409,-0.339536504849065,
-0.334248766111482,-0.311751482994435,-0.296929463123666,-0.273333274367298,
-0.268767070924094,-0.266635697594257,-0.264981867431886,-0.262985515668597,
-0.259114724534632,-0.254026115725754,-0.2413399079417,-0.199374122236426,
-0.193469181037138,-0.189763965424481,-0.18682365970767,-0.183489384362261,
-0.177722790788746,-0.146100973740853,-0.117370340801937,-0.113009879655894,
-0.110917218883706,-0.109265167824724,-0.107236116696215,-0.103202388991913,
-0.0773980882934182,-0.0523623833717121,-0.0400086742239438,-0.0354440959479153,
-0.0326707257230633,-0.0296762235914756,-0.0267196348771048,-0.0227468179464109,
-0.000459287936663319),.UNSPECIFIED.);
#3928=B_SPLINE_CURVE_WITH_KNOTS('',3,(#285578,#285579,#285580,#285581,#285582,
#285583,#285584,#285585,#285586,#285587,#285588,#285589,#285590,#285591,
#285592,#285593,#285594,#285595,#285596,#285597,#285598,#285599,#285600,
#285601,#285602,#285603,#285604,#285605,#285606,#285607,#285608,#285609,
#285610,#285611,#285612,#285613,#285614,#285615,#285616,#285617,#285618,
#285619,#285620,#285621,#285622,#285623,#285624,#285625,#285626,#285627,
#285628,#285629,#285630,#285631,#285632,#285633,#285634,#285635,#285636,
#285637,#285638,#285639,#285640,#285641,#285642,#285643,#285644,#285645,
#285646,#285647,#285648,#285649,#285650,#285651,#285652,#285653,#285654,
#285655,#285656,#285657,#285658,#285659,#285660,#285661,#285662,#285663,
#285664,#285665,#285666,#285667,#285668,#285669,#285670,#285671,#285672,
#285673,#285674,#285675,#285676,#285677,#285678,#285679,#285680,#285681,
#285682,#285683,#285684,#285685,#285686,#285687,#285688,#285689,#285690,
#285691,#285692,#285693,#285694,#285695,#285696,#285697,#285698,#285699,
#285700,#285701,#285702,#285703,#285704,#285705,#285706,#285707,#285708,
#285709,#285710,#285711,#285712,#285713,#285714,#285715,#285716,#285717,
#285718,#285719,#285720,#285721,#285722,#285723,#285724,#285725,#285726,
#285727,#285728,#285729,#285730,#285731,#285732,#285733,#285734,#285735,
#285736,#285737,#285738,#285739,#285740,#285741,#285742,#285743,#285744,
#285745,#285746,#285747,#285748,#285749,#285750,#285751,#285752,#285753,
#285754,#285755,#285756,#285757,#285758,#285759,#285760,#285761,#285762,
#285763,#285764,#285765,#285766,#285767,#285768,#285769,#285770,#285771,
#285772,#285773,#285774,#285775,#285776,#285777,#285778,#285779,#285780,
#285781,#285782,#285783,#285784,#285785,#285786,#285787,#285788,#285789,
#285790,#285791,#285792,#285793,#285794,#285795,#285796,#285797,#285798,
#285799,#285800,#285801,#285802,#285803,#285804,#285805,#285806,#285807,
#285808,#285809,#285810,#285811,#285812,#285813,#285814,#285815,#285816,
#285817,#285818,#285819,#285820,#285821,#285822,#285823,#285824,#285825,
#285826,#285827,#285828,#285829,#285830,#285831,#285832,#285833,#285834,
#285835,#285836,#285837,#285838,#285839,#285840,#285841,#285842,#285843,
#285844,#285845,#285846,#285847,#285848,#285849,#285850,#285851,#285852,
#285853,#285854,#285855,#285856,#285857,#285858,#285859,#285860,#285861,
#285862,#285863,#285864,#285865,#285866,#285867,#285868,#285869,#285870,
#285871,#285872,#285873,#285874,#285875,#285876,#285877,#285878,#285879,
#285880,#285881,#285882,#285883,#285884,#285885,#285886,#285887,#285888,
#285889,#285890,#285891,#285892,#285893,#285894,#285895,#285896,#285897,
#285898,#285899,#285900,#285901,#285902,#285903,#285904,#285905,#285906,
#285907,#285908,#285909,#285910,#285911,#285912,#285913,#285914,#285915,
#285916,#285917,#285918,#285919,#285920,#285921,#285922,#285923,#285924,
#285925,#285926,#285927,#285928,#285929,#285930,#285931,#285932,#285933,
#285934,#285935,#285936,#285937,#285938,#285939,#285940,#285941,#285942,
#285943,#285944,#285945,#285946,#285947,#285948,#285949,#285950,#285951,
#285952,#285953,#285954,#285955,#285956,#285957,#285958,#285959,#285960,
#285961,#285962,#285963,#285964,#285965,#285966,#285967,#285968,#285969,
#285970,#285971,#285972,#285973,#285974,#285975,#285976,#285977,#285978,
#285979,#285980,#285981,#285982,#285983,#285984,#285985,#285986,#285987,
#285988,#285989,#285990,#285991,#285992,#285993,#285994,#285995,#285996,
#285997,#285998,#285999),.UNSPECIFIED.,.F.,.F.,(4,2,2,2,2,2,2,2,2,2,2,2,
2,2,2,2,2,2,2,2,2,2,2,2,2,2,2,2,2,2,2,2,2,2,2,2,2,2,2,2,2,2,2,2,2,2,2,2,
2,2,2,2,2,2,2,2,2,2,2,2,2,2,2,2,2,2,2,2,2,2,2,2,2,2,2,2,2,2,2,2,2,2,2,2,
2,2,2,2,2,2,2,2,2,2,2,2,2,2,2,2,2,2,2,2,2,2,2,2,2,2,2,2,2,2,2,2,2,2,2,2,
2,2,2,2,2,2,2,2,2,2,2,2,2,2,2,2,2,2,2,2,2,2,2,2,2,2,2,2,2,2,2,2,2,2,2,2,
2,2,2,2,2,2,2,2,2,2,2,2,2,2,2,2,2,2,2,2,2,2,2,2,2,2,2,2,2,2,2,2,2,2,2,2,
2,2,2,2,2,2,2,2,2,2,2,2,2,2,2,2,2,2,4),(-1.96097617311119,-1.92648172026095,
-1.92144978303859,-1.91761256870394,-1.91562326363793,-1.91396921007816,
-1.91182977798171,-1.90738110749659,-1.88132017505689,-1.85816072997489,
-1.8449191029552,-1.84047048366102,-1.84033328447453,-1.84019566491065,
-1.84005707251167,-1.83991692533481,-1.8398751872902,-1.83982787418988,
-1.83977393865892,-1.83971205264128,-1.8396405041543,-1.83955704383589,
-1.83945864973141,-1.83934115347022,-1.83919861986885,-1.83902226156514,
-1.83812360742327,-1.83517857845841,-1.83142341418022,-1.82534566221748,
-1.79223855705023,-1.77352058243651,-1.76709413917351,-1.76247490024346,
-1.76033393844578,-1.75883734267968,-1.75691769147421,-1.75351015155785,
-1.7322010626931,-1.704303008726,-1.68963748892342,-1.68493937869517,-1.6818311871399,
-1.67884667853989,-1.6746284068573,-1.66460738859007,-1.62687776212102,
-1.61027952339574,-1.60643484654714,-1.60444390589062,-1.60278981460966,
-1.60065203101947,-1.59621227249215,-1.56989777605179,-1.54690343073262,
-1.53368668259779,-1.52914758706272,-1.52607151897191,-1.52306273569114,
-1.51871262471361,-1.50787595945546,-1.47109781867542,-1.4593345327151,
-1.45222042839303,-1.44969068610485,-1.44797971553756,-1.44618269262047,
-1.44324822989912,-1.43331912105908,-1.40667528154168,-1.38432102468044,
-1.3762312235098,-1.37244018340436,-1.3694908682763,-1.366207507867,-1.36068172848989,
-1.33343635568799,-1.31380030815897,-1.30314189678026,-1.2964895370781,
-1.29402229594152,-1.29232323886345,-1.29073223529663,-1.28793965234552,
-1.279339360943,-1.24862276845309,-1.23235306109823,-1.22511340472582,-1.21924332795144,
-1.21588718909187,-1.21294957191915,-1.20927683185984,-1.20348310431166,
-1.16676901274106,-1.14373330606955,-1.13972454604812,-1.13770041437847,
-1.13604810619861,-1.13394973188053,-1.12955951658998,-1.10111235522408,
-1.06897947212993,-1.06337971530366,-1.0600806289454,-1.05713437856048,
-1.05337108304634,-1.04726608968305,-1.01461889654089,-0.995589815322286,
-0.989103223382697,-0.984451522179699,-0.982304428340557,-0.980806932201921,
-0.978890870593016,-0.975406611278072,-0.948812683939885,-0.915322179147616,
-0.909259861495045,-0.905508906334006,-0.902564030144349,-0.899257850257001,
-0.893624431492202,-0.861829152006804,-0.833011838486564,-0.828659845685071,
-0.826568741387078,-0.824916662407224,-0.822886027352813,-0.818844606294295,
-0.792590734494492,-0.759747147692339,-0.753652532292492,-0.749892217609193,
-0.746946299185632,-0.743645504480912,-0.738037684882965,-0.705979328666654,
-0.67741971312468,-0.673039359346898,-0.670942830667103,-0.669290556234762,
-0.66726470896295,-0.663247474292977,-0.639326381450649,-0.603758430761133,
-0.597852264313704,-0.594146546988543,-0.591206005968892,-0.587871637222211,
-0.582105331041332,-0.550695345166428,-0.521712415915215,-0.517374470296042,
-0.515286008528386,-0.513633950570073,-0.511600792039232,-0.507546851776991,
-0.480096020660247,-0.448552928829871,-0.442411834691272,-0.438638075974812,
-0.435690610408103,-0.432397368939924,-0.426825469486252,-0.420054771595755,
-0.405416393889887,-0.387607902436536,-0.364682375318631,-0.361254646608957,
-0.359330312303794,-0.357834222486458,-0.355699449321314,-0.351114857249901,
-0.330815179228958,-0.292672923416853,-0.286675509216833,-0.282943304059214,
-0.2800002969124,-0.276682721816685,-0.270995662275378,-0.240195513443058,
-0.210394011935839,-0.206098172323915,-0.204017797183644,-0.202365941259967,
-0.200325364531526,-0.196233846329197,-0.190762107869839,-0.176508524886542,
-0.141976324150346,-0.13223993879323,-0.128473031436335,-0.125711656222681,
-0.122707884716176,-0.122661249473911,-0.122620081809211,-0.122480029330314,
-0.122341511730251,-0.122203946501924,-0.12206678052895,-0.117617805043081,
-0.104382708559042,-0.08124223812719,-0.0551039462552787,-0.0506554313418783,
-0.0485158069987081,-0.0468614766232517,-0.044871660251827,-0.0410330249596302,
-0.0359994959093764,-0.000459535627139337),.UNSPECIFIED.);
#3929=B_SPLINE_CURVE_WITH_KNOTS('',3,(#286001,#286002,#286003,#286004,#286005,
#286006,#286007,#286008,#286009,#286010,#286011,#286012,#286013,#286014,
#286015,#286016,#286017,#286018,#286019,#286020,#286021,#286022,#286023,
#286024,#286025,#286026,#286027,#286028,#286029,#286030,#286031,#286032,
#286033,#286034,#286035,#286036,#286037,#286038,#286039,#286040,#286041,
#286042,#286043,#286044,#286045,#286046,#286047,#286048,#286049,#286050,
#286051,#286052,#286053,#286054,#286055,#286056,#286057,#286058,#286059,
#286060,#286061,#286062,#286063,#286064,#286065,#286066,#286067,#286068,
#286069,#286070,#286071,#286072,#286073,#286074,#286075,#286076,#286077,
#286078,#286079,#286080,#286081,#286082,#286083,#286084,#286085,#286086,
#286087,#286088,#286089,#286090,#286091,#286092,#286093,#286094,#286095,
#286096,#286097,#286098,#286099,#286100,#286101,#286102,#286103,#286104,
#286105,#286106,#286107,#286108,#286109,#286110,#286111,#286112,#286113,
#286114,#286115,#286116,#286117,#286118,#286119,#286120,#286121,#286122,
#286123,#286124,#286125,#286126,#286127,#286128,#286129,#286130,#286131,
#286132,#286133,#286134,#286135,#286136,#286137,#286138,#286139,#286140,
#286141,#286142,#286143,#286144,#286145,#286146,#286147,#286148,#286149,
#286150,#286151,#286152,#286153,#286154,#286155,#286156,#286157,#286158,
#286159,#286160,#286161,#286162,#286163,#286164,#286165,#286166,#286167,
#286168,#286169,#286170,#286171,#286172,#286173,#286174,#286175,#286176,
#286177,#286178,#286179,#286180,#286181,#286182,#286183,#286184,#286185,
#286186,#286187,#286188,#286189,#286190,#286191,#286192,#286193,#286194,
#286195,#286196,#286197,#286198,#286199,#286200,#286201,#286202,#286203,
#286204,#286205,#286206,#286207,#286208,#286209,#286210,#286211,#286212,
#286213,#286214,#286215,#286216,#286217,#286218,#286219,#286220,#286221,
#286222,#286223,#286224,#286225,#286226,#286227,#286228,#286229,#286230,
#286231,#286232,#286233,#286234,#286235,#286236,#286237,#286238,#286239,
#286240,#286241,#286242,#286243,#286244,#286245,#286246,#286247,#286248,
#286249,#286250,#286251,#286252,#286253,#286254,#286255,#286256,#286257,
#286258,#286259,#286260,#286261,#286262,#286263,#286264,#286265,#286266,
#286267,#286268,#286269,#286270,#286271,#286272,#286273,#286274,#286275,
#286276,#286277,#286278,#286279,#286280,#286281,#286282,#286283,#286284,
#286285,#286286,#286287,#286288,#286289,#286290,#286291,#286292,#286293,
#286294,#286295,#286296,#286297,#286298,#286299,#286300,#286301,#286302,
#286303,#286304,#286305,#286306,#286307,#286308,#286309,#286310,#286311,
#286312,#286313,#286314,#286315,#286316,#286317,#286318,#286319,#286320,
#286321,#286322,#286323,#286324,#286325,#286326,#286327,#286328,#286329,
#286330,#286331,#286332,#286333,#286334,#286335,#286336,#286337,#286338,
#286339,#286340,#286341,#286342,#286343,#286344,#286345,#286346,#286347,
#286348,#286349,#286350,#286351,#286352,#286353,#286354,#286355,#286356,
#286357,#286358,#286359,#286360,#286361,#286362,#286363,#286364,#286365,
#286366,#286367,#286368,#286369,#286370,#286371,#286372,#286373,#286374,
#286375,#286376,#286377,#286378,#286379,#286380,#286381,#286382,#286383,
#286384,#286385,#286386,#286387,#286388,#286389,#286390,#286391,#286392,
#286393,#286394,#286395,#286396,#286397,#286398),.UNSPECIFIED.,.F.,.F.,
(4,2,2,2,2,2,2,2,2,2,2,2,2,2,2,2,2,2,2,2,2,2,2,2,2,2,2,2,2,2,2,2,2,2,2,
2,2,2,2,2,2,2,2,2,2,2,2,2,2,2,2,2,2,2,2,2,2,2,2,2,2,2,2,2,2,2,2,2,2,2,2,
2,2,2,2,2,2,2,2,2,2,2,2,2,2,2,2,2,2,2,2,2,2,2,2,2,2,2,2,2,2,2,2,2,2,2,2,
2,2,2,2,2,2,2,2,2,2,2,2,2,2,2,2,2,2,2,2,2,2,2,2,2,2,2,2,2,2,2,2,2,2,2,2,
2,2,2,2,2,2,2,2,2,2,2,2,2,2,2,2,2,2,2,2,2,2,2,2,2,2,2,2,2,2,2,2,2,2,2,2,
2,2,2,2,2,2,2,2,2,2,2,2,2,2,2,2,2,2,2,4),(-1.96116707136439,-1.94032938098075,
-1.93623603192376,-1.93323577925446,-1.93021664785143,-1.92747356243321,
-1.92307788032648,-1.91189426027027,-1.88795224819068,-1.86303303323596,
-1.85660660487735,-1.85412674889354,-1.85242549393443,-1.85083796869957,
-1.848062502269,-1.83960717823325,-1.80880726769486,-1.79248211697445,-1.78181740607288,
-1.77761070027276,-1.77459838702911,-1.77148041381797,-1.76673468902211,
-1.75284501180551,-1.71935975976403,-1.70802308246174,-1.70108455036899,
-1.69857832238842,-1.69687205873429,-1.69506796865554,-1.69210051955368,
-1.68182447539323,-1.65543615720249,-1.63323809174561,-1.62515476202088,
-1.62136518778792,-1.61841636630745,-1.61513289322957,-1.60960529993182,
-1.58311545464052,-1.56318472128824,-1.55223989871783,-1.54546569561789,
-1.54298180659112,-1.54127980998297,-1.539468411491,-1.53646743554575,-1.52581334495316,
-1.4962433237916,-1.48080103679117,-1.47379592459779,-1.4680742377852,-1.46474966063157,
-1.46180826605517,-1.45808869022918,-1.45213369790441,-1.41709670023302,
-1.3925201108095,-1.38862092302812,-1.38661896701896,-1.38496574920625,
-1.38284189925286,-1.37831525546671,-1.35336239090258,-1.32943655282561,
-1.31591870308003,-1.31134503070556,-1.30826210747142,-1.30525915133156,
-1.30093979646001,-1.29031364703222,-1.2532989429309,-1.24150734479943,
-1.23438183421352,-1.23185066196743,-1.23013946252314,-1.228342985901,-1.22541079976777,
-1.21550397169141,-1.18884530996934,-1.16648233078714,-1.15839252245577,
-1.15460157894644,-1.15165238023701,-1.14836919169945,-1.14284380528737,
-1.11557787562328,-1.09588150205664,-1.08527614035128,-1.08074062089714,
-1.07719824908455,-1.07526997308623,-1.07360776081509,-1.07141784600631,
-1.06639349297778,-1.03092004800497,-1.01455874279342,-1.00387784357576,
-0.999668525453434,-0.996655512267341,-0.993905367259333,-0.990184084665382,
-0.980774994246127,-0.966725522207575,-0.938861716387815,-0.924632520309472,
-0.92137879237249,-0.919512205278452,-0.917834135400416,-0.91548945237802,
-0.909668292717997,-0.900857179781513,-0.86390255649341,-0.849579730544484,
-0.844788208871641,-0.84166052731335,-0.83865373726345,-0.834479348532444,
-0.824038175838477,-0.808216833837496,-0.778109559374263,-0.768385999912533,
-0.765471972148649,-0.763679456975874,-0.761965631559021,-0.759421248052782,
-0.752194213394201,-0.74015246395096,-0.700955636462519,-0.692163065700046,
-0.688552455451004,-0.685556028806131,-0.682464485091984,-0.67784841739255,
-0.663953752639336,-0.638805750528158,-0.615573972090987,-0.611445832651618,
-0.609370179295457,-0.607687605243971,-0.605876304169358,-0.602876202218796,
-0.591034294566917,-0.562371522182849,-0.53964305779209,-0.534216374437366,
-0.530954279039788,-0.528000487123094,-0.524170293074934,-0.515859712085657,
-0.491277662271067,-0.460011135743046,-0.455415528562843,-0.45327882465695,
-0.451624789776603,-0.449632951343047,-0.445783953655136,-0.42269392421623,
-0.385763771615181,-0.379997799234613,-0.376333314440817,-0.373396512145373,
-0.370035009648928,-0.364138814150675,-0.356856637842032,-0.34043305319035,
-0.30393668717358,-0.299633358729507,-0.297551630209894,-0.295899857267152,
-0.293860814323333,-0.289776640144051,-0.284317680599918,-0.270117608809778,
-0.235767565068731,-0.225834395206718,-0.221626776433031,-0.21864397605268,
-0.215532529348914,-0.21081946700866,-0.196012422557768,-0.170819006834098,
-0.148749894710541,-0.144623829172003,-0.142548662776975,-0.140866188121952,
-0.139095923550034,-0.136412379258326,-0.133031834155479,-0.126201784087867,
-0.105290659463639,-0.0753270472301669,-0.0691473323490282,-0.0653626963230127,
-0.0624142743786168,-0.0591277139279507,-0.0535862383955478,-0.0232906407447269,
-0.000459678636155689),.UNSPECIFIED.);
#3930=B_SPLINE_CURVE_WITH_KNOTS('',3,(#286400,#286401,#286402,#286403,#286404,
#286405,#286406,#286407,#286408,#286409,#286410),.UNSPECIFIED.,.F.,.F.,
(4,1,1,1,1,1,1,1,4),(53.4070751110265,53.5035269063048,54.500862748857,
55.4981985914093,56.4955344339615,57.4928702765138,58.490206119066,59.4875419616182,
59.690260418206),.UNSPECIFIED.);
#3931=B_SPLINE_CURVE_WITH_KNOTS('',3,(#286412,#286413,#286414,#286415,#286416,
#286417,#286418,#286419,#286420,#286421,#286422,#286423,#286424,#286425,
#286426,#286427,#286428,#286429,#286430,#286431,#286432,#286433,#286434,
#286435,#286436,#286437,#286438,#286439,#286440,#286441,#286442,#286443,
#286444,#286445,#286446,#286447,#286448,#286449,#286450,#286451,#286452,
#286453,#286454,#286455,#286456,#286457,#286458,#286459,#286460,#286461,
#286462,#286463,#286464,#286465,#286466,#286467,#286468,#286469,#286470,
#286471,#286472,#286473,#286474,#286475,#286476,#286477,#286478,#286479,
#286480,#286481,#286482,#286483,#286484,#286485,#286486,#286487,#286488,
#286489,#286490,#286491,#286492,#286493,#286494,#286495,#286496,#286497,
#286498,#286499,#286500,#286501,#286502,#286503,#286504,#286505,#286506,
#286507,#286508,#286509,#286510,#286511,#286512,#286513,#286514,#286515,
#286516,#286517,#286518,#286519,#286520,#286521,#286522,#286523,#286524,
#286525,#286526,#286527,#286528,#286529,#286530,#286531,#286532,#286533,
#286534,#286535,#286536,#286537,#286538,#286539,#286540,#286541,#286542,
#286543,#286544,#286545,#286546,#286547,#286548,#286549,#286550,#286551,
#286552,#286553,#286554,#286555,#286556,#286557,#286558,#286559,#286560,
#286561,#286562,#286563,#286564,#286565,#286566,#286567,#286568,#286569,
#286570,#286571,#286572,#286573,#286574,#286575,#286576,#286577,#286578,
#286579,#286580,#286581,#286582,#286583,#286584,#286585,#286586,#286587,
#286588,#286589,#286590,#286591,#286592,#286593,#286594,#286595,#286596,
#286597,#286598,#286599,#286600,#286601,#286602,#286603,#286604,#286605,
#286606,#286607,#286608,#286609,#286610,#286611,#286612,#286613,#286614,
#286615,#286616,#286617,#286618,#286619,#286620,#286621,#286622,#286623,
#286624,#286625,#286626,#286627,#286628,#286629,#286630,#286631,#286632,
#286633,#286634,#286635,#286636,#286637,#286638,#286639,#286640,#286641,
#286642,#286643,#286644,#286645,#286646,#286647,#286648,#286649,#286650,
#286651,#286652,#286653,#286654,#286655,#286656,#286657,#286658,#286659,
#286660,#286661,#286662,#286663,#286664,#286665,#286666,#286667,#286668,
#286669,#286670,#286671,#286672,#286673,#286674,#286675,#286676,#286677,
#286678,#286679,#286680,#286681,#286682,#286683,#286684,#286685,#286686,
#286687,#286688,#286689,#286690,#286691,#286692,#286693,#286694,#286695,
#286696,#286697,#286698,#286699,#286700,#286701,#286702,#286703,#286704,
#286705,#286706,#286707,#286708,#286709,#286710,#286711,#286712,#286713,
#286714,#286715,#286716,#286717,#286718,#286719,#286720,#286721,#286722,
#286723,#286724,#286725,#286726,#286727,#286728,#286729,#286730,#286731,
#286732,#286733,#286734,#286735,#286736,#286737,#286738,#286739,#286740,
#286741,#286742,#286743,#286744,#286745,#286746,#286747,#286748,#286749,
#286750,#286751,#286752,#286753,#286754,#286755,#286756,#286757,#286758,
#286759,#286760,#286761,#286762,#286763,#286764,#286765,#286766,#286767,
#286768,#286769,#286770,#286771,#286772,#286773,#286774,#286775,#286776,
#286777,#286778,#286779,#286780,#286781,#286782,#286783,#286784,#286785,
#286786,#286787,#286788,#286789,#286790,#286791,#286792,#286793,#286794,
#286795,#286796,#286797,#286798,#286799,#286800,#286801,#286802,#286803,
#286804,#286805,#286806,#286807,#286808,#286809,#286810,#286811,#286812,
#286813,#286814,#286815,#286816,#286817,#286818,#286819,#286820,#286821,
#286822,#286823,#286824,#286825,#286826,#286827,#286828,#286829,#286830,
#286831,#286832,#286833,#286834,#286835,#286836,#286837,#286838,#286839,
#286840,#286841,#286842,#286843,#286844,#286845,#286846,#286847,#286848,
#286849,#286850,#286851,#286852,#286853,#286854,#286855,#286856,#286857,
#286858,#286859,#286860,#286861,#286862,#286863,#286864,#286865,#286866,
#286867,#286868,#286869),.UNSPECIFIED.,.F.,.F.,(4,2,2,2,2,2,2,2,2,2,2,2,
2,2,2,2,2,2,2,2,2,2,2,2,2,2,2,2,2,2,2,2,2,2,2,2,2,2,2,2,2,2,2,2,2,2,2,2,
2,2,2,2,2,2,2,2,2,2,2,2,2,2,2,2,2,2,2,2,2,2,2,2,2,2,2,2,2,2,2,2,2,2,2,2,
2,2,2,2,2,2,2,2,2,2,2,2,2,2,2,2,2,2,2,2,2,2,2,2,2,2,2,2,2,2,2,2,2,2,2,2,
2,2,2,2,2,2,2,2,2,2,2,2,2,2,2,2,2,2,2,2,2,2,2,2,2,2,2,2,2,2,2,2,2,2,2,2,
2,2,2,2,2,2,2,2,2,2,2,2,2,2,2,2,2,2,2,2,2,2,2,2,2,2,2,2,2,2,2,2,2,2,2,2,
2,2,2,2,2,2,2,2,2,2,2,2,2,2,2,2,2,2,2,2,2,2,2,2,2,2,2,2,2,2,2,2,2,2,2,2,
4),(-1.96125649093128,-1.93249964309487,-1.92527261925194,-1.9210310812038,
-1.9171621004257,-1.91420354232668,-1.91096114332999,-1.90562610438211,
-1.88472509267201,-1.8549121737987,-1.84243462342552,-1.839438444461,-1.837859686341,
-1.8362065093369,-1.83408216688999,-1.82955257743335,-1.80453203680034,
-1.78065987849674,-1.76715930968027,-1.76258773773602,-1.7595053320455,
-1.75650220216325,-1.75218139301695,-1.74154622625011,-1.70454442026726,
-1.69275469692247,-1.68563004953296,-1.68309906010746,-1.68138794946653,
-1.67959152902365,-1.67665936935549,-1.66675194487389,-1.64009519586762,
-1.61773364628296,-1.60964420709852,-1.60585343188556,-1.60290436216941,
-1.59962131525331,-1.59409616232599,-1.56683241856893,-1.54713963172143,
-1.53653236917927,-1.52990217928761,-1.52743816467588,-1.52573980893973,
-1.52392143847442,-1.52088882245048,-1.50987497741403,-1.48401341373018,
-1.46213438853691,-1.45406188916704,-1.45027420966382,-1.44732554704481,
-1.4440409027673,-1.43850802766859,-1.41194588076752,-1.39206979940513,
-1.3811415411255,-1.37651678627932,-1.3729207616357,-1.37098128361803,-1.36932115062559,
-1.36714882092381,-1.36222572958359,-1.32663074493653,-1.31025559665232,
-1.30298685510167,-1.29709860608208,-1.29373882674215,-1.29080190363784,
-1.28713513397081,-1.2813611814991,-1.2387500674556,-1.22630749131946,-1.21892181240517,
-1.21635708933794,-1.21463923891366,-1.21285268375927,-1.20996592290161,
-1.20050744894822,-1.17351847000204,-1.1509577008131,-1.142860667075,-1.13906840340673,
-1.13611902931045,-1.13283651687061,-1.127314403531,-1.09900825252285,-1.07732473567713,
-1.06859432629704,-1.06281189828915,-1.06047327355603,-1.05879618526777,
-1.05692684169353,-1.05366030888086,-1.03915274614539,-1.01124829593109,
-0.997427783183198,-0.987917091988905,-0.98388541486729,-0.980902644567638,
-0.977727971556189,-0.972712771385518,-0.954507472564632,-0.933976505964483,
-0.929353721577123,-0.909450560832053,-0.906049806438441,-0.904131598624798,
-0.902634601153879,-0.900491115575262,-0.895858600708775,-0.889408400241348,
-0.87056594422121,-0.837688115475842,-0.831595462859419,-0.82783583266088,
-0.824890138183091,-0.821589270069411,-0.815980514672311,-0.78369195274406,
-0.755424519020071,-0.751007968445111,-0.74890465680967,-0.747252241003928,
-0.745232601058283,-0.741246077878919,-0.735957638570671,-0.722467436509166,
-0.690672821384971,-0.678053870729042,-0.673453339480083,-0.670673448671575,
-0.667683515499592,-0.663608134238003,-0.653820837719149,-0.639420830021098,
-0.611046811063528,-0.597815549616595,-0.594613237786827,-0.592757761864305,
-0.591075655338963,-0.58870587344619,-0.582722093492122,-0.573563446114192,
-0.531681730296335,-0.521578376069416,-0.517349229493336,-0.514362646424345,
-0.511257104647362,-0.50657256770214,-0.492040807694588,-0.464651319189557,
-0.442634910922687,-0.439222407693773,-0.437301560184945,-0.435805009572928,
-0.433665436260411,-0.429054287771109,-0.422643833374612,-0.404007344541578,
-0.370823964571023,-0.364745656962799,-0.360990143698776,-0.358044861629998,
-0.354741529567779,-0.34912125617906,-0.342274806647899,-0.327379048541418,
-0.314658667233377,-0.288761494777877,-0.28424939209484,-0.282128192909907,
-0.280475051826967,-0.278470750167468,-0.274560236886838,-0.2509669969311,
-0.214793595741306,-0.208947437178412,-0.205259457968505,-0.202320764745333,
-0.198975370645524,-0.193155689374181,-0.162757416005791,-0.132753852753097,
-0.128489483515492,-0.126415283668854,-0.12476367526785,-0.124732297688759,
-0.124702296542198,-0.12467357295759,-0.1246460373232,-0.124619608225699,
-0.124594211530914,-0.124569779583865,-0.12454625051809,-0.124523567643961,
-0.12450167891428,-0.12448053645648,-0.124460096158748,-0.124440317305584,
-0.124421162255323,-0.124402596149197,-0.124384586658954,-0.124367103756732,
-0.124350119516051,-0.124333607925302,-0.124317544724245,-0.124301907254373,
-0.124286674331743,-0.124271826124383,-0.124257344045043,-0.124243210650526,
-0.124229409558503,-0.124215925361643,-0.124202743557482,-0.124189850476127,
-0.12202245600517,-0.11678894468266,-0.108990823794884,-0.0817257648201424,
-0.057378486359362,-0.0519080092400297,-0.0486365198836584,-0.0456848002917184,
-0.041872269708007,-0.0377109310250489,-0.0306901428147373,-0.0004594071072521),
 .UNSPECIFIED.);
#3932=B_SPLINE_CURVE_WITH_KNOTS('',3,(#286871,#286872,#286873,#286874,#286875,
#286876,#286877,#286878,#286879,#286880,#286881,#286882,#286883,#286884,
#286885,#286886,#286887,#286888,#286889,#286890,#286891,#286892,#286893,
#286894,#286895,#286896,#286897,#286898,#286899,#286900,#286901,#286902,
#286903,#286904,#286905,#286906,#286907,#286908,#286909,#286910,#286911,
#286912,#286913,#286914,#286915,#286916,#286917,#286918,#286919,#286920,
#286921,#286922,#286923,#286924,#286925,#286926,#286927,#286928,#286929,
#286930,#286931,#286932,#286933,#286934,#286935,#286936,#286937,#286938,
#286939,#286940,#286941,#286942,#286943,#286944,#286945,#286946,#286947,
#286948,#286949,#286950,#286951,#286952,#286953,#286954,#286955,#286956,
#286957,#286958,#286959,#286960,#286961,#286962,#286963,#286964,#286965,
#286966,#286967,#286968,#286969,#286970,#286971,#286972,#286973,#286974,
#286975,#286976,#286977,#286978,#286979,#286980,#286981,#286982,#286983,
#286984,#286985,#286986,#286987,#286988,#286989,#286990,#286991,#286992,
#286993,#286994,#286995,#286996,#286997,#286998,#286999,#287000,#287001,
#287002,#287003,#287004,#287005,#287006,#287007,#287008,#287009,#287010,
#287011,#287012,#287013,#287014,#287015,#287016,#287017,#287018,#287019,
#287020,#287021,#287022,#287023,#287024,#287025,#287026,#287027,#287028,
#287029,#287030,#287031,#287032,#287033,#287034,#287035,#287036,#287037,
#287038,#287039,#287040,#287041,#287042,#287043,#287044,#287045,#287046,
#287047,#287048,#287049,#287050,#287051,#287052,#287053,#287054,#287055,
#287056,#287057,#287058,#287059,#287060,#287061,#287062,#287063,#287064,
#287065,#287066,#287067,#287068,#287069,#287070,#287071,#287072,#287073,
#287074,#287075,#287076,#287077,#287078,#287079,#287080,#287081,#287082,
#287083,#287084,#287085,#287086,#287087,#287088,#287089,#287090,#287091,
#287092,#287093,#287094,#287095,#287096,#287097,#287098,#287099,#287100,
#287101,#287102,#287103,#287104,#287105,#287106,#287107,#287108,#287109,
#287110,#287111,#287112,#287113,#287114,#287115,#287116,#287117,#287118,
#287119,#287120,#287121,#287122,#287123,#287124,#287125,#287126,#287127,
#287128,#287129,#287130,#287131,#287132,#287133,#287134,#287135,#287136,
#287137,#287138,#287139,#287140,#287141,#287142,#287143,#287144,#287145,
#287146,#287147,#287148,#287149,#287150,#287151,#287152,#287153,#287154,
#287155,#287156,#287157,#287158,#287159,#287160,#287161,#287162,#287163,
#287164,#287165,#287166,#287167,#287168,#287169,#287170,#287171,#287172,
#287173,#287174,#287175,#287176,#287177,#287178,#287179,#287180,#287181,
#287182,#287183,#287184,#287185,#287186,#287187,#287188,#287189,#287190,
#287191,#287192,#287193,#287194,#287195,#287196,#287197,#287198,#287199,
#287200,#287201,#287202,#287203,#287204,#287205,#287206,#287207,#287208,
#287209,#287210,#287211,#287212,#287213,#287214,#287215,#287216,#287217,
#287218,#287219,#287220,#287221,#287222,#287223,#287224,#287225,#287226,
#287227,#287228,#287229,#287230,#287231,#287232,#287233,#287234,#287235,
#287236,#287237,#287238,#287239,#287240,#287241,#287242,#287243,#287244,
#287245,#287246,#287247,#287248,#287249,#287250,#287251,#287252,#287253,
#287254,#287255,#287256,#287257,#287258,#287259,#287260,#287261,#287262,
#287263,#287264,#287265,#287266,#287267,#287268,#287269,#287270,#287271,
#287272,#287273,#287274),.UNSPECIFIED.,.F.,.F.,(4,2,2,2,2,2,2,2,2,2,2,2,
2,2,2,2,2,2,2,2,2,2,2,2,2,2,2,2,2,2,2,2,2,2,2,2,2,2,2,2,2,2,2,2,2,2,2,2,
2,2,2,2,2,2,2,2,2,2,2,2,2,2,2,2,2,2,2,2,2,2,2,2,2,2,2,2,2,2,2,2,2,2,2,2,
2,2,2,2,2,2,2,2,2,2,2,2,2,2,2,2,2,2,2,2,2,2,2,2,2,2,2,2,2,2,2,2,2,2,2,2,
2,2,2,2,2,2,2,2,2,2,2,2,2,2,2,2,2,2,2,2,2,2,2,2,2,2,2,2,2,2,2,2,2,2,2,2,
2,2,2,2,2,2,2,2,2,2,2,2,2,2,2,2,2,2,2,2,2,2,2,2,2,2,2,2,2,2,2,2,2,2,2,2,
2,2,2,2,2,2,2,2,2,4),(-1.96117523376116,-1.9425871113232,-1.93582413289111,
-1.93356944763943,-1.9319048855407,-1.93023509530763,-1.92834224070789,
-1.92505361015502,-1.90952745767491,-1.88709371903652,-1.86295356598266,
-1.85735185262359,-1.85400524143428,-1.85106700210845,-1.8473816160519,
-1.84154365867909,-1.79907408936262,-1.78220084698977,-1.77798460336861,
-1.77591977381511,-1.77426832093338,-1.77221337093403,-1.76804783281997,
-1.7369360840567,-1.70806847270669,-1.70194596819273,-1.6985372411934,-1.69560460641459,
-1.692003467634,-1.68645167259274,-1.64768908377773,-1.62717173439072,-1.62256575632003,
-1.62042715145894,-1.61893074983333,-1.61700930405983,-1.61359407819643,
-1.59129697258016,-1.57384502960741,-1.55862153955374,-1.54844995952658,
-1.54431576349085,-1.54131593331185,-1.5385498964627,-1.53402574858458,
-1.5219627818578,-1.48963032564364,-1.47598560201299,-1.47065952452288,
-1.46665170565154,-1.46462781104101,-1.46297556343292,-1.46087709770335,
-1.45648613167355,-1.42804753523019,-1.39597946780613,-1.39034242557826,
-1.38703551358725,-1.38409081370666,-1.3803412211144,-1.37428346399596,
-1.32746837487048,-1.31804693994638,-1.31194252648618,-1.30955433813698,
-1.30786908115524,-1.3060211185988,-1.30285396005132,-1.29009812957261,
-1.26546705863994,-1.2484343821876,-1.23746315500973,-1.23321200009674,
-1.23019105196488,-1.22744838911326,-1.22305793816902,-1.21191343296223,
-1.17546609068989,-1.16374208899384,-1.1566436289,-1.15411570637544,-1.15240491070424,
-1.15060694637229,-1.14766895970902,-1.13770690909045,-1.11108203482744,
-1.0887383720867,-1.08064787184621,-1.07685636120765,-1.07390662107459,
-1.07062272720899,-1.06509590223077,-1.03787815120095,-1.01833260223083,
-1.00759302434389,-1.00090556981874,-0.998433219918652,-0.996733033796596,
-0.994916950281445,-0.991896022495409,-0.981018549502324,-0.956356948880598,
-0.928868120827255,-0.923345124084904,-0.920062118321725,-0.917112308735936,
-0.913319499134517,-0.905221499880774,-0.882711551884798,-0.855813147171446,
-0.846196196829128,-0.84329268917213,-0.841502292164372,-0.839786591086042,
-0.837233698164022,-0.829942586931405,-0.817741404974387,-0.777114842096857,
-0.769262526201464,-0.765514403805289,-0.762569569954733,-0.759261159669255,
-0.753618202526029,-0.746736476030524,-0.731721400596798,-0.7160024082303,
-0.711378480646719,-0.69155917495168,-0.688159106745386,-0.686240919769652,
-0.68474370743409,-0.68259961203249,-0.677964581606929,-0.671509947677267,
-0.652646107575983,-0.619792756218384,-0.613698152466842,-0.609937730003768,
-0.606991658963416,-0.603690622457731,-0.598082215027035,-0.566053751553693,
-0.537454379288816,-0.533078339530897,-0.530982560359543,-0.52933022158672,
-0.527303489724267,-0.523282157771495,-0.498987088380991,-0.463872587888669,
-0.45792526499283,-0.454207452086069,-0.45126564116114,-0.447938673114906,
-0.442207971923826,-0.410519851609205,-0.38178042053347,-0.377419948769166,
-0.375327117350919,-0.373674849154067,-0.3716454286692,-0.367610661170329,
-0.342028770352246,-0.30842566119763,-0.302368883386296,-0.298619314141658,
-0.295674308750209,-0.292366713449642,-0.286727684966135,-0.25462722712635,
-0.226184127271019,-0.221788662205397,-0.219689158400265,-0.218036650861948,
-0.216013111108445,-0.212007964384416,-0.206687384714323,-0.193066335281392,
-0.16081157631273,-0.148685318741221,-0.144151907571838,-0.14138391389431,
-0.138541736294864,-0.138443487584753,-0.138354902608545,-0.138274130023016,
-0.138199748716675,-0.138130644953762,-0.138065929582462,-0.138004880677656,
-0.134409769665758,-0.12988548965373,-0.121921998401925,-0.102914998011306,
-0.0732463525957487,-0.0670866595308566,-0.0646235313852827,-0.0629418291035602,
-0.061127853858408,-0.0581165951381371,-0.0461290615911358,-0.000459593433154411),
 .UNSPECIFIED.);
#3933=B_SPLINE_CURVE_WITH_KNOTS('',3,(#287276,#287277,#287278,#287279,#287280,
#287281,#287282,#287283,#287284,#287285,#287286,#287287,#287288,#287289,
#287290,#287291,#287292,#287293,#287294,#287295,#287296,#287297,#287298,
#287299,#287300,#287301,#287302,#287303,#287304,#287305,#287306,#287307,
#287308,#287309,#287310,#287311,#287312,#287313,#287314,#287315,#287316,
#287317,#287318,#287319,#287320,#287321,#287322,#287323,#287324,#287325,
#287326,#287327,#287328,#287329,#287330,#287331,#287332,#287333,#287334,
#287335,#287336,#287337,#287338,#287339,#287340,#287341,#287342,#287343,
#287344,#287345,#287346,#287347,#287348,#287349,#287350,#287351,#287352,
#287353,#287354,#287355,#287356,#287357,#287358,#287359,#287360,#287361,
#287362,#287363,#287364,#287365,#287366,#287367,#287368,#287369,#287370,
#287371,#287372,#287373,#287374,#287375,#287376,#287377,#287378,#287379,
#287380,#287381,#287382,#287383,#287384,#287385,#287386,#287387,#287388,
#287389,#287390,#287391,#287392,#287393,#287394,#287395,#287396,#287397,
#287398,#287399,#287400,#287401,#287402,#287403,#287404,#287405,#287406,
#287407,#287408,#287409,#287410,#287411,#287412,#287413,#287414,#287415,
#287416,#287417,#287418,#287419,#287420,#287421,#287422,#287423,#287424,
#287425,#287426,#287427,#287428,#287429,#287430,#287431,#287432,#287433,
#287434,#287435,#287436,#287437,#287438,#287439,#287440,#287441,#287442,
#287443,#287444,#287445,#287446,#287447,#287448,#287449,#287450,#287451,
#287452,#287453,#287454,#287455,#287456,#287457,#287458,#287459,#287460,
#287461,#287462,#287463,#287464,#287465,#287466,#287467,#287468,#287469,
#287470,#287471,#287472,#287473,#287474,#287475,#287476,#287477,#287478,
#287479,#287480,#287481,#287482,#287483,#287484,#287485,#287486,#287487,
#287488,#287489,#287490,#287491,#287492,#287493,#287494,#287495,#287496,
#287497,#287498,#287499,#287500,#287501,#287502,#287503,#287504,#287505,
#287506,#287507,#287508,#287509,#287510,#287511,#287512,#287513,#287514,
#287515,#287516,#287517,#287518,#287519,#287520,#287521,#287522,#287523,
#287524,#287525,#287526,#287527,#287528,#287529,#287530,#287531,#287532,
#287533,#287534,#287535,#287536,#287537,#287538,#287539,#287540,#287541,
#287542,#287543,#287544,#287545,#287546,#287547,#287548,#287549,#287550,
#287551,#287552,#287553,#287554,#287555,#287556,#287557,#287558,#287559,
#287560,#287561,#287562,#287563,#287564,#287565,#287566,#287567,#287568,
#287569,#287570,#287571,#287572,#287573,#287574,#287575,#287576,#287577,
#287578,#287579,#287580,#287581,#287582,#287583,#287584,#287585,#287586,
#287587,#287588,#287589,#287590,#287591,#287592,#287593,#287594,#287595,
#287596,#287597,#287598,#287599,#287600,#287601,#287602,#287603,#287604,
#287605,#287606,#287607,#287608,#287609,#287610,#287611,#287612,#287613,
#287614,#287615,#287616,#287617,#287618,#287619,#287620,#287621,#287622,
#287623,#287624,#287625,#287626,#287627,#287628,#287629,#287630,#287631,
#287632,#287633,#287634,#287635,#287636,#287637,#287638,#287639,#287640,
#287641,#287642,#287643,#287644,#287645,#287646,#287647,#287648,#287649,
#287650,#287651,#287652,#287653,#287654,#287655,#287656,#287657,#287658,
#287659,#287660,#287661,#287662,#287663,#287664,#287665),.UNSPECIFIED.,
 .F.,.F.,(4,2,2,2,2,2,2,2,2,2,2,2,2,2,2,2,2,2,2,2,2,2,2,2,2,2,2,2,2,2,2,
2,2,2,2,2,2,2,2,2,2,2,2,2,2,2,2,2,2,2,2,2,2,2,2,2,2,2,2,2,2,2,2,2,2,2,2,
2,2,2,2,2,2,2,2,2,2,2,2,2,2,2,2,2,2,2,2,2,2,2,2,2,2,2,2,2,2,2,2,2,2,2,2,
2,2,2,2,2,2,2,2,2,2,2,2,2,2,2,2,2,2,2,2,2,2,2,2,2,2,2,2,2,2,2,2,2,2,2,2,
2,2,2,2,2,2,2,2,2,2,2,2,2,2,2,2,2,2,2,2,2,2,2,2,2,2,2,2,2,2,2,2,2,2,2,2,
2,2,2,2,2,2,2,2,2,2,2,2,2,2,2,2,2,2,2,4),(-1.96104829234917,-1.95562578488271,
-1.95119962367166,-1.9482848213421,-1.94548168844373,-1.94232769765138,
-1.93740838667848,-1.92181122818972,-1.90144905710625,-1.87470367379065,
-1.87082277072753,-1.86882469190365,-1.86717146903657,-1.86504350710011,
-1.86049375427697,-1.83597398092297,-1.81176924572673,-1.79816448213047,
-1.79358138831612,-1.79049687231796,-1.78749594583543,-1.7838660451886,
-1.77501435278891,-1.73955410055214,-1.72505214493821,-1.71952255372207,
-1.71539875062142,-1.71335210337081,-1.71170073920461,-1.70962776509182,
-1.70536882564841,-1.67505875230187,-1.64498138287798,-1.63917503515137,
-1.63583269846025,-1.63289399116935,-1.62920240449327,-1.62334308302571,
-1.58114095177767,-1.56853818734285,-1.5610900005564,-1.55851754952362,
-1.55679826843684,-1.55501416342521,-1.5521380859804,-1.54277978083191,
-1.51571963128851,-1.49311746956612,-1.48501964397204,-1.4812274725302,
-1.47827836101775,-1.47499633604394,-1.46947552096949,-1.44309356049383,
-1.42310619217173,-1.41212046890976,-1.40532897658317,-1.40284272377062,
-1.40114028689987,-1.39932969338928,-1.39633237923103,-1.38572010344219,
-1.35612862553347,-1.34066956369736,-1.33365963792748,-1.32793489930486,
-1.32460968403595,-1.32166839762211,-1.31794986653969,-1.31199844562999,
-1.27023601667175,-1.25294264095831,-1.24867825362724,-1.24660407847479,
-1.24495250699374,-1.24290652808938,-1.23878687479586,-1.20706798089512,
-1.18209912131909,-1.17388276224925,-1.17006928578109,-1.16711753594338,
-1.16384672175825,-1.15837911859481,-1.13421216648516,-1.10676584821308,
-1.09515115893936,-1.09216800077745,-1.09036039983754,-1.08867578843895,
-1.08659208894007,-1.08140904374581,-1.05087864040884,-1.02670620654232,
-1.01835283322309,-1.01451505509316,-1.0115602372279,-1.00830184345696,
-1.00289288695995,-0.980626562145746,-0.965752131220844,-0.942226858389223,
-0.937709364879942,-0.935579053573708,-0.933922917316097,-0.931953590827468,
-0.928214337457664,-0.90287736406926,-0.868457023292409,-0.862455637045603,
-0.858722469045465,-0.855779609727459,-0.852463155423185,-0.846780446009887,
-0.81504180239075,-0.786271239235246,-0.78191521871105,-0.779823449258368,
-0.778171481381033,-0.776141767022511,-0.772104475446446,-0.746218497458143,
-0.712969865568958,-0.706895109473288,-0.703140686792894,-0.700195603748465,
-0.696891811739635,-0.691269041872597,-0.684418620676052,-0.669509057031735,
-0.656290903173045,-0.63092658892971,-0.626408254314294,-0.624285937770609,
-0.622632792960377,-0.620629542395053,-0.616724021250156,-0.594030907040117,
-0.556716632612083,-0.550994253014773,-0.547342682583301,-0.544406968692705,
-0.541036582341685,-0.535097577840513,-0.504358525383716,-0.474992338569497,
-0.470677188626253,-0.468593279390831,-0.466941572087641,-0.464904828710772,
-0.460831852670636,-0.455392417899417,-0.441274166276935,-0.407222546131526,
-0.396979000491341,-0.39272938866145,-0.389739251203292,-0.386639300102201,
-0.381981504688189,-0.3677011655834,-0.341224022370567,-0.319769261644209,
-0.315217033054216,-0.313088438463031,-0.311434984240698,-0.30943692280356,
-0.305556906668377,-0.279306805244778,-0.246182646921141,-0.240102127294107,
-0.236346162762977,-0.233401070820366,-0.230098518024297,-0.224480989536222,
-0.192473473150695,-0.16388621508564,-0.159509715836151,-0.157455203662948,
-0.155830625770511,-0.154253975644828,-0.150980029631323,-0.134319316703853,
-0.101223408466219,-0.0869708181774452,-0.082187148631304,-0.079061232020367,
-0.0760536828529272,-0.0718741958664859,-0.0613972647754574,-0.0454953477256854,
-0.0117766791592439,-0.00503669273596484,-0.00253609892261398,-0.00120573359873185,
-0.000459188421704137),.UNSPECIFIED.);
#3934=B_SPLINE_CURVE_WITH_KNOTS('',3,(#287666,#287667,#287668,#287669,#287670,
#287671,#287672,#287673,#287674,#287675,#287676,#287677,#287678,#287679,
#287680,#287681,#287682,#287683,#287684,#287685,#287686,#287687,#287688,
#287689,#287690,#287691,#287692,#287693,#287694,#287695,#287696,#287697,
#287698,#287699,#287700,#287701,#287702,#287703,#287704,#287705,#287706,
#287707,#287708,#287709,#287710,#287711,#287712,#287713,#287714,#287715,
#287716,#287717,#287718,#287719,#287720,#287721,#287722,#287723,#287724,
#287725,#287726,#287727,#287728,#287729,#287730,#287731,#287732,#287733,
#287734,#287735,#287736,#287737,#287738,#287739,#287740,#287741,#287742,
#287743,#287744,#287745,#287746,#287747,#287748,#287749,#287750,#287751,
#287752,#287753,#287754,#287755,#287756,#287757,#287758,#287759,#287760,
#287761,#287762,#287763,#287764,#287765,#287766,#287767,#287768,#287769,
#287770,#287771,#287772,#287773,#287774,#287775,#287776,#287777,#287778,
#287779,#287780,#287781,#287782,#287783,#287784,#287785,#287786,#287787,
#287788,#287789,#287790,#287791,#287792,#287793,#287794,#287795,#287796,
#287797,#287798,#287799,#287800,#287801,#287802,#287803,#287804,#287805,
#287806,#287807,#287808,#287809,#287810,#287811,#287812,#287813,#287814,
#287815,#287816,#287817,#287818,#287819,#287820,#287821,#287822,#287823,
#287824,#287825,#287826,#287827,#287828,#287829,#287830,#287831,#287832,
#287833,#287834,#287835,#287836,#287837,#287838,#287839,#287840,#287841,
#287842,#287843,#287844,#287845,#287846,#287847,#287848,#287849,#287850,
#287851,#287852,#287853,#287854,#287855,#287856,#287857,#287858,#287859,
#287860,#287861,#287862,#287863,#287864,#287865,#287866,#287867,#287868,
#287869,#287870,#287871,#287872,#287873,#287874,#287875,#287876,#287877,
#287878,#287879,#287880,#287881,#287882,#287883,#287884,#287885,#287886,
#287887,#287888,#287889,#287890,#287891,#287892,#287893,#287894,#287895,
#287896,#287897,#287898,#287899,#287900,#287901,#287902,#287903,#287904,
#287905,#287906,#287907,#287908,#287909,#287910,#287911,#287912,#287913,
#287914,#287915,#287916,#287917,#287918,#287919,#287920,#287921,#287922,
#287923,#287924,#287925,#287926,#287927,#287928,#287929,#287930,#287931,
#287932,#287933,#287934,#287935,#287936,#287937,#287938,#287939,#287940,
#287941,#287942,#287943,#287944,#287945,#287946,#287947,#287948,#287949,
#287950,#287951,#287952,#287953,#287954,#287955,#287956,#287957,#287958,
#287959,#287960,#287961,#287962,#287963,#287964,#287965,#287966,#287967,
#287968,#287969,#287970,#287971,#287972,#287973,#287974,#287975,#287976,
#287977,#287978,#287979,#287980,#287981,#287982,#287983,#287984,#287985,
#287986,#287987,#287988,#287989,#287990,#287991,#287992,#287993,#287994,
#287995,#287996,#287997,#287998,#287999,#288000,#288001,#288002,#288003,
#288004,#288005,#288006,#288007,#288008,#288009,#288010,#288011,#288012,
#288013,#288014,#288015,#288016,#288017,#288018,#288019,#288020,#288021,
#288022,#288023,#288024,#288025,#288026,#288027,#288028,#288029,#288030,
#288031,#288032,#288033,#288034,#288035,#288036,#288037,#288038,#288039,
#288040,#288041,#288042,#288043,#288044,#288045,#288046,#288047,#288048,
#288049,#288050,#288051,#288052,#288053,#288054,#288055,#288056,#288057,
#288058,#288059),.UNSPECIFIED.,.F.,.F.,(4,2,2,2,2,2,2,2,2,2,2,2,2,2,2,2,
2,2,2,2,2,2,2,2,2,2,2,2,2,2,2,2,2,2,2,2,2,2,2,2,2,2,2,2,2,2,2,2,2,2,2,2,
2,2,2,2,2,2,2,2,2,2,2,2,2,2,2,2,2,2,2,2,2,2,2,2,2,2,2,2,2,2,2,2,2,2,2,2,
2,2,2,2,2,2,2,2,2,2,2,2,2,2,2,2,2,2,2,2,2,2,2,2,2,2,2,2,2,2,2,2,2,2,2,2,
2,2,2,2,2,2,2,2,2,2,2,2,2,2,2,2,2,2,2,2,2,2,2,2,2,2,2,2,2,2,2,2,2,2,2,2,
2,2,2,2,2,2,2,2,2,2,2,2,2,2,2,2,2,2,2,2,2,2,2,2,2,2,2,2,2,2,2,2,2,2,2,2,
4),(-1.9611673957392,-1.96016519546567,-1.95806538538097,-1.95278185055767,
-1.92364544687139,-1.89436234085666,-1.88839906744968,-1.88502417177433,
-1.88208976907284,-1.87844663995391,-1.87138498223882,-1.82523864669928,
-1.81131457205485,-1.80817724511147,-1.80661198665112,-1.80503286300625,
-1.80294845355175,-1.79840870030172,-1.77335105337488,-1.74952112883501,
-1.73603458245084,-1.73146493035852,-1.72838314132594,-1.72538010075568,
-1.72174178211632,-1.71274134917748,-1.67740646933661,-1.66293791591079,
-1.65741613364037,-1.65329676537599,-1.65125099478705,-1.64959961310219,
-1.64752570551909,-1.64326198815116,-1.61301500819911,-1.58346032774662,
-1.57732951285517,-1.5739192553444,-1.57098700560496,-1.56738849405611,
-1.56184493976454,-1.52302542333784,-1.5025499704124,-1.49794839041937,
-1.49581071980139,-1.49431455817983,-1.49239285293329,-1.48897585029047,
-1.46653589014626,-1.44033503255081,-1.42522077937578,-1.4204772665667,
-1.41735980959863,-1.41438140923533,-1.41019723486105,-1.40045601130615,
-1.3659081961078,-1.35165105251854,-1.34617877205721,-1.34208748441745,
-1.34004718626234,-1.3383956443995,-1.33631579057709,-1.33202142795984,
-1.30224086670305,-1.27160103189081,-1.2658391302085,-1.26250603709949,
-1.25956586151176,-1.25585958926541,-1.2499503675809,-1.21439732416657,
-1.19017252824694,-1.18632138550885,-1.18432913671439,-1.18267507371549,
-1.1805387636451,-1.1759456998215,-1.15260536820296,-1.12759142186693,-1.11373749971027,
-1.10912588280886,-1.10603509595507,-1.10303772639204,-1.09874973639694,
-1.08829507911383,-1.04683355271912,-1.03769688604123,-1.03172377170882,
-1.02935553230645,-1.02767370017678,-1.0258177510275,-1.02261263008967,
-1.00932326852602,-0.981008977022601,-0.959635617359899,-0.954272034446866,
-0.951023485142151,-0.948066467553294,-0.944209850276027,-0.935747962742308,
-0.924003554405793,-0.903016213465774,-0.899570304842173,-0.878288119037644,
-0.874879972801479,-0.87296021427923,-0.87146362229038,-0.869322898507965,
-0.864705172039215,-0.858282536669326,-0.839584271391387,-0.806477244695053,
-0.80039366696955,-0.79663648932047,-0.793690859339245,-0.790388134409911,
-0.784771385638642,-0.777930488199467,-0.763053741948654,-0.751011459186111,
-0.724361076229272,-0.720316173979186,-0.718260704439915,-0.716582639652633,
-0.714759860196404,-0.711711225023784,-0.699209560324061,-0.666555405839308,
-0.648129225779971,-0.642946402973789,-0.639735216273813,-0.636764676574435,
-0.632819935596121,-0.623848778231175,-0.611118747481093,-0.591458523056005,
-0.587032305596243,-0.567115638374932,-0.56371437882382,-0.561795908648431,
-0.560300002934469,-0.558159234916667,-0.553533867101322,-0.547095395556165,
-0.528308420461051,-0.495312692365467,-0.489225328597204,-0.485469200234375,
-0.482526532002409,-0.479229443962417,-0.473628359517275,-0.441294490502044,
-0.413061951103913,-0.408642309859204,-0.406539593377406,-0.404888207682348,
-0.402870625101657,-0.398892978374733,-0.373718499471914,-0.339483567433424,
-0.333460015780257,-0.329719324433717,-0.326774321659905,-0.323459406606933,
-0.317789233447674,-0.285697930154697,-0.257383744529701,-0.252972870071412,
-0.250868802025502,-0.249211428455891,-0.247178898514742,-0.24315520439613,
-0.219066434949421,-0.183997054195899,-0.178069014690526,-0.174351947776504,
-0.171403285390817,-0.168060339157487,-0.162280065897901,-0.130174799117912,
-0.101962090833413,-0.0975347085064821,-0.0954288346192596,-0.0937818577306343,
-0.091782605764983,-0.0878475325360492,-0.0826388017654838,-0.0694404849422195,
-0.041018148063621,-0.0250328156673991,-0.020094173685207,-0.0169509929212847,
-0.0141621129991528,-0.0112755590203426,-0.00655231744414157,-0.000479338372087868),
 .UNSPECIFIED.);
#3935=B_SPLINE_CURVE_WITH_KNOTS('',3,(#288062,#288063,#288064,#288065,#288066,
#288067,#288068,#288069,#288070,#288071,#288072,#288073,#288074,#288075,
#288076,#288077,#288078,#288079,#288080,#288081,#288082,#288083),
 .UNSPECIFIED.,.F.,.F.,(4,2,2,2,2,2,2,2,2,2,4),(-0.474818783494366,-0.449281592936105,
-0.422497485793653,-0.381203422480266,-0.329907980372939,-0.265893426931644,
-0.195666061625486,-0.136911508948015,-0.0686118601292609,-0.0311014517309063,
-2.45319125318871E-5),.UNSPECIFIED.);
#3936=B_SPLINE_CURVE_WITH_KNOTS('',3,(#288084,#288085,#288086,#288087,#288088,
#288089,#288090,#288091,#288092,#288093,#288094,#288095,#288096,#288097,
#288098,#288099,#288100,#288101,#288102,#288103,#288104,#288105,#288106,
#288107,#288108,#288109,#288110,#288111,#288112,#288113,#288114,#288115,
#288116,#288117,#288118,#288119,#288120,#288121,#288122,#288123,#288124,
#288125,#288126,#288127,#288128,#288129,#288130,#288131,#288132,#288133,
#288134,#288135,#288136,#288137,#288138,#288139,#288140,#288141,#288142,
#288143,#288144),.UNSPECIFIED.,.F.,.F.,(4,3,3,3,3,3,3,3,3,3,3,3,3,3,3,3,
3,3,3,3,4),(-0.271362855059921,-0.249815156703991,-0.228817954605844,-0.214757059032555,
-0.202695986178297,-0.199258382274391,-0.179079040584676,-0.172574372312687,
-0.151002575773601,-0.132127253801901,-0.128545223737615,-0.108660382312346,
-0.0889046320299183,-0.0695673553379917,-0.0643976613730527,-0.0611873083345303,
-0.0424332578302701,-0.0240014673407122,-0.00742675770561789,-0.00610701619818059,
-1.67978587627156E-14),.UNSPECIFIED.);
#3937=B_SPLINE_CURVE_WITH_KNOTS('',3,(#288146,#288147,#288148,#288149,#288150,
#288151,#288152,#288153,#288154,#288155,#288156,#288157,#288158,#288159,
#288160,#288161,#288162,#288163,#288164,#288165,#288166,#288167,#288168,
#288169,#288170,#288171,#288172,#288173,#288174,#288175,#288176,#288177,
#288178,#288179,#288180,#288181,#288182,#288183,#288184,#288185,#288186,
#288187,#288188,#288189,#288190,#288191,#288192,#288193,#288194,#288195,
#288196,#288197,#288198,#288199,#288200,#288201,#288202,#288203,#288204,
#288205,#288206,#288207,#288208,#288209,#288210,#288211,#288212,#288213,
#288214,#288215,#288216,#288217,#288218,#288219,#288220,#288221,#288222,
#288223,#288224,#288225,#288226,#288227,#288228,#288229,#288230,#288231,
#288232,#288233,#288234,#288235,#288236,#288237,#288238,#288239,#288240,
#288241,#288242,#288243,#288244,#288245,#288246,#288247,#288248,#288249,
#288250,#288251),.UNSPECIFIED.,.F.,.F.,(4,3,3,3,3,3,3,3,3,3,3,3,3,3,3,3,
3,3,3,3,3,3,3,3,3,3,3,3,3,3,3,3,3,3,3,4),(-0.468287143792459,-0.449159592277506,
-0.442679572366002,-0.439139523917826,-0.418501747794262,-0.397540534942074,
-0.376759689901926,-0.369408338867191,-0.366188435771172,-0.344993296658329,
-0.324164935680159,-0.314417154781481,-0.302674036643168,-0.298303152413865,
-0.294792657786698,-0.273759483634418,-0.252453791079512,-0.23671297526563,
-0.228622459040654,-0.22484613779528,-0.221071692886511,-0.199520974492535,
-0.177947952659577,-0.156760757052952,-0.151824997028116,-0.148277425274246,
-0.12652726456846,-0.106361541521481,-0.105236270462937,-0.0835127492652271,
-0.0784406535722348,-0.0733870619889256,-0.0516031153801045,-0.029512914496819,
-0.0074997402847098,-5.64290021016797E-6),.UNSPECIFIED.);
#3938=B_SPLINE_CURVE_WITH_KNOTS('',3,(#288255,#288256,#288257,#288258),
 .UNSPECIFIED.,.F.,.F.,(4,4),(-0.468408500436428,-0.468287143792459),
 .UNSPECIFIED.);
#3939=B_SPLINE_CURVE_WITH_KNOTS('',3,(#288683,#288684,#288685,#288686,#288687,
#288688,#288689,#288690,#288691,#288692,#288693,#288694,#288695,#288696,
#288697,#288698,#288699,#288700,#288701,#288702,#288703,#288704,#288705,
#288706,#288707,#288708,#288709,#288710,#288711,#288712,#288713,#288714,
#288715,#288716,#288717,#288718,#288719,#288720,#288721,#288722,#288723,
#288724,#288725,#288726,#288727,#288728,#288729,#288730,#288731,#288732,
#288733,#288734,#288735,#288736,#288737,#288738,#288739,#288740,#288741,
#288742,#288743,#288744,#288745,#288746,#288747,#288748,#288749,#288750,
#288751,#288752,#288753,#288754,#288755,#288756,#288757,#288758,#288759,
#288760,#288761,#288762,#288763,#288764),.UNSPECIFIED.,.F.,.F.,(4,3,3,3,
3,3,3,3,3,3,3,3,3,3,3,3,3,3,3,3,3,3,3,3,3,3,3,4),(-0.364629307890661,-0.350885759085945,
-0.329296488089375,-0.313741431878983,-0.309365163672801,-0.288066104157163,
-0.266903491756204,-0.264006177467146,-0.26029818106468,-0.239602719874145,
-0.219188969841738,-0.199417322698614,-0.194876880502573,-0.191399047668888,
-0.171813366976952,-0.166173598315468,-0.146078147584166,-0.126706873608775,
-0.123379860192083,-0.103933041502093,-0.0846705822529982,-0.065567586070534,
-0.0621782887363481,-0.05894467115978,-0.0403543924363754,-0.0220984153978988,
-0.00442511139655304,0.),.UNSPECIFIED.);
#3940=B_SPLINE_CURVE_WITH_KNOTS('',3,(#289197,#289198,#289199,#289200,#289201,
#289202,#289203,#289204,#289205,#289206,#289207,#289208,#289209,#289210,
#289211,#289212,#289213,#289214,#289215,#289216,#289217,#289218,#289219,
#289220,#289221,#289222,#289223,#289224,#289225,#289226,#289227,#289228,
#289229,#289230,#289231,#289232,#289233,#289234,#289235,#289236,#289237,
#289238,#289239,#289240,#289241,#289242,#289243,#289244,#289245,#289246,
#289247,#289248,#289249,#289250,#289251,#289252,#289253,#289254,#289255,
#289256,#289257,#289258,#289259,#289260,#289261,#289262,#289263,#289264,
#289265,#289266,#289267,#289268,#289269,#289270,#289271,#289272,#289273,
#289274,#289275,#289276,#289277,#289278),.UNSPECIFIED.,.F.,.F.,(4,3,3,3,
3,3,3,3,3,3,3,3,3,3,3,3,3,3,3,3,3,3,3,3,3,3,3,4),(-0.366397579005845,-0.355461226466819,
-0.337381714695455,-0.327214164040339,-0.321649482146298,-0.302845846606557,
-0.288386907394637,-0.281257238921911,-0.277593927902022,-0.258058508053395,
-0.238234782514783,-0.218411056976172,-0.214856426708649,-0.194426531580489,
-0.187209422476688,-0.167411754208573,-0.156894426252658,-0.149523127563347,
-0.145921626399787,-0.125575048930976,-0.104563171293481,-0.0835512936559854,
-0.0752831225832569,-0.0721648689176682,-0.0505208253806571,-0.028827309114918,
-0.00759789022673524,-5.75490197052316E-15),.UNSPECIFIED.);
#4558=LINE('',#288253,#5195);
#4559=LINE('',#289282,#5196);
#4560=LINE('',#289284,#5197);
#4561=LINE('',#289286,#5198);
#4562=LINE('',#289287,#5199);
#4563=LINE('',#289290,#5200);
#4564=LINE('',#289292,#5201);
#4565=LINE('',#289293,#5202);
#4566=LINE('',#289296,#5203);
#4567=LINE('',#289298,#5204);
#4568=LINE('',#289299,#5205);
#4569=LINE('',#289302,#5206);
#4570=LINE('',#289304,#5207);
#4571=LINE('',#289305,#5208);
#4572=LINE('',#289308,#5209);
#4573=LINE('',#289310,#5210);
#4574=LINE('',#289311,#5211);
#4575=LINE('',#289313,#5212);
#4576=LINE('',#289314,#5213);
#4577=LINE('',#289321,#5214);
#5195=VECTOR('',#20114,1.5);
#5196=VECTOR('',#20119,10.);
#5197=VECTOR('',#20120,10.);
#5198=VECTOR('',#20121,10.);
#5199=VECTOR('',#20122,10.);
#5200=VECTOR('',#20125,10.);
#5201=VECTOR('',#20126,10.);
#5202=VECTOR('',#20127,10.);
#5203=VECTOR('',#20130,10.);
#5204=VECTOR('',#20131,10.);
#5205=VECTOR('',#20132,10.);
#5206=VECTOR('',#20135,10.);
#5207=VECTOR('',#20136,10.);
#5208=VECTOR('',#20137,10.);
#5209=VECTOR('',#20140,10.);
#5210=VECTOR('',#20141,10.);
#5211=VECTOR('',#20142,10.);
#5212=VECTOR('',#20145,10.);
#5213=VECTOR('',#20146,10.);
#5214=VECTOR('',#20155,3.5);
#7316=VERTEX_POINT('',#279131);
#7317=VERTEX_POINT('',#279132);
#7318=VERTEX_POINT('',#279194);
#7319=VERTEX_POINT('',#279196);
#7320=VERTEX_POINT('',#279231);
#7321=VERTEX_POINT('',#279422);
#7322=VERTEX_POINT('',#279433);
#7323=VERTEX_POINT('',#279627);
#7324=VERTEX_POINT('',#279818);
#7325=VERTEX_POINT('',#279829);
#7326=VERTEX_POINT('',#280020);
#7327=VERTEX_POINT('',#280032);
#7328=VERTEX_POINT('',#280043);
#7329=VERTEX_POINT('',#280234);
#7330=VERTEX_POINT('',#280246);
#7331=VERTEX_POINT('',#280257);
#7332=VERTEX_POINT('',#280448);
#7333=VERTEX_POINT('',#280459);
#7334=VERTEX_POINT('',#280650);
#7335=VERTEX_POINT('',#280661);
#7336=VERTEX_POINT('',#280670);
#7337=VERTEX_POINT('',#280672);
#7338=VERTEX_POINT('',#280761);
#7339=VERTEX_POINT('',#280772);
#7340=VERTEX_POINT('',#280963);
#7341=VERTEX_POINT('',#281157);
#7342=VERTEX_POINT('',#281168);
#7343=VERTEX_POINT('',#281359);
#7344=VERTEX_POINT('',#281550);
#7345=VERTEX_POINT('',#281561);
#7346=VERTEX_POINT('',#281572);
#7347=VERTEX_POINT('',#281763);
#7348=VERTEX_POINT('',#281774);
#7349=VERTEX_POINT('',#281785);
#7350=VERTEX_POINT('',#281976);
#7351=VERTEX_POINT('',#282170);
#7352=VERTEX_POINT('',#282192);
#7353=VERTEX_POINT('',#282193);
#7354=VERTEX_POINT('',#282315);
#7355=VERTEX_POINT('',#282317);
#7356=VERTEX_POINT('',#282403);
#7357=VERTEX_POINT('',#282860);
#7358=VERTEX_POINT('',#283271);
#7359=VERTEX_POINT('',#283282);
#7360=VERTEX_POINT('',#283681);
#7361=VERTEX_POINT('',#283692);
#7362=VERTEX_POINT('',#284105);
#7363=VERTEX_POINT('',#284116);
#7364=VERTEX_POINT('',#284517);
#7365=VERTEX_POINT('',#284922);
#7366=VERTEX_POINT('',#285071);
#7367=VERTEX_POINT('',#285073);
#7368=VERTEX_POINT('',#285186);
#7369=VERTEX_POINT('',#285577);
#7370=VERTEX_POINT('',#286000);
#7371=VERTEX_POINT('',#286399);
#7372=VERTEX_POINT('',#286411);
#7373=VERTEX_POINT('',#286870);
#7374=VERTEX_POINT('',#287275);
#7375=VERTEX_POINT('',#288061);
#7376=VERTEX_POINT('',#288145);
#7377=VERTEX_POINT('',#288252);
#7378=VERTEX_POINT('',#289280);
#7379=VERTEX_POINT('',#289281);
#7380=VERTEX_POINT('',#289283);
#7381=VERTEX_POINT('',#289285);
#7382=VERTEX_POINT('',#289289);
#7383=VERTEX_POINT('',#289291);
#7384=VERTEX_POINT('',#289295);
#7385=VERTEX_POINT('',#289297);
#7386=VERTEX_POINT('',#289301);
#7387=VERTEX_POINT('',#289303);
#7388=VERTEX_POINT('',#289307);
#7389=VERTEX_POINT('',#289309);
#7390=VERTEX_POINT('',#289317);
#7391=VERTEX_POINT('',#289320);
#10073=EDGE_CURVE('',#7316,#7317,#3880,.T.);
#10074=EDGE_CURVE('',#7317,#7318,#1982,.F.);
#10075=EDGE_CURVE('',#7318,#7319,#3881,.T.);
#10076=EDGE_CURVE('',#7319,#7320,#3882,.T.);
#10077=EDGE_CURVE('',#7320,#7321,#3883,.T.);
#10078=EDGE_CURVE('',#7321,#7322,#3884,.T.);
#10079=EDGE_CURVE('',#7322,#7323,#3885,.T.);
#10080=EDGE_CURVE('',#7323,#7324,#3886,.T.);
#10081=EDGE_CURVE('',#7324,#7325,#3887,.T.);
#10082=EDGE_CURVE('',#7325,#7326,#3888,.T.);
#10083=EDGE_CURVE('',#7326,#7327,#3889,.T.);
#10084=EDGE_CURVE('',#7327,#7328,#3890,.T.);
#10085=EDGE_CURVE('',#7328,#7329,#3891,.T.);
#10086=EDGE_CURVE('',#7329,#7330,#3892,.T.);
#10087=EDGE_CURVE('',#7330,#7331,#3893,.T.);
#10088=EDGE_CURVE('',#7331,#7332,#3894,.T.);
#10089=EDGE_CURVE('',#7332,#7333,#3895,.T.);
#10090=EDGE_CURVE('',#7333,#7334,#3896,.T.);
#10091=EDGE_CURVE('',#7334,#7335,#3897,.T.);
#10092=EDGE_CURVE('',#7335,#7336,#1983,.T.);
#10093=EDGE_CURVE('',#7336,#7337,#3898,.T.);
#10094=EDGE_CURVE('',#7337,#7338,#3899,.T.);
#10095=EDGE_CURVE('',#7338,#7339,#3900,.T.);
#10096=EDGE_CURVE('',#7339,#7340,#3901,.T.);
#10097=EDGE_CURVE('',#7340,#7341,#3902,.T.);
#10098=EDGE_CURVE('',#7341,#7342,#3903,.T.);
#10099=EDGE_CURVE('',#7342,#7343,#3904,.T.);
#10100=EDGE_CURVE('',#7343,#7344,#3905,.T.);
#10101=EDGE_CURVE('',#7344,#7345,#3906,.T.);
#10102=EDGE_CURVE('',#7345,#7346,#3907,.T.);
#10103=EDGE_CURVE('',#7346,#7347,#3908,.T.);
#10104=EDGE_CURVE('',#7347,#7348,#3909,.T.);
#10105=EDGE_CURVE('',#7348,#7349,#3910,.T.);
#10106=EDGE_CURVE('',#7349,#7350,#3911,.T.);
#10107=EDGE_CURVE('',#7350,#7351,#3912,.T.);
#10108=EDGE_CURVE('',#7351,#7316,#3913,.T.);
#10109=EDGE_CURVE('',#7352,#7353,#3914,.T.);
#10110=EDGE_CURVE('',#7353,#7354,#1984,.T.);
#10111=EDGE_CURVE('',#7355,#7354,#3915,.T.);
#10112=EDGE_CURVE('',#7356,#7355,#3916,.F.);
#10113=EDGE_CURVE('',#7357,#7356,#3917,.F.);
#10114=EDGE_CURVE('',#7358,#7357,#3918,.T.);
#10115=EDGE_CURVE('',#7359,#7358,#3919,.F.);
#10116=EDGE_CURVE('',#7360,#7359,#3920,.T.);
#10117=EDGE_CURVE('',#7361,#7360,#3921,.F.);
#10118=EDGE_CURVE('',#7362,#7361,#3922,.T.);
#10119=EDGE_CURVE('',#7363,#7362,#3923,.F.);
#10120=EDGE_CURVE('',#7364,#7363,#3924,.F.);
#10121=EDGE_CURVE('',#7365,#7364,#3925,.T.);
#10122=EDGE_CURVE('',#7366,#7365,#1985,.T.);
#10123=EDGE_CURVE('',#7366,#7367,#3926,.T.);
#10124=EDGE_CURVE('',#7367,#7368,#3927,.T.);
#10125=EDGE_CURVE('',#7368,#7369,#3928,.T.);
#10126=EDGE_CURVE('',#7369,#7370,#3929,.T.);
#10127=EDGE_CURVE('',#7370,#7371,#3930,.T.);
#10128=EDGE_CURVE('',#7371,#7372,#3931,.T.);
#10129=EDGE_CURVE('',#7372,#7373,#3932,.T.);
#10130=EDGE_CURVE('',#7373,#7374,#3933,.T.);
#10131=EDGE_CURVE('',#7374,#7352,#3934,.T.);
#10132=EDGE_CURVE('',#7354,#7375,#3935,.T.);
#10133=EDGE_CURVE('',#7336,#7353,#3936,.T.);
#10134=EDGE_CURVE('',#7376,#7335,#3937,.T.);
#10135=EDGE_CURVE('',#7376,#7377,#4558,.T.);
#10136=EDGE_CURVE('',#7377,#7377,#1986,.T.);
#10137=EDGE_CURVE('',#7375,#7376,#3938,.T.);
#10138=EDGE_CURVE('',#7317,#7366,#3939,.T.);
#10139=EDGE_CURVE('',#7365,#7318,#3940,.T.);
#10140=EDGE_CURVE('',#7378,#7379,#4559,.T.);
#10141=EDGE_CURVE('',#7378,#7380,#4560,.T.);
#10142=EDGE_CURVE('',#7380,#7381,#4561,.T.);
#10143=EDGE_CURVE('',#7379,#7381,#4562,.T.);
#10144=EDGE_CURVE('',#7382,#7378,#4563,.T.);
#10145=EDGE_CURVE('',#7382,#7383,#4564,.T.);
#10146=EDGE_CURVE('',#7383,#7380,#4565,.T.);
#10147=EDGE_CURVE('',#7384,#7382,#4566,.T.);
#10148=EDGE_CURVE('',#7384,#7385,#4567,.T.);
#10149=EDGE_CURVE('',#7385,#7383,#4568,.T.);
#10150=EDGE_CURVE('',#7386,#7384,#4569,.T.);
#10151=EDGE_CURVE('',#7386,#7387,#4570,.T.);
#10152=EDGE_CURVE('',#7387,#7385,#4571,.T.);
#10153=EDGE_CURVE('',#7388,#7386,#4572,.T.);
#10154=EDGE_CURVE('',#7388,#7389,#4573,.T.);
#10155=EDGE_CURVE('',#7389,#7387,#4574,.T.);
#10156=EDGE_CURVE('',#7379,#7388,#4575,.T.);
#10157=EDGE_CURVE('',#7381,#7389,#4576,.T.);
#10158=EDGE_CURVE('',#7390,#7390,#1987,.T.);
#10159=EDGE_CURVE('',#7390,#7391,#4577,.T.);
#10160=EDGE_CURVE('',#7391,#7391,#1988,.T.);
#15523=ORIENTED_EDGE('',*,*,#10073,.T.);
#15524=ORIENTED_EDGE('',*,*,#10074,.T.);
#15525=ORIENTED_EDGE('',*,*,#10075,.T.);
#15526=ORIENTED_EDGE('',*,*,#10076,.T.);
#15527=ORIENTED_EDGE('',*,*,#10077,.T.);
#15528=ORIENTED_EDGE('',*,*,#10078,.T.);
#15529=ORIENTED_EDGE('',*,*,#10079,.T.);
#15530=ORIENTED_EDGE('',*,*,#10080,.T.);
#15531=ORIENTED_EDGE('',*,*,#10081,.T.);
#15532=ORIENTED_EDGE('',*,*,#10082,.T.);
#15533=ORIENTED_EDGE('',*,*,#10083,.T.);
#15534=ORIENTED_EDGE('',*,*,#10084,.T.);
#15535=ORIENTED_EDGE('',*,*,#10085,.T.);
#15536=ORIENTED_EDGE('',*,*,#10086,.T.);
#15537=ORIENTED_EDGE('',*,*,#10087,.T.);
#15538=ORIENTED_EDGE('',*,*,#10088,.T.);
#15539=ORIENTED_EDGE('',*,*,#10089,.T.);
#15540=ORIENTED_EDGE('',*,*,#10090,.T.);
#15541=ORIENTED_EDGE('',*,*,#10091,.T.);
#15542=ORIENTED_EDGE('',*,*,#10092,.T.);
#15543=ORIENTED_EDGE('',*,*,#10093,.T.);
#15544=ORIENTED_EDGE('',*,*,#10094,.T.);
#15545=ORIENTED_EDGE('',*,*,#10095,.T.);
#15546=ORIENTED_EDGE('',*,*,#10096,.T.);
#15547=ORIENTED_EDGE('',*,*,#10097,.T.);
#15548=ORIENTED_EDGE('',*,*,#10098,.T.);
#15549=ORIENTED_EDGE('',*,*,#10099,.T.);
#15550=ORIENTED_EDGE('',*,*,#10100,.T.);
#15551=ORIENTED_EDGE('',*,*,#10101,.T.);
#15552=ORIENTED_EDGE('',*,*,#10102,.T.);
#15553=ORIENTED_EDGE('',*,*,#10103,.T.);
#15554=ORIENTED_EDGE('',*,*,#10104,.T.);
#15555=ORIENTED_EDGE('',*,*,#10105,.T.);
#15556=ORIENTED_EDGE('',*,*,#10106,.T.);
#15557=ORIENTED_EDGE('',*,*,#10107,.T.);
#15558=ORIENTED_EDGE('',*,*,#10108,.T.);
#15559=ORIENTED_EDGE('',*,*,#10109,.T.);
#15560=ORIENTED_EDGE('',*,*,#10110,.T.);
#15561=ORIENTED_EDGE('',*,*,#10111,.F.);
#15562=ORIENTED_EDGE('',*,*,#10112,.F.);
#15563=ORIENTED_EDGE('',*,*,#10113,.F.);
#15564=ORIENTED_EDGE('',*,*,#10114,.F.);
#15565=ORIENTED_EDGE('',*,*,#10115,.F.);
#15566=ORIENTED_EDGE('',*,*,#10116,.F.);
#15567=ORIENTED_EDGE('',*,*,#10117,.F.);
#15568=ORIENTED_EDGE('',*,*,#10118,.F.);
#15569=ORIENTED_EDGE('',*,*,#10119,.F.);
#15570=ORIENTED_EDGE('',*,*,#10120,.F.);
#15571=ORIENTED_EDGE('',*,*,#10121,.F.);
#15572=ORIENTED_EDGE('',*,*,#10122,.F.);
#15573=ORIENTED_EDGE('',*,*,#10123,.T.);
#15574=ORIENTED_EDGE('',*,*,#10124,.T.);
#15575=ORIENTED_EDGE('',*,*,#10125,.T.);
#15576=ORIENTED_EDGE('',*,*,#10126,.T.);
#15577=ORIENTED_EDGE('',*,*,#10127,.T.);
#15578=ORIENTED_EDGE('',*,*,#10128,.T.);
#15579=ORIENTED_EDGE('',*,*,#10129,.T.);
#15580=ORIENTED_EDGE('',*,*,#10130,.T.);
#15581=ORIENTED_EDGE('',*,*,#10131,.T.);
#15582=ORIENTED_EDGE('',*,*,#10132,.F.);
#15583=ORIENTED_EDGE('',*,*,#10110,.F.);
#15584=ORIENTED_EDGE('',*,*,#10133,.F.);
#15585=ORIENTED_EDGE('',*,*,#10092,.F.);
#15586=ORIENTED_EDGE('',*,*,#10134,.F.);
#15587=ORIENTED_EDGE('',*,*,#10135,.T.);
#15588=ORIENTED_EDGE('',*,*,#10136,.F.);
#15589=ORIENTED_EDGE('',*,*,#10135,.F.);
#15590=ORIENTED_EDGE('',*,*,#10137,.F.);
#15591=ORIENTED_EDGE('',*,*,#10133,.T.);
#15592=ORIENTED_EDGE('',*,*,#10109,.F.);
#15593=ORIENTED_EDGE('',*,*,#10131,.F.);
#15594=ORIENTED_EDGE('',*,*,#10130,.F.);
#15595=ORIENTED_EDGE('',*,*,#10129,.F.);
#15596=ORIENTED_EDGE('',*,*,#10128,.F.);
#15597=ORIENTED_EDGE('',*,*,#10127,.F.);
#15598=ORIENTED_EDGE('',*,*,#10126,.F.);
#15599=ORIENTED_EDGE('',*,*,#10125,.F.);
#15600=ORIENTED_EDGE('',*,*,#10124,.F.);
#15601=ORIENTED_EDGE('',*,*,#10123,.F.);
#15602=ORIENTED_EDGE('',*,*,#10138,.F.);
#15603=ORIENTED_EDGE('',*,*,#10073,.F.);
#15604=ORIENTED_EDGE('',*,*,#10108,.F.);
#15605=ORIENTED_EDGE('',*,*,#10107,.F.);
#15606=ORIENTED_EDGE('',*,*,#10106,.F.);
#15607=ORIENTED_EDGE('',*,*,#10105,.F.);
#15608=ORIENTED_EDGE('',*,*,#10104,.F.);
#15609=ORIENTED_EDGE('',*,*,#10103,.F.);
#15610=ORIENTED_EDGE('',*,*,#10102,.F.);
#15611=ORIENTED_EDGE('',*,*,#10101,.F.);
#15612=ORIENTED_EDGE('',*,*,#10100,.F.);
#15613=ORIENTED_EDGE('',*,*,#10099,.F.);
#15614=ORIENTED_EDGE('',*,*,#10098,.F.);
#15615=ORIENTED_EDGE('',*,*,#10097,.F.);
#15616=ORIENTED_EDGE('',*,*,#10096,.F.);
#15617=ORIENTED_EDGE('',*,*,#10095,.F.);
#15618=ORIENTED_EDGE('',*,*,#10094,.F.);
#15619=ORIENTED_EDGE('',*,*,#10093,.F.);
#15620=ORIENTED_EDGE('',*,*,#10132,.T.);
#15621=ORIENTED_EDGE('',*,*,#10137,.T.);
#15622=ORIENTED_EDGE('',*,*,#10134,.T.);
#15623=ORIENTED_EDGE('',*,*,#10091,.F.);
#15624=ORIENTED_EDGE('',*,*,#10090,.F.);
#15625=ORIENTED_EDGE('',*,*,#10089,.F.);
#15626=ORIENTED_EDGE('',*,*,#10088,.F.);
#15627=ORIENTED_EDGE('',*,*,#10087,.F.);
#15628=ORIENTED_EDGE('',*,*,#10086,.F.);
#15629=ORIENTED_EDGE('',*,*,#10085,.F.);
#15630=ORIENTED_EDGE('',*,*,#10084,.F.);
#15631=ORIENTED_EDGE('',*,*,#10083,.F.);
#15632=ORIENTED_EDGE('',*,*,#10082,.F.);
#15633=ORIENTED_EDGE('',*,*,#10081,.F.);
#15634=ORIENTED_EDGE('',*,*,#10080,.F.);
#15635=ORIENTED_EDGE('',*,*,#10079,.F.);
#15636=ORIENTED_EDGE('',*,*,#10078,.F.);
#15637=ORIENTED_EDGE('',*,*,#10077,.F.);
#15638=ORIENTED_EDGE('',*,*,#10076,.F.);
#15639=ORIENTED_EDGE('',*,*,#10075,.F.);
#15640=ORIENTED_EDGE('',*,*,#10139,.F.);
#15641=ORIENTED_EDGE('',*,*,#10121,.T.);
#15642=ORIENTED_EDGE('',*,*,#10120,.T.);
#15643=ORIENTED_EDGE('',*,*,#10119,.T.);
#15644=ORIENTED_EDGE('',*,*,#10118,.T.);
#15645=ORIENTED_EDGE('',*,*,#10117,.T.);
#15646=ORIENTED_EDGE('',*,*,#10116,.T.);
#15647=ORIENTED_EDGE('',*,*,#10115,.T.);
#15648=ORIENTED_EDGE('',*,*,#10114,.T.);
#15649=ORIENTED_EDGE('',*,*,#10113,.T.);
#15650=ORIENTED_EDGE('',*,*,#10112,.T.);
#15651=ORIENTED_EDGE('',*,*,#10111,.T.);
#15652=ORIENTED_EDGE('',*,*,#10140,.F.);
#15653=ORIENTED_EDGE('',*,*,#10141,.T.);
#15654=ORIENTED_EDGE('',*,*,#10142,.T.);
#15655=ORIENTED_EDGE('',*,*,#10143,.F.);
#15656=ORIENTED_EDGE('',*,*,#10144,.F.);
#15657=ORIENTED_EDGE('',*,*,#10145,.T.);
#15658=ORIENTED_EDGE('',*,*,#10146,.T.);
#15659=ORIENTED_EDGE('',*,*,#10141,.F.);
#15660=ORIENTED_EDGE('',*,*,#10147,.F.);
#15661=ORIENTED_EDGE('',*,*,#10148,.T.);
#15662=ORIENTED_EDGE('',*,*,#10149,.T.);
#15663=ORIENTED_EDGE('',*,*,#10145,.F.);
#15664=ORIENTED_EDGE('',*,*,#10150,.F.);
#15665=ORIENTED_EDGE('',*,*,#10151,.T.);
#15666=ORIENTED_EDGE('',*,*,#10152,.T.);
#15667=ORIENTED_EDGE('',*,*,#10148,.F.);
#15668=ORIENTED_EDGE('',*,*,#10153,.F.);
#15669=ORIENTED_EDGE('',*,*,#10154,.T.);
#15670=ORIENTED_EDGE('',*,*,#10155,.T.);
#15671=ORIENTED_EDGE('',*,*,#10151,.F.);
#15672=ORIENTED_EDGE('',*,*,#10156,.F.);
#15673=ORIENTED_EDGE('',*,*,#10143,.T.);
#15674=ORIENTED_EDGE('',*,*,#10157,.T.);
#15675=ORIENTED_EDGE('',*,*,#10154,.F.);
#15676=ORIENTED_EDGE('',*,*,#10157,.F.);
#15677=ORIENTED_EDGE('',*,*,#10142,.F.);
#15678=ORIENTED_EDGE('',*,*,#10146,.F.);
#15679=ORIENTED_EDGE('',*,*,#10149,.F.);
#15680=ORIENTED_EDGE('',*,*,#10152,.F.);
#15681=ORIENTED_EDGE('',*,*,#10155,.F.);
#15682=ORIENTED_EDGE('',*,*,#10158,.T.);
#15683=ORIENTED_EDGE('',*,*,#10138,.T.);
#15684=ORIENTED_EDGE('',*,*,#10122,.T.);
#15685=ORIENTED_EDGE('',*,*,#10139,.T.);
#15686=ORIENTED_EDGE('',*,*,#10074,.F.);
#15687=ORIENTED_EDGE('',*,*,#10158,.F.);
#15688=ORIENTED_EDGE('',*,*,#10159,.T.);
#15689=ORIENTED_EDGE('',*,*,#10160,.T.);
#15690=ORIENTED_EDGE('',*,*,#10159,.F.);
#15691=ORIENTED_EDGE('',*,*,#10160,.F.);
#15692=ORIENTED_EDGE('',*,*,#10140,.T.);
#15693=ORIENTED_EDGE('',*,*,#10156,.T.);
#15694=ORIENTED_EDGE('',*,*,#10153,.T.);
#15695=ORIENTED_EDGE('',*,*,#10150,.T.);
#15696=ORIENTED_EDGE('',*,*,#10147,.T.);
#15697=ORIENTED_EDGE('',*,*,#10144,.T.);
#15698=ORIENTED_EDGE('',*,*,#10136,.T.);
#16188=CYLINDRICAL_SURFACE('',#17843,1.954);
#16189=CYLINDRICAL_SURFACE('',#17846,1.5555);
#16190=CYLINDRICAL_SURFACE('',#17860,3.5);
#16825=ADVANCED_FACE('',(#1057),#16188,.T.);
#16826=ADVANCED_FACE('',(#1058),#16189,.T.);
#16827=ADVANCED_FACE('',(#1059),#118,.T.);
#16828=ADVANCED_FACE('',(#1060),#301,.F.);
#16829=ADVANCED_FACE('',(#1061),#302,.F.);
#16830=ADVANCED_FACE('',(#1062),#413,.F.);
#16831=ADVANCED_FACE('',(#1063),#414,.F.);
#16832=ADVANCED_FACE('',(#1064),#415,.F.);
#16833=ADVANCED_FACE('',(#1065),#416,.F.);
#16834=ADVANCED_FACE('',(#1066),#417,.F.);
#16835=ADVANCED_FACE('',(#1067),#418,.F.);
#16836=ADVANCED_FACE('',(#1068),#419,.F.);
#16837=ADVANCED_FACE('',(#1069,#271),#420,.T.);
#16838=ADVANCED_FACE('',(#1070),#16190,.T.);
#16839=ADVANCED_FACE('',(#1071,#272),#421,.F.);
#16840=ADVANCED_FACE('',(#1072),#422,.T.);
#16857=CLOSED_SHELL('',(#16825,#16826,#16827,#16828,#16829,#16830,#16831,
#16832,#16833,#16834,#16835,#16836,#16837,#16838,#16839,#16840));
#17842=AXIS2_PLACEMENT_3D('',#279129,#20098,#20099);
#17843=AXIS2_PLACEMENT_3D('',#279130,#20100,#20101);
#17844=AXIS2_PLACEMENT_3D('',#279195,#20102,#20103);
#17845=AXIS2_PLACEMENT_3D('',#280671,#20104,#20105);
#17846=AXIS2_PLACEMENT_3D('',#282191,#20106,#20107);
#17847=AXIS2_PLACEMENT_3D('',#282316,#20108,#20109);
#17848=AXIS2_PLACEMENT_3D('',#285072,#20110,#20111);
#17849=AXIS2_PLACEMENT_3D('',#288060,#20112,#20113);
#17850=AXIS2_PLACEMENT_3D('',#288254,#20115,#20116);
#17851=AXIS2_PLACEMENT_3D('',#289279,#20117,#20118);
#17852=AXIS2_PLACEMENT_3D('',#289288,#20123,#20124);
#17853=AXIS2_PLACEMENT_3D('',#289294,#20128,#20129);
#17854=AXIS2_PLACEMENT_3D('',#289300,#20133,#20134);
#17855=AXIS2_PLACEMENT_3D('',#289306,#20138,#20139);
#17856=AXIS2_PLACEMENT_3D('',#289312,#20143,#20144);
#17857=AXIS2_PLACEMENT_3D('',#289315,#20147,#20148);
#17858=AXIS2_PLACEMENT_3D('',#289316,#20149,#20150);
#17859=AXIS2_PLACEMENT_3D('',#289318,#20151,#20152);
#17860=AXIS2_PLACEMENT_3D('',#289319,#20153,#20154);
#17861=AXIS2_PLACEMENT_3D('',#289322,#20156,#20157);
#17862=AXIS2_PLACEMENT_3D('',#289323,#20158,#20159);
#17863=AXIS2_PLACEMENT_3D('',#289324,#20160,#20161);
#20098=DIRECTION('axis',(0.,0.,1.));
#20099=DIRECTION('refdir',(1.,0.,0.));
#20100=DIRECTION('center_axis',(0.,0.,1.));
#20101=DIRECTION('ref_axis',(1.,0.,0.));
#20102=DIRECTION('center_axis',(0.,0.,-1.));
#20103=DIRECTION('ref_axis',(1.,0.,0.));
#20104=DIRECTION('center_axis',(0.,0.,-1.));
#20105=DIRECTION('ref_axis',(1.,0.,0.));
#20106=DIRECTION('center_axis',(0.,0.,1.));
#20107=DIRECTION('ref_axis',(1.,1.29731060939901E-13,0.));
#20108=DIRECTION('center_axis',(0.,0.,-1.));
#20109=DIRECTION('ref_axis',(1.,1.29731060939901E-13,0.));
#20110=DIRECTION('center_axis',(0.,0.,-1.));
#20111=DIRECTION('ref_axis',(1.,1.29731060939901E-13,0.));
#20112=DIRECTION('center_axis',(0.,0.,-1.));
#20113=DIRECTION('ref_axis',(1.,0.,0.));
#20114=DIRECTION('',(0.707106781186548,-8.65956056235494E-17,0.707106781186547));
#20115=DIRECTION('center_axis',(0.,0.,1.));
#20116=DIRECTION('ref_axis',(1.,0.,0.));
#20117=DIRECTION('center_axis',(-1.60246890531964E-16,-1.,0.));
#20118=DIRECTION('ref_axis',(1.,-1.60246890531964E-16,0.));
#20119=DIRECTION('',(1.,-1.60246890531964E-16,0.));
#20120=DIRECTION('',(0.,0.,1.));
#20121=DIRECTION('',(1.,-1.60246890531964E-16,0.));
#20122=DIRECTION('',(0.,0.,1.));
#20123=DIRECTION('center_axis',(-0.866025403784439,-0.5,0.));
#20124=DIRECTION('ref_axis',(0.5,-0.866025403784439,0.));
#20125=DIRECTION('',(0.5,-0.866025403784439,0.));
#20126=DIRECTION('',(0.,0.,1.));
#20127=DIRECTION('',(0.5,-0.866025403784439,0.));
#20128=DIRECTION('center_axis',(-0.866025403784439,0.5,0.));
#20129=DIRECTION('ref_axis',(-0.5,-0.866025403784439,0.));
#20130=DIRECTION('',(-0.5,-0.866025403784439,0.));
#20131=DIRECTION('',(0.,0.,1.));
#20132=DIRECTION('',(-0.5,-0.866025403784439,0.));
#20133=DIRECTION('center_axis',(1.60246890531964E-16,1.,0.));
#20134=DIRECTION('ref_axis',(-1.,1.60246890531964E-16,0.));
#20135=DIRECTION('',(-1.,1.60246890531964E-16,0.));
#20136=DIRECTION('',(0.,0.,1.));
#20137=DIRECTION('',(-1.,1.60246890531964E-16,0.));
#20138=DIRECTION('center_axis',(0.866025403784439,0.5,0.));
#20139=DIRECTION('ref_axis',(-0.5,0.866025403784439,0.));
#20140=DIRECTION('',(-0.5,0.866025403784439,0.));
#20141=DIRECTION('',(0.,0.,1.));
#20142=DIRECTION('',(-0.5,0.866025403784439,0.));
#20143=DIRECTION('center_axis',(0.866025403784439,-0.5,0.));
#20144=DIRECTION('ref_axis',(0.5,0.866025403784439,0.));
#20145=DIRECTION('',(0.5,0.866025403784439,0.));
#20146=DIRECTION('',(0.5,0.866025403784439,0.));
#20147=DIRECTION('center_axis',(0.,0.,1.));
#20148=DIRECTION('ref_axis',(1.,0.,0.));
#20149=DIRECTION('center_axis',(0.,0.,1.));
#20150=DIRECTION('ref_axis',(1.,0.,0.));
#20151=DIRECTION('center_axis',(0.,0.,1.));
#20152=DIRECTION('ref_axis',(1.,0.,0.));
#20153=DIRECTION('center_axis',(0.,0.,1.));
#20154=DIRECTION('ref_axis',(1.,0.,0.));
#20155=DIRECTION('',(0.,0.,-1.));
#20156=DIRECTION('center_axis',(0.,0.,1.));
#20157=DIRECTION('ref_axis',(1.,0.,0.));
#20158=DIRECTION('center_axis',(0.,0.,1.));
#20159=DIRECTION('ref_axis',(1.,0.,0.));
#20160=DIRECTION('center_axis',(0.,0.,1.));
#20161=DIRECTION('ref_axis',(1.,0.,0.));
#279129=CARTESIAN_POINT('',(0.,0.,0.));
#279130=CARTESIAN_POINT('Origin',(0.,0.,0.));
#279131=CARTESIAN_POINT('',(-1.95399958625128,0.00127158556192198,0.225869692124231));
#279132=CARTESIAN_POINT('',(0.86152788258768,1.75382031791287,3.93122677751275E-5));
#279133=CARTESIAN_POINT('Ctrl Pts',(-1.95399958625128,0.00127158556192198,
0.225869692124231));
#279134=CARTESIAN_POINT('Ctrl Pts',(-1.95395604885434,0.0681739302723082,
0.222037301306047));
#279135=CARTESIAN_POINT('Ctrl Pts',(-1.95047678667107,0.134971424000874,
0.218204910487863));
#279136=CARTESIAN_POINT('Ctrl Pts',(-1.94359242694592,0.201406250941909,
0.214372519669679));
#279137=CARTESIAN_POINT('Ctrl Pts',(-1.93654044018152,0.269458697209641,
0.21044681409867));
#279138=CARTESIAN_POINT('Ctrl Pts',(-1.92589625907381,0.337273009132259,
0.206521108527662));
#279139=CARTESIAN_POINT('Ctrl Pts',(-1.91168600925926,0.404441098310242,
0.202595402956653));
#279140=CARTESIAN_POINT('Ctrl Pts',(-1.89749720503346,0.471507819867273,
0.19867562191676));
#279141=CARTESIAN_POINT('Ctrl Pts',(-1.87975311483401,0.537929778979427,
0.194755840876867));
#279142=CARTESIAN_POINT('Ctrl Pts',(-1.85853156400509,0.603304587747175,
0.190836059836973));
#279143=CARTESIAN_POINT('Ctrl Pts',(-1.83733531306058,0.668601458049552,
0.186920951877195));
#279144=CARTESIAN_POINT('Ctrl Pts',(-1.81266998680926,0.732853193984308,
0.183005843917416));
#279145=CARTESIAN_POINT('Ctrl Pts',(-1.78466392427241,0.795669955069697,
0.179090735957637));
#279146=CARTESIAN_POINT('Ctrl Pts',(-1.7566757359944,0.858446624726809,
0.17517812673016));
#279147=CARTESIAN_POINT('Ctrl Pts',(-1.72535124054766,0.919789690158248,
0.171265517502682));
#279148=CARTESIAN_POINT('Ctrl Pts',(-1.69086730727631,0.979328213207478,
0.167352908275204));
#279149=CARTESIAN_POINT('Ctrl Pts',(-1.65639367565598,1.0388489498551,0.16344146789162));
#279150=CARTESIAN_POINT('Ctrl Pts',(-1.61876272549717,1.09656579076339,
0.159530027508035));
#279151=CARTESIAN_POINT('Ctrl Pts',(-1.57819694541281,1.15213297908257,
0.155618587124451));
#279152=CARTESIAN_POINT('Ctrl Pts',(-1.53762951278187,1.2077024310675,0.151706987398745));
#279153=CARTESIAN_POINT('Ctrl Pts',(-1.49412730369477,1.26112166244711,
0.14779538767304));
#279154=CARTESIAN_POINT('Ctrl Pts',(-1.44795468666975,1.31207592209868,
0.143883787947335));
#279155=CARTESIAN_POINT('Ctrl Pts',(-1.4017348387758,1.36308230385452,0.139968186970113));
#279156=CARTESIAN_POINT('Ctrl Pts',(-1.35283946070058,1.41161831784349,
0.13605258599289));
#279157=CARTESIAN_POINT('Ctrl Pts',(-1.30157089688553,1.45740495414987,
0.132136985015667));
#279158=CARTESIAN_POINT('Ctrl Pts',(-1.25027274650581,1.50321801345654,
0.128219124385103));
#279159=CARTESIAN_POINT('Ctrl Pts',(-1.1965990661533,1.54627822984259,0.124301263754539));
#279160=CARTESIAN_POINT('Ctrl Pts',(-1.14088434801228,1.58634766191419,
0.120383403123975));
#279161=CARTESIAN_POINT('Ctrl Pts',(-1.08507638548269,1.62648415435723,
0.116458985545244));
#279162=CARTESIAN_POINT('Ctrl Pts',(-1.02722097917664,1.66361960726873,
0.112534567966514));
#279163=CARTESIAN_POINT('Ctrl Pts',(-0.96767980974077,1.69756053966274,
0.108610150387783));
#279164=CARTESIAN_POINT('Ctrl Pts',(-0.94062675434164,1.7129819016053,0.10682705665327));
#279165=CARTESIAN_POINT('Ctrl Pts',(-0.913225994787098,1.72774442491995,
0.105043962918756));
#279166=CARTESIAN_POINT('Ctrl Pts',(-0.885512812090751,1.74183324679004,
0.103260869184242));
#279167=CARTESIAN_POINT('Ctrl Pts',(-0.825177116348573,1.77250669483943,
0.0993788105183649));
#279168=CARTESIAN_POINT('Ctrl Pts',(-0.763117235362137,1.8001066486546,
0.0954967518524874));
#279169=CARTESIAN_POINT('Ctrl Pts',(-0.699682069082541,1.82443443351751,
0.0916146931866098));
#279170=CARTESIAN_POINT('Ctrl Pts',(-0.636353223996944,1.84872144353446,
0.0877391410869908));
#279171=CARTESIAN_POINT('Ctrl Pts',(-0.571654134652549,1.86974699526494,
0.0838635889873719));
#279172=CARTESIAN_POINT('Ctrl Pts',(-0.505957111893772,1.88735884264867,
0.0799880368877529));
#279173=CARTESIAN_POINT('Ctrl Pts',(-0.440321572265943,1.90495420783162,
0.0761161117573211));
#279174=CARTESIAN_POINT('Ctrl Pts',(-0.373690432405684,1.9191420711908,
0.0722441866268893));
#279175=CARTESIAN_POINT('Ctrl Pts',(-0.306453340920287,1.92981925315269,
0.0683722614964574));
#279176=CARTESIAN_POINT('Ctrl Pts',(-0.239255063254954,1.9404902715193,
0.064502571504429));
#279177=CARTESIAN_POINT('Ctrl Pts',(-0.171452022206664,1.94765454848065,
0.0606328815124006));
#279178=CARTESIAN_POINT('Ctrl Pts',(-0.103444394209851,1.95125991536406,
0.0567631915203721));
#279179=CARTESIAN_POINT('Ctrl Pts',(-0.035451640385408,1.9548644937058,
0.0528943478809905));
#279180=CARTESIAN_POINT('Ctrl Pts',(0.0327451105783654,1.95491168108245,
0.049025504241609));
#279181=CARTESIAN_POINT('Ctrl Pts',(0.100742171473057,1.95140129519453,
0.0451566606022274));
#279182=CARTESIAN_POINT('Ctrl Pts',(0.168794206077408,1.94788807125844,
0.0412846891116688));
#279183=CARTESIAN_POINT('Ctrl Pts',(0.236645725644037,1.94081155162635,
0.0374127176211102));
#279184=CARTESIAN_POINT('Ctrl Pts',(0.303895816327973,1.93022364839372,
0.0335407461305516));
#279185=CARTESIAN_POINT('Ctrl Pts',(0.371171480218994,1.91963171889675,
0.0296673022445249));
#279186=CARTESIAN_POINT('Ctrl Pts',(0.4378447675752,1.90552584870393,0.0257938583584982));
#279187=CARTESIAN_POINT('Ctrl Pts',(0.503525519732653,1.88800901771627,
0.0219204144724715));
#279188=CARTESIAN_POINT('Ctrl Pts',(0.569321331754245,1.87046150065808,
0.0180401850684257));
#279189=CARTESIAN_POINT('Ctrl Pts',(0.634120656256508,1.84949124013714,
0.0141599556643799));
#279190=CARTESIAN_POINT('Ctrl Pts',(0.697549773038983,1.82525075376872,
0.010279726260334));
#279191=CARTESIAN_POINT('Ctrl Pts',(0.753348915082634,1.80392618847929,
0.00686625492948106));
#279192=CARTESIAN_POINT('Ctrl Pts',(0.808087758634527,1.78007167123815,
0.00345278359862809));
#279193=CARTESIAN_POINT('Ctrl Pts',(0.86152788258768,1.75382031791287,3.93122677751275E-5));
#279194=CARTESIAN_POINT('',(-0.861525859670574,1.75382131162752,1.38777878078145E-16));
#279195=CARTESIAN_POINT('Origin',(0.,0.,0.));
#279196=CARTESIAN_POINT('',(-1.95399890369145,0.00206987260420434,0.124130307921836));
#279197=CARTESIAN_POINT('Ctrl Pts',(-0.861525859670572,1.75382131162752,
2.28983498828939E-15));
#279198=CARTESIAN_POINT('Ctrl Pts',(-0.924648224743909,1.7228138483964,
0.00400973887597992));
#279199=CARTESIAN_POINT('Ctrl Pts',(-0.986141954375339,1.68837147644998,
0.00801947775195755));
#279200=CARTESIAN_POINT('Ctrl Pts',(-1.04562636415511,1.65069122084773,
0.0120292166279352));
#279201=CARTESIAN_POINT('Ctrl Pts',(-1.10691784192122,1.61186628239718,
0.016160766761403));
#279202=CARTESIAN_POINT('Ctrl Pts',(-1.16607547468266,1.56960374308896,
0.0202923168948708));
#279203=CARTESIAN_POINT('Ctrl Pts',(-1.2227115584002,1.52416942790313,0.0244238670283386));
#279204=CARTESIAN_POINT('Ctrl Pts',(-1.27763825025648,1.48010641248774,
0.0284307186002357));
#279205=CARTESIAN_POINT('Ctrl Pts',(-1.33019308928818,1.43306069927262,
0.0324375701721327));
#279206=CARTESIAN_POINT('Ctrl Pts',(-1.38005457172536,1.38331680357752,
0.0364444217440298));
#279207=CARTESIAN_POINT('Ctrl Pts',(-1.42991716849446,1.3335717961784,0.0404513628632568));
#279208=CARTESIAN_POINT('Ctrl Pts',(-1.47708596403036,1.28112881053544,
0.0444583039824838));
#279209=CARTESIAN_POINT('Ctrl Pts',(-1.52127632765451,1.2263092329906,0.0484652451017108));
#279210=CARTESIAN_POINT('Ctrl Pts',(-1.5654796248828,1.17147361089088,0.0524733589696091));
#279211=CARTESIAN_POINT('Ctrl Pts',(-1.60670246957715,1.11426037168743,
0.0564814728375075));
#279212=CARTESIAN_POINT('Ctrl Pts',(-1.64470141560668,1.05502286871014,
0.0604895867054059));
#279213=CARTESIAN_POINT('Ctrl Pts',(-1.6827217597034,0.995752007753191,
0.0644999576330076));
#279214=CARTESIAN_POINT('Ctrl Pts',(-1.7175143488718,0.934455003168418,
0.0685103285606093));
#279215=CARTESIAN_POINT('Ctrl Pts',(-1.74888057041762,0.871511761490194,
0.072520699488211));
#279216=CARTESIAN_POINT('Ctrl Pts',(-1.78029554444285,0.808470687209157,
0.0765373037303931));
#279217=CARTESIAN_POINT('Ctrl Pts',(-1.80827331765284,0.743778680594848,
0.0805539079725752));
#279218=CARTESIAN_POINT('Ctrl Pts',(-1.83266272864314,0.677837239344568,
0.0845705122147573));
#279219=CARTESIAN_POINT('Ctrl Pts',(-1.85707426487929,0.611835978256916,
0.0885907601839796));
#279220=CARTESIAN_POINT('Ctrl Pts',(-1.87789081935113,0.544583462735634,
0.092611008153202));
#279221=CARTESIAN_POINT('Ctrl Pts',(-1.89501134508785,0.476495542464292,
0.0966312561224243));
#279222=CARTESIAN_POINT('Ctrl Pts',(-1.91216338868066,0.408282276435159,
0.100658905125871));
#279223=CARTESIAN_POINT('Ctrl Pts',(-1.92560573312532,0.339230985221237,
0.104686554129318));
#279224=CARTESIAN_POINT('Ctrl Pts',(-1.9352886455049,0.269766303640422,
0.108714203132765));
#279225=CARTESIAN_POINT('Ctrl Pts',(-1.93726980603249,0.255553566829941,
0.109538275365564));
#279226=CARTESIAN_POINT('Ctrl Pts',(-1.93909376069024,0.241323532685976,
0.110362347598363));
#279227=CARTESIAN_POINT('Ctrl Pts',(-1.94076035206736,0.227079844643627,
0.111186419831162));
#279228=CARTESIAN_POINT('Ctrl Pts',(-1.94948619402753,0.15250357328286,
0.115501049179361));
#279229=CARTESIAN_POINT('Ctrl Pts',(-1.9539191335491,0.0773743671059711,
0.119815678527559));
#279230=CARTESIAN_POINT('Ctrl Pts',(-1.9539989036906,0.0020698734084197,
0.124130307875758));
#279231=CARTESIAN_POINT('',(-1.95389301601064,0.000918145502495154,0.824130263912385));
#279232=CARTESIAN_POINT('Ctrl Pts',(-1.95399890369145,0.00206987260420564,
0.124130307921836));
#279233=CARTESIAN_POINT('Ctrl Pts',(-1.95406962240973,-0.0646899355598776,
0.127955362887828));
#279234=CARTESIAN_POINT('Ctrl Pts',(-1.95071485453637,-0.131608847044638,
0.131780417853821));
#279235=CARTESIAN_POINT('Ctrl Pts',(-1.94391230496763,-0.198295109862623,
0.135605472819813));
#279236=CARTESIAN_POINT('Ctrl Pts',(-1.93712036320297,-0.264877383021508,
0.139424563046665));
#279237=CARTESIAN_POINT('Ctrl Pts',(-1.92689135584406,-0.33122721849863,
0.143243653273517));
#279238=CARTESIAN_POINT('Ctrl Pts',(-1.91325499737006,-0.396952534994404,
0.147062743500369));
#279239=CARTESIAN_POINT('Ctrl Pts',(-1.89963031317816,-0.462621583103922,
0.150878564149294));
#279240=CARTESIAN_POINT('Ctrl Pts',(-1.88260415795907,-0.527666668135914,
0.15469438479822));
#279241=CARTESIAN_POINT('Ctrl Pts',(-1.86225788543312,-0.591702263086903,
0.158510205447145));
#279242=CARTESIAN_POINT('Ctrl Pts',(-1.84192136891004,-0.655707153079655,
0.162324196416597));
#279243=CARTESIAN_POINT('Ctrl Pts',(-1.81826804529352,-0.718703021080917,
0.166138187386048));
#279244=CARTESIAN_POINT('Ctrl Pts',(-1.79142952719964,-0.780318043542037,
0.1699521783555));
#279245=CARTESIAN_POINT('Ctrl Pts',(-1.76459377488551,-0.841926716413331,
0.173765776283169));
#279246=CARTESIAN_POINT('Ctrl Pts',(-1.73457368712652,-0.902154353896972,
0.177579374210839));
#279247=CARTESIAN_POINT('Ctrl Pts',(-1.7015487426134,-0.960649715822971,
0.181392972138508));
#279248=CARTESIAN_POINT('Ctrl Pts',(-1.66849242384863,-1.01920064932472,
0.185210193048224));
#279249=CARTESIAN_POINT('Ctrl Pts',(-1.6324258052211,-1.07601557265378,
0.189027413957941));
#279250=CARTESIAN_POINT('Ctrl Pts',(-1.59357334566683,-1.13076964585198,
0.192844634867658));
#279251=CARTESIAN_POINT('Ctrl Pts',(-1.55470101203149,-1.18555172723556,
0.196663808388835));
#279252=CARTESIAN_POINT('Ctrl Pts',(-1.51304032592502,-1.23827045919599,
0.200482981910012));
#279253=CARTESIAN_POINT('Ctrl Pts',(-1.46885600537764,-1.28863417441338,
0.204302155431189));
#279254=CARTESIAN_POINT('Ctrl Pts',(-1.42459380221032,-1.33908666451838,
0.208128060916016));
#279255=CARTESIAN_POINT('Ctrl Pts',(-1.37779945106309,-1.38717548865719,
0.211953966400843));
#279256=CARTESIAN_POINT('Ctrl Pts',(-1.32877363457237,-1.43264672130478,
0.215779871885671));
#279257=CARTESIAN_POINT('Ctrl Pts',(-1.30061249035615,-1.45876606070468,
0.217977527811222));
#279258=CARTESIAN_POINT('Ctrl Pts',(-1.27171567625023,-1.48402247386527,
0.220175183736774));
#279259=CARTESIAN_POINT('Ctrl Pts',(-1.24214451955084,-1.50837428795038,
0.222372839662326));
#279260=CARTESIAN_POINT('Ctrl Pts',(-1.18934685645933,-1.5518531037709,
0.226296632645057));
#279261=CARTESIAN_POINT('Ctrl Pts',(-1.13416061912592,-1.59264129349927,
0.230220425627789));
#279262=CARTESIAN_POINT('Ctrl Pts',(-1.07689083932768,-1.63046684117529,
0.23414421861052));
#279263=CARTESIAN_POINT('Ctrl Pts',(-1.01970717829159,-1.668235509126,0.238062111235406));
#279264=CARTESIAN_POINT('Ctrl Pts',(-0.960446599313705,-1.70305010949116,
0.241980003860292));
#279265=CARTESIAN_POINT('Ctrl Pts',(-0.89944693364595,-1.73467899438337,
0.245897896485178));
#279266=CARTESIAN_POINT('Ctrl Pts',(-0.838519344608369,-1.76627050688322,
0.249811159765055));
#279267=CARTESIAN_POINT('Ctrl Pts',(-0.775857183549963,-1.79468355593104,
0.253724423044932));
#279268=CARTESIAN_POINT('Ctrl Pts',(-0.711825428870553,-1.81973090285714,
0.25763768632481));
#279269=CARTESIAN_POINT('Ctrl Pts',(-0.64783411101502,-1.84476243208214,
0.261548478331819));
#279270=CARTESIAN_POINT('Ctrl Pts',(-0.582475370960143,-1.8664322977552,
0.265459270338828));
#279271=CARTESIAN_POINT('Ctrl Pts',(-0.516135449431958,-1.88460080596387,
0.269370062345837));
#279272=CARTESIAN_POINT('Ctrl Pts',(-0.449814856770113,-1.9027640205777,
0.273279714900549));
#279273=CARTESIAN_POINT('Ctrl Pts',(-0.38251412278591,-1.91742777368561,
0.277189367455261));
#279274=CARTESIAN_POINT('Ctrl Pts',(-0.314634262868098,-1.9285023413596,
0.281099020009973));
#279275=CARTESIAN_POINT('Ctrl Pts',(-0.246751092056681,-1.93957744920434,
0.285008863261066));
#279276=CARTESIAN_POINT('Ctrl Pts',(-0.178289223454827,-1.94706294757461,
0.288918706512159));
#279277=CARTESIAN_POINT('Ctrl Pts',(-0.109657688950741,-1.95092060096099,
0.292828549763252));
#279278=CARTESIAN_POINT('Ctrl Pts',(-0.0409547879490927,-1.95478226572804,
0.296742458664645));
#279279=CARTESIAN_POINT('Ctrl Pts',(0.0279176406827614,-1.95500852899902,
0.300656367566038));
#279280=CARTESIAN_POINT('Ctrl Pts',(0.0965486492807848,-1.95161327068711,
0.304570276467431));
#279281=CARTESIAN_POINT('Ctrl Pts',(0.165219803870349,-1.94821602630486,
0.308486474825979));
#279282=CARTESIAN_POINT('Ctrl Pts',(0.233648769520342,-1.94119309345488,
0.312402673184526));
#279283=CARTESIAN_POINT('Ctrl Pts',(0.301430589707728,-1.93061016251041,
0.316318871543074));
#279284=CARTESIAN_POINT('Ctrl Pts',(0.369327280566128,-1.92000929654478,
0.320241706730376));
#279285=CARTESIAN_POINT('Ctrl Pts',(0.436574157399652,-1.90583649145238,
0.324164541917678));
#279286=CARTESIAN_POINT('Ctrl Pts',(0.502778157531278,-1.88820817822333,
0.32808737710498));
#279287=CARTESIAN_POINT('Ctrl Pts',(0.533560358420196,-1.88001172063662,
0.329911337901149));
#279288=CARTESIAN_POINT('Ctrl Pts',(0.564117343255775,-1.87106892339258,
0.331735298697319));
#279289=CARTESIAN_POINT('Ctrl Pts',(0.594411056057898,-1.8613950404028,
0.333559259493488));
#279290=CARTESIAN_POINT('Ctrl Pts',(0.659594398880924,-1.84057963109751,
0.337483897673332));
#279291=CARTESIAN_POINT('Ctrl Pts',(0.723807350727231,-1.81629647786615,
0.341408535853176));
#279292=CARTESIAN_POINT('Ctrl Pts',(0.786655984201979,-1.78865546221714,
0.34533317403302));
#279293=CARTESIAN_POINT('Ctrl Pts',(0.849412399165395,-1.76105500454329,
0.349252053546837));
#279294=CARTESIAN_POINT('Ctrl Pts',(0.910808024201147,-1.7301066599176,
0.353170933060653));
#279295=CARTESIAN_POINT('Ctrl Pts',(0.970465215395659,-1.69596971249697,
0.35708981257447));
#279296=CARTESIAN_POINT('Ctrl Pts',(1.03005507208741,-1.66187129512334,
0.361004268886352));
#279297=CARTESIAN_POINT('Ctrl Pts',(1.08790996866424,-1.62459166521176,
0.364918725198235));
#279298=CARTESIAN_POINT('Ctrl Pts',(1.1436749754053,-1.58433694352928,0.368833181510118));
#279299=CARTESIAN_POINT('Ctrl Pts',(1.19940659356289,-1.54410632384575,
0.372745294091427));
#279300=CARTESIAN_POINT('Ctrl Pts',(1.25305040793731,-1.50090443257899,
0.376657406672736));
#279301=CARTESIAN_POINT('Ctrl Pts',(1.30428003732066,-1.45498095666123,
0.380569519254044));
#279302=CARTESIAN_POINT('Ctrl Pts',(1.35549639405906,-1.40906937866266,
0.384480618279684));
#279303=CARTESIAN_POINT('Ctrl Pts',(1.40429944299621,-1.3604379429279,0.388391717305323));
#279304=CARTESIAN_POINT('Ctrl Pts',(1.45039689124339,-1.30937575121563,
0.392302816330962));
#279305=CARTESIAN_POINT('Ctrl Pts',(1.49649805312221,-1.25830944590971,
0.396214230436539));
#279306=CARTESIAN_POINT('Ctrl Pts',(1.53989285511708,-1.20481236120016,
0.400125644542115));
#279307=CARTESIAN_POINT('Ctrl Pts',(1.58032801561469,-1.14920814610032,
0.404037058647691));
#279308=CARTESIAN_POINT('Ctrl Pts',(1.62080705206791,-1.09354359519265,
0.407952717005783));
#279309=CARTESIAN_POINT('Ctrl Pts',(1.65831974925713,-1.03576774794434,
0.411868375363875));
#279310=CARTESIAN_POINT('Ctrl Pts',(1.69265564610032,-0.976234020983042,
0.415784033721968));
#279311=CARTESIAN_POINT('Ctrl Pts',(1.72701253630214,-0.916663894422599,
0.419702086158205));
#279312=CARTESIAN_POINT('Ctrl Pts',(1.75818853823833,-0.855334185779185,
0.423620138594443));
#279313=CARTESIAN_POINT('Ctrl Pts',(1.78602003479096,-0.792621243296755,
0.42753819103068));
#279314=CARTESIAN_POINT('Ctrl Pts',(1.81389969051431,-0.72979978335471,
0.431463023201374));
#279315=CARTESIAN_POINT('Ctrl Pts',(1.83842311533252,-0.665590769809821,
0.435387855372068));
#279316=CARTESIAN_POINT('Ctrl Pts',(1.85947581564609,-0.600387950434814,
0.439312687542762));
#279317=CARTESIAN_POINT('Ctrl Pts',(1.86918995906384,-0.570302045576213,
0.441123684803391));
#279318=CARTESIAN_POINT('Ctrl Pts',(1.8781658653323,-0.54000472245759,0.442934682064021));
#279319=CARTESIAN_POINT('Ctrl Pts',(1.88639596582335,-0.509535337464828,
0.444745679324651));
#279320=CARTESIAN_POINT('Ctrl Pts',(1.90417601728029,-0.443710231972858,
0.44865810111311));
#279321=CARTESIAN_POINT('Ctrl Pts',(1.91854275019372,-0.376819134628719,
0.452570522901568));
#279322=CARTESIAN_POINT('Ctrl Pts',(1.92937313881236,-0.309249561405273,
0.456482944690027));
#279323=CARTESIAN_POINT('Ctrl Pts',(1.9401869556771,-0.241783377485532,
0.460389380018231));
#279324=CARTESIAN_POINT('Ctrl Pts',(1.94747508855052,-0.173641261023044,
0.464295815346436));
#279325=CARTESIAN_POINT('Ctrl Pts',(1.95116474653031,-0.105224198249775,
0.46820225067464));
#279326=CARTESIAN_POINT('Ctrl Pts',(1.95484996606166,-0.0368894373069517,
0.4721039867836));
#279327=CARTESIAN_POINT('Ctrl Pts',(1.95494528057357,0.0317191227619464,
0.47600572289256));
#279328=CARTESIAN_POINT('Ctrl Pts',(1.95142952386527,0.100193878989584,
0.47990745900152));
#279329=CARTESIAN_POINT('Ctrl Pts',(1.94791602675104,0.168624626155676,
0.483806687445553));
#279330=CARTESIAN_POINT('Ctrl Pts',(1.94079608694011,0.236921248335345,
0.487705915889587));
#279331=CARTESIAN_POINT('Ctrl Pts',(1.93010061963535,0.304676218440552,
0.49160514433362));
#279332=CARTESIAN_POINT('Ctrl Pts',(1.9194083283643,0.372411068614334,0.495503214896412));
#279333=CARTESIAN_POINT('Ctrl Pts',(1.90514269399046,0.439604098723601,
0.499401285459204));
#279334=CARTESIAN_POINT('Ctrl Pts',(1.88738626341259,0.505854813836402,
0.503299356021995));
#279335=CARTESIAN_POINT('Ctrl Pts',(1.86962896642995,0.572108761577267,
0.507197616786693));
#279336=CARTESIAN_POINT('Ctrl Pts',(1.84838066534311,0.637419826993278,
0.511095877551392));
#279337=CARTESIAN_POINT('Ctrl Pts',(1.82377413864022,0.701401376693196,
0.514994138316089));
#279338=CARTESIAN_POINT('Ctrl Pts',(1.79914144699063,0.765450960124916,
0.518896544232454));
#279339=CARTESIAN_POINT('Ctrl Pts',(1.77114358069267,0.828167744912018,
0.522798950148818));
#279340=CARTESIAN_POINT('Ctrl Pts',(1.73996160430977,0.889184803923099,
0.526701356065182));
#279341=CARTESIAN_POINT('Ctrl Pts',(1.70876110556513,0.950238107591229,
0.530606080044174));
#279342=CARTESIAN_POINT('Ctrl Pts',(1.6743729803604,1.00958924919398,0.534510804023165));
#279343=CARTESIAN_POINT('Ctrl Pts',(1.63702301426926,1.06689814450714,0.538415528002157));
#279344=CARTESIAN_POINT('Ctrl Pts',(1.59960798031843,1.12430687838912,0.542327054451367));
#279345=CARTESIAN_POINT('Ctrl Pts',(1.55922109804311,1.17966586668971,0.546238580900578));
#279346=CARTESIAN_POINT('Ctrl Pts',(1.51612945757764,1.23266681137497,0.550150107349788));
#279347=CARTESIAN_POINT('Ctrl Pts',(1.49489686758029,1.25878202341652,0.552077437951797));
#279348=CARTESIAN_POINT('Ctrl Pts',(1.47300819005873,1.28432529019343,0.554004768553805));
#279349=CARTESIAN_POINT('Ctrl Pts',(1.45049855981685,1.30926312403934,0.555932099155814));
#279350=CARTESIAN_POINT('Ctrl Pts',(1.40472845234233,1.35997063558188,0.55985104974918));
#279351=CARTESIAN_POINT('Ctrl Pts',(1.35620559048947,1.4083754866274,0.563770000342546));
#279352=CARTESIAN_POINT('Ctrl Pts',(1.30519070746797,1.45416409567121,0.567688950935912));
#279353=CARTESIAN_POINT('Ctrl Pts',(1.25425265348505,1.49988374650905,0.571601999541692));
#279354=CARTESIAN_POINT('Ctrl Pts',(1.20083038977689,1.54299464937113,0.575515048147471));
#279355=CARTESIAN_POINT('Ctrl Pts',(1.14522307837355,1.58321827325249,0.579428096753251));
#279356=CARTESIAN_POINT('Ctrl Pts',(1.08968122685999,1.62339454663409,0.583336538991199));
#279357=CARTESIAN_POINT('Ctrl Pts',(1.03195983261817,1.66069000451881,0.587244981229147));
#279358=CARTESIAN_POINT('Ctrl Pts',(0.972391486925007,1.69486601126926,
0.591153423467096));
#279359=CARTESIAN_POINT('Ctrl Pts',(0.912860539003305,1.72902056188432,
0.595059411934876));
#279360=CARTESIAN_POINT('Ctrl Pts',(0.851485365306069,1.76005930221187,
0.598965400402657));
#279361=CARTESIAN_POINT('Ctrl Pts',(0.788626611815159,1.78778747817993,
0.602871388870437));
#279362=CARTESIAN_POINT('Ctrl Pts',(0.725785787387798,1.81550774530154,
0.606776263241746));
#279363=CARTESIAN_POINT('Ctrl Pts',(0.661462672826329,1.83991912427526,
0.610681137613056));
#279364=CARTESIAN_POINT('Ctrl Pts',(0.596039893333901,1.86087410792738,
0.614586011984365));
#279365=CARTESIAN_POINT('Ctrl Pts',(0.530613362105011,1.88183029326455,
0.618491110284704));
#279366=CARTESIAN_POINT('Ctrl Pts',(0.464087509733959,1.89932954221597,
0.622396208585044));
#279367=CARTESIAN_POINT('Ctrl Pts',(0.396860461678409,1.9132740979683,0.626301306885383));
#279368=CARTESIAN_POINT('Ctrl Pts',(0.329561975791958,1.92723347169709,
0.630210554880824));
#279369=CARTESIAN_POINT('Ctrl Pts',(0.2615612895033,1.93763051365435,0.634119802876266));
#279370=CARTESIAN_POINT('Ctrl Pts',(0.193266079982631,1.94441873636523,
0.638029050871707));
#279371=CARTESIAN_POINT('Ctrl Pts',(0.124930149413867,1.95121100655682,
0.641940629757949));
#279372=CARTESIAN_POINT('Ctrl Pts',(0.0562998373073983,1.95439015220606,
0.645852208644192));
#279373=CARTESIAN_POINT('Ctrl Pts',(-0.012215527754201,1.95396181663862,
0.649763787530434));
#279374=CARTESIAN_POINT('Ctrl Pts',(-0.0808491282404187,1.95353274190212,
0.653682116540391));
#279375=CARTESIAN_POINT('Ctrl Pts',(-0.149366895216171,1.9494837898546,
0.657600445550349));
#279376=CARTESIAN_POINT('Ctrl Pts',(-0.217363844836177,1.94187253931818,
0.661518774560306));
#279377=CARTESIAN_POINT('Ctrl Pts',(-0.249755674678064,1.93824675413756,
0.663385356035863));
#279378=CARTESIAN_POINT('Ctrl Pts',(-0.282029455866692,1.93381332843034,
0.66525193751142));
#279379=CARTESIAN_POINT('Ctrl Pts',(-0.314142410573999,1.9285825224446,
0.667118518986977));
#279380=CARTESIAN_POINT('Ctrl Pts',(-0.381558581303711,1.91760125608019,
0.67103711746488));
#279381=CARTESIAN_POINT('Ctrl Pts',(-0.44853151726403,1.90305909627577,
0.674955715942784));
#279382=CARTESIAN_POINT('Ctrl Pts',(-0.514656430893057,1.88500524087877,
0.678874314420688));
#279383=CARTESIAN_POINT('Ctrl Pts',(-0.580681976046049,1.86697851571149,
0.682787024268459));
#279384=CARTESIAN_POINT('Ctrl Pts',(-0.645861557457656,1.84545069682505,
0.686699734116229));
#279385=CARTESIAN_POINT('Ctrl Pts',(-0.709799023038066,1.82052227311127,
0.690612443964));
#279386=CARTESIAN_POINT('Ctrl Pts',(-0.773661569352443,1.79562305948879,
0.694520569060916));
#279387=CARTESIAN_POINT('Ctrl Pts',(-0.836284434412466,1.7673313324856,
0.698428694157831));
#279388=CARTESIAN_POINT('Ctrl Pts',(-0.897286881557168,1.7357972958227,
0.702336819254747));
#279389=CARTESIAN_POINT('Ctrl Pts',(-0.958251240337448,1.70428294820404,
0.706242504218523));
#279390=CARTESIAN_POINT('Ctrl Pts',(-1.01759675234698,1.66953053205859,
0.710148189182298));
#279391=CARTESIAN_POINT('Ctrl Pts',(-1.07496436257844,1.63173760733346,
0.714053874146073));
#279392=CARTESIAN_POINT('Ctrl Pts',(-1.13231581651118,1.59395532613661,
0.717958459161416));
#279393=CARTESIAN_POINT('Ctrl Pts',(-1.18769006402541,1.55313450665621,
0.721863044176759));
#279394=CARTESIAN_POINT('Ctrl Pts',(-1.24075585318281,1.50951678122259,
0.725767629192101));
#279395=CARTESIAN_POINT('Ctrl Pts',(-1.29382488510409,1.46589639038086,
0.72967245281027));
#279396=CARTESIAN_POINT('Ctrl Pts',(-1.34458480034009,1.41947906847847,
0.73357727642844));
#279397=CARTESIAN_POINT('Ctrl Pts',(-1.39273776541595,1.37054642999943,
0.737482100046609));
#279398=CARTESIAN_POINT('Ctrl Pts',(-1.44094220223177,1.32156148637076,
0.741391097614722));
#279399=CARTESIAN_POINT('Ctrl Pts',(-1.48653378203202,1.27005621153404,
0.745300095182835));
#279400=CARTESIAN_POINT('Ctrl Pts',(-1.5292525883575,1.21634802626629,0.749209092750949));
#279401=CARTESIAN_POINT('Ctrl Pts',(-1.57199701479702,1.16260763013054,
0.753120434695511));
#279402=CARTESIAN_POINT('Ctrl Pts',(-1.61186495341211,1.10666209469884,
0.757031776640074));
#279403=CARTESIAN_POINT('Ctrl Pts',(-1.64863941199854,1.0488584695778,0.760943118584636));
#279404=CARTESIAN_POINT('Ctrl Pts',(-1.68547755590406,0.99095474122068,
0.76486123411797));
#279405=CARTESIAN_POINT('Ctrl Pts',(-1.71921128586498,0.931186928883176,
0.768779349651304));
#279406=CARTESIAN_POINT('Ctrl Pts',(-1.74966961716525,0.869926566308211,
0.772697465184638));
#279407=CARTESIAN_POINT('Ctrl Pts',(-1.76419992629248,0.840701984150862,
0.774566623062472));
#279408=CARTESIAN_POINT('Ctrl Pts',(-1.7779855241982,0.811138014747312,
0.776435780940305));
#279409=CARTESIAN_POINT('Ctrl Pts',(-1.79101180145104,0.781276344876198,
0.778304938818138));
#279410=CARTESIAN_POINT('Ctrl Pts',(-1.82108266615991,0.712341359289296,
0.78261984725843));
#279411=CARTESIAN_POINT('Ctrl Pts',(-1.84720652553836,0.641584118440989,
0.786934755698722));
#279412=CARTESIAN_POINT('Ctrl Pts',(-1.86918209141702,0.56945088385734,
0.791249664139013));
#279413=CARTESIAN_POINT('Ctrl Pts',(-1.89109060934678,0.49753772940508,
0.79555140769599));
#279414=CARTESIAN_POINT('Ctrl Pts',(-1.9088759398764,0.42425724395805,0.799853151252965));
#279415=CARTESIAN_POINT('Ctrl Pts',(-1.92238492518644,0.350074562651913,
0.804154894809942));
#279416=CARTESIAN_POINT('Ctrl Pts',(-1.93582638752964,0.276262674163655,
0.80843513664189));
#279417=CARTESIAN_POINT('Ctrl Pts',(-1.94503401527278,0.201557885078121,
0.812715378473838));
#279418=CARTESIAN_POINT('Ctrl Pts',(-1.94990505686432,0.12643681906369,
0.816995620305786));
#279419=CARTESIAN_POINT('Ctrl Pts',(-1.95261153457162,0.0846975962104973,
0.819373834263172));
#279420=CARTESIAN_POINT('Ctrl Pts',(-1.95398008893921,0.0428301635186168,
0.821752048220558));
#279421=CARTESIAN_POINT('Ctrl Pts',(-1.95399978425297,0.000918226197701749,
0.824130262177944));
#279422=CARTESIAN_POINT('',(-1.95399925675175,-0.00170429269710383,1.52413032610373));
#279423=CARTESIAN_POINT('Ctrl Pts',(-1.95118672945361,0.000916100096969453,
0.824130307875757));
#279424=CARTESIAN_POINT('Ctrl Pts',(-1.94959408276249,-0.382490737583375,
0.845917324800272));
#279425=CARTESIAN_POINT('Ctrl Pts',(-1.65494759972259,-1.42039331085723,
0.904766481668509));
#279426=CARTESIAN_POINT('Ctrl Pts',(0.0320890232727861,-2.30962717925355,
1.00067777848046));
#279427=CARTESIAN_POINT('Ctrl Pts',(1.95839267869744,-1.22482325334232,
1.11186419831163));
#279428=CARTESIAN_POINT('Ctrl Pts',(2.0907344889796,0.982002812028434,1.22305061814279));
#279429=CARTESIAN_POINT('Ctrl Pts',(0.307867124228207,2.28925546628533,
1.33423703797395));
#279430=CARTESIAN_POINT('Ctrl Pts',(-1.55595354203437,1.57636391564955,
1.4345969345516));
#279431=CARTESIAN_POINT('Ctrl Pts',(-1.94903067523895,0.458983666015645,
1.49789469118554));
#279432=CARTESIAN_POINT('Ctrl Pts',(-1.95287184048439,-0.001702989282844,
1.52413030787576));
#279433=CARTESIAN_POINT('',(-1.9539999995111,4.37108594993626E-5,2.22413030791928));
#279434=CARTESIAN_POINT('Ctrl Pts',(-1.95399925675175,-0.00170429269710383,
1.52413032610373));
#279435=CARTESIAN_POINT('Ctrl Pts',(-1.95392656932596,-0.0850416068845222,
1.52887359761229));
#279436=CARTESIAN_POINT('Ctrl Pts',(-1.9485186276568,-0.168144569686724,
1.53361686912084));
#279437=CARTESIAN_POINT('Ctrl Pts',(-1.93788759724531,-0.25041497647464,
1.5383601406294));
#279438=CARTESIAN_POINT('Ctrl Pts',(-1.92709355836742,-0.333946857674933,
1.54317614200369));
#279439=CARTESIAN_POINT('Ctrl Pts',(-1.91091509568121,-0.416620496621874,
1.54799214337797));
#279440=CARTESIAN_POINT('Ctrl Pts',(-1.88951825859737,-0.497832050421777,
1.55280814475226));
#279441=CARTESIAN_POINT('Ctrl Pts',(-1.88388806507971,-0.519201412723879,
1.55407538904693));
#279442=CARTESIAN_POINT('Ctrl Pts',(-1.87789681471551,-0.540469658625722,
1.5553426333416));
#279443=CARTESIAN_POINT('Ctrl Pts',(-1.87154807587892,-0.561626031869897,
1.55660987763628));
#279444=CARTESIAN_POINT('Ctrl Pts',(-1.85192043594831,-0.627032671985691,
1.56052766593411));
#279445=CARTESIAN_POINT('Ctrl Pts',(-1.82882094278616,-0.691539084024109,
1.56444545423193));
#279446=CARTESIAN_POINT('Ctrl Pts',(-1.802350646318,-0.754750387689271,
1.56836324252976));
#279447=CARTESIAN_POINT('Ctrl Pts',(-1.77592026363396,-0.817866376882526,
1.57227512330945));
#279448=CARTESIAN_POINT('Ctrl Pts',(-1.74612935349376,-0.879690683267352,
1.57618700408915));
#279449=CARTESIAN_POINT('Ctrl Pts',(-1.71312871159643,-0.939843613322961,
1.58009888486884));
#279450=CARTESIAN_POINT('Ctrl Pts',(-1.68016694859202,-0.999925675686545,
1.58400615696261));
#279451=CARTESIAN_POINT('Ctrl Pts',(-1.64400319934452,-1.05833984305939,
1.58791342905637));
#279452=CARTESIAN_POINT('Ctrl Pts',(-1.60483556458594,-1.1147281330621,
1.59182070115013));
#279453=CARTESIAN_POINT('Ctrl Pts',(-1.56569253448401,-1.17108100059105,
1.59572551874061));
#279454=CARTESIAN_POINT('Ctrl Pts',(-1.52354964208937,-1.22541011206912,
1.59963033633109));
#279455=CARTESIAN_POINT('Ctrl Pts',(-1.47864914422619,-1.27738510570585,
1.60353515392156));
#279456=CARTESIAN_POINT('Ctrl Pts',(-1.43376144462226,-1.32934528459721,
1.60743885849837));
#279457=CARTESIAN_POINT('Ctrl Pts',(-1.38611802137467,-1.37895230557505,
1.61134256307518));
#279458=CARTESIAN_POINT('Ctrl Pts',(-1.33600123801422,-1.4259090756512,
1.61524626765199));
#279459=CARTESIAN_POINT('Ctrl Pts',(-1.28588154257544,-1.47286857419042,
1.61915019905687));
#279460=CARTESIAN_POINT('Ctrl Pts',(-1.2332885624588,-1.51717718157874,
1.62305413046175));
#279461=CARTESIAN_POINT('Ctrl Pts',(-1.17853998361191,-1.55857611525009,
1.62695806186663));
#279462=CARTESIAN_POINT('Ctrl Pts',(-1.1237330345662,-1.60001918639569,
1.63086615544809));
#279463=CARTESIAN_POINT('Ctrl Pts',(-1.06676629344045,-1.63854609552244,
1.63477424902955));
#279464=CARTESIAN_POINT('Ctrl Pts',(-1.00798804288102,-1.67394029326284,
1.638682342611));
#279465=CARTESIAN_POINT('Ctrl Pts',(-0.949174653644986,-1.70935565027995,
1.64259277251984));
#279466=CARTESIAN_POINT('Ctrl Pts',(-0.888548034036203,-1.74163433747435,
1.64650320242868));
#279467=CARTESIAN_POINT('Ctrl Pts',(-0.826480287686199,-1.77060620524896,
1.65041363233753));
#279468=CARTESIAN_POINT('Ctrl Pts',(-0.764305074334288,-1.79962823627184,
1.65433083294779));
#279469=CARTESIAN_POINT('Ctrl Pts',(-0.700684210020102,-1.82533183617092,
1.65824803355805));
#279470=CARTESIAN_POINT('Ctrl Pts',(-0.636008116819952,-1.84759564714229,
1.66216523416832));
#279471=CARTESIAN_POINT('Ctrl Pts',(-0.605017007693411,-1.85826388885644,
1.66404225526802));
#279472=CARTESIAN_POINT('Ctrl Pts',(-0.573783806829276,-1.86814307416366,
1.66591927636773));
#279473=CARTESIAN_POINT('Ctrl Pts',(-0.542352307151149,-1.87722400765807,
1.66779629746744));
#279474=CARTESIAN_POINT('Ctrl Pts',(-0.4767474116325,-1.89617804100721,
1.67171407976843));
#279475=CARTESIAN_POINT('Ctrl Pts',(-0.410017392047881,-1.91172646298042,
1.67563186206942));
#279476=CARTESIAN_POINT('Ctrl Pts',(-0.34254886834496,-1.92374017808944,
1.67954964437041));
#279477=CARTESIAN_POINT('Ctrl Pts',(-0.275182079368546,-1.93573577790626,
1.68346151910904));
#279478=CARTESIAN_POINT('Ctrl Pts',(-0.207079476767389,-1.94420716324699,
1.68737339384767));
#279479=CARTESIAN_POINT('Ctrl Pts',(-0.138641878894337,-1.94907527546184,
1.6912852685863));
#279480=CARTESIAN_POINT('Ctrl Pts',(-0.0702849098335151,-1.95393765237741,
1.69519253460366));
#279481=CARTESIAN_POINT('Ctrl Pts',(-0.00159421772505816,-1.95520515229954,
1.69909980062101));
#279482=CARTESIAN_POINT('Ctrl Pts',(0.0670219865489309,-1.95285023832321,
1.70300706663836));
#279483=CARTESIAN_POINT('Ctrl Pts',(0.135595086525049,-1.95049680369007,
1.70691187813407));
#279484=CARTESIAN_POINT('Ctrl Pts',(0.204093300905156,-1.9445254859769,
1.71081668962978));
#279485=CARTESIAN_POINT('Ctrl Pts',(0.27210769921077,-1.93496082648467,
1.71472150112549));
#279486=CARTESIAN_POINT('Ctrl Pts',(0.340102710776028,-1.92539889329119,
1.71862519959854));
#279487=CARTESIAN_POINT('Ctrl Pts',(0.407613693072952,-1.91224572006381,
1.72252889807159));
#279488=CARTESIAN_POINT('Ctrl Pts',(0.474237937445677,-1.89557758445474,
1.72643259654464));
#279489=CARTESIAN_POINT('Ctrl Pts',(0.540866053088966,-1.87890848032643,
1.73033652184613));
#279490=CARTESIAN_POINT('Ctrl Pts',(0.606606851861831,-1.85872413021012,
1.73424044714761));
#279491=CARTESIAN_POINT('Ctrl Pts',(0.671070676876058,-1.83515125987944,
1.73814437244909));
#279492=CARTESIAN_POINT('Ctrl Pts',(0.735603230811031,-1.81155325703551,
1.74205245996982));
#279493=CARTESIAN_POINT('Ctrl Pts',(0.798855630951643,-1.78455969333248,
1.74596054749054));
#279494=CARTESIAN_POINT('Ctrl Pts',(0.860457130100616,-1.75434589726742,
1.74986863501126));
#279495=CARTESIAN_POINT('Ctrl Pts',(0.922095456014425,-1.72411403871397,
1.7537790588748));
#279496=CARTESIAN_POINT('Ctrl Pts',(0.982080486999279,-1.69065835612698,
1.75768948273834));
#279497=CARTESIAN_POINT('Ctrl Pts',(1.04006755942586,-1.65419934464681,
1.76159990660188));
#279498=CARTESIAN_POINT('Ctrl Pts',(1.09815503484188,-1.6176772054109,1.76551710125466));
#279499=CARTESIAN_POINT('Ctrl Pts',(1.15423724526712,-1.57814164174512,
1.76943429590743));
#279500=CARTESIAN_POINT('Ctrl Pts',(1.20800060313945,-1.53585498756059,
1.77335149056021));
#279501=CARTESIAN_POINT('Ctrl Pts',(1.23376339898637,-1.5155916989209,1.77522856613967));
#279502=CARTESIAN_POINT('Ctrl Pts',(1.25899425580077,-1.49469726976515,
1.77710564171914));
#279503=CARTESIAN_POINT('Ctrl Pts',(1.28366170827141,-1.47320352250384,
1.7789827172986));
#279504=CARTESIAN_POINT('Ctrl Pts',(1.3351469234973,-1.42834237581362,1.78290049682282));
#279505=CARTESIAN_POINT('Ctrl Pts',(1.38437988714249,-1.38068991879112,
1.78681827634703));
#279506=CARTESIAN_POINT('Ctrl Pts',(1.43104256868493,-1.33050109605804,
1.79073605587124));
#279507=CARTESIAN_POINT('Ctrl Pts',(1.47763488741356,-1.28038795321888,
1.79464792776259));
#279508=CARTESIAN_POINT('Ctrl Pts',(1.52166428365344,-1.22774639247634,
1.79855979965393));
#279509=CARTESIAN_POINT('Ctrl Pts',(1.56284708215548,-1.17287040963531,
1.80247167154528));
#279510=CARTESIAN_POINT('Ctrl Pts',(1.6039813607217,-1.11805907949545,1.80637893462469));
#279511=CARTESIAN_POINT('Ctrl Pts',(1.64227540820047,-1.0610189470505,1.8102861977041));
#279512=CARTESIAN_POINT('Ctrl Pts',(1.67748484117931,-1.0020781444646,1.81419346078352));
#279513=CARTESIAN_POINT('Ctrl Pts',(1.7126721552897,-0.943174368997536,
1.81809826928668));
#279514=CARTESIAN_POINT('Ctrl Pts',(1.74477844706838,-0.882372713324816,
1.82200307778984));
#279515=CARTESIAN_POINT('Ctrl Pts',(1.77360270918012,-0.820030139683255,
1.825907886293));
#279516=CARTESIAN_POINT('Ctrl Pts',(1.80241875488326,-0.757705336906271,
1.82981158172335));
#279517=CARTESIAN_POINT('Ctrl Pts',(1.82795442174516,-0.693840934467796,
1.83371527715371));
#279518=CARTESIAN_POINT('Ctrl Pts',(1.85005555332991,-0.628816705879527,
1.83761897258407));
#279519=CARTESIAN_POINT('Ctrl Pts',(1.87215796886587,-0.563788699749949,
1.84152289479714));
#279520=CARTESIAN_POINT('Ctrl Pts',(1.89082529708749,-0.497601200331658,
1.84542681701021));
#279521=CARTESIAN_POINT('Ctrl Pts',(1.90595285153498,-0.430650354377729,
1.84933073922327));
#279522=CARTESIAN_POINT('Ctrl Pts',(1.92109653424097,-0.363628128707158,
1.85323882360722));
#279523=CARTESIAN_POINT('Ctrl Pts',(1.93269280284966,-0.295841413118037,
1.85714690799117));
#279524=CARTESIAN_POINT('Ctrl Pts',(1.94068806489674,-0.227696804473273,
1.86105499237512));
#279525=CARTESIAN_POINT('Ctrl Pts',(1.94868810662962,-0.159511457974536,
1.86496541306965));
#279526=CARTESIAN_POINT('Ctrl Pts',(1.95308282598641,-0.0909682836632935,
1.86887583376419));
#279527=CARTESIAN_POINT('Ctrl Pts',(1.95387072493651,-0.0224764373531737,
1.87278625445873));
#279528=CARTESIAN_POINT('Ctrl Pts',(1.95465998810928,0.0461340004717905,
1.87670344592584));
#279529=CARTESIAN_POINT('Ctrl Pts',(1.95182998677124,0.11469244159376,1.88062063739294));
#279530=CARTESIAN_POINT('Ctrl Pts',(1.94543122643806,0.182793170549961,
1.88453782886004));
#279531=CARTESIAN_POINT('Ctrl Pts',(1.94236496563336,0.215426772231656,
1.88641493161661));
#279532=CARTESIAN_POINT('Ctrl Pts',(1.93847997567259,0.247955398226014,
1.88829203437319));
#279533=CARTESIAN_POINT('Ctrl Pts',(1.93378594678926,0.280335356315162,
1.89016913712976));
#279534=CARTESIAN_POINT('Ctrl Pts',(1.9239888350599,0.347916974382912,1.89408691988968));
#279535=CARTESIAN_POINT('Ctrl Pts',(1.91062524938797,0.415118643649139,
1.89800470264961));
#279536=CARTESIAN_POINT('Ctrl Pts',(1.89373707840404,0.481534918648398,
1.90192248540953));
#279537=CARTESIAN_POINT('Ctrl Pts',(1.87687437290302,0.547851045294272,
1.90583436058893));
#279538=CARTESIAN_POINT('Ctrl Pts',(1.85649775003331,0.61338365508765,1.90974623576834));
#279539=CARTESIAN_POINT('Ctrl Pts',(1.83270053654601,0.677735009678545,
1.91365811094774));
#279540=CARTESIAN_POINT('Ctrl Pts',(1.80893135959259,0.742010549135241,
1.91756537737658));
#279541=CARTESIAN_POINT('Ctrl Pts',(1.7817497653383,0.805107138040061,1.92147264380543));
#279542=CARTESIAN_POINT('Ctrl Pts',(1.75129906377595,0.86664155751815,1.92537991023427));
#279543=CARTESIAN_POINT('Ctrl Pts',(1.72086749130787,0.928137321147573,
1.92928472212301));
#279544=CARTESIAN_POINT('Ctrl Pts',(1.68717110299145,0.988072422073371,
1.93318953401176));
#279545=CARTESIAN_POINT('Ctrl Pts',(1.65040094626024,1.04608446914353,1.93709434590051));
#279546=CARTESIAN_POINT('Ctrl Pts',(1.61364127062815,1.10407998024896,1.94099804474748));
#279547=CARTESIAN_POINT('Ctrl Pts',(1.57380982914045,1.16015311031874,1.94490174359446));
#279548=CARTESIAN_POINT('Ctrl Pts',(1.53114223179459,1.21396847818017,1.94880544244144));
#279549=CARTESIAN_POINT('Ctrl Pts',(1.48847215542045,1.26778697276604,1.95270936809705));
#279550=CARTESIAN_POINT('Ctrl Pts',(1.44296590369202,1.3193470607829,1.95661329375267));
#279551=CARTESIAN_POINT('Ctrl Pts',(1.39489965817954,1.36834606134947,1.96051721940829));
#279552=CARTESIAN_POINT('Ctrl Pts',(1.34678216663865,1.41739730240515,1.96442530725056));
#279553=CARTESIAN_POINT('Ctrl Pts',(1.29609957951229,1.46388165480261,1.96833339509282));
#279554=CARTESIAN_POINT('Ctrl Pts',(1.24316455237532,1.50753371296216,1.97224148293508));
#279555=CARTESIAN_POINT('Ctrl Pts',(1.19019787973408,1.55121186710139,1.97615190710203));
#279556=CARTESIAN_POINT('Ctrl Pts',(1.13497648281745,1.59205406464089,1.98006233126897));
#279557=CARTESIAN_POINT('Ctrl Pts',(1.07784340175706,1.62983729288809,1.98397275543592));
#279558=CARTESIAN_POINT('Ctrl Pts',(1.02061139683592,1.66768594142666,1.98788995036069));
#279559=CARTESIAN_POINT('Ctrl Pts',(0.961461525323312,1.70246480033226,
1.99180714528546));
#279560=CARTESIAN_POINT('Ctrl Pts',(0.900762120884259,1.73399642490407,
1.99572434021024));
#279561=CARTESIAN_POINT('Ctrl Pts',(0.871675703213898,1.74910599658103,
1.99760141246047));
#279562=CARTESIAN_POINT('Ctrl Pts',(0.842233784874234,1.76347064403427,
1.9994784847107));
#279563=CARTESIAN_POINT('Ctrl Pts',(0.812478334269017,1.7770748313854,2.00135555696093));
#279564=CARTESIAN_POINT('Ctrl Pts',(0.750373447598841,1.80546917583313,
2.00527333864467));
#279565=CARTESIAN_POINT('Ctrl Pts',(0.686654915849971,1.83066036058571,
2.0091911203284));
#279566=CARTESIAN_POINT('Ctrl Pts',(0.621686174808076,1.85246384581522,
2.01310890201214));
#279567=CARTESIAN_POINT('Ctrl Pts',(0.556815399598003,1.87423445374815,
2.017020776105));
#279568=CARTESIAN_POINT('Ctrl Pts',(0.49069861913138,1.89262734494918,2.02093265019786));
#279569=CARTESIAN_POINT('Ctrl Pts',(0.423720670561041,1.90750538487819,
2.02484452429072));
#279570=CARTESIAN_POINT('Ctrl Pts',(0.356821631821588,1.9223658962976,2.0287517896231));
#279571=CARTESIAN_POINT('Ctrl Pts',(0.289063917933306,1.9337196743245,2.03265905495547));
#279572=CARTESIAN_POINT('Ctrl Pts',(0.220847253844517,1.94147945919326,
2.03656632028784));
#279573=CARTESIAN_POINT('Ctrl Pts',(0.152673443490873,1.94923436936211,
2.0404711310746));
#279574=CARTESIAN_POINT('Ctrl Pts',(0.0840417425782409,1.9533997095032,
2.04437594186135));
#279575=CARTESIAN_POINT('Ctrl Pts',(0.0153602452684157,1.95393962620786,
2.04828075264811));
#279576=CARTESIAN_POINT('Ctrl Pts',(-0.0533016747448948,1.95447938901212,
2.05218445038926));
#279577=CARTESIAN_POINT('Ctrl Pts',(-0.122012871243881,1.95139577597591,
2.05608814813042));
#279578=CARTESIAN_POINT('Ctrl Pts',(-0.190363797093479,1.94470502255642,
2.05999184587157));
#279579=CARTESIAN_POINT('Ctrl Pts',(-0.258718694160792,1.93801388040131,
2.06389577041922));
#279580=CARTESIAN_POINT('Ctrl Pts',(-0.326712789629498,1.92771523225302,
2.06779969496686));
#279581=CARTESIAN_POINT('Ctrl Pts',(-0.393942028521599,1.91387713246287,
2.0717036195145));
#279582=CARTESIAN_POINT('Ctrl Pts',(-0.461242944243122,1.90002427910515,
2.07561170625316));
#279583=CARTESIAN_POINT('Ctrl Pts',(-0.527776893161754,1.88262454245478,
2.07951979299182));
#279584=CARTESIAN_POINT('Ctrl Pts',(-0.59315137805678,1.86179683174866,
2.08342787973048));
#279585=CARTESIAN_POINT('Ctrl Pts',(-0.658564945011555,1.8409566698571,
2.08733830279468));
#279586=CARTESIAN_POINT('Ctrl Pts',(-0.72281720814349,1.81668462930955,
2.09124872585889));
#279587=CARTESIAN_POINT('Ctrl Pts',(-0.785534829123767,1.78914813032166,
2.0951591489231));
#279588=CARTESIAN_POINT('Ctrl Pts',(-0.84836104363242,1.76156395277809,
2.09907634275812));
#279589=CARTESIAN_POINT('Ctrl Pts',(-0.909646873401562,1.73070425670226,
2.10299353659315));
#279590=CARTESIAN_POINT('Ctrl Pts',(-0.969043566553686,1.69678241566823,
2.10691073042818));
#279591=CARTESIAN_POINT('Ctrl Pts',(-0.997505898385083,1.68052739127875,
2.10878781254948));
#279592=CARTESIAN_POINT('Ctrl Pts',(-1.02553487068763,1.66356986657697,
2.11066489467079));
#279593=CARTESIAN_POINT('Ctrl Pts',(-1.05309468069113,1.64593669182629,
2.11254197679209));
#279594=CARTESIAN_POINT('Ctrl Pts',(-1.11061657059442,1.6091333344546,2.11645975819579));
#279595=CARTESIAN_POINT('Ctrl Pts',(-1.166321110383,1.56923783920942,2.12037753959948));
#279596=CARTESIAN_POINT('Ctrl Pts',(-1.21985623987019,1.52645561810678,
2.12429532100318));
#279597=CARTESIAN_POINT('Ctrl Pts',(-1.27331064405205,1.48373790806248,
2.12820719480745));
#279598=CARTESIAN_POINT('Ctrl Pts',(-1.32460174890658,1.43814241566986,
2.13211906861172));
#279599=CARTESIAN_POINT('Ctrl Pts',(-1.37340573420718,1.38991823113694,
2.13603094241599));
#279600=CARTESIAN_POINT('Ctrl Pts',(-1.42215222112183,1.34175086189805,
2.1399382074485));
#279601=CARTESIAN_POINT('Ctrl Pts',(-1.4684170595732,1.29096129530906,2.143845472481));
#279602=CARTESIAN_POINT('Ctrl Pts',(-1.51191027484992,1.2378381642215,2.1477527375135));
#279603=CARTESIAN_POINT('Ctrl Pts',(-1.55537616759355,1.18474840520122,
2.15165754799355));
#279604=CARTESIAN_POINT('Ctrl Pts',(-1.59607358003439,1.12932836944604,
2.1555623584736));
#279605=CARTESIAN_POINT('Ctrl Pts',(-1.63375120303759,1.07190158436921,
2.15946716895365));
#279606=CARTESIAN_POINT('Ctrl Pts',(-1.67141808617182,1.01449116858795,
2.16337086638172));
#279607=CARTESIAN_POINT('Ctrl Pts',(-1.70606661888143,0.955075550173974,
2.16727456380979));
#279608=CARTESIAN_POINT('Ctrl Pts',(-1.73748847963734,0.894007708651057,
2.17117826123786));
#279609=CARTESIAN_POINT('Ctrl Pts',(-1.76891216596912,0.832936319153111,
2.1750821854665));
#279610=CARTESIAN_POINT('Ctrl Pts',(-1.79710858533814,0.770212954604344,
2.17898610969513));
#279611=CARTESIAN_POINT('Ctrl Pts',(-1.82191594105054,0.706214063684601,
2.18289003392377));
#279612=CARTESIAN_POINT('Ctrl Pts',(-1.8467497452228,0.64214694009562,2.18679812033657));
#279613=CARTESIAN_POINT('Ctrl Pts',(-1.86818709655051,0.576802035764591,
2.19070620674938));
#279614=CARTESIAN_POINT('Ctrl Pts',(-1.88611520045465,0.510573648569824,
2.19461429316218));
#279615=CARTESIAN_POINT('Ctrl Pts',(-1.90405402208717,0.444305668907904,
2.19852471589616));
#279616=CARTESIAN_POINT('Ctrl Pts',(-1.91847931777625,0.377153636328863,
2.20243513863013));
#279617=CARTESIAN_POINT('Ctrl Pts',(-1.92932944490711,0.30952203962631,
2.2063455613641));
#279618=CARTESIAN_POINT('Ctrl Pts',(-1.94019835867385,0.241773341053369,
2.21026275486556));
#279619=CARTESIAN_POINT('Ctrl Pts',(-1.94747969671305,0.173543910054779,
2.21417994836703));
#279620=CARTESIAN_POINT('Ctrl Pts',(-1.95116376058966,0.105242478883757,
2.21809714186849));
#279621=CARTESIAN_POINT('Ctrl Pts',(-1.95292913182754,0.0725130295219804,
2.21997422678674));
#279622=CARTESIAN_POINT('Ctrl Pts',(-1.95386925313585,0.0397670322126749,
2.221851311705));
#279623=CARTESIAN_POINT('Ctrl Pts',(-1.95398728496305,0.00704912780047304,
2.22372839662325));
#279624=CARTESIAN_POINT('Ctrl Pts',(-1.95399570907482,0.0047140009923209,
2.22386236704075));
#279625=CARTESIAN_POINT('Ctrl Pts',(-1.95399994727307,0.00237885907428622,
2.22399633745825));
#279626=CARTESIAN_POINT('Ctrl Pts',(-1.95399999951108,4.37116182806309E-5,
2.22413030787575));
#279627=CARTESIAN_POINT('',(-1.95399927934589,0.00167818823651517,2.92413028797392));
#279628=CARTESIAN_POINT('Ctrl Pts',(-1.9539999995111,4.3710859498061E-5,
2.22413030791928));
#279629=CARTESIAN_POINT('Ctrl Pts',(-1.95400152612208,-0.0682001511849845,
2.22804554619099));
#279630=CARTESIAN_POINT('Ctrl Pts',(-1.95042359878162,-0.136580523234795,
2.2319607844627));
#279631=CARTESIAN_POINT('Ctrl Pts',(-1.94324927802393,-0.204690604228606,
2.23587602273441));
#279632=CARTESIAN_POINT('Ctrl Pts',(-1.93608577702256,-0.272697966860162,
2.23978535634624));
#279633=CARTESIAN_POINT('Ctrl Pts',(-1.92533669762871,-0.340435361385916,
2.24369468995806));
#279634=CARTESIAN_POINT('Ctrl Pts',(-1.91103711244139,-0.407496202278842,
2.24760402356988));
#279635=CARTESIAN_POINT('Ctrl Pts',(-1.89675434668933,-0.474478164976527,
2.25150875895156));
#279636=CARTESIAN_POINT('Ctrl Pts',(-1.87892947097966,-0.540784674814253,
2.25541349433325));
#279637=CARTESIAN_POINT('Ctrl Pts',(-1.85764911067538,-0.606016321238107,
2.25931822971493));
#279638=CARTESIAN_POINT('Ctrl Pts',(-1.83638206857691,-0.671207142766151,
2.26322052133773));
#279639=CARTESIAN_POINT('Ctrl Pts',(-1.81166398405568,-0.735323967876062,
2.26712281296053));
#279640=CARTESIAN_POINT('Ctrl Pts',(-1.78363171766969,-0.797981137447913,
2.27102510458334));
#279641=CARTESIAN_POINT('Ctrl Pts',(-1.7556073414111,-0.860620671162447,
2.27492629784407));
#279642=CARTESIAN_POINT('Ctrl Pts',(-1.72427083618383,-0.92180091536956,
2.27882749110481));
#279643=CARTESIAN_POINT('Ctrl Pts',(-1.689807040121,-0.981156545693654,
2.28272868436555));
#279644=CARTESIAN_POINT('Ctrl Pts',(-1.65534107616103,-1.0405159097011,
2.28663012302542));
#279645=CARTESIAN_POINT('Ctrl Pts',(-1.61774768050431,-1.09805000720077,
2.29053156168529));
#279646=CARTESIAN_POINT('Ctrl Pts',(-1.57725653045632,-1.15342006100679,
2.29443300034516));
#279647=CARTESIAN_POINT('Ctrl Pts',(-1.53672212888753,-1.20884925956495,
2.29833860641334));
#279648=CARTESIAN_POINT('Ctrl Pts',(-1.49328408741571,-1.26210940305978,
2.30224421248153));
#279649=CARTESIAN_POINT('Ctrl Pts',(-1.44721351258141,-1.31289338828474,
2.30614981854971));
#279650=CARTESIAN_POINT('Ctrl Pts',(-1.40111509400187,-1.36370806590612,
2.31005778505514));
#279651=CARTESIAN_POINT('Ctrl Pts',(-1.35238132578439,-1.4120432602486,
2.31396575156056));
#279652=CARTESIAN_POINT('Ctrl Pts',(-1.30131944495118,-1.45762948042085,
2.31787371806598));
#279653=CARTESIAN_POINT('Ctrl Pts',(-1.25016960736101,-1.50329422523855,
2.32178841624784));
#279654=CARTESIAN_POINT('Ctrl Pts',(-1.1966840380014,-1.54620023786575,
2.3257031144297));
#279655=CARTESIAN_POINT('Ctrl Pts',(-1.1412014931318,-1.58611952641463,
2.32961781261156));
#279656=CARTESIAN_POINT('Ctrl Pts',(-1.11617689440725,-1.60412454366199,
2.33138348055918));
#279657=CARTESIAN_POINT('Ctrl Pts',(-1.09074641105524,-1.62152256671591,
2.3331491485068));
#279658=CARTESIAN_POINT('Ctrl Pts',(-1.06494276013452,-1.63829573570741,
2.33491481645442));
#279659=CARTESIAN_POINT('Ctrl Pts',(-1.00768790033717,-1.67551316055615,
2.33883259813192));
#279660=CARTESIAN_POINT('Ctrl Pts',(-0.948365952049804,-1.70979950585628,
2.34275037980941));
#279661=CARTESIAN_POINT('Ctrl Pts',(-0.887309266746829,-1.74091879912453,
2.34666816148691));
#279662=CARTESIAN_POINT('Ctrl Pts',(-0.826344648363723,-1.77199116784283,
2.35058003557067));
#279663=CARTESIAN_POINT('Ctrl Pts',(-0.76365091914729,-1.79990574067459,
2.35449190965443));
#279664=CARTESIAN_POINT('Ctrl Pts',(-0.699588569647908,-1.82447028839003,
2.35840378373819));
#279665=CARTESIAN_POINT('Ctrl Pts',(-0.635601695046089,-1.84900589544474,
2.36231104905723));
#279666=CARTESIAN_POINT('Ctrl Pts',(-0.570249859649652,-1.87019914048092,
2.36621831437628));
#279667=CARTESIAN_POINT('Ctrl Pts',(-0.503915613413959,-1.88790493790276,
2.37012557969532));
#279668=CARTESIAN_POINT('Ctrl Pts',(-0.437623038422356,-1.90559961252382,
2.37403039046614));
#279669=CARTESIAN_POINT('Ctrl Pts',(-0.370349751079686,-1.9198110587845,
2.37793520123695));
#279670=CARTESIAN_POINT('Ctrl Pts',(-0.302494138213879,-1.93044380812969,
2.38184001200777));
#279671=CARTESIAN_POINT('Ctrl Pts',(-0.234657867275876,-1.94107352665898,
2.38574370973038));
#279672=CARTESIAN_POINT('Ctrl Pts',(-0.166240086147915,-1.94812649717215,
2.38964740745299));
#279673=CARTESIAN_POINT('Ctrl Pts',(-0.0976482778165805,-1.95155856018708,
2.3935511051756));
#279674=CARTESIAN_POINT('Ctrl Pts',(-0.0290524843175811,-1.95499082260404,
2.39745502970211));
#279675=CARTESIAN_POINT('Ctrl Pts',(0.0397168649642915,-1.95480173782241,
2.40135895422863));
#279676=CARTESIAN_POINT('Ctrl Pts',(0.10825010022352,-1.95099920958508,
2.40526287875514));
#279677=CARTESIAN_POINT('Ctrl Pts',(0.176856402509035,-1.94719262726465,
2.40917096546888));
#279678=CARTESIAN_POINT('Ctrl Pts',(0.245225596207588,-1.93976494033833,
2.41307905218261));
#279679=CARTESIAN_POINT('Ctrl Pts',(0.312951966113218,-1.92877605410941,
2.41698713889635));
#279680=CARTESIAN_POINT('Ctrl Pts',(0.380718824040376,-1.91778059852999,
2.42089756193343));
#279681=CARTESIAN_POINT('Ctrl Pts',(0.447841612492412,-1.90321981097262,
2.42480798497051));
#279682=CARTESIAN_POINT('Ctrl Pts',(0.513926434020998,-1.88520439751621,
2.42871840800759));
#279683=CARTESIAN_POINT('Ctrl Pts',(0.580125679224455,-1.8671577909694,
2.43263560181235));
#279684=CARTESIAN_POINT('Ctrl Pts',(0.645282903573845,-1.84564477427755,
2.43655279561712));
#279685=CARTESIAN_POINT('Ctrl Pts',(0.709021772010433,-1.82082512252418,
2.44046998942189));
#279686=CARTESIAN_POINT('Ctrl Pts',(0.739564835988387,-1.80893177973338,
2.44234707170978));
#279687=CARTESIAN_POINT('Ctrl Pts',(0.769782543884459,-1.79627985217198,
2.44422415399768));
#279688=CARTESIAN_POINT('Ctrl Pts',(0.799635534081065,-1.78289063395232,
2.44610123628558));
#279689=CARTESIAN_POINT('Ctrl Pts',(0.86194366948292,-1.75494511773228,
2.45001901794111));
#279690=CARTESIAN_POINT('Ctrl Pts',(0.922908864854092,-1.7236738544009,
2.45393679959663));
#279691=CARTESIAN_POINT('Ctrl Pts',(0.982152683406715,-1.68922825765999,
2.45785458125216));
#279692=CARTESIAN_POINT('Ctrl Pts',(1.0413071686328,-1.65483460118586,2.46176645531299));
#279693=CARTESIAN_POINT('Ctrl Pts',(1.0987450065672,-1.61727635613494,2.46567832937382));
#279694=CARTESIAN_POINT('Ctrl Pts',(1.15410927115323,-1.57675229197175,
2.46959020343466));
#279695=CARTESIAN_POINT('Ctrl Pts',(1.20940830844943,-1.53627597114802,
2.47349746872944));
#279696=CARTESIAN_POINT('Ctrl Pts',(1.26263822904503,-1.49284105985327,
2.47740473402422));
#279697=CARTESIAN_POINT('Ctrl Pts',(1.31346977031877,-1.44669041693749,
2.481311999319));
#279698=CARTESIAN_POINT('Ctrl Pts',(1.36426937915338,-1.40056876591451,
2.48521681006474));
#279699=CARTESIAN_POINT('Ctrl Pts',(1.41267323395259,-1.35173509741243,
2.48912162081047));
#279700=CARTESIAN_POINT('Ctrl Pts',(1.45838518664059,-1.30047247083023,
2.4930264315562));
#279701=CARTESIAN_POINT('Ctrl Pts',(1.50408410933938,-1.24922445643221,
2.49693012925297));
#279702=CARTESIAN_POINT('Ctrl Pts',(1.54709232587545,-1.19554922541606,
2.50083382694973));
#279703=CARTESIAN_POINT('Ctrl Pts',(1.58715187801053,-1.13976528992931,
2.50473752464649));
#279704=CARTESIAN_POINT('Ctrl Pts',(1.62721375758841,-1.08397811341984,
2.50864144914641));
#279705=CARTESIAN_POINT('Ctrl Pts',(1.66432634774585,-1.02608239031074,
2.51254537364634));
#279706=CARTESIAN_POINT('Ctrl Pts',(1.69827425857821,-0.966426687675084,
2.51644929814626));
#279707=CARTESIAN_POINT('Ctrl Pts',(1.73225836312498,-0.906707382849745,
2.52035738483246));
#279708=CARTESIAN_POINT('Ctrl Pts',(1.76307081094299,-0.845224782145801,
2.52426547151866));
#279709=CARTESIAN_POINT('Ctrl Pts',(1.79054205715451,-0.782352312938932,
2.52817355820485));
#279710=CARTESIAN_POINT('Ctrl Pts',(1.8180297261589,-0.719442257467103,
2.53208398121382));
#279711=CARTESIAN_POINT('Ctrl Pts',(1.8421720453558,-0.6551411405343,2.53599440422279));
#279712=CARTESIAN_POINT('Ctrl Pts',(1.86284856742513,-0.589839990880701,
2.53990482723176));
#279713=CARTESIAN_POINT('Ctrl Pts',(1.88356089020309,-0.524425774463525,
2.5438220210078));
#279714=CARTESIAN_POINT('Ctrl Pts',(1.9007953153205,-0.458008545412891,
2.54773921478384));
#279715=CARTESIAN_POINT('Ctrl Pts',(1.91448215111361,-0.390991167505634,
2.55165640855989));
#279716=CARTESIAN_POINT('Ctrl Pts',(1.92104075445974,-0.358877068554237,
2.55353349107884));
#279717=CARTESIAN_POINT('Ctrl Pts',(1.92678551273033,-0.326625259875533,
2.55541057359779));
#279718=CARTESIAN_POINT('Ctrl Pts',(1.93171298819275,-0.294280361640803,
2.55728765611674));
#279719=CARTESIAN_POINT('Ctrl Pts',(1.94199744457105,-0.226771208628695,
2.56120543783516));
#279720=CARTESIAN_POINT('Ctrl Pts',(1.94875912359902,-0.158588169546824,
2.56512321955358));
#279721=CARTESIAN_POINT('Ctrl Pts',(1.95192016769347,-0.0901313427808721,
2.569041001272));
#279722=CARTESIAN_POINT('Ctrl Pts',(1.95507644527331,-0.0217777415491875,
2.57295287539683));
#279723=CARTESIAN_POINT('Ctrl Pts',(1.95464284070292,0.0468483405377008,
2.57686474952166));
#279724=CARTESIAN_POINT('Ctrl Pts',(1.95059295217582,0.115339216756569,
2.58077662364648));
#279725=CARTESIAN_POINT('Ctrl Pts',(1.94654783501475,0.183749400621046,
2.58468388900661));
#279726=CARTESIAN_POINT('Ctrl Pts',(1.93889492419678,0.252024206184032,
2.58859115436673));
#279727=CARTESIAN_POINT('Ctrl Pts',(1.9276598632852,0.319755299376386,2.59249841972685));
#279728=CARTESIAN_POINT('Ctrl Pts',(1.91643186025083,0.387443843824019,
2.59640323053872));
#279729=CARTESIAN_POINT('Ctrl Pts',(1.90162625130672,0.454588869187506,
2.60030804135058));
#279730=CARTESIAN_POINT('Ctrl Pts',(1.88332041162024,0.520788082788541,
2.60421285216245));
#279731=CARTESIAN_POINT('Ctrl Pts',(1.86501978992884,0.5869684266094,2.60811654992603));
#279732=CARTESIAN_POINT('Ctrl Pts',(1.84322104918359,0.652203019899014,
2.61202024768961));
#279733=CARTESIAN_POINT('Ctrl Pts',(1.81805205683821,0.716102449811733,
2.61592394545318));
#279734=CARTESIAN_POINT('Ctrl Pts',(1.79288160218125,0.780005592263864,
2.61982787002053));
#279735=CARTESIAN_POINT('Ctrl Pts',(1.76434068984971,0.842572960514409,
2.62373179458788));
#279736=CARTESIAN_POINT('Ctrl Pts',(1.73260551634365,0.903434626708295,
2.62763571915523));
#279737=CARTESIAN_POINT('Ctrl Pts',(1.70083650823985,0.964361180840896,
2.63154380590929));
#279738=CARTESIAN_POINT('Ctrl Pts',(1.66586667032203,1.02357796654965,2.63545189266335));
#279739=CARTESIAN_POINT('Ctrl Pts',(1.62791793851127,1.08074011005108,2.6393599794174));
#279740=CARTESIAN_POINT('Ctrl Pts',(1.58994652028003,1.13793642608901,2.64327040249458));
#279741=CARTESIAN_POINT('Ctrl Pts',(1.54899295736738,1.19307526035967,2.64718082557175));
#279742=CARTESIAN_POINT('Ctrl Pts',(1.50532058755956,1.24584346074028,2.65109124864892));
#279743=CARTESIAN_POINT('Ctrl Pts',(1.4615726005026,1.29870302749678,2.655008442493));
#279744=CARTESIAN_POINT('Ctrl Pts',(1.41509674402807,1.34918340621439,2.65892563633708));
#279745=CARTESIAN_POINT('Ctrl Pts',(1.36619381046245,1.39700768510917,2.66284283018116));
#279746=CARTESIAN_POINT('Ctrl Pts',(1.34275999120437,1.41992462333875,2.66471991210341));
#279747=CARTESIAN_POINT('Ctrl Pts',(1.31876935571298,1.44223224835895,2.66659699402565));
#279748=CARTESIAN_POINT('Ctrl Pts',(1.29425753923292,1.4639034879864,2.6684740759479));
#279749=CARTESIAN_POINT('Ctrl Pts',(1.24309730769296,1.50913496391558,2.67239185763658));
#279750=CARTESIAN_POINT('Ctrl Pts',(1.18946147848789,1.55177115595393,2.67630963932525));
#279751=CARTESIAN_POINT('Ctrl Pts',(1.13364409416159,1.59152978852818,2.68022742101392));
#279752=CARTESIAN_POINT('Ctrl Pts',(1.07791087645525,1.63122846935516,2.68413929510864));
#279753=CARTESIAN_POINT('Ctrl Pts',(1.02000302965254,1.66805791900372,2.68805116920335));
#279754=CARTESIAN_POINT('Ctrl Pts',(0.960248861394475,1.70177499223329,
2.69196304329807));
#279755=CARTESIAN_POINT('Ctrl Pts',(0.900565092366708,1.73545234177374,
2.69587030862768));
#279756=CARTESIAN_POINT('Ctrl Pts',(0.839039748354085,1.76602435662461,
2.69977757395729));
#279757=CARTESIAN_POINT('Ctrl Pts',(0.77602988848427,1.79329127923466,2.70368483928691));
#279758=CARTESIAN_POINT('Ctrl Pts',(0.713059611479431,1.82054107273321,
2.70758965006804));
#279759=CARTESIAN_POINT('Ctrl Pts',(0.648607119030157,1.84448969764631,
2.71149446084917));
#279760=CARTESIAN_POINT('Ctrl Pts',(0.583052430532476,1.86498414557609,
2.7153992716303));
#279761=CARTESIAN_POINT('Ctrl Pts',(0.517516428098966,1.88547275165721,
2.71930296936297));
#279762=CARTESIAN_POINT('Ctrl Pts',(0.450879322648276,1.9025089885884,2.72320666709565));
#279763=CARTESIAN_POINT('Ctrl Pts',(0.383537675186315,1.91598926189911,
2.72711036482832));
#279764=CARTESIAN_POINT('Ctrl Pts',(0.316192115195746,1.92947031840946,
2.73101428936461));
#279765=CARTESIAN_POINT('Ctrl Pts',(0.248142414838569,1.93939490706247,
2.7349182139009));
#279766=CARTESIAN_POINT('Ctrl Pts',(0.17979495337632,1.94571060919665,2.73882213843719));
#279767=CARTESIAN_POINT('Ctrl Pts',(0.111374622960162,1.95203304484511,
2.74273022516021));
#279768=CARTESIAN_POINT('Ctrl Pts',(0.0426563887231679,1.95473886985672,
2.74663831188322));
#279769=CARTESIAN_POINT('Ctrl Pts',(-0.0259496355521265,1.95382768339859,
2.75054639860624));
#279770=CARTESIAN_POINT('Ctrl Pts',(-0.0945966737171027,1.95291595221715,
2.75445682165234));
#279771=CARTESIAN_POINT('Ctrl Pts',(-0.163130877432424,1.94838293864801,
2.75836724469843));
#279772=CARTESIAN_POINT('Ctrl Pts',(-0.231146352647582,1.94028022812627,
2.76227766774453));
#279773=CARTESIAN_POINT('Ctrl Pts',(-0.299279594391147,1.93216348803131,
2.7661948615578));
#279774=CARTESIAN_POINT('Ctrl Pts',(-0.36689183048276,1.9204647987446,2.77011205537106));
#279775=CARTESIAN_POINT('Ctrl Pts',(-0.433587323431622,1.90528686369255,
2.77402924918433));
#279776=CARTESIAN_POINT('Ctrl Pts',(-0.465547172365731,1.89801374087798,
2.77590633138258));
#279777=CARTESIAN_POINT('Ctrl Pts',(-0.497296741324567,1.88994243911198,
2.77778341358082));
#279778=CARTESIAN_POINT('Ctrl Pts',(-0.528793965500402,1.881088233457,2.77966049577907));
#279779=CARTESIAN_POINT('Ctrl Pts',(-0.594533893257536,1.86260803860376,
2.78357827746733));
#279780=CARTESIAN_POINT('Ctrl Pts',(-0.659434484196362,1.84064078252868,
2.78749605915558));
#279781=CARTESIAN_POINT('Ctrl Pts',(-0.723099151368537,1.81528058913494,
2.79141384084384));
#279782=CARTESIAN_POINT('Ctrl Pts',(-0.786667819059477,1.78995863618945,
2.79532571493803));
#279783=CARTESIAN_POINT('Ctrl Pts',(-0.849003808257224,1.76125408025483,
2.79923758903223));
#279784=CARTESIAN_POINT('Ctrl Pts',(-0.909724845911147,1.72931104915569,
2.80314946312642));
#279785=CARTESIAN_POINT('Ctrl Pts',(-0.970374345217748,1.6974056516633,
2.80705672845538));
#279786=CARTESIAN_POINT('Ctrl Pts',(-1.02941223831299,1.66226958436928,
2.81096399378433));
#279787=CARTESIAN_POINT('Ctrl Pts',(-1.08647713215179,1.62409465281775,
2.81487125911329));
#279788=CARTESIAN_POINT('Ctrl Pts',(-1.14350617775877,1.58594370280205,
2.81877606989368));
#279789=CARTESIAN_POINT('Ctrl Pts',(-1.198564274746,1.54475794831463,2.82268088067407));
#279790=CARTESIAN_POINT('Ctrl Pts',(-1.25131687373763,1.50077382756346,
2.82658569145446));
#279791=CARTESIAN_POINT('Ctrl Pts',(-1.30405443584069,1.456802244286,2.83048938918629));
#279792=CARTESIAN_POINT('Ctrl Pts',(-1.35448742683864,1.41003419312665,
2.83439308691811));
#279793=CARTESIAN_POINT('Ctrl Pts',(-1.40231385925453,1.36074679501465,
2.83829678464993));
#279794=CARTESIAN_POINT('Ctrl Pts',(-1.45014307037028,1.31145653332119,
2.8422007091853));
#279795=CARTESIAN_POINT('Ctrl Pts',(-1.49536508146451,1.25964698892887,
2.84610463372067));
#279796=CARTESIAN_POINT('Ctrl Pts',(-1.53771559154354,1.20563127013358,
2.85000855825604));
#279797=CARTESIAN_POINT('Ctrl Pts',(-1.58011125380827,1.15155796223815,
2.85391664497801));
#279798=CARTESIAN_POINT('Ctrl Pts',(-1.61962900111618,1.09527417369821,
2.85782473169997));
#279799=CARTESIAN_POINT('Ctrl Pts',(-1.65604622383594,1.03712434380779,
2.86173281842194));
#279800=CARTESIAN_POINT('Ctrl Pts',(-1.69248521741219,0.978939750925921,
2.86564324146691));
#279801=CARTESIAN_POINT('Ctrl Pts',(-1.72581975869414,0.918887326763719,
2.86955366451188));
#279802=CARTESIAN_POINT('Ctrl Pts',(-1.75587321392212,0.857336139813785,
2.87346408755686));
#279803=CARTESIAN_POINT('Ctrl Pts',(-1.78597870570537,0.795678379036743,
2.8773812813689));
#279804=CARTESIAN_POINT('Ctrl Pts',(-1.81279158057834,0.732517128725427,
2.88129847518093));
#279805=CARTESIAN_POINT('Ctrl Pts',(-1.83618366859166,0.668240626718617,
2.88521566899297));
#279806=CARTESIAN_POINT('Ctrl Pts',(-1.84739293580489,0.637439935214873,
2.88709275119873));
#279807=CARTESIAN_POINT('Ctrl Pts',(-1.85781745224111,0.606383365739943,
2.88896983340448));
#279808=CARTESIAN_POINT('Ctrl Pts',(-1.86744725673438,0.575114547994793,
2.89084691561023));
#279809=CARTESIAN_POINT('Ctrl Pts',(-1.89195310352142,0.495541919348942,
2.89562369887442));
#279810=CARTESIAN_POINT('Ctrl Pts',(-1.91138829262048,0.41433886039205,
2.90040048213861));
#279811=CARTESIAN_POINT('Ctrl Pts',(-1.92557302732791,0.33209112669148,
2.9051772654028));
#279812=CARTESIAN_POINT('Ctrl Pts',(-1.93956135918817,0.250982200970493,
2.90988790898565));
#279813=CARTESIAN_POINT('Ctrl Pts',(-1.94844357914405,0.168857321384975,
2.9145985525685));
#279814=CARTESIAN_POINT('Ctrl Pts',(-1.9520933534157,0.0862991283284693,
2.91930919615135));
#279815=CARTESIAN_POINT('Ctrl Pts',(-1.95333846968525,0.0581344962967553,
2.92091622675888));
#279816=CARTESIAN_POINT('Ctrl Pts',(-1.95397502425442,0.0299196156356976,
2.9225232573664));
#279817=CARTESIAN_POINT('Ctrl Pts',(-1.95399927934589,0.00167818823651517,
2.92413028797392));
#279818=CARTESIAN_POINT('',(-1.95391614919261,-0.000969648952806235,3.62413035429011));
#279819=CARTESIAN_POINT('Ctrl Pts',(-1.95274315056508,0.00167675988910205,
2.92413030787576));
#279820=CARTESIAN_POINT('Ctrl Pts',(-1.94901804708373,-0.45438081105706,
2.95009798373097));
#279821=CARTESIAN_POINT('Ctrl Pts',(-1.562324701513,-1.56703485389375,3.0131277995299));
#279822=CARTESIAN_POINT('Ctrl Pts',(0.291342892527357,-2.29141958423336,
3.11321975527255));
#279823=CARTESIAN_POINT('Ctrl Pts',(2.08359330569799,-0.997057334412019,
3.22440617510372));
#279824=CARTESIAN_POINT('Ctrl Pts',(1.96718185643315,1.21065268979667,3.33559259493487));
#279825=CARTESIAN_POINT('Ctrl Pts',(0.0487464827200954,2.30935232741887,
3.44677901476604));
#279826=CARTESIAN_POINT('Ctrl Pts',(-1.64937842670566,1.42982133530745,
3.54295825241301));
#279827=CARTESIAN_POINT('Ctrl Pts',(-1.94952253842872,0.387114015523011,
3.60207535011624));
#279828=CARTESIAN_POINT('Ctrl Pts',(-1.95125983814034,-0.000967513988672578,
3.62413030787576));
#279829=CARTESIAN_POINT('',(-1.95399963679489,-0.00119138802316145,4.32413030787576));
#279830=CARTESIAN_POINT('Ctrl Pts',(-1.95399975937833,-0.000969716153049057,
3.62413035575105));
#279831=CARTESIAN_POINT('Ctrl Pts',(-1.95396212499893,-0.0768038332389409,
3.62843403175574));
#279832=CARTESIAN_POINT('Ctrl Pts',(-1.94950568155316,-0.152487481613112,
3.63273770776042));
#279833=CARTESIAN_POINT('Ctrl Pts',(-1.94070759056848,-0.227530323055786,
3.63704138376511));
#279834=CARTESIAN_POINT('Ctrl Pts',(-1.93187850028117,-0.30283757137454,
3.64136022339508));
#279835=CARTESIAN_POINT('Ctrl Pts',(-1.91867725116394,-0.3774991953551,
3.64567906302506));
#279836=CARTESIAN_POINT('Ctrl Pts',(-1.90123179448794,-0.451036210994379,
3.64999790265503));
#279837=CARTESIAN_POINT('Ctrl Pts',(-1.88370328269169,-0.524923324988201,
3.65433730361232));
#279838=CARTESIAN_POINT('Ctrl Pts',(-1.86189020038226,-0.597674812201765,
3.6586767045696));
#279839=CARTESIAN_POINT('Ctrl Pts',(-1.8359705771302,-0.668825866659036,
3.66301610552688));
#279840=CARTESIAN_POINT('Ctrl Pts',(-1.82375412133664,-0.70236083369884,
3.66506135516071));
#279841=CARTESIAN_POINT('Ctrl Pts',(-1.81062610442916,-0.735540604450197,
3.66710660479454));
#279842=CARTESIAN_POINT('Ctrl Pts',(-1.79660870731119,-0.768318392864322,
3.66915185442836));
#279843=CARTESIAN_POINT('Ctrl Pts',(-1.76975765651418,-0.831105945668458,
3.67306963612123));
#279844=CARTESIAN_POINT('Ctrl Pts',(-1.73955787060529,-0.892608953619772,
3.67698741781409));
#279845=CARTESIAN_POINT('Ctrl Pts',(-1.706154118717,-0.952446388614617,
3.68090519950696));
#279846=CARTESIAN_POINT('Ctrl Pts',(-1.67280073609843,-1.01219359518505,
3.68481707360586));
#279847=CARTESIAN_POINT('Ctrl Pts',(-1.63625321359155,-1.07027978709881,
3.68872894770477));
#279848=CARTESIAN_POINT('Ctrl Pts',(-1.5967040452091,-1.12634461512137,
3.69264082180368));
#279849=CARTESIAN_POINT('Ctrl Pts',(-1.55720147158485,-1.1823433905008,
3.69654808713747));
#279850=CARTESIAN_POINT('Ctrl Pts',(-1.51470455759503,-1.23632513147622,
3.70045535247126));
#279851=CARTESIAN_POINT('Ctrl Pts',(-1.46945036390749,-1.28795637659516,
3.70436261780505));
#279852=CARTESIAN_POINT('Ctrl Pts',(-1.4242245989555,-1.33955518690765,
3.70826742859035));
#279853=CARTESIAN_POINT('Ctrl Pts',(-1.37624531381229,-1.38880606126236,
3.71217223937565));
#279854=CARTESIAN_POINT('Ctrl Pts',(-1.32579034293607,-1.43540794430624,
3.71607705016094));
#279855=CARTESIAN_POINT('Ctrl Pts',(-1.27534975401894,-1.48199654369612,
3.71998074789776));
#279856=CARTESIAN_POINT('Ctrl Pts',(-1.22243524148878,-1.5259373170701,
3.72388444563457));
#279857=CARTESIAN_POINT('Ctrl Pts',(-1.16736075532149,-1.56696677276043,
3.72778814337138));
#279858=CARTESIAN_POINT('Ctrl Pts',(-1.11228306934399,-1.60799861224915,
3.73169206791179));
#279859=CARTESIAN_POINT('Ctrl Pts',(-1.0550455566399,-1.64611850636757,
3.7355959924522));
#279860=CARTESIAN_POINT('Ctrl Pts',(-0.995992962315415,-1.68110499940312,
3.73949991699262));
#279861=CARTESIAN_POINT('Ctrl Pts',(-0.936877408802782,-1.71612879344506,
3.74340800371968));
#279862=CARTESIAN_POINT('Ctrl Pts',(-0.87594333574339,-1.74801226809313,
3.74731609044674));
#279863=CARTESIAN_POINT('Ctrl Pts',(-0.813561146877509,-1.77657937067032,
3.75122417717381));
#279864=CARTESIAN_POINT('Ctrl Pts',(-0.751141664840921,-1.80516355116434,
3.75513460022391));
#279865=CARTESIAN_POINT('Ctrl Pts',(-0.687272801642316,-1.83042723289383,
3.75904502327402));
#279866=CARTESIAN_POINT('Ctrl Pts',(-0.622343418737791,-1.8522431452576,
3.76295544632413));
#279867=CARTESIAN_POINT('Ctrl Pts',(-0.557301612772591,-1.87409683114592,
3.76687264014131));
#279868=CARTESIAN_POINT('Ctrl Pts',(-0.491196095925404,-1.89249070112647,
3.77078983395849));
#279869=CARTESIAN_POINT('Ctrl Pts',(-0.424428450934365,-1.90734802541053,
3.77470702777567));
#279870=CARTESIAN_POINT('Ctrl Pts',(-0.392434028086504,-1.91446751443243,
3.77658410993696));
#279871=CARTESIAN_POINT('Ctrl Pts',(-0.360287677037997,-1.92077569274014,
3.77846119209824));
#279872=CARTESIAN_POINT('Ctrl Pts',(-0.328033950954508,-1.92626834242303,
3.78033827425953));
#279873=CARTESIAN_POINT('Ctrl Pts',(-0.260715076915098,-1.93773241299857,
3.78425605595242));
#279874=CARTESIAN_POINT('Ctrl Pts',(-0.192660782914911,-1.94568603633619,
3.78817383764531));
#279875=CARTESIAN_POINT('Ctrl Pts',(-0.124269743834863,-1.95004436635868,
3.7920916193382));
#279876=CARTESIAN_POINT('Ctrl Pts',(-0.0559818310953371,-1.95439612448765,
3.79600349343714));
#279877=CARTESIAN_POINT('Ctrl Pts',(0.0126413319566921,-1.9551633175741,
3.79991536753607));
#279878=CARTESIAN_POINT('Ctrl Pts',(0.0811925829564603,-1.95231241466955,
3.80382724163501));
#279879=CARTESIAN_POINT('Ctrl Pts',(0.149663070463653,-1.94946487054945,
3.80773450696882));
#279880=CARTESIAN_POINT('Ctrl Pts',(0.218061324959097,-1.94300771642214,
3.81164177230263));
#279881=CARTESIAN_POINT('Ctrl Pts',(0.285978626207468,-1.93295944741541,
3.81554903763644));
#279882=CARTESIAN_POINT('Ctrl Pts',(0.353853261730547,-1.92291749074261,
3.81945384842176));
#279883=CARTESIAN_POINT('Ctrl Pts',(0.421247057755176,-1.90928896606093,
3.82335865920708));
#279884=CARTESIAN_POINT('Ctrl Pts',(0.487756429378236,-1.89214419788773,
3.8272634699924));
#279885=CARTESIAN_POINT('Ctrl Pts',(0.554246842808509,-1.87500431675243,
3.83116716772923));
#279886=CARTESIAN_POINT('Ctrl Pts',(0.619852856111499,-1.85435030456257,
3.83507086546606));
#279887=CARTESIAN_POINT('Ctrl Pts',(0.684182878795401,-1.83030319574743,
3.83897456320289));
#279888=CARTESIAN_POINT('Ctrl Pts',(0.748516639033264,-1.80625468980287,
3.84287848774333));
#279889=CARTESIAN_POINT('Ctrl Pts',(0.811573801526584,-1.778812870503,3.84678241228376));
#279890=CARTESIAN_POINT('Ctrl Pts',(0.87298141219139,-1.74814743484877,
3.85068633682419));
#279891=CARTESIAN_POINT('Ctrl Pts',(0.934454492855615,-1.71744930510283,
3.85459442355128));
#279892=CARTESIAN_POINT('Ctrl Pts',(0.994274070876336,-1.6835209202206,
3.85850251027836));
#279893=CARTESIAN_POINT('Ctrl Pts',(1.05209144211596,-1.64657814798641,
3.86241059700544));
#279894=CARTESIAN_POINT('Ctrl Pts',(1.10994337759795,-1.60961329071263,
3.86632102005557));
#279895=CARTESIAN_POINT('Ctrl Pts',(1.1657903240518,-1.5696307461132,3.8702314431057));
#279896=CARTESIAN_POINT('Ctrl Pts',(1.21931456974782,-1.52688833252491,
3.87414186615583));
#279897=CARTESIAN_POINT('Ctrl Pts',(1.27293149088987,-1.48407191187323,
3.87805905997304));
#279898=CARTESIAN_POINT('Ctrl Pts',(1.324217316999,-1.43848641142785,3.88197625379024));
#279899=CARTESIAN_POINT('Ctrl Pts',(1.3728899158051,-1.39042773241929,3.88589344760744));
#279900=CARTESIAN_POINT('Ctrl Pts',(1.39621336397132,-1.36739846880307,
3.88777052976852));
#279901=CARTESIAN_POINT('Ctrl Pts',(1.41893733450694,-1.34380181306207,
3.88964761192961));
#279902=CARTESIAN_POINT('Ctrl Pts',(1.44103413586229,-1.31967292132544,
3.89152469409069));
#279903=CARTESIAN_POINT('Ctrl Pts',(1.48715382397003,-1.26931192366867,
3.8954424757836));
#279904=CARTESIAN_POINT('Ctrl Pts',(1.53072194029792,-1.21643029835566,
3.8993602574765));
#279905=CARTESIAN_POINT('Ctrl Pts',(1.57145110770361,-1.16131710402332,
3.90327803916941));
#279906=CARTESIAN_POINT('Ctrl Pts',(1.61211885989988,-1.1062870144679,3.90718991326836));
#279907=CARTESIAN_POINT('Ctrl Pts',(1.64995586900205,-1.04903242657542,
3.91110178736731));
#279908=CARTESIAN_POINT('Ctrl Pts',(1.68471328268377,-0.989877343486992,
3.91501366146626));
#279909=CARTESIAN_POINT('Ctrl Pts',(1.71942974700163,-0.930791953818331,
3.91892092680009));
#279910=CARTESIAN_POINT('Ctrl Pts',(1.75107357350287,-0.86981093790479,
3.92282819213392));
#279911=CARTESIAN_POINT('Ctrl Pts',(1.77943878785213,-0.807287805114966,
3.92673545746775));
#279912=CARTESIAN_POINT('Ctrl Pts',(1.80778618314172,-0.74480394942772,
3.93064026825309));
#279913=CARTESIAN_POINT('Ctrl Pts',(1.8328588490844,-0.680780345575904,
3.93454507903843));
#279914=CARTESIAN_POINT('Ctrl Pts',(1.85449715161248,-0.615594277638437,
3.93844988982377));
#279915=CARTESIAN_POINT('Ctrl Pts',(1.87612928624121,-0.550426790692054,
3.94235358756062));
#279916=CARTESIAN_POINT('Ctrl Pts',(1.89432884588759,-0.484097964155095,
3.94625728529747));
#279917=CARTESIAN_POINT('Ctrl Pts',(1.90898531342313,-0.417002485765723,
3.95016098303431));
#279918=CARTESIAN_POINT('Ctrl Pts',(1.92364263249479,-0.349903109150335,
3.95406490757476));
#279919=CARTESIAN_POINT('Ctrl Pts',(1.93475634826849,-0.282037473443222,
3.95796883211521));
#279920=CARTESIAN_POINT('Ctrl Pts',(1.94226693980362,-0.213810978543884,
3.96187275665566));
#279921=CARTESIAN_POINT('Ctrl Pts',(1.94978553878959,-0.145511743661093,
3.96578084338277));
#279922=CARTESIAN_POINT('Ctrl Pts',(1.95369329309856,-0.07685137174546,
3.96968893010987));
#279923=CARTESIAN_POINT('Ctrl Pts',(1.95398262631379,-0.00823990678708126,
3.97359701683697));
#279924=CARTESIAN_POINT('Ctrl Pts',(1.95427213249751,0.0604125753129308,
3.97750743988712));
#279925=CARTESIAN_POINT('Ctrl Pts',(1.95093893639689,0.129015600790377,
3.98141786293727));
#279926=CARTESIAN_POINT('Ctrl Pts',(1.94402751373659,0.197162435152151,
3.98532828598742));
#279927=CARTESIAN_POINT('Ctrl Pts',(1.9371041241785,0.265427263484444,3.98924547980464));
#279928=CARTESIAN_POINT('Ctrl Pts',(1.92659021785465,0.333233838271852,
3.99316267362186));
#279929=CARTESIAN_POINT('Ctrl Pts',(1.9125815583624,0.400184685629107,3.99707986743908));
#279930=CARTESIAN_POINT('Ctrl Pts',(1.90586874146888,0.432266897308478,
3.99895694960001));
#279931=CARTESIAN_POINT('Ctrl Pts',(1.89835418863101,0.464152826721439,
4.00083403176094));
#279932=CARTESIAN_POINT('Ctrl Pts',(1.89005243657592,0.495800148238614,
4.00271111392186));
#279933=CARTESIAN_POINT('Ctrl Pts',(1.87272530359401,0.561853355418326,
4.00662889561475));
#279934=CARTESIAN_POINT('Ctrl Pts',(1.85189695753908,0.627128366384856,
4.01054667730764));
#279935=CARTESIAN_POINT('Ctrl Pts',(1.82765456893729,0.691227008039081,
4.01446445900053));
#279936=CARTESIAN_POINT('Ctrl Pts',(1.80344873525345,0.755228995826995,
4.01837633309947));
#279937=CARTESIAN_POINT('Ctrl Pts',(1.77583924855178,0.818057678262382,
4.0222882071984));
#279938=CARTESIAN_POINT('Ctrl Pts',(1.74496352607143,0.879328319048321,
4.02620008129734));
#279939=CARTESIAN_POINT('Ctrl Pts',(1.71412417974974,0.940526773975238,
4.03010734663115));
#279940=CARTESIAN_POINT('Ctrl Pts',(1.68002646034958,1.00017039550476,4.03401461196496));
#279941=CARTESIAN_POINT('Ctrl Pts',(1.64285582086269,1.05789448994575,4.03792187729878));
#279942=CARTESIAN_POINT('Ctrl Pts',(1.60570853201348,1.11558232204545,4.0418266880841));
#279943=CARTESIAN_POINT('Ctrl Pts',(1.56549241812117,1.17135260634642,4.04573149886942));
#279944=CARTESIAN_POINT('Ctrl Pts',(1.52243802768505,1.22486670779251,4.04963630965474));
#279945=CARTESIAN_POINT('Ctrl Pts',(1.47939590970637,1.27836555528828,4.05354000739157));
#279946=CARTESIAN_POINT('Ctrl Pts',(1.43351742949258,1.32960911346225,4.0574437051284));
#279947=CARTESIAN_POINT('Ctrl Pts',(1.38507438176285,1.37829059235862,4.06134740286523));
#279948=CARTESIAN_POINT('Ctrl Pts',(1.3366285195074,1.42697489963347,4.06525132740567));
#279949=CARTESIAN_POINT('Ctrl Pts',(1.28561814275682,1.47309648516515,4.0691552519461));
#279950=CARTESIAN_POINT('Ctrl Pts',(1.23235168747768,1.51638561005139,4.07305917648653));
#279951=CARTESIAN_POINT('Ctrl Pts',(1.1790284419284,1.55972088783222,4.07696726321362));
#279952=CARTESIAN_POINT('Ctrl Pts',(1.12344470004525,1.60021736735284,4.0808753499407));
#279953=CARTESIAN_POINT('Ctrl Pts',(1.06594095345878,1.63764644650162,4.08478343666779));
#279954=CARTESIAN_POINT('Ctrl Pts',(1.00840283012026,1.67509790141285,4.08869385971792));
#279955=CARTESIAN_POINT('Ctrl Pts',(0.948942843700564,1.7094780601652,4.09260428276805));
#279956=CARTESIAN_POINT('Ctrl Pts',(0.887926915685403,1.74060385855065,
4.09651470581818));
#279957=CARTESIAN_POINT('Ctrl Pts',(0.826805340626195,1.77178355021774,
4.10043189963539));
#279958=CARTESIAN_POINT('Ctrl Pts',(0.764122896196409,1.7996974351293,4.10434909345259));
#279959=CARTESIAN_POINT('Ctrl Pts',(0.700265518251073,1.8242105700682,4.10826628726979));
#279960=CARTESIAN_POINT('Ctrl Pts',(0.669665667800006,1.83595703206448,
4.11014336943087));
#279961=CARTESIAN_POINT('Ctrl Pts',(0.638796247998107,1.84692334047467,
4.11202045159194));
#279962=CARTESIAN_POINT('Ctrl Pts',(0.607700707576638,1.85709877228188,
4.11389753375302));
#279963=CARTESIAN_POINT('Ctrl Pts',(0.542799159034894,1.87833658556371,
4.11781531544591));
#279964=CARTESIAN_POINT('Ctrl Pts',(0.476654019198033,1.89621024025539,
4.12173309713881));
#279965=CARTESIAN_POINT('Ctrl Pts',(0.409647154276951,1.91057719262866,
4.1256508788317));
#279966=CARTESIAN_POINT('Ctrl Pts',(0.342741328510495,1.924922481181,4.12956275293064));
#279967=CARTESIAN_POINT('Ctrl Pts',(0.274976833630437,1.93577145929668,
4.13347462702958));
#279968=CARTESIAN_POINT('Ctrl Pts',(0.206751476288704,1.9430310926623,4.13738650112851));
#279969=CARTESIAN_POINT('Ctrl Pts',(0.138606498488652,1.95028217310822,
4.14129376646233));
#279970=CARTESIAN_POINT('Ctrl Pts',(0.0700022234489896,1.9539522553612,
4.14520103179615));
#279971=CARTESIAN_POINT('Ctrl Pts',(0.00134564850247342,1.95399953665043,
4.14910829712997));
#279972=CARTESIAN_POINT('Ctrl Pts',(-0.0672677963061884,1.95404678823751,
4.1530131079153));
#279973=CARTESIAN_POINT('Ctrl Pts',(-0.135932984977147,1.95047575303684,
4.15691791870062));
#279974=CARTESIAN_POINT('Ctrl Pts',(-0.204240378871569,1.94329664941779,
4.16082272948595));
#279975=CARTESIAN_POINT('Ctrl Pts',(-0.272528302055187,1.93611959216945,
4.16472642722279));
#279976=CARTESIAN_POINT('Ctrl Pts',(-0.340458143866954,1.92533655954889,
4.16863012495963));
#279977=CARTESIAN_POINT('Ctrl Pts',(-0.407624773494297,1.91100969229194,
4.17253382269646));
#279978=CARTESIAN_POINT('Ctrl Pts',(-0.474795305481489,1.89668199264854,
4.1764377472369));
#279979=CARTESIAN_POINT('Ctrl Pts',(-0.541202056624897,1.87881015472464,
4.18034167177734));
#279980=CARTESIAN_POINT('Ctrl Pts',(-0.606451174777268,1.85750719315196,
4.18424559631777));
#279981=CARTESIAN_POINT('Ctrl Pts',(-0.671769858569542,1.83618151933128,
4.18815368304486));
#279982=CARTESIAN_POINT('Ctrl Pts',(-0.735927977641656,1.81141757432175,
4.19206176977195));
#279983=CARTESIAN_POINT('Ctrl Pts',(-0.798548877421209,1.78337760734213,
4.19596985649904));
#279984=CARTESIAN_POINT('Ctrl Pts',(-0.861207213077057,1.75532087757662,
4.19988027954918));
#279985=CARTESIAN_POINT('Ctrl Pts',(-0.9223260626507,1.72398445264218,4.20379070259932));
#279986=CARTESIAN_POINT('Ctrl Pts',(-0.981553258851392,1.68957663337246,
4.20770112564945));
#279987=CARTESIAN_POINT('Ctrl Pts',(-1.04088300496669,1.6551092381114,4.21161831946666));
#279988=CARTESIAN_POINT('Ctrl Pts',(-1.09831414899737,1.6175601035556,4.21553551328387));
#279989=CARTESIAN_POINT('Ctrl Pts',(-1.15352411681735,1.57718043099728,
4.21945270710108));
#279990=CARTESIAN_POINT('Ctrl Pts',(-1.17998021027151,1.55783087451258,
4.22132978926211));
#279991=CARTESIAN_POINT('Ctrl Pts',(-1.20592676926254,1.5378319476531,4.22320687142315));
#279992=CARTESIAN_POINT('Ctrl Pts',(-1.23133123397787,1.51721435276316,
4.22508395358418));
#279993=CARTESIAN_POINT('Ctrl Pts',(-1.28366054183447,1.4747452638708,4.22895045545216));
#279994=CARTESIAN_POINT('Ctrl Pts',(-1.33390722678967,1.42947038638983,
4.23281695732014));
#279995=CARTESIAN_POINT('Ctrl Pts',(-1.38174895723329,1.38162434083391,
4.23668345918812));
#279996=CARTESIAN_POINT('Ctrl Pts',(-1.42950834973302,1.33386064064839,
4.24054330661841));
#279997=CARTESIAN_POINT('Ctrl Pts',(-1.47487064950818,1.28353491123766,
4.24440315404871));
#279998=CARTESIAN_POINT('Ctrl Pts',(-1.51754621895637,1.23092220441879,
4.24826300147901));
#279999=CARTESIAN_POINT('Ctrl Pts',(-1.56018088697644,1.17835992305117,
4.2521191495264));
#280000=CARTESIAN_POINT('Ctrl Pts',(-1.60013361002202,1.12351539844574,
4.25597529757378));
#280001=CARTESIAN_POINT('Ctrl Pts',(-1.63715237493145,1.06669963028789,
4.25983144562117));
#280002=CARTESIAN_POINT('Ctrl Pts',(-1.67414915694421,1.00991760110441,
4.26368530376763));
#280003=CARTESIAN_POINT('Ctrl Pts',(-1.70821515935737,0.951167072327578,
4.2675391619141));
#280004=CARTESIAN_POINT('Ctrl Pts',(-1.73914059576239,0.890789530793455,
4.27139302006056));
#280005=CARTESIAN_POINT('Ctrl Pts',(-1.77005894046059,0.830425834814093,
4.27524599445451));
#280006=CARTESIAN_POINT('Ctrl Pts',(-1.79783791881047,0.768436317333705,
4.27909896884846));
#280007=CARTESIAN_POINT('Ctrl Pts',(-1.82231376045984,0.705186896105353,
4.28295194324241));
#280008=CARTESIAN_POINT('Ctrl Pts',(-1.84680713976431,0.641892154820181,
4.286807678405));
#280009=CARTESIAN_POINT('Ctrl Pts',(-1.86799247153181,0.577336179322571,
4.29066341356758));
#280010=CARTESIAN_POINT('Ctrl Pts',(-1.8857547148499,0.511903462990225,
4.29451914873017));
#280011=CARTESIAN_POINT('Ctrl Pts',(-1.90352379915543,0.44644554576498,
4.29837636889864));
#280012=CARTESIAN_POINT('Ctrl Pts',(-1.91786706209594,0.380110710336096,
4.30223358906712));
#280013=CARTESIAN_POINT('Ctrl Pts',(-1.928720466767,0.313294368085472,4.30609080923559));
#280014=CARTESIAN_POINT('Ctrl Pts',(-1.93959038616316,0.246376356952387,
4.30995389861586));
#280015=CARTESIAN_POINT('Ctrl Pts',(-1.94695979284876,0.178975879837656,
4.31381698799612));
#280016=CARTESIAN_POINT('Ctrl Pts',(-1.95081656980679,0.11149309829426,
4.31768007737639));
#280017=CARTESIAN_POINT('Ctrl Pts',(-1.95296313333969,0.0739342558889111,
4.31983015420951));
#280018=CARTESIAN_POINT('Ctrl Pts',(-1.95402252639623,0.0363499266629029,
4.32198023104264));
#280019=CARTESIAN_POINT('Ctrl Pts',(-1.95399963679489,-0.00119138802316145,
4.32413030787576));
#280020=CARTESIAN_POINT('',(-1.95491180920002,0.00168629508682236,5.02413030787576));
#280021=CARTESIAN_POINT('Ctrl Pts',(-1.95628130950281,-0.00119277919923279,
4.32413030787576));
#280022=CARTESIAN_POINT('Ctrl Pts',(-1.95678939935296,-0.0719326340995119,
4.32817699638895));
#280023=CARTESIAN_POINT('Ctrl Pts',(-1.92119163391235,-0.790036186264717,
4.3692858248459));
#280024=CARTESIAN_POINT('Ctrl Pts',(-1.03336074967815,-2.06582911991838,
4.44745679324649));
#280025=CARTESIAN_POINT('Ctrl Pts',(1.17604813820198,-1.98806317010009,
4.55864321307768));
#280026=CARTESIAN_POINT('Ctrl Pts',(2.308145909957,-0.0891451065749571,
4.66982963290883));
#280027=CARTESIAN_POINT('Ctrl Pts',(1.32588189186438,1.89143374203366,4.78101605274001));
#280028=CARTESIAN_POINT('Ctrl Pts',(-0.87094746107776,2.13937722520349,
4.89220247257116));
#280029=CARTESIAN_POINT('Ctrl Pts',(-1.89060957867978,0.891720152086083,
4.97324055761641));
#280030=CARTESIAN_POINT('Ctrl Pts',(-1.95601481281436,0.122766393772507,
5.01721650271795));
#280031=CARTESIAN_POINT('Ctrl Pts',(-1.95491180920002,0.00168629508682236,
5.02413030787576));
#280032=CARTESIAN_POINT('',(-1.95368862328322,0.000190359573322832,5.72413029305739));
#280033=CARTESIAN_POINT('Ctrl Pts',(-1.95491180920002,0.00168629508682236,
5.02413030787576));
#280034=CARTESIAN_POINT('Ctrl Pts',(-1.95010205227512,-0.526295513449078,
5.05427864266167));
#280035=CARTESIAN_POINT('Ctrl Pts',(-1.45672934504036,-1.71125831262365,
5.12148911739128));
#280036=CARTESIAN_POINT('Ctrl Pts',(0.546914192237962,-2.24418565586851,
5.22576173206465));
#280037=CARTESIAN_POINT('Ctrl Pts',(2.18241236833561,-0.756677372605435,
5.33694815189581));
#280038=CARTESIAN_POINT('Ctrl Pts',(1.8187261335199,1.4239802115651,5.44813457172697));
#280039=CARTESIAN_POINT('Ctrl Pts',(-0.210992142997612,2.3002101441543,
5.55932099155813));
#280040=CARTESIAN_POINT('Ctrl Pts',(-1.73051050228896,1.28176270503949,
5.65131951958487));
#280041=CARTESIAN_POINT('Ctrl Pts',(-1.95107685069972,0.314893123742393,
5.70625590766786));
#280042=CARTESIAN_POINT('Ctrl Pts',(-1.95080468628648,0.000192495437545256,
5.72413015580714));
#280043=CARTESIAN_POINT('',(-1.95399919113549,-0.00177793190781093,6.42413030787576));
#280044=CARTESIAN_POINT('Ctrl Pts',(-1.95399999074999,0.000190128972365512,
5.72413030787576));
#280045=CARTESIAN_POINT('Ctrl Pts',(-1.95400695766447,-0.0714104832721157,
5.72819040273808));
#280046=CARTESIAN_POINT('Ctrl Pts',(-1.95007410706244,-0.142947655190763,
5.7322504976004));
#280047=CARTESIAN_POINT('Ctrl Pts',(-1.94224815867481,-0.213981518183981,
5.73631059246272));
#280048=CARTESIAN_POINT('Ctrl Pts',(-1.93440297274652,-0.285189994752401,
5.74038066774353));
#280049=CARTESIAN_POINT('Ctrl Pts',(-1.92264561855474,-0.355892259408381,
5.74445074302434));
#280050=CARTESIAN_POINT('Ctrl Pts',(-1.90707440104829,-0.425656233205034,
5.74852081830515));
#280051=CARTESIAN_POINT('Ctrl Pts',(-1.89148335587747,-0.495509041202204,
5.75259607623058));
#280052=CARTESIAN_POINT('Ctrl Pts',(-1.87206888637711,-0.564420760982678,
5.75667133415601));
#280053=CARTESIAN_POINT('Ctrl Pts',(-1.84897907873107,-0.631974972933889,
5.76074659208144));
#280054=CARTESIAN_POINT('Ctrl Pts',(-1.82582832708131,-0.699707489711552,
5.76483260637773));
#280055=CARTESIAN_POINT('Ctrl Pts',(-1.7989830101632,-0.766074934944469,
5.76891862067403));
#280056=CARTESIAN_POINT('Ctrl Pts',(-1.76863934637469,-0.830680963099129,
5.77300463497032));
#280057=CARTESIAN_POINT('Ctrl Pts',(-1.74713003595734,-0.876477381227694,
5.77590103372036));
#280058=CARTESIAN_POINT('Ctrl Pts',(-1.7238638766991,-0.921389208871823,
5.7787974324704));
#280059=CARTESIAN_POINT('Ctrl Pts',(-1.69892406073975,-0.965283914628009,
5.78169383122045));
#280060=CARTESIAN_POINT('Ctrl Pts',(-1.66518949487991,-1.02465760225439,
5.78561161291334));
#280061=CARTESIAN_POINT('Ctrl Pts',(-1.62827169589097,-1.08237868309912,
5.78952939460623));
#280062=CARTESIAN_POINT('Ctrl Pts',(-1.58835732078115,-1.13808480418681,
5.79344717629913));
#280063=CARTESIAN_POINT('Ctrl Pts',(-1.54850313226142,-1.19370692642781,
5.79735905039807));
#280064=CARTESIAN_POINT('Ctrl Pts',(-1.50566161943795,-1.24731972220939,
5.80127092449702));
#280065=CARTESIAN_POINT('Ctrl Pts',(-1.46006453905744,-1.29858674788672,
5.80518279859596));
#280066=CARTESIAN_POINT('Ctrl Pts',(-1.41452117876825,-1.3497933734402,
5.80909006392978));
#280067=CARTESIAN_POINT('Ctrl Pts',(-1.36622902381806,-1.39865935166361,
5.8129973292636));
#280068=CARTESIAN_POINT('Ctrl Pts',(-1.31546109495625,-1.44487996306147,
5.81690459459742));
#280069=CARTESIAN_POINT('Ctrl Pts',(-1.26472505856466,-1.49107153861907,
5.82080940538275));
#280070=CARTESIAN_POINT('Ctrl Pts',(-1.21151669639395,-1.53462071338429,
5.82471421616808));
#280071=CARTESIAN_POINT('Ctrl Pts',(-1.15614590441891,-1.57525954931096,
5.8286190269534));
#280072=CARTESIAN_POINT('Ctrl Pts',(-1.10079089563535,-1.61588680132298,
5.83252272469024));
#280073=CARTESIAN_POINT('Ctrl Pts',(-1.0432750771052,-1.6536050703696,5.83642642242708));
#280074=CARTESIAN_POINT('Ctrl Pts',(-0.983940011845606,-1.68818780148693,
5.84033012016392));
#280075=CARTESIAN_POINT('Ctrl Pts',(-0.924601499237589,-1.72277254184994,
5.84423404470436));
#280076=CARTESIAN_POINT('Ctrl Pts',(-0.86344395639434,-1.75422113707409,
5.84813796924479));
#280077=CARTESIAN_POINT('Ctrl Pts',(-0.800834824256486,-1.78235226155159,
5.85204189378522));
#280078=CARTESIAN_POINT('Ctrl Pts',(-0.738158941111589,-1.81051337815363,
5.85594998051232));
#280079=CARTESIAN_POINT('Ctrl Pts',(-0.674028829703269,-1.83534976327845,
5.85985806723941));
#280080=CARTESIAN_POINT('Ctrl Pts',(-0.608832326659619,-1.85672808941273,
5.86376615396651));
#280081=CARTESIAN_POINT('Ctrl Pts',(-0.543596847998696,-1.87811919588672,
5.86767657701665));
#280082=CARTESIAN_POINT('Ctrl Pts',(-0.477294183944824,-1.89604800065007,
5.87158700006679));
#280083=CARTESIAN_POINT('Ctrl Pts',(-0.410325031879865,-1.91043172299164,
5.87549742311693));
#280084=CARTESIAN_POINT('Ctrl Pts',(-0.343239924962017,-1.92484035026863,
5.87941461693414));
#280085=CARTESIAN_POINT('Ctrl Pts',(-0.275486512352373,-1.9356915663438,
5.88333181075135));
#280086=CARTESIAN_POINT('Ctrl Pts',(-0.207472454490163,-1.94295424048736,
5.88724900456856));
#280087=CARTESIAN_POINT('Ctrl Pts',(-0.174880762409147,-1.94643444512169,
5.88912608672958));
#280088=CARTESIAN_POINT('Ctrl Pts',(-0.142229245578587,-1.94909140723278,
5.89100316889061));
#280089=CARTESIAN_POINT('Ctrl Pts',(-0.10956264897586,-1.95092594066238,
5.89288025105163));
#280090=CARTESIAN_POINT('Ctrl Pts',(-0.0413820456987845,-1.95475491609815,
5.89679803274453));
#280091=CARTESIAN_POINT('Ctrl Pts',(0.0271349625788011,-1.95501304933571,
5.90071581443743));
#280092=CARTESIAN_POINT('Ctrl Pts',(0.0955826930932434,-1.95166081806779,
5.90463359613032));
#280093=CARTESIAN_POINT('Ctrl Pts',(0.163927211782491,-1.94831364160454,
5.90854547022926));
#280094=CARTESIAN_POINT('Ctrl Pts',(0.232202172605333,-1.94136692891848,
5.9124573443282));
#280095=CARTESIAN_POINT('Ctrl Pts',(0.299999223724627,-1.93083310147838,
5.91636921842713));
#280096=CARTESIAN_POINT('Ctrl Pts',(0.36771639991021,-1.9203116844419,5.92027648376095));
#280097=CARTESIAN_POINT('Ctrl Pts',(0.434956300770375,-1.90621162097472,
5.92418374909477));
#280098=CARTESIAN_POINT('Ctrl Pts',(0.501314871010041,-1.88859720430382,
5.92809101442859));
#280099=CARTESIAN_POINT('Ctrl Pts',(0.567631754720954,-1.87099385302935,
5.93199582521391));
#280100=CARTESIAN_POINT('Ctrl Pts',(0.633067931630309,-1.84988065386142,
5.93590063599924));
#280101=CARTESIAN_POINT('Ctrl Pts',(0.697230271724011,-1.8253728244366,
5.93980544678456));
#280102=CARTESIAN_POINT('Ctrl Pts',(0.761374322635581,-1.80087198085669,
5.94370914452139));
#280103=CARTESIAN_POINT('Ctrl Pts',(0.82424479816093,-1.77297860335807,
5.94761284225823));
#280104=CARTESIAN_POINT('Ctrl Pts',(0.885466183466893,-1.74185695105441,
5.95151653999506));
#280105=CARTESIAN_POINT('Ctrl Pts',(0.946691125716006,-1.71073349059258,
5.95542046453551));
#280106=CARTESIAN_POINT('Ctrl Pts',(1.0062663501162,-1.67638160817138,5.95932438907595));
#280107=CARTESIAN_POINT('Ctrl Pts',(1.06384032697169,-1.63901182384654,
5.96322831361639));
#280108=CARTESIAN_POINT('Ctrl Pts',(1.1214756865807,-1.60160219755862,5.96713640034348));
#280109=CARTESIAN_POINT('Ctrl Pts',(1.17710512704552,-1.56116851643907,
5.97104448707057));
#280110=CARTESIAN_POINT('Ctrl Pts',(1.23040640188764,-1.51796445485193,
5.97495257379766));
#280111=CARTESIAN_POINT('Ctrl Pts',(1.28373954117012,-1.47473456511625,
5.97886299684779));
#280112=CARTESIAN_POINT('Ctrl Pts',(1.33474137947926,-1.4287313283828,5.98277341989792));
#280113=CARTESIAN_POINT('Ctrl Pts',(1.38312517923919,-1.38024662236666,
5.98668384294805));
#280114=CARTESIAN_POINT('Ctrl Pts',(1.43159275393453,-1.33167796669928,
5.99060103676526));
#280115=CARTESIAN_POINT('Ctrl Pts',(1.47743291421019,-1.28061963225268,
5.99451823058246));
#280116=CARTESIAN_POINT('Ctrl Pts',(1.52039855491997,-1.22739734161243,
5.99843542439967));
#280117=CARTESIAN_POINT('Ctrl Pts',(1.54098728284033,-1.20189372422914,
6.00031250656071));
#280118=CARTESIAN_POINT('Ctrl Pts',(1.56091658765482,-1.17589365098658,
6.00218958872174));
#280119=CARTESIAN_POINT('Ctrl Pts',(1.5801629025028,-1.14943516631166,6.00406667088278));
#280120=CARTESIAN_POINT('Ctrl Pts',(1.6203331526561,-1.09421192194183,6.00798445257567));
#280121=CARTESIAN_POINT('Ctrl Pts',(1.6576848181063,-1.03677064632778,6.01190223426856));
#280122=CARTESIAN_POINT('Ctrl Pts',(1.6919648133459,-0.977430851978471,
6.01582001596145));
#280123=CARTESIAN_POINT('Ctrl Pts',(1.72619311803498,-0.918180535664875,
6.0197318900604));
#280124=CARTESIAN_POINT('Ctrl Pts',(1.75735870071082,-0.857037804707003,
6.02364376415934));
#280125=CARTESIAN_POINT('Ctrl Pts',(1.78525068244455,-0.794352567082953,
6.02755563825828));
#280126=CARTESIAN_POINT('Ctrl Pts',(1.81310980330664,-0.731741181921824,
6.0314629035921));
#280127=CARTESIAN_POINT('Ctrl Pts',(1.83770278376103,-0.667591346615471,
6.03537016892591));
#280128=CARTESIAN_POINT('Ctrl Pts',(1.85886466614673,-0.602277471728109,
6.03927743425973));
#280129=CARTESIAN_POINT('Ctrl Pts',(1.880013254614,-0.537004627090752,6.04318224504505));
#280130=CARTESIAN_POINT('Ctrl Pts',(1.89773486933775,-0.470569660400064,
6.04708705583038));
#280131=CARTESIAN_POINT('Ctrl Pts',(1.91191327041299,-0.403365400621706,
6.0509918666157));
#280132=CARTESIAN_POINT('Ctrl Pts',(1.92608762999975,-0.336180297110703,
6.05489556435254));
#280133=CARTESIAN_POINT('Ctrl Pts',(1.93672067937389,-0.268226816978515,
6.05879926208938));
#280134=CARTESIAN_POINT('Ctrl Pts',(1.94374693976471,-0.19990956494203,
6.06270295982621));
#280135=CARTESIAN_POINT('Ctrl Pts',(1.95077360837903,-0.131588343694882,
6.06660688436665));
#280136=CARTESIAN_POINT('Ctrl Pts',(1.95419302418105,-0.0629037982441252,
6.07051080890709));
#280137=CARTESIAN_POINT('Ctrl Pts',(1.9539915851719,0.00573455119522264,
6.07441473344753));
#280138=CARTESIAN_POINT('Ctrl Pts',(1.95378993139764,0.0744460797185567,
6.07832282017462));
#280139=CARTESIAN_POINT('Ctrl Pts',(1.94995972003222,0.143110821006934,
6.08223090690171));
#280140=CARTESIAN_POINT('Ctrl Pts',(1.94253948650132,0.211320475541774,
6.0861389936288));
#280141=CARTESIAN_POINT('Ctrl Pts',(1.93511481702416,0.279570907009037,
6.09004941667894));
#280142=CARTESIAN_POINT('Ctrl Pts',(1.92409593303982,0.347365224592687,
6.09395983972909));
#280143=CARTESIAN_POINT('Ctrl Pts',(1.9095727208377,0.414304264801236,6.09787026277923));
#280144=CARTESIAN_POINT('Ctrl Pts',(1.89502436217815,0.481359207724846,
6.10178745659643));
#280145=CARTESIAN_POINT('Ctrl Pts',(1.8769596945833,0.547555443231403,6.10570465041364));
#280146=CARTESIAN_POINT('Ctrl Pts',(1.8555185272343,0.612508771439441,6.10962184423084));
#280147=CARTESIAN_POINT('Ctrl Pts',(1.84524412299988,0.643633790871349,
6.11149892639188));
#280148=CARTESIAN_POINT('Ctrl Pts',(1.83419510797748,0.674473704393274,
6.11337600855291));
#280149=CARTESIAN_POINT('Ctrl Pts',(1.82239068168999,0.704988087338717,
6.11525309071394));
#280150=CARTESIAN_POINT('Ctrl Pts',(1.79775288683777,0.768676663872773,
6.11917087240684));
#280151=CARTESIAN_POINT('Ctrl Pts',(1.76972346344802,0.831198647850554,
6.12308865409974));
#280152=CARTESIAN_POINT('Ctrl Pts',(1.7384337605741,0.892168179266775,6.12700643579263));
#280153=CARTESIAN_POINT('Ctrl Pts',(1.70719123921109,0.953045775178734,
6.13091830989157));
#280154=CARTESIAN_POINT('Ctrl Pts',(1.67269841792492,1.01237513024198,6.13483018399051));
#280155=CARTESIAN_POINT('Ctrl Pts',(1.63513506494257,1.0697893808574,6.13874205808944));
#280156=CARTESIAN_POINT('Ctrl Pts',(1.59761596713474,1.1271359890107,6.14264932342326));
#280157=CARTESIAN_POINT('Ctrl Pts',(1.55703379014821,1.18257156394681,6.14655658875708));
#280158=CARTESIAN_POINT('Ctrl Pts',(1.51361378233008,1.23575455408444,6.1504638540909));
#280159=CARTESIAN_POINT('Ctrl Pts',(1.47022105100985,1.28890413460766,6.15436866487623));
#280160=CARTESIAN_POINT('Ctrl Pts',(1.4239943356286,1.33980355712585,6.15827347566155));
#280161=CARTESIAN_POINT('Ctrl Pts',(1.37520076718637,1.38814222971928,6.16217828644688));
#280162=CARTESIAN_POINT('Ctrl Pts',(1.32642110712801,1.43646712359483,6.16608198418372));
#280163=CARTESIAN_POINT('Ctrl Pts',(1.27507639582117,1.48223237047387,6.16998568192057));
#280164=CARTESIAN_POINT('Ctrl Pts',(1.2214711719523,1.52516365551028,6.17388937965741));
#280165=CARTESIAN_POINT('Ctrl Pts',(1.16786283363695,1.56809743484071,6.17779330419785));
#280166=CARTESIAN_POINT('Ctrl Pts',(1.11199410761861,1.60819661988606,6.1816972287383));
#280167=CARTESIAN_POINT('Ctrl Pts',(1.05420177961638,1.64522782855557,6.18560115327874));
#280168=CARTESIAN_POINT('Ctrl Pts',(0.996347836064562,1.68229851821421,
6.18950924000583));
#280169=CARTESIAN_POINT('Ctrl Pts',(0.936566612649027,1.71629443770833,
6.19341732673292));
#280170=CARTESIAN_POINT('Ctrl Pts',(0.875222126577904,1.74702668243746,
6.19732541346001));
#280171=CARTESIAN_POINT('Ctrl Pts',(0.813840967693204,1.77777729944346,
6.20123583651014));
#280172=CARTESIAN_POINT('Ctrl Pts',(0.750895137187055,1.80526016178985,
6.20514625956027));
#280173=CARTESIAN_POINT('Ctrl Pts',(0.686768805473429,1.82933447128419,
6.2090566826104));
#280174=CARTESIAN_POINT('Ctrl Pts',(0.622531441155418,1.8534504646424,6.21297387642761));
#280175=CARTESIAN_POINT('Ctrl Pts',(0.557109964922358,1.87414597763536,
6.21689107024481));
#280176=CARTESIAN_POINT('Ctrl Pts',(0.490903029007325,1.89133027684522,
6.22080826406202));
#280177=CARTESIAN_POINT('Ctrl Pts',(0.459177292640448,1.89956483020201,
6.22268534622305));
#280178=CARTESIAN_POINT('Ctrl Pts',(0.427271334890899,1.90699388526211,
6.22456242838408));
#280179=CARTESIAN_POINT('Ctrl Pts',(0.395229534069158,1.91361166786772,
6.22643951054511));
#280180=CARTESIAN_POINT('Ctrl Pts',(0.328352983179174,1.92742407740317,
6.23035729223801));
#280181=CARTESIAN_POINT('Ctrl Pts',(0.260618638799617,1.93775391997469,
6.2342750739309));
#280182=CARTESIAN_POINT('Ctrl Pts',(0.192421963113393,1.94450245258564,
6.2381928556238));
#280183=CARTESIAN_POINT('Ctrl Pts',(0.124328120688549,1.95124080913433,
6.24210472972274));
#280184=CARTESIAN_POINT('Ctrl Pts',(0.0557738161708393,1.95440852512743,
6.24601660382169));
#280185=CARTESIAN_POINT('Ctrl Pts',(-0.0128352105518403,1.95395784431755,
6.24992847792063));
#280186=CARTESIAN_POINT('Ctrl Pts',(-0.0813634057135774,1.95350769447619,
6.25383574325445));
#280187=CARTESIAN_POINT('Ctrl Pts',(-0.149945705409045,1.94944761739019,
6.25774300858827));
#280188=CARTESIAN_POINT('Ctrl Pts',(-0.218172992541176,1.94178179652752,
6.26165027392209));
#280189=CARTESIAN_POINT('Ctrl Pts',(-0.286357419214523,1.93412079134216,
6.26555508470742));
#280190=CARTESIAN_POINT('Ctrl Pts',(-0.354186787917246,1.9228585904466,
6.26945989549274));
#280191=CARTESIAN_POINT('Ctrl Pts',(-0.421255300329508,1.9080513546402,
6.27336470627807));
#280192=CARTESIAN_POINT('Ctrl Pts',(-0.488304695168545,1.89324833956875,
6.27726840401491));
#280193=CARTESIAN_POINT('Ctrl Pts',(-0.55459318406643,1.87490240157934,
6.28117210175175));
#280194=CARTESIAN_POINT('Ctrl Pts',(-0.619725181528424,1.85312079999647,
6.28507579948859));
#280195=CARTESIAN_POINT('Ctrl Pts',(-0.684860963138907,1.83133793290943,
6.28897972402904));
#280196=CARTESIAN_POINT('Ctrl Pts',(-0.748839654142734,1.80611916438945,
6.29288364856949));
#280197=CARTESIAN_POINT('Ctrl Pts',(-0.811282591432585,1.77762103859018,
6.29678757310993));
#280198=CARTESIAN_POINT('Ctrl Pts',(-0.873792102539848,1.74909252938638,
6.30069565983702));
#280199=CARTESIAN_POINT('Ctrl Pts',(-0.934762143815345,1.71727788995467,
6.30460374656412));
#280200=CARTESIAN_POINT('Ctrl Pts',(-0.993836671823604,1.68238065542213,
6.30851183329121));
#280201=CARTESIAN_POINT('Ctrl Pts',(-1.0529465156247,1.64746255870842,6.31242225634134));
#280202=CARTESIAN_POINT('Ctrl Pts',(-1.11015818107475,1.60945847159518,
6.31633267939148));
#280203=CARTESIAN_POINT('Ctrl Pts',(-1.16514513040121,1.56861493844166,
6.32024310244162));
#280204=CARTESIAN_POINT('Ctrl Pts',(-1.22022728779632,1.52770068607284,
6.32416029625883));
#280205=CARTESIAN_POINT('Ctrl Pts',(-1.27307666220068,1.48393748879884,
6.32807749007604));
#280206=CARTESIAN_POINT('Ctrl Pts',(-1.32340094106983,1.43761119541255,
6.33199468389326));
#280207=CARTESIAN_POINT('Ctrl Pts',(-1.34751585867119,1.41541207457285,
6.33387176605426));
#280208=CARTESIAN_POINT('Ctrl Pts',(-1.37105151764471,1.3926249344352,6.33574884821527));
#280209=CARTESIAN_POINT('Ctrl Pts',(-1.39397901335,1.36928394072952,6.33762593037627));
#280210=CARTESIAN_POINT('Ctrl Pts',(-1.44117183502743,1.32123999524655,
6.34148962333414));
#280211=CARTESIAN_POINT('Ctrl Pts',(-1.48598395771404,1.27064520587233,
6.34535331629201));
#280212=CARTESIAN_POINT('Ctrl Pts',(-1.5281218119321,1.21776833917513,6.34921700924988));
#280213=CARTESIAN_POINT('Ctrl Pts',(-1.57020241583544,1.16496331328036,
6.35307545282707));
#280214=CARTESIAN_POINT('Ctrl Pts',(-1.60961563734762,1.10988274487347,
6.35693389640426));
#280215=CARTESIAN_POINT('Ctrl Pts',(-1.64610459419185,1.05283221121909,
6.36079233998145));
#280216=CARTESIAN_POINT('Ctrl Pts',(-1.68255730843301,0.995838342923919,
6.3646469511652));
#280217=CARTESIAN_POINT('Ctrl Pts',(-1.71609124364471,0.936878812047662,
6.36850156234894));
#280218=CARTESIAN_POINT('Ctrl Pts',(-1.74649095490027,0.87629067349342,
6.37235617353269));
#280219=CARTESIAN_POINT('Ctrl Pts',(-1.77687157268618,0.815740589175113,
6.37620836370983));
#280220=CARTESIAN_POINT('Ctrl Pts',(-1.80412164463283,0.753564377846253,
6.38006055388697));
#280221=CARTESIAN_POINT('Ctrl Pts',(-1.82807111724676,0.690124619389999,
6.38391274406411));
#280222=CARTESIAN_POINT('Ctrl Pts',(-1.85202294598191,0.626678619804194,
6.38776531321524));
#280223=CARTESIAN_POINT('Ctrl Pts',(-1.87267333389262,0.561969293509401,
6.39161788236636));
#280224=CARTESIAN_POINT('Ctrl Pts',(-1.88990057293408,0.496378710687146,
6.39547045151749));
#280225=CARTESIAN_POINT('Ctrl Pts',(-1.90712859132636,0.430785160583011,
6.39932319495672));
#280226=CARTESIAN_POINT('Ctrl Pts',(-1.92093303579742,0.36431076788473,
6.40317593839596));
#280227=CARTESIAN_POINT('Ctrl Pts',(-1.93124288827011,0.297349804953888,
6.40702868183519));
#280228=CARTESIAN_POINT('Ctrl Pts',(-1.94156260508316,0.230324774595253,
6.41088511153208));
#280229=CARTESIAN_POINT('Ctrl Pts',(-1.948380995502,0.16281274812497,6.41474154122897));
#280230=CARTESIAN_POINT('Ctrl Pts',(-1.95167885002433,0.0952137929487952,
6.41859797092586));
#280231=CARTESIAN_POINT('Ctrl Pts',(-1.95325585638024,0.0628885398960482,
6.42044208324249));
#280232=CARTESIAN_POINT('Ctrl Pts',(-1.954028600145,0.0305434300892876,
6.42228619555913));
#280233=CARTESIAN_POINT('Ctrl Pts',(-1.95399919113549,-0.00177793190781093,
6.42413030787576));
#280234=CARTESIAN_POINT('',(-1.95675615924934,0.000851174274233985,7.12413030787576));
#280235=CARTESIAN_POINT('Ctrl Pts',(-1.95421427783755,-0.00177812761388513,
6.42413030787576));
#280236=CARTESIAN_POINT('Ctrl Pts',(-1.95554703085897,-0.145994290672205,
6.43235765531965));
#280237=CARTESIAN_POINT('Ctrl Pts',(-1.87512506264653,-0.938395085048426,
6.47764714270725));
#280238=CARTESIAN_POINT('Ctrl Pts',(-0.794746594271796,-2.16883891577301,
6.55999877003861));
#280239=CARTESIAN_POINT('Ctrl Pts',(1.39194049181098,-1.84336270411812,
6.67118518986975));
#280240=CARTESIAN_POINT('Ctrl Pts',(2.30354969961481,0.17071371673631,6.78237160970092));
#280241=CARTESIAN_POINT('Ctrl Pts',(1.10500744564588,2.02840896683697,6.89355802953208));
#280242=CARTESIAN_POINT('Ctrl Pts',(-1.10576956804582,2.02799360306211,
7.00474444936326));
#280243=CARTESIAN_POINT('Ctrl Pts',(-1.9337773035453,0.743553653930807,
7.08160187547781));
#280244=CARTESIAN_POINT('Ctrl Pts',(-1.95701686505733,0.0485985200318871,
7.12139716164864));
#280245=CARTESIAN_POINT('Ctrl Pts',(-1.95675615924934,0.000851174274233985,
7.12413030787576));
#280246=CARTESIAN_POINT('',(-1.95399958925359,0.00126696360743394,7.82413030787576));
#280247=CARTESIAN_POINT('Ctrl Pts',(-1.95675615924934,0.000851174274233985,
7.12413030787576));
#280248=CARTESIAN_POINT('Ctrl Pts',(-1.95348162971424,-0.598867317271105,
7.15845930159236));
#280249=CARTESIAN_POINT('Ctrl Pts',(-1.33749233620385,-1.85186615856446,
7.2298504352527));
#280250=CARTESIAN_POINT('Ctrl Pts',(0.795561506911455,-2.16854012653626,
7.33830370885674));
#280251=CARTESIAN_POINT('Ctrl Pts',(2.25360188555758,-0.506717804195069,
7.44949012868789));
#280252=CARTESIAN_POINT('Ctrl Pts',(1.64724516703786,1.6192800101739,7.56067654851907));
#280253=CARTESIAN_POINT('Ctrl Pts',(-0.468059588377089,2.26194708457213,
7.67186296835022));
#280254=CARTESIAN_POINT('Ctrl Pts',(-1.80012985616923,1.13299355714076,
7.75968060691936));
#280255=CARTESIAN_POINT('Ctrl Pts',(-1.95308798861268,0.242106011541422,
7.8104361055448));
#280256=CARTESIAN_POINT('Ctrl Pts',(-1.95166131896414,0.00128028472646311,
7.8241294642265));
#280257=CARTESIAN_POINT('',(-1.95399942135932,-0.00150377106857099,8.52413030787576));
#280258=CARTESIAN_POINT('Ctrl Pts',(-1.9539995892536,0.00126696360743394,
7.82413030787576));
#280259=CARTESIAN_POINT('Ctrl Pts',(-1.95404443793575,-0.067901800190388,
7.8280585559228));
#280260=CARTESIAN_POINT('Ctrl Pts',(-1.95041224119463,-0.137089327859001,
7.83198680396985));
#280261=CARTESIAN_POINT('Ctrl Pts',(-1.94312353915447,-0.205880818882736,
7.83591505201689));
#280262=CARTESIAN_POINT('Ctrl Pts',(-1.93583412258889,-0.274679053668013,
7.8398436851576));
#280263=CARTESIAN_POINT('Ctrl Pts',(-1.92488754124365,-0.343080694373507,
7.84377231829832));
#280264=CARTESIAN_POINT('Ctrl Pts',(-1.91035611453868,-0.410676899331691,
7.84770095143903));
#280265=CARTESIAN_POINT('Ctrl Pts',(-1.8958068870018,-0.478355908869621,
7.85163439711052));
#280266=CARTESIAN_POINT('Ctrl Pts',(-1.87766414568324,-0.54522703855923,
7.855567842782));
#280267=CARTESIAN_POINT('Ctrl Pts',(-1.85605105652718,-0.610893178521688,
7.85950128845349));
#280268=CARTESIAN_POINT('Ctrl Pts',(-1.83442503942436,-0.676598596921187,
7.8634370869296));
#280269=CARTESIAN_POINT('Ctrl Pts',(-1.80932471570444,-0.741097139190985,
7.86737288540572));
#280270=CARTESIAN_POINT('Ctrl Pts',(-1.78092171510111,-0.804011097362054,
7.87130868388183));
#280271=CARTESIAN_POINT('Ctrl Pts',(-1.75246007613188,-0.867054942221865,
7.87525260786533));
#280272=CARTESIAN_POINT('Ctrl Pts',(-1.72068235784896,-0.928507235402445,
7.87919653184883));
#280273=CARTESIAN_POINT('Ctrl Pts',(-1.68580637056182,-0.988014615769008,
7.88314045583233));
#280274=CARTESIAN_POINT('Ctrl Pts',(-1.65310109503736,-1.04381820505823,
7.88683890655907));
#280275=CARTESIAN_POINT('Ctrl Pts',(-1.61767184319614,-1.09791144835028,
7.89053735728581));
#280276=CARTESIAN_POINT('Ctrl Pts',(-1.57973087609372,-1.15002885142772,
7.89423580801255));
#280277=CARTESIAN_POINT('Ctrl Pts',(-1.53953987794175,-1.20523699741716,
7.89815358970541));
#280278=CARTESIAN_POINT('Ctrl Pts',(-1.49637144867376,-1.25844539685319,
7.90207137139828));
#280279=CARTESIAN_POINT('Ctrl Pts',(-1.4504517700784,-1.30931495931133,
7.90598915309115));
#280280=CARTESIAN_POINT('Ctrl Pts',(-1.40460133342585,-1.3601078159335,
7.90990102719005));
#280281=CARTESIAN_POINT('Ctrl Pts',(-1.35600820786029,-1.40856847255519,
7.91381290128896));
#280282=CARTESIAN_POINT('Ctrl Pts',(-1.3049404788002,-1.45438865052939,
7.91772477538787));
#280283=CARTESIAN_POINT('Ctrl Pts',(-1.25393291506304,-1.50015484557043,
7.92163204072166));
#280284=CARTESIAN_POINT('Ctrl Pts',(-1.2004569023679,-1.54328641317032,
7.92553930605545));
#280285=CARTESIAN_POINT('Ctrl Pts',(-1.14481796507741,-1.58351123356799,
7.92944657138924));
#280286=CARTESIAN_POINT('Ctrl Pts',(-1.0892139802301,-1.62371078468811,
7.93335138217454));
#280287=CARTESIAN_POINT('Ctrl Pts',(-1.03145016389223,-1.66100692322339,
7.93725619295983));
#280288=CARTESIAN_POINT('Ctrl Pts',(-0.971864550243031,-1.69516822055539,
7.94116100374513));
#280289=CARTESIAN_POINT('Ctrl Pts',(-0.91229592120101,-1.72931978036551,
7.94506470148194));
#280290=CARTESIAN_POINT('Ctrl Pts',(-0.85090695233309,-1.76033802825822,
7.94896839921874));
#280291=CARTESIAN_POINT('Ctrl Pts',(-0.788062495477797,-1.7880362141806,
7.95287209695555));
#280292=CARTESIAN_POINT('Ctrl Pts',(-0.725214387379388,-1.81573600935885,
7.95677602149597));
#280293=CARTESIAN_POINT('Ctrl Pts',(-0.660911074630634,-1.84011516352156,
7.96067994603638));
#280294=CARTESIAN_POINT('Ctrl Pts',(-0.595538042169783,-1.86103477676495,
7.9645838705768));
#280295=CARTESIAN_POINT('Ctrl Pts',(-0.530095311957344,-1.88197669354778,
7.96849195730386));
#280296=CARTESIAN_POINT('Ctrl Pts',(-0.463581055431145,-1.8994515581827,
7.97240004403092));
#280297=CARTESIAN_POINT('Ctrl Pts',(-0.396395632058983,-1.91337045625894,
7.97630813075798));
#280298=CARTESIAN_POINT('Ctrl Pts',(-0.329170044057961,-1.92729767529749,
7.98021855380809));
#280299=CARTESIAN_POINT('Ctrl Pts',(-0.261272977100312,-1.93766462274403,
7.9841289768582));
#280300=CARTESIAN_POINT('Ctrl Pts',(-0.193111891627182,-1.94443405578903,
7.98803939990831));
#280301=CARTESIAN_POINT('Ctrl Pts',(-0.124832787508198,-1.95121520988154,
7.99195659372549));
#280302=CARTESIAN_POINT('Ctrl Pts',(-0.0562892437003932,-1.95438639463801,
7.99587378754267));
#280303=CARTESIAN_POINT('Ctrl Pts',(0.0121101626753464,-1.95396247250554,
7.99979098135985));
#280304=CARTESIAN_POINT('Ctrl Pts',(0.0448865101176289,-1.95375933303638,
8.00166806352114));
#280305=CARTESIAN_POINT('Ctrl Pts',(0.0776298214714477,-1.95273144156208,
8.00354514568243));
#280306=CARTESIAN_POINT('Ctrl Pts',(0.110295726423287,-1.95088463337348,
8.00542222784371));
#280307=CARTESIAN_POINT('Ctrl Pts',(0.178474886102253,-1.94703003848094,
8.0093400095367));
#280308=CARTESIAN_POINT('Ctrl Pts',(0.246587176902543,-1.93958941362714,
8.01325779122968));
#280309=CARTESIAN_POINT('Ctrl Pts',(0.314225044159618,-1.92856906063093,
8.01717557292266));
#280310=CARTESIAN_POINT('Ctrl Pts',(0.381760920778319,-1.91756532514327,
8.02108744702169));
#280311=CARTESIAN_POINT('Ctrl Pts',(0.448823311960776,-1.90299265271881,
8.02499932112072));
#280312=CARTESIAN_POINT('Ctrl Pts',(0.515007846170036,-1.88490925998662,
8.02891119521974));
#280313=CARTESIAN_POINT('Ctrl Pts',(0.581114405228445,-1.86684717216037,
8.03281846055364));
#280314=CARTESIAN_POINT('Ctrl Pts',(0.646344688998125,-1.84528270747954,
8.03672572588755));
#280315=CARTESIAN_POINT('Ctrl Pts',(0.710304422502188,-1.82032514331199,
8.04063299122145));
#280316=CARTESIAN_POINT('Ctrl Pts',(0.7742239764295,-1.79538325751442,8.04453780200686));
#280317=CARTESIAN_POINT('Ctrl Pts',(0.836874106082847,-1.76705267894244,
8.04844261279227));
#280318=CARTESIAN_POINT('Ctrl Pts',(0.897877113400025,-1.73549205968579,
8.05234742357768));
#280319=CARTESIAN_POINT('Ctrl Pts',(0.958862732088378,-1.70394043663963,
8.0562511213146));
#280320=CARTESIAN_POINT('Ctrl Pts',(1.01820172371542,-1.66916082660839,
8.06015481905152));
#280321=CARTESIAN_POINT('Ctrl Pts',(1.07553940315965,-1.6313586338543,8.06405851678843));
#280322=CARTESIAN_POINT('Ctrl Pts',(1.13288041390487,-1.59355424480481,
8.06796244132895));
#280323=CARTESIAN_POINT('Ctrl Pts',(1.18821947227951,-1.55272719731684,
8.07186636586947));
#280324=CARTESIAN_POINT('Ctrl Pts',(1.24123092337494,-1.50912616929725,
8.07577029040999));
#280325=CARTESIAN_POINT('Ctrl Pts',(1.29429889286668,-1.46547865584612,
8.07967837713716));
#280326=CARTESIAN_POINT('Ctrl Pts',(1.34503392183809,-1.41905157268594,
8.08358646386434));
#280327=CARTESIAN_POINT('Ctrl Pts',(1.39314430114039,-1.37013318921923,
8.08749455059151));
#280328=CARTESIAN_POINT('Ctrl Pts',(1.44128344167438,-1.32118556148171,
8.09140497364173));
#280329=CARTESIAN_POINT('Ctrl Pts',(1.48679448377884,-1.26974403790752,
8.09531539669194));
#280330=CARTESIAN_POINT('Ctrl Pts',(1.52942529415635,-1.21613086039076,
8.09922581974216));
#280331=CARTESIAN_POINT('Ctrl Pts',(1.57212991835997,-1.16242485344553,
8.10314301355945));
#280332=CARTESIAN_POINT('Ctrl Pts',(1.61194407207022,-1.10654008830249,
8.10706020737674));
#280333=CARTESIAN_POINT('Ctrl Pts',(1.6486588056391,-1.04882798522382,8.11097740119403));
#280334=CARTESIAN_POINT('Ctrl Pts',(1.6662521580787,-1.02117289227349,8.11285448335431));
#280335=CARTESIAN_POINT('Ctrl Pts',(1.68313449029611,-0.993098564907489,
8.1147315655146));
#280336=CARTESIAN_POINT('Ctrl Pts',(1.69928665847842,-0.964645454204422,
8.11660864767488));
#280337=CARTESIAN_POINT('Ctrl Pts',(1.73299891153957,-0.905259094579355,
8.12052642936771));
#280338=CARTESIAN_POINT('Ctrl Pts',(1.76366125052136,-0.843985380605829,
8.12444421106054));
#280339=CARTESIAN_POINT('Ctrl Pts',(1.79105808563739,-0.781170233606551,
8.12836199275337));
#280340=CARTESIAN_POINT('Ctrl Pts',(1.81841360926896,-0.718449805101552,
8.13227386685224));
#280341=CARTESIAN_POINT('Ctrl Pts',(1.8425132063164,-0.654193003792113,
8.13618574095111));
#280342=CARTESIAN_POINT('Ctrl Pts',(1.86318664099535,-0.58877121262547,
8.14009761504998));
#280343=CARTESIAN_POINT('Ctrl Pts',(1.88383571931665,-0.523426497985717,
8.14400488038373));
#280344=CARTESIAN_POINT('Ctrl Pts',(1.90106650428336,-0.456919986223647,
8.14791214571749));
#280345=CARTESIAN_POINT('Ctrl Pts',(1.91475714328836,-0.38964224902621,
8.15181941105124));
#280346=CARTESIAN_POINT('Ctrl Pts',(1.92843918181849,-0.32240677577918,
8.1557242218365));
#280347=CARTESIAN_POINT('Ctrl Pts',(1.93858538801781,-0.254401519164342,
8.15962903262176));
#280348=CARTESIAN_POINT('Ctrl Pts',(1.94512438775213,-0.186029879782499,
8.16353384340702));
#280349=CARTESIAN_POINT('Ctrl Pts',(1.95166152357443,-0.117677729424321,
8.16743754114379));
#280350=CARTESIAN_POINT('Ctrl Pts',(1.95459344727363,-0.0489598931344899,
8.17134123888057));
#280351=CARTESIAN_POINT('Ctrl Pts',(1.95390054740418,0.0197142297250717,
8.17524493661734));
#280352=CARTESIAN_POINT('Ctrl Pts',(1.95320760727746,0.0883923425296247,
8.17914886115773));
#280353=CARTESIAN_POINT('Ctrl Pts',(1.94888943298335,0.157026244931154,
8.18305278569811));
#280354=CARTESIAN_POINT('Ctrl Pts',(1.94097851366729,0.225207480963497,
8.1869567102385));
#280355=CARTESIAN_POINT('Ctrl Pts',(1.93305916008916,0.29346140872608,8.19086479696552));
#280356=CARTESIAN_POINT('Ctrl Pts',(1.92153947388549,0.361261217316709,
8.19477288369255));
#280357=CARTESIAN_POINT('Ctrl Pts',(1.90650361446225,0.42820552079856,8.19868097041958));
#280358=CARTESIAN_POINT('Ctrl Pts',(1.89145876633754,0.495189844763646,
8.20259139346965));
#280359=CARTESIAN_POINT('Ctrl Pts',(1.87289369457593,0.561317172028689,
8.20650181651973));
#280360=CARTESIAN_POINT('Ctrl Pts',(1.8509425580627,0.626200963551082,8.2104122395698));
#280361=CARTESIAN_POINT('Ctrl Pts',(1.82895341388883,0.691197099194167,
8.21432943338695));
#280362=CARTESIAN_POINT('Ctrl Pts',(1.8035666854114,0.75494494486457,8.21824662720409));
#280363=CARTESIAN_POINT('Ctrl Pts',(1.77496445739794,0.817078438691188,
8.22216382102124));
#280364=CARTESIAN_POINT('Ctrl Pts',(1.76125854074122,0.846852220215407,
8.22404090318284));
#280365=CARTESIAN_POINT('Ctrl Pts',(1.74681494509785,0.876255681653442,
8.22591798534444));
#280366=CARTESIAN_POINT('Ctrl Pts',(1.73165728971869,0.905250811081732,
8.22779506750604));
#280367=CARTESIAN_POINT('Ctrl Pts',(1.70002074979301,0.965768453610346,
8.23171284919877));
#280368=CARTESIAN_POINT('Ctrl Pts',(1.66514510420117,1.02474587641108,8.2356306308915));
#280369=CARTESIAN_POINT('Ctrl Pts',(1.62720421763237,1.0818144175964,8.23954841258423));
#280370=CARTESIAN_POINT('Ctrl Pts',(1.58932054184508,1.13879690555163,8.24346028668299));
#280371=CARTESIAN_POINT('Ctrl Pts',(1.54838106833165,1.19387581803668,8.24737216078176));
#280372=CARTESIAN_POINT('Ctrl Pts',(1.5046056404242,1.24670680867784,8.25128403488052));
#280373=CARTESIAN_POINT('Ctrl Pts',(1.46088178643246,1.29947555661371,8.25519130021417));
#280374=CARTESIAN_POINT('Ctrl Pts',(1.41432892603191,1.35000126537272,8.25909856554782));
#280375=CARTESIAN_POINT('Ctrl Pts',(1.36520925125971,1.3979698495586,8.26300583088147));
#280376=CARTESIAN_POINT('Ctrl Pts',(1.31612043352268,1.44590829982572,8.26691064166662));
#280377=CARTESIAN_POINT('Ctrl Pts',(1.2644683512111,1.49129246909334,8.27081545245178));
#280378=CARTESIAN_POINT('Ctrl Pts',(1.21055333592218,1.53384374070102,8.27472026323693));
#280379=CARTESIAN_POINT('Ctrl Pts',(1.15665368886223,1.57638288326297,8.2786239609736));
#280380=CARTESIAN_POINT('Ctrl Pts',(1.10049277533017,1.61609042652526,8.28252765871026));
#280381=CARTESIAN_POINT('Ctrl Pts',(1.0424040224913,1.65272800360312,8.28643135644693));
#280382=CARTESIAN_POINT('Ctrl Pts',(0.98431189471428,1.68936770931261,8.2903352809872));
#280383=CARTESIAN_POINT('Ctrl Pts',(0.924292122746999,1.72293683442513,
8.29423920552746));
#280384=CARTESIAN_POINT('Ctrl Pts',(0.862705578322242,1.75324130830062,
8.29814313006773));
#280385=CARTESIAN_POINT('Ctrl Pts',(0.801053373126938,1.78357809142685,
8.30205121679465));
#280386=CARTESIAN_POINT('Ctrl Pts',(0.737831504082082,1.81064305936345,
8.30595930352158));
#280387=CARTESIAN_POINT('Ctrl Pts',(0.673422905481371,1.83428939657106,
8.3098673902485));
#280388=CARTESIAN_POINT('Ctrl Pts',(0.608975802286412,1.85794986997539,
8.31377781329848));
#280389=CARTESIAN_POINT('Ctrl Pts',(0.543341027819345,1.87818750030037,
8.31768823634846));
#280390=CARTESIAN_POINT('Ctrl Pts',(0.476916137788858,1.89490553788746,
8.32159865939843));
#280391=CARTESIAN_POINT('Ctrl Pts',(0.410376235277159,1.91165252219893,
8.32551585321547));
#280392=CARTESIAN_POINT('Ctrl Pts',(0.343043969273922,1.92486765613821,
8.32943304703251));
#280393=CARTESIAN_POINT('Ctrl Pts',(0.275325661415558,1.93450556478034,
8.33335024084955));
#280394=CARTESIAN_POINT('Ctrl Pts',(0.242875689906377,1.93912395928451,
8.3352273230121));
#280395=CARTESIAN_POINT('Ctrl Pts',(0.210337126602138,1.94292170846408,
8.33710440517465));
#280396=CARTESIAN_POINT('Ctrl Pts',(0.177754717559067,1.94589806012173,
8.3389814873372));
#280397=CARTESIAN_POINT('Ctrl Pts',(0.109749827722278,1.95211019951037,
8.34289926903069));
#280398=CARTESIAN_POINT('Ctrl Pts',(0.0412838019476793,1.95476545318489,
8.34681705072418));
#280399=CARTESIAN_POINT('Ctrl Pts',(-0.0272393081980585,1.95381012897592,
8.35073483241766));
#280400=CARTESIAN_POINT('Ctrl Pts',(-0.0956590928540732,1.95285624529323,
8.35464670651719));
#280401=CARTESIAN_POINT('Ctrl Pts',(-0.16413530308866,1.94830259557962,
8.35855858061671));
#280402=CARTESIAN_POINT('Ctrl Pts',(-0.232259402482933,1.94014730625236,
8.36247045471623));
#280403=CARTESIAN_POINT('Ctrl Pts',(-0.300303241632396,1.93200162505971,
8.36637772005063));
#280404=CARTESIAN_POINT('Ctrl Pts',(-0.367995307640907,1.92026278958752,
8.37028498538504));
#280405=CARTESIAN_POINT('Ctrl Pts',(-0.434929543107837,1.90498091657948,
8.37419225071944));
#280406=CARTESIAN_POINT('Ctrl Pts',(-0.501821730412533,1.88970864366131,
8.37809706150536));
#280407=CARTESIAN_POINT('Ctrl Pts',(-0.567956552980499,1.87089785758528,
8.38200187229127));
#280408=CARTESIAN_POINT('Ctrl Pts',(-0.632937090255617,1.84864995057982,
8.38590668307718));
#280409=CARTESIAN_POINT('Ctrl Pts',(-0.697899105125326,1.82640838523864,
8.38981038081461));
#280410=CARTESIAN_POINT('Ctrl Pts',(-0.7617070226247,1.80073180316959,8.39371407855204));
#280411=CARTESIAN_POINT('Ctrl Pts',(-0.823979810726255,1.77177122437281,
8.39761777628947));
#280412=CARTESIAN_POINT('Ctrl Pts',(-0.886256216856737,1.74280896297573,
8.40152170083048));
#280413=CARTESIAN_POINT('Ctrl Pts',(-0.946996871492811,1.71056253582719,
8.4054256253715));
#280414=CARTESIAN_POINT('Ctrl Pts',(-1.00584309447748,1.6752300347391,8.40932954991251));
#280415=CARTESIAN_POINT('Ctrl Pts',(-1.0647520566267,1.63985986374652,8.41323763664018));
#280416=CARTESIAN_POINT('Ctrl Pts',(-1.12176213366443,1.60139730620336,
8.41714572336785));
#280417=CARTESIAN_POINT('Ctrl Pts',(-1.17654240083538,1.56008460637125,
8.42105381009552));
#280418=CARTESIAN_POINT('Ctrl Pts',(-1.23135541661431,1.51874720907997,
8.42496423314622));
#280419=CARTESIAN_POINT('Ctrl Pts',(-1.28393559288869,1.474556595086,8.42887465619693));
#280420=CARTESIAN_POINT('Ctrl Pts',(-1.33398615540298,1.4277944309995,8.43278507924764));
#280421=CARTESIAN_POINT('Ctrl Pts',(-1.38412337879653,1.38095129978591,
8.4367022730654));
#280422=CARTESIAN_POINT('Ctrl Pts',(-1.43172190553461,1.33152808596602,
8.44061946688316));
#280423=CARTESIAN_POINT('Ctrl Pts',(-1.47652338535857,1.27984166696091,
8.44453666070093));
#280424=CARTESIAN_POINT('Ctrl Pts',(-1.49799182992469,1.25507402478496,
8.44641374285674));
#280425=CARTESIAN_POINT('Ctrl Pts',(-1.51881862517038,1.22978715877023,
8.44829082501255));
#280426=CARTESIAN_POINT('Ctrl Pts',(-1.53897888756308,1.20401826549065,
8.45016790716836));
#280427=CARTESIAN_POINT('Ctrl Pts',(-1.58104064327307,1.15025483360024,
8.45408419404734));
#280428=CARTESIAN_POINT('Ctrl Pts',(-1.62036837644652,1.09417386838946,
8.45800048092632));
#280429=CARTESIAN_POINT('Ctrl Pts',(-1.65669693711659,1.0360845807889,8.4619167678053));
#280430=CARTESIAN_POINT('Ctrl Pts',(-1.69297183985178,0.978081092106694,
8.4658272702584));
#280431=CARTESIAN_POINT('Ctrl Pts',(-1.72625609860507,0.918075577768491,
8.46973777271151));
#280432=CARTESIAN_POINT('Ctrl Pts',(-1.756325419742,0.85640937638964,8.47364827516461));
#280433=CARTESIAN_POINT('Ctrl Pts',(-1.78636063875987,0.794813111679201,
8.47755434265161));
#280434=CARTESIAN_POINT('Ctrl Pts',(-1.8131879412576,0.731560336950756,
8.4814604101386));
#280435=CARTESIAN_POINT('Ctrl Pts',(-1.8366278587371,0.667018821706528,
8.4853664776256));
#280436=CARTESIAN_POINT('Ctrl Pts',(-1.86005037352256,0.602525224559474,
8.48926964509822));
#280437=CARTESIAN_POINT('Ctrl Pts',(-1.88009032732257,0.536745246884614,
8.49317281257085));
#280438=CARTESIAN_POINT('Ctrl Pts',(-1.89661621162106,0.470066958864574,
8.49707598004347));
#280439=CARTESIAN_POINT('Ctrl Pts',(-1.91313511727448,0.403416828133862,
8.50097749926419));
#280440=CARTESIAN_POINT('Ctrl Pts',(-1.92614278481498,0.33586961789548,
8.5048790184849));
#280441=CARTESIAN_POINT('Ctrl Pts',(-1.9355579650531,0.267827115728595,
8.50878053770561));
#280442=CARTESIAN_POINT('Ctrl Pts',(-1.94497445087806,0.199775178225063,
8.51268259794328));
#280443=CARTESIAN_POINT('Ctrl Pts',(-1.95079738608773,0.131228298643438,
8.51658465818095));
#280444=CARTESIAN_POINT('Ctrl Pts',(-1.95299713534415,0.0625954418271417,
8.52048671841862));
#280445=CARTESIAN_POINT('Ctrl Pts',(-1.95368181495021,0.0412332264607191,
8.52170124823767));
#280446=CARTESIAN_POINT('Ctrl Pts',(-1.95401586470436,0.0198627037635852,
8.52291577805671));
#280447=CARTESIAN_POINT('Ctrl Pts',(-1.95399942135932,-0.00150377106857099,
8.52413030787576));
#280448=CARTESIAN_POINT('',(-1.95425084356951,-0.000465081590652265,9.22413026128937));
#280449=CARTESIAN_POINT('Ctrl Pts',(-1.9521545497156,-0.00151646469114672,
8.52413111087899));
#280450=CARTESIAN_POINT('Ctrl Pts',(-1.9537147512388,-0.219593375837535,
8.53653884958584));
#280451=CARTESIAN_POINT('Ctrl Pts',(-1.81934971248804,-1.08720016982708,
8.58600872823641));
#280452=CARTESIAN_POINT('Ctrl Pts',(-0.546070872269969,-2.24439100726284,
8.67254074683069));
#280453=CARTESIAN_POINT('Ctrl Pts',(1.59021074792358,-1.67532509350279,
8.78372716666185));
#280454=CARTESIAN_POINT('Ctrl Pts',(2.26979033427429,0.42841128879651,8.89491358649301));
#280455=CARTESIAN_POINT('Ctrl Pts',(0.870143500653463,2.13970434291615,
9.00610000632417));
#280456=CARTESIAN_POINT('Ctrl Pts',(-1.29798992125702,1.89417448969363,
9.11583872315943));
#280457=CARTESIAN_POINT('Ctrl Pts',(-1.9550702218924,0.621448895034945,
9.18851530005095));
#280458=CARTESIAN_POINT('Ctrl Pts',(-1.95707450182562,-0.000456599506395794,
9.22412973699875));
#280459=CARTESIAN_POINT('',(-1.95399918605333,0.00178350859616108,9.92413029181523));
#280460=CARTESIAN_POINT('Ctrl Pts',(-1.95399994447223,-0.000465835275089229,
9.22413030787576));
#280461=CARTESIAN_POINT('Ctrl Pts',(-1.95399392795271,-0.0257028223412335,
9.22557782057934));
#280462=CARTESIAN_POINT('Ctrl Pts',(-1.9534990074032,-0.0509333767812854,
9.22702533328292));
#280463=CARTESIAN_POINT('Ctrl Pts',(-1.95251580652132,-0.0761447653119341,
9.2284728459865));
#280464=CARTESIAN_POINT('Ctrl Pts',(-1.94985471318939,-0.14438093062052,
9.2323906276671));
#280465=CARTESIAN_POINT('Ctrl Pts',(-1.94360696888932,-0.212612981054866,
9.23630840934769));
#280466=CARTESIAN_POINT('Ctrl Pts',(-1.93377174360208,-0.280433314080482,
9.24022619102828));
#280467=CARTESIAN_POINT('Ctrl Pts',(-1.92395134877935,-0.348151381320416,
9.24413806511444));
#280468=CARTESIAN_POINT('Ctrl Pts',(-1.91055427893775,-0.415458480304355,
9.24804993920061));
#280469=CARTESIAN_POINT('Ctrl Pts',(-1.89363166661572,-0.481949282798708,
9.25196181328677));
#280470=CARTESIAN_POINT('Ctrl Pts',(-1.87672899163178,-0.548361749301861,
9.25586907860717));
#280471=CARTESIAN_POINT('Ctrl Pts',(-1.85630914401874,-0.613959354774945,
9.25977634392756));
#280472=CARTESIAN_POINT('Ctrl Pts',(-1.83247448589422,-0.678345972603016,
9.26368360924796));
#280473=CARTESIAN_POINT('Ctrl Pts',(-1.80865480073123,-0.742692142678599,
9.26758842001948));
#280474=CARTESIAN_POINT('Ctrl Pts',(-1.7814247307963,-0.805828373825665,
9.271493230791));
#280475=CARTESIAN_POINT('Ctrl Pts',(-1.75093629541242,-0.867374249910283,
9.27539804156252));
#280476=CARTESIAN_POINT('Ctrl Pts',(-1.72045655062073,-0.928902582618118,
9.27930173928519));
#280477=CARTESIAN_POINT('Ctrl Pts',(-1.68672050243156,-0.988841019529823,
9.28320543700786));
#280478=CARTESIAN_POINT('Ctrl Pts',(-1.64992731783472,-1.04683133591937,
9.28710913473053));
#280479=CARTESIAN_POINT('Ctrl Pts',(-1.61313199556873,-1.10482502152286,
9.29101305925646));
#280480=CARTESIAN_POINT('Ctrl Pts',(-1.57327944999038,-1.16086994783955,
9.29491698378238));
#280481=CARTESIAN_POINT('Ctrl Pts',(-1.53061262304348,-1.21463615876523,
9.29882090830831));
#280482=CARTESIAN_POINT('Ctrl Pts',(-1.48790030667198,-1.2684596927724,
9.30272899502049));
#280483=CARTESIAN_POINT('Ctrl Pts',(-1.44236802729647,-1.31999927675665,
9.30663708173266));
#280484=CARTESIAN_POINT('Ctrl Pts',(-1.39429890623535,-1.36895820245577,
9.31054516844483));
#280485=CARTESIAN_POINT('Ctrl Pts',(-1.34620104861037,-1.41794639665955,
9.3144555914798));
#280486=CARTESIAN_POINT('Ctrl Pts',(-1.29556369382531,-1.46435052975933,
9.31836601451477));
#280487=CARTESIAN_POINT('Ctrl Pts',(-1.24270462293738,-1.50791286887873,
9.32227643754975));
#280488=CARTESIAN_POINT('Ctrl Pts',(-1.18975402833414,-1.55155063473297,
9.32619363135156));
#280489=CARTESIAN_POINT('Ctrl Pts',(-1.13457443531577,-1.59233649370928,
9.33011082515338));
#280490=CARTESIAN_POINT('Ctrl Pts',(-1.07751355441331,-1.63005537944439,
9.33402801895519));
#280491=CARTESIAN_POINT('Ctrl Pts',(-1.05017051899833,-1.64812991338353,
9.33590510124268));
#280492=CARTESIAN_POINT('Ctrl Pts',(-1.0223958727625,-1.66550087107444,
9.33778218353017));
#280493=CARTESIAN_POINT('Ctrl Pts',(-0.994229725646667,-1.68214840386945,
9.33965926581765));
#280494=CARTESIAN_POINT('Ctrl Pts',(-0.935442307976532,-1.71689456420062,
9.34357704768472));
#280495=CARTESIAN_POINT('Ctrl Pts',(-0.874714461285793,-1.74862429952429,
9.3474948295518));
#280496=CARTESIAN_POINT('Ctrl Pts',(-0.812388281868093,-1.77711600057042,
9.35141261141887));
#280497=CARTESIAN_POINT('Ctrl Pts',(-0.750156083619173,-1.80556473919867,
9.35532448569266));
#280498=CARTESIAN_POINT('Ctrl Pts',(-0.686330779660388,-1.8307849308271,
9.35923635996645));
#280499=CARTESIAN_POINT('Ctrl Pts',(-0.621280717555777,-1.85259986775164,
9.36314823424024));
#280500=CARTESIAN_POINT('Ctrl Pts',(-0.556307294020607,-1.8743891034623,
9.36705549974904));
#280501=CARTESIAN_POINT('Ctrl Pts',(-0.490112442267491,-1.89278089641617,
9.37096276525785));
#280502=CARTESIAN_POINT('Ctrl Pts',(-0.423084542207245,-1.907646578941,
9.37487003076666));
#280503=CARTESIAN_POINT('Ctrl Pts',(-0.356098749147802,-1.92250292282765,
9.37877484172697));
#280504=CARTESIAN_POINT('Ctrl Pts',(-0.288281425102331,-1.93383744402462,
9.38267965268727));
#280505=CARTESIAN_POINT('Ctrl Pts',(-0.220034660137484,-1.94157172114197,
9.38658446364758));
#280506=CARTESIAN_POINT('Ctrl Pts',(-0.151807348605316,-1.94930379363849,
9.39048816155912));
#280507=CARTESIAN_POINT('Ctrl Pts',(-0.0831513277768723,-1.95343760390027,
9.39439185947066));
#280508=CARTESIAN_POINT('Ctrl Pts',(-0.0144755912376161,-1.95394638034372,
9.39829555738221));
#280509=CARTESIAN_POINT('Ctrl Pts',(0.0542041353306073,-1.95445518634685,
9.40219948209682));
#280510=CARTESIAN_POINT('Ctrl Pts',(0.122903087897137,-1.95133853930137,
9.40610340681144));
#280511=CARTESIAN_POINT('Ctrl Pts',(0.191212304539026,-1.94462177674551,
9.41000733152605));
#280512=CARTESIAN_POINT('Ctrl Pts',(0.25959434932033,-1.93789785308689,
9.41391541842532));
#280513=CARTESIAN_POINT('Ctrl Pts',(0.327585338355061,-1.92756620205989,
9.41782350532459));
#280514=CARTESIAN_POINT('Ctrl Pts',(0.394782474607588,-1.91370394725587,
9.42173159222386));
#280515=CARTESIAN_POINT('Ctrl Pts',(0.462019782474208,-1.89983340535539,
9.42564201544529));
#280516=CARTESIAN_POINT('Ctrl Pts',(0.528461817064993,-1.88242818378407,
9.42955243866672));
#280517=CARTESIAN_POINT('Ctrl Pts',(0.593719751138159,-1.86161565773079,
9.43346286188815));
#280518=CARTESIAN_POINT('Ctrl Pts',(0.659090677089639,-1.84076709550131,
9.43738005587349));
#280519=CARTESIAN_POINT('Ctrl Pts',(0.723272950577194,-1.81649962782296,
9.44129724985883));
#280520=CARTESIAN_POINT('Ctrl Pts',(0.785897379849404,-1.78898890671402,
9.44521444384417));
#280521=CARTESIAN_POINT('Ctrl Pts',(0.815906386758424,-1.77580604134623,
9.44709152444572));
#280522=CARTESIAN_POINT('Ctrl Pts',(0.845558037813433,-1.76187913176989,
9.44896860504728));
#280523=CARTESIAN_POINT('Ctrl Pts',(0.874813913746812,-1.74723112847585,
9.45084568564883));
#280524=CARTESIAN_POINT('Ctrl Pts',(0.935875823308645,-1.71665829399845,
9.45476346702694));
#280525=CARTESIAN_POINT('Ctrl Pts',(0.995454422971764,-1.68281990134536,
9.45868124840505));
#280526=CARTESIAN_POINT('Ctrl Pts',(1.05317806525755,-1.6458833381684,9.46259902978317));
#280527=CARTESIAN_POINT('Ctrl Pts',(1.11081466648952,-1.60900247136222,
9.46651090356768));
#280528=CARTESIAN_POINT('Ctrl Pts',(1.16660145045014,-1.56903296867654,
9.47042277735219));
#280529=CARTESIAN_POINT('Ctrl Pts',(1.2201902769734,-1.52618861481128,9.4743346511367));
#280530=CARTESIAN_POINT('Ctrl Pts',(1.27371596797137,-1.48339473790106,
9.47824191615812));
#280531=CARTESIAN_POINT('Ctrl Pts',(1.32504846188176,-1.43773304216034,
9.48214918117953));
#280532=CARTESIAN_POINT('Ctrl Pts',(1.37386913391756,-1.38946018398103,
9.48605644620094));
#280533=CARTESIAN_POINT('Ctrl Pts',(1.42265913676749,-1.3412176508505,9.48996125667529));
#280534=CARTESIAN_POINT('Ctrl Pts',(1.46894009876917,-1.29036755428633,
9.49386606714963));
#280535=CARTESIAN_POINT('Ctrl Pts',(1.51242819112343,-1.23720530498988,
9.49777087762398));
#280536=CARTESIAN_POINT('Ctrl Pts',(1.55590388741544,-1.18405820932551,
9.50167457505172));
#280537=CARTESIAN_POINT('Ctrl Pts',(1.59658798306032,-1.12860064989383,
9.50557827247946));
#280538=CARTESIAN_POINT('Ctrl Pts',(1.63423631380887,-1.07116183213761,
9.5094819699072));
#280539=CARTESIAN_POINT('Ctrl Pts',(1.67188683193616,-1.01371967716972,
9.51338589414087));
#280540=CARTESIAN_POINT('Ctrl Pts',(1.70650096743113,-0.954296448211486,
9.51728981837454));
#280541=CARTESIAN_POINT('Ctrl Pts',(1.73787836531886,-0.893249566110533,
9.52119374260821));
#280542=CARTESIAN_POINT('Ctrl Pts',(1.76928921640753,-0.832137598510083,
9.52510182903412));
#280543=CARTESIAN_POINT('Ctrl Pts',(1.79745621761414,-0.769398961467298,
9.52900991546003));
#280544=CARTESIAN_POINT('Ctrl Pts',(1.82222587580868,-0.705413961821904,
9.53291800188593));
#280545=CARTESIAN_POINT('Ctrl Pts',(1.84701034175947,-0.641390710769463,
9.53682842463763));
#280546=CARTESIAN_POINT('Ctrl Pts',(1.86839326946516,-0.576120081838372,
9.54073884738932));
#280547=CARTESIAN_POINT('Ctrl Pts',(1.88627096818667,-0.509997877030984,
9.54464927014102));
#280548=CARTESIAN_POINT('Ctrl Pts',(1.9041796215831,-0.443761183698757,
9.54856646366713));
#280549=CARTESIAN_POINT('Ctrl Pts',(1.91857082955659,-0.376670452434719,
9.55248365719323));
#280550=CARTESIAN_POINT('Ctrl Pts',(1.92939211486288,-0.309131148713524,
9.55640085071933));
#280551=CARTESIAN_POINT('Ctrl Pts',(1.9345775802555,-0.276766904340046,
9.55827793563955));
#280552=CARTESIAN_POINT('Ctrl Pts',(1.93894407361411,-0.24429972281665,
9.56015502055977));
#280553=CARTESIAN_POINT('Ctrl Pts',(1.94249005994572,-0.211774330389899,
9.56203210547999));
#280554=CARTESIAN_POINT('Ctrl Pts',(1.94989111050475,-0.143888543110564,
9.56594988719119));
#280555=CARTESIAN_POINT('Ctrl Pts',(1.95374388824642,-0.0754794566134533,
9.56986766890239));
#280556=CARTESIAN_POINT('Ctrl Pts',(1.95398763962716,-0.00695012117103305,
9.57378545061359));
#280557=CARTESIAN_POINT('Ctrl Pts',(1.9542310234568,0.0614758793399152,
9.57769732472768));
#280558=CARTESIAN_POINT('Ctrl Pts',(1.9508761796019,0.130021280932181,9.58160919884176));
#280559=CARTESIAN_POINT('Ctrl Pts',(1.9439140867026,0.198277642509685,9.58552107295584));
#280560=CARTESIAN_POINT('Ctrl Pts',(1.93696019618472,0.266453587936497,
9.58942833830012));
#280561=CARTESIAN_POINT('Ctrl Pts',(1.92640754657478,0.334340682531275,
9.59333560364439));
#280562=CARTESIAN_POINT('Ctrl Pts',(1.91229914225534,0.401532054174392,
9.59724286898867));
#280563=CARTESIAN_POINT('Ctrl Pts',(1.89819960086187,0.468681216072203,
9.60114767978155));
#280564=CARTESIAN_POINT('Ctrl Pts',(1.88054883659959,0.535135041591085,
9.60505249057444));
#280565=CARTESIAN_POINT('Ctrl Pts',(1.85944128135171,0.600494896901805,
9.60895730136732));
#280566=CARTESIAN_POINT('Ctrl Pts',(1.83833974273168,0.665836121635859,
9.61286099910883));
#280567=CARTESIAN_POINT('Ctrl Pts',(1.8137835202986,0.730083527240458,9.61676469685034));
#280568=CARTESIAN_POINT('Ctrl Pts',(1.78591694410828,0.792853497657011,
9.62066839459184));
#280569=CARTESIAN_POINT('Ctrl Pts',(1.75804874889923,0.855627114942712,
9.62457231913407));
#280570=CARTESIAN_POINT('Ctrl Pts',(1.72687002005523,0.916922677998517,
9.62847624367631));
#280571=CARTESIAN_POINT('Ctrl Pts',(1.6925725433236,0.976378095610029,9.63238016821854));
#280572=CARTESIAN_POINT('Ctrl Pts',(1.65823850022118,1.03589690181609,9.63628825494313));
#280573=CARTESIAN_POINT('Ctrl Pts',(1.62077931967228,1.09357122025362,9.64019634166771));
#280574=CARTESIAN_POINT('Ctrl Pts',(1.58043141874474,1.14906593833621,9.6441044283923));
#280575=CARTESIAN_POINT('Ctrl Pts',(1.54005939715703,1.20459383210343,9.64801485143748));
#280576=CARTESIAN_POINT('Ctrl Pts',(1.49679552824238,1.25793915013662,9.65192527448265));
#280577=CARTESIAN_POINT('Ctrl Pts',(1.45091624290589,1.30880023535751,9.65583569752783));
#280578=CARTESIAN_POINT('Ctrl Pts',(1.4049575191604,1.35974938480302,9.65975289133639));
#280579=CARTESIAN_POINT('Ctrl Pts',(1.35637468886931,1.408205369227,9.66367008514496));
#280580=CARTESIAN_POINT('Ctrl Pts',(1.30548006065421,1.45390433359086,9.66758727895352));
#280581=CARTESIAN_POINT('Ctrl Pts',(1.28109183753958,1.47580284386788,9.66946436107273));
#280582=CARTESIAN_POINT('Ctrl Pts',(1.25617324331868,1.49706888778729,9.67134144319194));
#280583=CARTESIAN_POINT('Ctrl Pts',(1.23076103348846,1.51767693480741,9.67321852531115));
#280584=CARTESIAN_POINT('Ctrl Pts',(1.17772152207824,1.56068935884959,9.6771363081071));
#280585=CARTESIAN_POINT('Ctrl Pts',(1.12231914613281,1.60100345598076,9.68105409090304));
#280586=CARTESIAN_POINT('Ctrl Pts',(1.06485969922456,1.63834972486566,9.68497187369899));
#280587=CARTESIAN_POINT('Ctrl Pts',(1.00748689488888,1.67563967965451,9.68888374890622));
#280588=CARTESIAN_POINT('Ctrl Pts',(0.948063584768635,1.70997042179073,
9.69279562411345));
#280589=CARTESIAN_POINT('Ctrl Pts',(0.886928130547235,1.74111300358248,
9.69670749932068));
#280590=CARTESIAN_POINT('Ctrl Pts',(0.825864702858087,1.77221889484496,
9.70061476576514));
#280591=CARTESIAN_POINT('Ctrl Pts',(0.763093573443617,1.80014386317943,
9.70452203220959));
#280592=CARTESIAN_POINT('Ctrl Pts',(0.698979982238847,1.82470353329777,
9.70842929865404));
#280593=CARTESIAN_POINT('Ctrl Pts',(0.63490666723961,1.84924777501314,9.71233411055082));
#280594=CARTESIAN_POINT('Ctrl Pts',(0.569493021733619,1.87043073654641,
9.71623892244759));
#280595=CARTESIAN_POINT('Ctrl Pts',(0.50312523483442,1.88811572687503,9.72014373434437));
#280596=CARTESIAN_POINT('Ctrl Pts',(0.436776365779002,1.90579567617546,
9.7240474331918));
#280597=CARTESIAN_POINT('Ctrl Pts',(0.369474370405364,1.9199795070017,9.72795113203924));
#280598=CARTESIAN_POINT('Ctrl Pts',(0.30161986072208,1.93058060168903,9.73185483088668));
#280599=CARTESIAN_POINT('Ctrl Pts',(0.233761408758226,1.94118231228959,
9.73575875653519));
#280600=CARTESIAN_POINT('Ctrl Pts',(0.16535086523266,1.94820080007547,9.73966268218371));
#280601=CARTESIAN_POINT('Ctrl Pts',(0.0967964727854304,1.95160099478769,
9.74356660783222));
#280602=CARTESIAN_POINT('Ctrl Pts',(0.0281689909856538,1.95500481462182,
9.74747469565602));
#280603=CARTESIAN_POINT('Ctrl Pts',(-0.0406021534803314,1.95478261821084,
9.75138278347983));
#280604=CARTESIAN_POINT('Ctrl Pts',(-0.109107201405195,1.95095146495281,
9.75529087130363));
#280605=CARTESIAN_POINT('Ctrl Pts',(-0.177653202756922,1.94711802136933,
9.75920129544561));
#280606=CARTESIAN_POINT('Ctrl Pts',(-0.245932301819509,1.93967138048742,
9.7631117195876));
#280607=CARTESIAN_POINT('Ctrl Pts',(-0.313541168509378,1.92868036119254,
9.76702214372958));
#280608=CARTESIAN_POINT('Ctrl Pts',(-0.381267097335567,1.91767031137308,
9.77093933861963));
#280609=CARTESIAN_POINT('Ctrl Pts',(-0.448319997089675,1.90310373898713,
9.77485653350969));
#280610=CARTESIAN_POINT('Ctrl Pts',(-0.514308861291142,1.88510010216896,
9.77877372839975));
#280611=CARTESIAN_POINT('Ctrl Pts',(-0.545929924096169,1.8764729779195,
9.78065080064727));
#280612=CARTESIAN_POINT('Ctrl Pts',(-0.577306919049007,1.86705735905819,
9.78252787289479));
#280613=CARTESIAN_POINT('Ctrl Pts',(-0.608398470454078,1.85687029734151,
9.78440494514231));
#280614=CARTESIAN_POINT('Ctrl Pts',(-0.673291997182021,1.83560811093022,
9.78832272449265));
#280615=CARTESIAN_POINT('Ctrl Pts',(-0.737198494728991,1.81089776173608,
9.79224050384299));
#280616=CARTESIAN_POINT('Ctrl Pts',(-0.799725743186057,1.78285017196777,
9.79615828319333));
#280617=CARTESIAN_POINT('Ctrl Pts',(-0.862158707222957,1.75484487497267,
9.80007015495037));
#280618=CARTESIAN_POINT('Ctrl Pts',(-0.923216104460824,1.72351252419629,
9.8039820267074));
#280619=CARTESIAN_POINT('Ctrl Pts',(-0.982522144707224,1.68901339105406,
9.80789389846443));
#280620=CARTESIAN_POINT('Ctrl Pts',(-1.04175831382631,1.65455490290033,
9.81180116146849));
#280621=CARTESIAN_POINT('Ctrl Pts',(-1.09924680053732,1.61693728822309,
9.81570842447254));
#280622=CARTESIAN_POINT('Ctrl Pts',(-1.1546347054922,1.57636756401321,9.8196156874766));
#280623=CARTESIAN_POINT('Ctrl Pts',(-1.20998781580716,1.53582332567334,
9.823520495941));
#280624=CARTESIAN_POINT('Ctrl Pts',(-1.26324256596937,1.49233094658935,
9.8274253044054));
#280625=CARTESIAN_POINT('Ctrl Pts',(-1.31407477610489,1.44614089313762,
9.8313301128698));
#280626=CARTESIAN_POINT('Ctrl Pts',(-1.36489249690147,1.39996400581302,
9.83523380829794));
#280627=CARTESIAN_POINT('Ctrl Pts',(-1.41328868452497,1.35109130130369,
9.83913750372606));
#280628=CARTESIAN_POINT('Ctrl Pts',(-1.45897342346685,1.29981250556279,
9.8430411991542));
#280629=CARTESIAN_POINT('Ctrl Pts',(-1.50466081686196,1.24853073033315,
9.84694512140155));
#280630=CARTESIAN_POINT('Ctrl Pts',(-1.5476361234311,1.1948429553569,9.85084904364891));
#280631=CARTESIAN_POINT('Ctrl Pts',(-1.58764861207919,1.13907325689045,
9.85475296589626));
#280632=CARTESIAN_POINT('Ctrl Pts',(-1.62770376064663,1.08324409871732,
9.85866105036931));
#280633=CARTESIAN_POINT('Ctrl Pts',(-1.66478949978036,1.02532898773864,
9.86256913484235));
#280634=CARTESIAN_POINT('Ctrl Pts',(-1.69869808581193,0.965681527864581,
9.8664772193154));
#280635=CARTESIAN_POINT('Ctrl Pts',(-1.73262694316917,0.905998409379368,
9.87038764013043));
#280636=CARTESIAN_POINT('Ctrl Pts',(-1.76337464704755,0.844581320891091,
9.87429806094546));
#280637=CARTESIAN_POINT('Ctrl Pts',(-1.79078043651937,0.781806515820568,
9.87820848176048));
#280638=CARTESIAN_POINT('Ctrl Pts',(-1.81823367859699,0.718923017363106,
9.88212567339514));
#280639=CARTESIAN_POINT('Ctrl Pts',(-1.84233328455078,0.654677570732816,
9.88604286502981));
#280640=CARTESIAN_POINT('Ctrl Pts',(-1.86296772943102,0.589463518038743,
9.88996005666447));
#280641=CARTESIAN_POINT('Ctrl Pts',(-1.87285567397083,0.558213201395993,
9.89183715943414));
#280642=CARTESIAN_POINT('Ctrl Pts',(-1.88194866833356,0.526740643156299,
9.89371426220381));
#280643=CARTESIAN_POINT('Ctrl Pts',(-1.89023861760682,0.495089859023457,
9.89559136497348));
#280644=CARTESIAN_POINT('Ctrl Pts',(-1.91241236797386,0.410431127932456,
9.90061219282851));
#280645=CARTESIAN_POINT('Ctrl Pts',(-1.92890876017623,0.324228031161974,
9.90563302068355));
#280646=CARTESIAN_POINT('Ctrl Pts',(-1.93955619828592,0.237145005620355,
9.91065384853858));
#280647=CARTESIAN_POINT('Ctrl Pts',(-1.94908248889442,0.159231595856335,
9.91514599629746));
#280648=CARTESIAN_POINT('Ctrl Pts',(-1.95392723381153,0.0806138670398988,
9.91963814405634));
#280649=CARTESIAN_POINT('Ctrl Pts',(-1.95399918605333,0.00178350859616108,
9.92413029181523));
#280650=CARTESIAN_POINT('',(-1.95093054978418,-0.000550606481354719,10.6241303078758));
#280651=CARTESIAN_POINT('Ctrl Pts',(-1.9535343393295,0.00178280253715055,
9.92413030787576));
#280652=CARTESIAN_POINT('Ctrl Pts',(-1.94919764294582,-0.481552375812319,
9.95167946685205));
#280653=CARTESIAN_POINT('Ctrl Pts',(-1.523943549881,-1.62193885960754,10.0162907657721));
#280654=CARTESIAN_POINT('Ctrl Pts',(0.388631330803288,-2.27693917494034,
10.1179642046358));
#280655=CARTESIAN_POINT('Ctrl Pts',(2.12415308786741,-0.907447137301165,
10.2291506244669));
#280656=CARTESIAN_POINT('Ctrl Pts',(1.91385514681522,1.29330245229283,10.3403370442982));
#280657=CARTESIAN_POINT('Ctrl Pts',(-0.0496108271125428,2.30933734912718,
10.4515234641293));
#280658=CARTESIAN_POINT('Ctrl Pts',(-1.68147873779689,1.37393834407351,
10.5461212186551));
#280659=CARTESIAN_POINT('Ctrl Pts',(-1.95001820365716,0.359852200961074,
10.6036568332373));
#280660=CARTESIAN_POINT('Ctrl Pts',(-1.95093054978418,-0.000550606481354719,
10.6241303078758));
#280661=CARTESIAN_POINT('',(1.56057659382855,1.17255425406022,11.046));
#280662=CARTESIAN_POINT('Ctrl Pts',(-1.95093054978418,-0.000550606481354719,
10.6241303078758));
#280663=CARTESIAN_POINT('Ctrl Pts',(-1.95166977968097,-0.292567552961119,
10.640718973181));
#280664=CARTESIAN_POINT('Ctrl Pts',(-1.75310453654278,-1.23604956259639,
10.69436977843));
#280665=CARTESIAN_POINT('Ctrl Pts',(-0.290505442625576,-2.29155305943217,
10.7850827236229));
#280666=CARTESIAN_POINT('Ctrl Pts',(1.76839371692331,-1.48603171255786,
10.8962691434539));
#280667=CARTESIAN_POINT('Ctrl Pts',(2.111645059346,0.208752628450599,10.983241568913));
#280668=CARTESIAN_POINT('Ctrl Pts',(1.69759382901609,0.992979671982257,
11.0331518544284));
#280669=CARTESIAN_POINT('Ctrl Pts',(1.56057659382855,1.17255425406022,11.046));
#280670=CARTESIAN_POINT('',(1.88426091070916,-0.517374932107736,11.0459974907899));
#280671=CARTESIAN_POINT('Origin',(0.,0.,11.046));
#280672=CARTESIAN_POINT('',(-1.95388960244062,-0.00113872704447003,10.7258697407189));
#280673=CARTESIAN_POINT('Ctrl Pts',(1.88426091070916,-0.517374932107736,
11.0459974907899));
#280674=CARTESIAN_POINT('Ctrl Pts',(1.86515675297054,-0.586951588078024,
11.0419101437675));
#280675=CARTESIAN_POINT('Ctrl Pts',(1.84221826837054,-0.655383383450449,
11.0378227967452));
#280676=CARTESIAN_POINT('Ctrl Pts',(1.81561644938194,-0.722255431778618,
11.0337354497228));
#280677=CARTESIAN_POINT('Ctrl Pts',(1.78893195159019,-0.78933531931215,
11.0296353991722));
#280678=CARTESIAN_POINT('Ctrl Pts',(1.75856152345182,-0.854845383446217,
11.0255353486216));
#280679=CARTESIAN_POINT('Ctrl Pts',(1.72472347046363,-0.918392590579804,
11.0214352980709));
#280680=CARTESIAN_POINT('Ctrl Pts',(1.69082799031288,-0.982047644810721,
11.0173282892515));
#280681=CARTESIAN_POINT('Ctrl Pts',(1.65345337053807,-1.04373284494727,
11.013221280432));
#280682=CARTESIAN_POINT('Ctrl Pts',(1.61286122882079,-1.10308415661122,
11.0091142716125));
#280683=CARTESIAN_POINT('Ctrl Pts',(1.57215179605288,-1.16260696397377,
11.0049953955853));
#280684=CARTESIAN_POINT('Ctrl Pts',(1.52820651784718,-1.21978207539512,
11.0008765195581));
#280685=CARTESIAN_POINT('Ctrl Pts',(1.48132746950652,-1.27427819885824,
10.9967576435308));
#280686=CARTESIAN_POINT('Ctrl Pts',(1.46404643467158,-1.29436711792273,
10.9952393012729));
#280687=CARTESIAN_POINT('Ctrl Pts',(1.44636708492743,-1.31409236689375,
10.993720959015));
#280688=CARTESIAN_POINT('Ctrl Pts',(1.42830572605192,-1.33343869485151,
10.992202616757));
#280689=CARTESIAN_POINT('Ctrl Pts',(1.38162613769539,-1.38343928625238,
10.9882784606582));
#280690=CARTESIAN_POINT('Ctrl Pts',(1.33222699407779,-1.43108308891436,
10.9843543045593));
#280691=CARTESIAN_POINT('Ctrl Pts',(1.2803753524773,-1.47606062096671,10.9804301484605));
#280692=CARTESIAN_POINT('Ctrl Pts',(1.22860156563048,-1.52097061967643,
10.9765118844453));
#280693=CARTESIAN_POINT('Ctrl Pts',(1.17438295715036,-1.56322197525663,
10.97259362043));
#280694=CARTESIAN_POINT('Ctrl Pts',(1.11802436066742,-1.60254096014867,
10.9686753564148));
#280695=CARTESIAN_POINT('Ctrl Pts',(1.06173221962825,-1.64181358191684,
10.9647617126348));
#280696=CARTESIAN_POINT('Ctrl Pts',(1.0033055027343,-1.67816042176417,10.9608480688548));
#280697=CARTESIAN_POINT('Ctrl Pts',(0.943081743355728,-1.71134824782951,
10.9569344250748));
#280698=CARTESIAN_POINT('Ctrl Pts',(0.882895921614319,-1.74451516740019,
10.9530232466739));
#280699=CARTESIAN_POINT('Ctrl Pts',(0.820915731556803,-1.77452678518832,
10.949112068273));
#280700=CARTESIAN_POINT('Ctrl Pts',(0.757505980477138,-1.80119423981462,
10.9452008898721));
#280701=CARTESIAN_POINT('Ctrl Pts',(0.694114617435391,-1.82785396121128,
10.9412908456642));
#280702=CARTESIAN_POINT('Ctrl Pts',(0.629294967989068,-1.85117125490152,
10.9373808014563));
#280703=CARTESIAN_POINT('Ctrl Pts',(0.563432998143645,-1.87100487882925,
10.9334707572484));
#280704=CARTESIAN_POINT('Ctrl Pts',(0.497567738156177,-1.89083949354788,
10.9295605177138));
#280705=CARTESIAN_POINT('Ctrl Pts',(0.43066052440524,-1.90718995407429,
10.9256502781792));
#280706=CARTESIAN_POINT('Ctrl Pts',(0.363111980267009,-1.91996502306333,
10.9217400386447));
#280707=CARTESIAN_POINT('Ctrl Pts',(0.295493257140132,-1.93275336460226,
10.9178257365998));
#280708=CARTESIAN_POINT('Ctrl Pts',(0.227232356321995,-1.94195880982462,
10.9139114345549));
#280709=CARTESIAN_POINT('Ctrl Pts',(0.158738590832598,-1.94754154250442,
10.90999713251));
#280710=CARTESIAN_POINT('Ctrl Pts',(0.0902047060866323,-1.9531275451911,
10.906080537718));
#280711=CARTESIAN_POINT('Ctrl Pts',(0.0214381751924879,-1.95508659739389,
10.9021639429259));
#280712=CARTESIAN_POINT('Ctrl Pts',(-0.0471508747100471,-1.95343103154784,
10.8982473481339));
#280713=CARTESIAN_POINT('Ctrl Pts',(-0.11585583910553,-1.95177266781969,
10.8943241343538));
#280714=CARTESIAN_POINT('Ctrl Pts',(-0.184382235370864,-1.94648753112932,
10.8904009205737));
#280715=CARTESIAN_POINT('Ctrl Pts',(-0.252325118724455,-1.93763981030033,
10.8864777067936));
#280716=CARTESIAN_POINT('Ctrl Pts',(-0.28342128150148,-1.93359037710698,
10.8846821266196));
#280717=CARTESIAN_POINT('Ctrl Pts',(-0.314395359941127,-1.92879539009223,
10.8828865464456));
#280718=CARTESIAN_POINT('Ctrl Pts',(-0.345209459210633,-1.92326452399858,
10.8810909662716));
#280719=CARTESIAN_POINT('Ctrl Pts',(-0.412565791002198,-1.9111746411031,
10.8771660196782));
#280720=CARTESIAN_POINT('Ctrl Pts',(-0.479414437377039,-1.89551908549188,
10.8732410730847));
#280721=CARTESIAN_POINT('Ctrl Pts',(-0.545350411357199,-1.87635522458636,
10.8693161264912));
#280722=CARTESIAN_POINT('Ctrl Pts',(-0.611189766467242,-1.85721944532544,
10.8653969312939));
#280723=CARTESIAN_POINT('Ctrl Pts',(-0.676118636925346,-1.83458570069962,
10.8614777360966));
#280724=CARTESIAN_POINT('Ctrl Pts',(-0.739741712477614,-1.80856246749198,
10.8575585408992));
#280725=CARTESIAN_POINT('Ctrl Pts',(-0.803293110238869,-1.78256855207282,
10.8536437610693));
#280726=CARTESIAN_POINT('Ctrl Pts',(-0.865541183529176,-1.75319291700574,
10.8497289812394));
#280727=CARTESIAN_POINT('Ctrl Pts',(-0.926107008533286,-1.72059344667633,
10.8458142014094));
#280728=CARTESIAN_POINT('Ctrl Pts',(-0.98663665358324,-1.68801345015648,
10.8419017601352));
#280729=CARTESIAN_POINT('Ctrl Pts',(-1.0454856136025,-1.6522136708149,10.8379893188609));
#280730=CARTESIAN_POINT('Ctrl Pts',(-1.10229756290302,-1.61339892240514,
10.8340768775867));
#280731=CARTESIAN_POINT('Ctrl Pts',(-1.15909486171909,-1.57459418341901,
10.8301654452403));
#280732=CARTESIAN_POINT('Ctrl Pts',(-1.21385578849959,-1.5327762953315,
10.826254012894));
#280733=CARTESIAN_POINT('Ctrl Pts',(-1.26625265023858,-1.48819361165265,
10.8223425805476));
#280734=CARTESIAN_POINT('Ctrl Pts',(-1.31865378746122,-1.44360729011214,
10.8184308290359));
#280735=CARTESIAN_POINT('Ctrl Pts',(-1.36869010521002,-1.39625604443166,
10.8145190775241));
#280736=CARTESIAN_POINT('Ctrl Pts',(-1.41606806015514,-1.34642758773298,
10.8106073260124));
#280737=CARTESIAN_POINT('Ctrl Pts',(-1.46349737566049,-1.2965451139824,
10.8066913339261));
#280738=CARTESIAN_POINT('Ctrl Pts',(-1.50826223907816,-1.24418042568486,
10.8027753418398));
#280739=CARTESIAN_POINT('Ctrl Pts',(-1.55010765966135,-1.18965635519641,
10.7988593497535));
#280740=CARTESIAN_POINT('Ctrl Pts',(-1.59197869446824,-1.13509890968821,
10.7949409606285));
#280741=CARTESIAN_POINT('Ctrl Pts',(-1.63092645233119,-1.0783798550431,
10.7910225715034));
#280742=CARTESIAN_POINT('Ctrl Pts',(-1.66673937701486,-1.01985089552744,
10.7871041823783));
#280743=CARTESIAN_POINT('Ctrl Pts',(-1.70261410256806,-0.961220935028945,
10.7831790314526));
#280744=CARTESIAN_POINT('Ctrl Pts',(-1.7353429648826,-0.900775266527879,
10.7792538805269));
#280745=CARTESIAN_POINT('Ctrl Pts',(-1.7647608287876,-0.838889275874307,
10.7753287296012));
#280746=CARTESIAN_POINT('Ctrl Pts',(-1.77812492871317,-0.81077538678439,
10.7735455916629));
#280747=CARTESIAN_POINT('Ctrl Pts',(-1.79080638760702,-0.782364507779672,
10.7717624537246));
#280748=CARTESIAN_POINT('Ctrl Pts',(-1.80279310312774,-0.753692926406397,
10.7699793157862));
#280749=CARTESIAN_POINT('Ctrl Pts',(-1.83203733004641,-0.683742302288633,
10.7656289588927));
#280750=CARTESIAN_POINT('Ctrl Pts',(-1.85724198247572,-0.612002710327624,
10.7612786019992));
#280751=CARTESIAN_POINT('Ctrl Pts',(-1.8782090960143,-0.538930971135593,
10.7569282451058));
#280752=CARTESIAN_POINT('Ctrl Pts',(-1.89910485491189,-0.466107907456626,
10.7525926932141));
#280753=CARTESIAN_POINT('Ctrl Pts',(-1.91579170679192,-0.39196200964791,
10.7482571413224));
#280754=CARTESIAN_POINT('Ctrl Pts',(-1.92812013154444,-0.316968071472601,
10.7439215894308));
#280755=CARTESIAN_POINT('Ctrl Pts',(-1.9403801743362,-0.242390101487888,
10.7396100855051));
#280756=CARTESIAN_POINT('Ctrl Pts',(-1.94832987646409,-0.166973753229426,
10.7352985815794));
#280757=CARTESIAN_POINT('Ctrl Pts',(-1.95187032663603,-0.0912043200609277,
10.7309870776538));
#280758=CARTESIAN_POINT('Ctrl Pts',(-1.95327104971236,-0.0612273430197019,
10.7292812993631));
#280759=CARTESIAN_POINT('Ctrl Pts',(-1.95398215067413,-0.0311952786312452,
10.7275755210725));
#280760=CARTESIAN_POINT('Ctrl Pts',(-1.95399966813507,-0.00113882749166742,
10.7258697427818));
#280761=CARTESIAN_POINT('',(-1.95399929720026,0.00165726911154443,10.0258696715299));
#280762=CARTESIAN_POINT('Ctrl Pts',(-1.95129684289216,-0.00113636086278679,
10.7258696921242));
#280763=CARTESIAN_POINT('Ctrl Pts',(-1.94942963316978,0.391854106201406,
10.7035356831831));
#280764=CARTESIAN_POINT('Ctrl Pts',(-1.64371581331279,1.43936972202558,
10.6441644574134));
#280765=CARTESIAN_POINT('Ctrl Pts',(0.0645886152005409,2.30833217918205,
10.5477560148154));
#280766=CARTESIAN_POINT('Ctrl Pts',(1.97414006873681,1.19827380577986,10.4366443643299));
#280767=CARTESIAN_POINT('Ctrl Pts',(2.07762111854432,-1.00830526181525,
10.3255327138444));
#280768=CARTESIAN_POINT('Ctrl Pts',(0.280201048116129,-2.29226437530736,
10.2144210633591));
#280769=CARTESIAN_POINT('Ctrl Pts',(-1.56609100264734,-1.56119761498329,
10.1145333894522));
#280770=CARTESIAN_POINT('Ctrl Pts',(-1.94902777514884,-0.451727225472274,
10.051682932374));
#280771=CARTESIAN_POINT('Ctrl Pts',(-1.95268202714777,0.00165579016441021,
10.0258696921242));
#280772=CARTESIAN_POINT('',(-1.95399999964781,3.70990612662463E-5,9.32586969217469));
#280773=CARTESIAN_POINT('Ctrl Pts',(-1.95399929720026,0.00165726911154443,
10.0258696715299));
#280774=CARTESIAN_POINT('Ctrl Pts',(-1.95392946016848,0.0839984592389699,
10.0211847229765));
#280775=CARTESIAN_POINT('Ctrl Pts',(-1.94865101160301,0.166113796242972,
10.0164997744231));
#280776=CARTESIAN_POINT('Ctrl Pts',(-1.93827214842649,0.24742085327267,
10.0118148258697));
#280777=CARTESIAN_POINT('Ctrl Pts',(-1.92775063089284,0.32984545138108,
10.0070654841056));
#280778=CARTESIAN_POINT('Ctrl Pts',(-1.9119876083715,0.411439382463031,
10.0023161423414));
#280779=CARTESIAN_POINT('Ctrl Pts',(-1.89114465504996,0.49161762954147,
9.99756680057726));
#280780=CARTESIAN_POINT('Ctrl Pts',(-1.88329047104473,0.521830944135401,
9.99577712118087));
#280781=CARTESIAN_POINT('Ctrl Pts',(-1.87471542987959,0.551843453374223,
9.99398744178449));
#280782=CARTESIAN_POINT('Ctrl Pts',(-1.86542991659206,0.581624643806756,
9.9921977623881));
#280783=CARTESIAN_POINT('Ctrl Pts',(-1.84510108849325,0.646824776759485,
9.98827960690498));
#280784=CARTESIAN_POINT('Ctrl Pts',(-1.82130956062044,0.711087059136883,
9.98436145142186));
#280785=CARTESIAN_POINT('Ctrl Pts',(-1.79416071012429,0.774017665332199,
9.98044329593874));
#280786=CARTESIAN_POINT('Ctrl Pts',(-1.76705273820747,0.836853515626944,
9.97653104010245));
#280787=CARTESIAN_POINT('Ctrl Pts',(-1.73659766970729,0.898361221218455,
9.97261878426615));
#280788=CARTESIAN_POINT('Ctrl Pts',(-1.70295045843072,0.95816268771572,
9.96870652842986));
#280789=CARTESIAN_POINT('Ctrl Pts',(-1.66934281055982,1.01789383784532,
9.96479887274196));
#280790=CARTESIAN_POINT('Ctrl Pts',(-1.63255071431331,1.07592230667678,
9.96089121705406));
#280791=CARTESIAN_POINT('Ctrl Pts',(-1.59277618877594,1.1318922265253,9.95698356136616));
#280792=CARTESIAN_POINT('Ctrl Pts',(-1.55302658987783,1.18782707010369,
9.95307835460058));
#280793=CARTESIAN_POINT('Ctrl Pts',(-1.51029855364633,1.24170552378917,
9.94917314783501));
#280794=CARTESIAN_POINT('Ctrl Pts',(-1.46483795145502,1.29319982059117,
9.94526794106944));
#280795=CARTESIAN_POINT('Ctrl Pts',(-1.41939024798578,1.34467950670634,
9.94136384234411));
#280796=CARTESIAN_POINT('Ctrl Pts',(-1.37121184308229,1.39377601027969,
9.93745974361878));
#280797=CARTESIAN_POINT('Ctrl Pts',(-1.32058835050876,1.44019526748998,
9.93355564489345));
#280798=CARTESIAN_POINT('Ctrl Pts',(-1.26996186003076,1.48661727363149,
9.92965131496884));
#280799=CARTESIAN_POINT('Ctrl Pts',(-1.21689035867317,1.53036138810924,
9.92574698504423));
#280800=CARTESIAN_POINT('Ctrl Pts',(-1.16169436477441,1.57117223844217,
9.92184265511962));
#280801=CARTESIAN_POINT('Ctrl Pts',(-1.10643958069217,1.61202655709969,
9.9179341666274));
#280802=CARTESIAN_POINT('Ctrl Pts',(-1.04905618441536,1.64994108355012,
9.91402567813517));
#280803=CARTESIAN_POINT('Ctrl Pts',(-0.989894830055331,1.68470300807879,
9.91011718964295));
#280804=CARTESIAN_POINT('Ctrl Pts',(-0.930698064328628,1.71948573955601,
9.90620636170261));
#280805=CARTESIAN_POINT('Ctrl Pts',(-0.869721659241525,1.75111188711872,
9.90229553376227));
#280806=CARTESIAN_POINT('Ctrl Pts',(-0.807339587395694,1.77941529459082,
9.89838470582192));
#280807=CARTESIAN_POINT('Ctrl Pts',(-0.744849809313426,1.80776756952448,
9.89446712561212));
#280808=CARTESIAN_POINT('Ctrl Pts',(-0.680949978412429,1.83278547520301,
9.89054954540231));
#280809=CARTESIAN_POINT('Ctrl Pts',(-0.616031852958404,1.85435184259639,
9.8866319651925));
#280810=CARTESIAN_POINT('Ctrl Pts',(-0.585398453399131,1.86452852506809,
9.88478334742923));
#280811=CARTESIAN_POINT('Ctrl Pts',(-0.554538496038118,1.87393739140249,
9.88293472966596));
#280812=CARTESIAN_POINT('Ctrl Pts',(-0.523493898671034,1.88257008848388,
9.88108611190269));
#280813=CARTESIAN_POINT('Ctrl Pts',(-0.457695228505216,1.90086699152254,
9.87716798763038));
#280814=CARTESIAN_POINT('Ctrl Pts',(-0.390805720697579,1.91574636522992,
9.87324986335807));
#280815=CARTESIAN_POINT('Ctrl Pts',(-0.323213364846653,1.92708306016749,
9.86933173908576));
#280816=CARTESIAN_POINT('Ctrl Pts',(-0.255722787104298,1.93840268472257,
9.86541951458233));
#280817=CARTESIAN_POINT('Ctrl Pts',(-0.187531942915477,1.94619013677017,
9.8615072900789));
#280818=CARTESIAN_POINT('Ctrl Pts',(-0.119042505200818,1.9503704473652,
9.85759506557547));
#280819=CARTESIAN_POINT('Ctrl Pts',(-0.0506336004842804,1.95454584256076,
9.85368744124367));
#280820=CARTESIAN_POINT('Ctrl Pts',(0.0180727118285098,1.95512249004676,
9.84977981691187));
#280821=CARTESIAN_POINT('Ctrl Pts',(0.0866678945075832,1.95207701591449,
9.84587219258007));
#280822=CARTESIAN_POINT('Ctrl Pts',(0.155220088415557,1.94903345038842,
9.84196701716614));
#280823=CARTESIAN_POINT('Ctrl Pts',(0.223660800552973,1.94237228795691,
9.8380618417522));
#280824=CARTESIAN_POINT('Ctrl Pts',(0.291581307004438,1.9321222376976,9.83415666633826));
#280825=CARTESIAN_POINT('Ctrl Pts',(0.359482542861863,1.92187509561092,
9.8302525989115));
#280826=CARTESIAN_POINT('Ctrl Pts',(0.426863379891022,1.90804116046147,
9.82634853148473));
#280827=CARTESIAN_POINT('Ctrl Pts',(0.493321843646891,1.89070081149314,
9.82244446405797));
#280828=CARTESIAN_POINT('Ctrl Pts',(0.559784244811242,1.87335943517581,
9.81854016533022));
#280829=CARTESIAN_POINT('Ctrl Pts',(0.625323688914603,1.85251135926445,
9.81463586660247));
#280830=CARTESIAN_POINT('Ctrl Pts',(0.689551766031441,1.8282872755568,9.81073156787472));
#280831=CARTESIAN_POINT('Ctrl Pts',(0.753848260189182,1.80403738786746,
9.80682311020936));
#280832=CARTESIAN_POINT('Ctrl Pts',(0.816830138475845,1.77640448941032,
9.80291465254399));
#280833=CARTESIAN_POINT('Ctrl Pts',(0.878128394929078,1.74556767901427,
9.79900619487863));
#280834=CARTESIAN_POINT('Ctrl Pts',(0.939463344701322,1.71471240961162,
9.79509539759886));
#280835=CARTESIAN_POINT('Ctrl Pts',(0.999112239694252,1.68064965530552,
9.79118460031908));
#280836=CARTESIAN_POINT('Ctrl Pts',(1.05673261311193,1.64360341456984,9.78727380303931));
#280837=CARTESIAN_POINT('Ctrl Pts',(1.11445248075737,1.60649320536441,9.78335625290925));
#280838=CARTESIAN_POINT('Ctrl Pts',(1.17013643709931,1.56638951518068,9.7794387027792));
#280839=CARTESIAN_POINT('Ctrl Pts',(1.22347351659946,1.52355786046338,9.77552115264914));
#280840=CARTESIAN_POINT('Ctrl Pts',(1.24864607779852,1.50334335941209,9.77367225557184));
#280841=CARTESIAN_POINT('Ctrl Pts',(1.27329641311365,1.48252178617763,9.77182335849455));
#280842=CARTESIAN_POINT('Ctrl Pts',(1.29739475006501,1.4611238354444,9.76997446141725));
#280843=CARTESIAN_POINT('Ctrl Pts',(1.34846286826111,1.41577825498361,9.76605636139788));
#280844=CARTESIAN_POINT('Ctrl Pts',(1.39725203878253,1.36766221144679,9.76213826137852));
#280845=CARTESIAN_POINT('Ctrl Pts',(1.44344663175065,1.31703372063425,9.75822016135916));
#280846=CARTESIAN_POINT('Ctrl Pts',(1.48957165964721,1.2664814719609,9.75430796166039));
#280847=CARTESIAN_POINT('Ctrl Pts',(1.53310953554373,1.21342464541315,9.75039576196162));
#280848=CARTESIAN_POINT('Ctrl Pts',(1.57377935816454,1.15815997678007,9.74648356226285));
#280849=CARTESIAN_POINT('Ctrl Pts',(1.61440135181701,1.10296030110531,9.74257596343183));
#280850=CARTESIAN_POINT('Ctrl Pts',(1.65216170069637,1.04555833430942,9.73866836460082));
#280851=CARTESIAN_POINT('Ctrl Pts',(1.68681912017229,0.986284571420027,
9.7347607657698));
#280852=CARTESIAN_POINT('Ctrl Pts',(1.72145481591177,0.927047962122052,
9.73085561627427));
#280853=CARTESIAN_POINT('Ctrl Pts',(1.75299119270281,0.865942307792211,
9.72695046677873));
#280854=CARTESIAN_POINT('Ctrl Pts',(1.78123061543365,0.803326518074594,
9.72304531728319));
#280855=CARTESIAN_POINT('Ctrl Pts',(1.80946202320625,0.740728500070822,
9.71914127615345));
#280856=CARTESIAN_POINT('Ctrl Pts',(1.83439813240783,0.676621645724216,
9.71523723502371));
#280857=CARTESIAN_POINT('Ctrl Pts',(1.85588837394989,0.611387228716484,
9.71133319389397));
#280858=CARTESIAN_POINT('Ctrl Pts',(1.87737988684293,0.546148952476197,
9.70742892180328));
#280859=CARTESIAN_POINT('Ctrl Pts',(1.89542497588251,0.479783449127808,
9.70352464971259));
#280860=CARTESIAN_POINT('Ctrl Pts',(1.90992269513095,0.412687894932391,
9.6996203776219));
#280861=CARTESIAN_POINT('Ctrl Pts',(1.92443585650675,0.345520874454898,
9.69571194692766));
#280862=CARTESIAN_POINT('Ctrl Pts',(1.93539400338419,0.277622732978139,
9.6918035162334));
#280863=CARTESIAN_POINT('Ctrl Pts',(1.94274738051021,0.209400610125006,
9.68789508553916));
#280864=CARTESIAN_POINT('Ctrl Pts',(1.95010515898673,0.141137653044288,
9.68398431546082));
#280865=CARTESIAN_POINT('Ctrl Pts',(1.95385384678693,0.0725508198725638,
9.68007354538249));
#280866=CARTESIAN_POINT('Ctrl Pts',(1.95399580425165,0.00404931684999055,
9.67616277530415));
#280867=CARTESIAN_POINT('Ctrl Pts',(1.95413800683621,-0.064570468631866,
9.67224525244694));
#280868=CARTESIAN_POINT('Ctrl Pts',(1.95066107432734,-0.133104138904127,
9.66832772958974));
#280869=CARTESIAN_POINT('Ctrl Pts',(1.94361933414002,-0.201146424171811,
9.66441020673253));
#280870=CARTESIAN_POINT('Ctrl Pts',(1.94029552286363,-0.233263444826869,
9.66256107479895));
#280871=CARTESIAN_POINT('Ctrl Pts',(1.93617822033419,-0.265271118839659,
9.66071194286538));
#280872=CARTESIAN_POINT('Ctrl Pts',(1.93127706196271,-0.297127767024027,
9.65886281093181));
#280873=CARTESIAN_POINT('Ctrl Pts',(1.92089200596725,-0.364628763757224,
9.65494468847634));
#280874=CARTESIAN_POINT('Ctrl Pts',(1.90694321368401,-0.431718450463748,
9.65102656602087));
#280875=CARTESIAN_POINT('Ctrl Pts',(1.88947618824516,-0.497991700788822,
9.6471084435654));
#280876=CARTESIAN_POINT('Ctrl Pts',(1.87203546493705,-0.564165155776617,
9.64319622108239));
#280877=CARTESIAN_POINT('Ctrl Pts',(1.85108714710729,-0.629524142503438,
9.63928399859937));
#280878=CARTESIAN_POINT('Ctrl Pts',(1.82672810542462,-0.693671701060218,
9.63537177611637));
#280879=CARTESIAN_POINT('Ctrl Pts',(1.80239770805064,-0.757743827155699,
9.63146415409794));
#280880=CARTESIAN_POINT('Ctrl Pts',(1.77466472600995,-0.820606896584117,
9.6275565320795));
#280881=CARTESIAN_POINT('Ctrl Pts',(1.74367588225073,-0.881878913262543,
9.62364891006107));
#280882=CARTESIAN_POINT('Ctrl Pts',(1.71270646072224,-0.943112527758108,
9.61974373714133));
#280883=CARTESIAN_POINT('Ctrl Pts',(1.6784854468909,-1.0027566296655,9.61583856422158));
#280884=CARTESIAN_POINT('Ctrl Pts',(1.64120711430444,-1.06045047407056,
9.61193339130183));
#280885=CARTESIAN_POINT('Ctrl Pts',(1.6039393601304,-1.1181279467863,9.60802932654672));
#280886=CARTESIAN_POINT('Ctrl Pts',(1.56361627629858,-1.17385584769113,
9.6041252617916));
#280887=CARTESIAN_POINT('Ctrl Pts',(1.52047645787945,-1.22730083558774,
9.60022119703648));
#280888=CARTESIAN_POINT('Ctrl Pts',(1.47733408551607,-1.28074898751064,
9.59631690115467));
#280889=CARTESIAN_POINT('Ctrl Pts',(1.43137495843991,-1.33191357696582,
9.59241260527286));
#280890=CARTESIAN_POINT('Ctrl Pts',(1.38287795279402,-1.38049432004489,
9.58850830939105));
#280891=CARTESIAN_POINT('Ctrl Pts',(1.33432929017605,-1.42912680928965,
9.58459985481736));
#280892=CARTESIAN_POINT('Ctrl Pts',(1.28323770233214,-1.47516961083117,
9.58069140024367));
#280893=CARTESIAN_POINT('Ctrl Pts',(1.22991820784531,-1.5183600370171,9.57678294566998));
#280894=CARTESIAN_POINT('Ctrl Pts',(1.17656679810194,-1.56157631553988,
9.5728721516268));
#280895=CARTESIAN_POINT('Ctrl Pts',(1.12098522577274,-1.60193653173919,
9.56896135758363));
#280896=CARTESIAN_POINT('Ctrl Pts',(1.06351852024582,-1.63922065540126,
9.56505056354045));
#280897=CARTESIAN_POINT('Ctrl Pts',(1.00595258855654,-1.67656915652283,
9.56113301683795));
#280898=CARTESIAN_POINT('Ctrl Pts',(0.946495453155029,-1.71083071894422,
9.55721547013546));
#280899=CARTESIAN_POINT('Ctrl Pts',(0.885517030936552,-1.74183110200769,
9.55329792343296));
#280900=CARTESIAN_POINT('Ctrl Pts',(0.856737722436668,-1.75646200840605,
9.55144900243744));
#280901=CARTESIAN_POINT('Ctrl Pts',(0.827619845882305,-1.77036719945058,
9.54960008144191));
#280902=CARTESIAN_POINT('Ctrl Pts',(0.798203626448538,-1.78353216139334,
9.54775116044638));
#280903=CARTESIAN_POINT('Ctrl Pts',(0.735866635916521,-1.81143051555908,
9.54383304408707));
#280904=CARTESIAN_POINT('Ctrl Pts',(0.671941682099769,-1.83611208857875,
9.53991492772776));
#280905=CARTESIAN_POINT('Ctrl Pts',(0.606793768634314,-1.85739530589117,
9.53599681136844));
#280906=CARTESIAN_POINT('Ctrl Pts',(0.541743956876402,-1.87864647428831,
9.53208459502779));
#280907=CARTESIAN_POINT('Ctrl Pts',(0.475475304134359,-1.89650929158128,
9.52817237868714));
#280908=CARTESIAN_POINT('Ctrl Pts',(0.40837382317573,-1.9108497639911,9.52426016234649));
#280909=CARTESIAN_POINT('Ctrl Pts',(0.341351249028786,-1.92517337297347,
9.52035254650814));
#280910=CARTESIAN_POINT('Ctrl Pts',(0.273498270409407,-1.93598276091421,
9.5164449306698));
#280911=CARTESIAN_POINT('Ctrl Pts',(0.205215377115653,-1.94319392984727,
9.51253731483146));
#280912=CARTESIAN_POINT('Ctrl Pts',(0.136975280478163,-1.95040057914293,
9.50863214811154));
#280913=CARTESIAN_POINT('Ctrl Pts',(0.0683062917338641,-1.95401343149313,
9.50472698139161));
#280914=CARTESIAN_POINT('Ctrl Pts',(-0.000383152612268429,-1.95399996243451,
9.50082181467169));
#280915=CARTESIAN_POINT('Ctrl Pts',(-0.0690531048552257,-1.95398649719803,
9.49691775612659));
#280916=CARTESIAN_POINT('Ctrl Pts',(-0.137743009527492,-1.95034875348325,
9.49301369758149));
#280917=CARTESIAN_POINT('Ctrl Pts',(-0.206043403666329,-1.94310630584268,
9.48910963903639));
#280918=CARTESIAN_POINT('Ctrl Pts',(-0.274347841289605,-1.9358634294385,
9.48520534936524));
#280919=CARTESIAN_POINT('Ctrl Pts',(-0.342262233732601,-1.92501547984492,
9.48130105969409));
#280920=CARTESIAN_POINT('Ctrl Pts',(-0.409383032875655,-1.91063380384456,
9.47739677002295));
#280921=CARTESIAN_POINT('Ctrl Pts',(-0.476575327105888,-1.8962368089089,
9.47348832161808));
#280922=CARTESIAN_POINT('Ctrl Pts',(-0.542971859168175,-1.87829867899792,
9.46957987321322));
#280923=CARTESIAN_POINT('Ctrl Pts',(-0.608181054045808,-1.85694151913832,
9.46567142480836));
#280924=CARTESIAN_POINT('Ctrl Pts',(-0.673429281264656,-1.8355715754995,
9.46176063691914));
#280925=CARTESIAN_POINT('Ctrl Pts',(-0.737488298079319,-1.81077870649935,
9.45784984902991));
#280926=CARTESIAN_POINT('Ctrl Pts',(-0.799986080817993,-1.78273337055698,
9.45393906114068));
#280927=CARTESIAN_POINT('Ctrl Pts',(-0.862591778313896,-1.75463960880675,
9.45002152050428));
#280928=CARTESIAN_POINT('Ctrl Pts',(-0.923630424102178,-1.72328239607513,
9.44610397986789));
#280929=CARTESIAN_POINT('Ctrl Pts',(-0.982754956533872,-1.68887793976004,
9.44218643923149));
#280930=CARTESIAN_POINT('Ctrl Pts',(-1.01066018500859,-1.6726399388062,
9.44033746280797));
#280931=CARTESIAN_POINT('Ctrl Pts',(-1.03813945426592,-1.65572375887166,
9.43848848638446));
#280932=CARTESIAN_POINT('Ctrl Pts',(-1.06515874540712,-1.63815531836353,
9.43663950996094));
#280933=CARTESIAN_POINT('Ctrl Pts',(-1.12238295685082,-1.60094708262117,
9.43272355904791));
#280934=CARTESIAN_POINT('Ctrl Pts',(-1.1777692421661,-1.56066262208641,
9.42880760813489));
#280935=CARTESIAN_POINT('Ctrl Pts',(-1.23096726891726,-1.51750966483063,
9.42489165722186));
#280936=CARTESIAN_POINT('Ctrl Pts',(-1.28408516591199,-1.47442170690219,
9.42098160472672));
#280937=CARTESIAN_POINT('Ctrl Pts',(-1.33502096627577,-1.42847413475499,
9.41707155223158));
#280938=CARTESIAN_POINT('Ctrl Pts',(-1.38345288580186,-1.37991815437239,
9.41316149973645));
#280939=CARTESIAN_POINT('Ctrl Pts',(-1.43182791638115,-1.33141920866056,
9.4092560400547));
#280940=CARTESIAN_POINT('Ctrl Pts',(-1.47770456085395,-1.28031828647394,
9.40535058037296));
#280941=CARTESIAN_POINT('Ctrl Pts',(-1.52079516373974,-1.22690589286457,
9.40144512069121));
#280942=CARTESIAN_POINT('Ctrl Pts',(-1.5638588372244,-1.17352687924241,
9.39754210172004));
#280943=CARTESIAN_POINT('Ctrl Pts',(-1.60413961432025,-1.11783964209058,
9.39363908274887));
#280944=CARTESIAN_POINT('Ctrl Pts',(-1.64138876046339,-1.06016929639773,
9.38973606377771));
#280945=CARTESIAN_POINT('Ctrl Pts',(-1.67862744266192,-1.00251515132597,
9.38583414123367));
#280946=CARTESIAN_POINT('Ctrl Pts',(-1.71283591744884,-0.942879417137435,
9.38193221868963));
#280947=CARTESIAN_POINT('Ctrl Pts',(-1.7438086567614,-0.881616338666651,
9.3780302961456));
#280948=CARTESIAN_POINT('Ctrl Pts',(-1.77478335054919,-0.820349394306968,
9.37412812737823));
#280949=CARTESIAN_POINT('Ctrl Pts',(-1.80252168363909,-0.757455342500285,
9.37022595861086));
#280950=CARTESIAN_POINT('Ctrl Pts',(-1.82686482955528,-0.693311542190061,
9.3663237898435));
#280951=CARTESIAN_POINT('Ctrl Pts',(-1.85123394068469,-0.629099323958101,
9.36241745889248));
#280952=CARTESIAN_POINT('Ctrl Pts',(-1.87220046275567,-0.563635158397182,
9.35851112794145));
#280953=CARTESIAN_POINT('Ctrl Pts',(-1.88965470883647,-0.497313866056611,
9.35460479699043));
#280954=CARTESIAN_POINT('Ctrl Pts',(-1.90711949726443,-0.430952515721802,
9.35069610661942));
#280955=CARTESIAN_POINT('Ctrl Pts',(-1.9210676880021,-0.363733490610373,
9.34678741624842));
#280956=CARTESIAN_POINT('Ctrl Pts',(-1.93144082198622,-0.296061397627586,
9.34287872587741));
#280957=CARTESIAN_POINT('Ctrl Pts',(-1.94183178681567,-0.228272980048507,
9.33896331668318));
#280958=CARTESIAN_POINT('Ctrl Pts',(-1.94863538206911,-0.160030430071143,
9.33504790748895));
#280959=CARTESIAN_POINT('Ctrl Pts',(-1.95184512111298,-0.0917421559996565,
9.33113249829473));
#280960=CARTESIAN_POINT('Ctrl Pts',(-1.95328321978465,-0.061146124705292,
9.32937822958805));
#280961=CARTESIAN_POINT('Ctrl Pts',(-1.95400058020809,-0.0305408923189653,
9.32762396088137));
#280962=CARTESIAN_POINT('Ctrl Pts',(-1.95399999964781,3.70990612790232E-5,
9.32586969217469));
#280963=CARTESIAN_POINT('',(-1.95399927652111,-0.00168147404713564,8.62586971137284));
#280964=CARTESIAN_POINT('Ctrl Pts',(-1.9539999996478,3.7099940636846E-5,
9.32586969212423));
#280965=CARTESIAN_POINT('Ctrl Pts',(-1.95399996193804,0.00202321828658315,
9.32575574790799));
#280966=CARTESIAN_POINT('Ctrl Pts',(-1.95399689608245,0.00400933322525912,
9.32564180369175));
#280967=CARTESIAN_POINT('Ctrl Pts',(-1.95399080210547,0.00599543886719613,
9.32552785947551));
#280968=CARTESIAN_POINT('Ctrl Pts',(-1.95378125295234,0.0742902087533993,
9.32160974260204));
#280969=CARTESIAN_POINT('Ctrl Pts',(-1.94998647820361,0.142709361266959,
9.31769162572858));
#280970=CARTESIAN_POINT('Ctrl Pts',(-1.94259109676834,0.210845513958356,
9.31377350885511));
#280971=CARTESIAN_POINT('Ctrl Pts',(-1.93520685155423,0.278879064874356,
9.30986129201755));
#280972=CARTESIAN_POINT('Ctrl Pts',(-1.92423281289038,0.346629976652652,
9.30594907517999));
#280973=CARTESIAN_POINT('Ctrl Pts',(-1.90970561062772,0.413691286755018,
9.30203685834243));
#280974=CARTESIAN_POINT('Ctrl Pts',(-1.89519549147666,0.480673736810946,
9.29812924203536));
#280975=CARTESIAN_POINT('Ctrl Pts',(-1.87714061055141,0.546967717256504,
9.29422162572828));
#280976=CARTESIAN_POINT('Ctrl Pts',(-1.85562912332395,0.612173632780749,
9.29031400942121));
#280977=CARTESIAN_POINT('Ctrl Pts',(-1.83413111862874,0.677338679868087,
9.28640884225037));
#280978=CARTESIAN_POINT('Ctrl Pts',(-1.80918095895894,0.741416548748044,
9.28250367507953));
#280979=CARTESIAN_POINT('Ctrl Pts',(-1.78091698643134,0.804021571501862,
9.2785985079087));
#280980=CARTESIAN_POINT('Ctrl Pts',(-1.75266103454561,0.866608828442106,
9.27469444893124));
#280981=CARTESIAN_POINT('Ctrl Pts',(-1.72109333892136,0.927723620876592,
9.27079038995378));
#280982=CARTESIAN_POINT('Ctrl Pts',(-1.68640015220877,0.987000773368607,
9.26688633097632));
#280983=CARTESIAN_POINT('Ctrl Pts',(-1.65170491178014,1.04628143486198,
9.26298204089215));
#280984=CARTESIAN_POINT('Ctrl Pts',(-1.61388406360739,1.10372381722284,
9.25907775080797));
#280985=CARTESIAN_POINT('Ctrl Pts',(-1.57316861808235,1.15898943009886,
9.2551734607238));
#280986=CARTESIAN_POINT('Ctrl Pts',(-1.5324098040119,1.21431390980565,9.25126501193819));
#280987=CARTESIAN_POINT('Ctrl Pts',(-1.48875053175819,1.26745659602186,
9.24735656315258));
#280988=CARTESIAN_POINT('Ctrl Pts',(-1.44246315346738,1.31811078854887,
9.24344811436696));
#280989=CARTESIAN_POINT('Ctrl Pts',(-1.39614806910291,1.36879530097824,
9.23953732611487));
#280990=CARTESIAN_POINT('Ctrl Pts',(-1.34720209849604,1.41698801013024,
9.23562653786278));
#280991=CARTESIAN_POINT('Ctrl Pts',(-1.29593362662677,1.46241992443279,
9.23171574961069));
#280992=CARTESIAN_POINT('Ctrl Pts',(-1.24457663004418,1.5079302855281,9.22779820864301));
#280993=CARTESIAN_POINT('Ctrl Pts',(-1.19088951303049,1.5506700313444,9.22388066767533));
#280994=CARTESIAN_POINT('Ctrl Pts',(-1.13521209408202,1.59041173959762,
9.21996312670766));
#280995=CARTESIAN_POINT('Ctrl Pts',(-1.10893386970745,1.60916874281778,
9.21811415413513));
#280996=CARTESIAN_POINT('Ctrl Pts',(-1.08221268097153,1.62725855388008,
9.2162651815626));
#280997=CARTESIAN_POINT('Ctrl Pts',(-1.05508614414225,1.6446608247414,9.21441620899007));
#280998=CARTESIAN_POINT('Ctrl Pts',(-0.99760291608811,1.68153758165571,
9.21049809320841));
#280999=CARTESIAN_POINT('Ctrl Pts',(-0.938070067537558,1.71547013168315,
9.20657997742674));
#281000=CARTESIAN_POINT('Ctrl Pts',(-0.876821466214148,1.74622453206513,
9.20266186164508));
#281001=CARTESIAN_POINT('Ctrl Pts',(-0.815665095345652,1.77693262131058,
9.19874964591));
#281002=CARTESIAN_POINT('Ctrl Pts',(-0.752798535366085,1.80447184003791,
9.19483743017492));
#281003=CARTESIAN_POINT('Ctrl Pts',(-0.688583519414288,1.82865216396969,
9.19092521443984));
#281004=CARTESIAN_POINT('Ctrl Pts',(-0.624444016629962,1.85280405323049,
9.18701759924557));
#281005=CARTESIAN_POINT('Ctrl Pts',(-0.558959665258295,1.8736047196763,
9.18310998405131));
#281006=CARTESIAN_POINT('Ctrl Pts',(-0.492513964600165,1.89091141904475,
9.17920236885705));
#281007=CARTESIAN_POINT('Ctrl Pts',(-0.426109909535906,1.90820727124376,
9.17529720280477));
#281008=CARTESIAN_POINT('Ctrl Pts',(-0.358746175356759,1.92201337669609,
9.1713920367525));
#281009=CARTESIAN_POINT('Ctrl Pts',(-0.290821790346487,1.9322367055461,
9.16748687070022));
#281010=CARTESIAN_POINT('Ctrl Pts',(-0.222916680733751,1.94245713324762,
9.16358281284536));
#281011=CARTESIAN_POINT('Ctrl Pts',(-0.154451722304109,1.94909672951791,
9.1596787549905));
#281012=CARTESIAN_POINT('Ctrl Pts',(-0.085834722571209,1.95211382875106,
9.15577469713565));
#281013=CARTESIAN_POINT('Ctrl Pts',(-0.0172136609901176,1.95513110658425,
9.15187040817639));
#281014=CARTESIAN_POINT('Ctrl Pts',(0.0515589682466065,1.95452544260284,
9.14796611921714));
#281015=CARTESIAN_POINT('Ctrl Pts',(0.120073490884842,1.95030724676568,
9.14406183025789));
#281016=CARTESIAN_POINT('Ctrl Pts',(0.188660992684123,1.94608455786076,
9.14015338259298));
#281017=CARTESIAN_POINT('Ctrl Pts',(0.256989347325235,1.93824168809354,
9.13624493492807));
#281018=CARTESIAN_POINT('Ctrl Pts',(0.324653155537779,1.92684102317741,
9.13233648726316));
#281019=CARTESIAN_POINT('Ctrl Pts',(0.392357465063601,1.91543353420106,
9.128425700131));
#281020=CARTESIAN_POINT('Ctrl Pts',(0.459395956391263,1.90046411903233,
9.12451491299884));
#281021=CARTESIAN_POINT('Ctrl Pts',(0.525375357239391,1.88204589051531,
9.12060412586668));
#281022=CARTESIAN_POINT('Ctrl Pts',(0.591468684253714,1.86359585937299,
9.11668658600596));
#281023=CARTESIAN_POINT('Ctrl Pts',(0.656498805063163,1.84168528654545,
9.11276904614524));
#281024=CARTESIAN_POINT('Ctrl Pts',(0.720090312766324,1.81647624302111,
9.10885150628451));
#281025=CARTESIAN_POINT('Ctrl Pts',(0.750103942494326,1.80457819365156,
9.10700252369122));
#281026=CARTESIAN_POINT('Ctrl Pts',(0.779797435246854,1.79194605366362,
9.10515354109793));
#281027=CARTESIAN_POINT('Ctrl Pts',(0.809133289056376,1.77860038247517,
9.10330455850463));
#281028=CARTESIAN_POINT('Ctrl Pts',(0.871297889362895,1.7503200289992,9.09938644299205));
#281029=CARTESIAN_POINT('Ctrl Pts',(0.93210127792186,1.71872057975743,9.09546832747948));
#281030=CARTESIAN_POINT('Ctrl Pts',(0.991165798830189,1.6839555692563,9.0915502119669));
#281031=CARTESIAN_POINT('Ctrl Pts',(1.05014137802159,1.64924290929786,9.0876379965093));
#281032=CARTESIAN_POINT('Ctrl Pts',(1.1073828657791,1.611374396046,9.0837257810517));
#281033=CARTESIAN_POINT('Ctrl Pts',(1.1625343808032,1.57055079938553,9.07981356559411));
#281034=CARTESIAN_POINT('Ctrl Pts',(1.21762104065478,1.52977520904733,9.07590595068843));
#281035=CARTESIAN_POINT('Ctrl Pts',(1.27062221530796,1.48605172799656,9.07199833578276));
#281036=CARTESIAN_POINT('Ctrl Pts',(1.32120993095599,1.4396250617238,9.06809072087708));
#281037=CARTESIAN_POINT('Ctrl Pts',(1.37176594009198,1.39322749397099,9.06418555512013));
#281038=CARTESIAN_POINT('Ctrl Pts',(1.41991112929024,1.34413043370474,9.06028038936318));
#281039=CARTESIAN_POINT('Ctrl Pts',(1.46535086112881,1.29261860337419,9.05637522360622));
#281040=CARTESIAN_POINT('Ctrl Pts',(1.5107776981295,1.24112139101507,9.05247116605298));
#281041=CARTESIAN_POINT('Ctrl Pts',(1.55350027665158,1.18721113765168,9.04856710849973));
#281042=CARTESIAN_POINT('Ctrl Pts',(1.59326234360062,1.13120780781617,9.04466305094648));
#281043=CARTESIAN_POINT('Ctrl Pts',(1.63302676424328,1.07520116289444,9.04075876229471));
#281044=CARTESIAN_POINT('Ctrl Pts',(1.66983004272211,1.01710159807387,9.03685447364293));
#281045=CARTESIAN_POINT('Ctrl Pts',(1.70345865811394,0.957258899199503,
9.03295018499115));
#281046=CARTESIAN_POINT('Ctrl Pts',(1.7371230934199,0.897352458172525,9.02904173764052));
#281047=CARTESIAN_POINT('Ctrl Pts',(1.767605875719,0.835699607288608,9.02513329028989));
#281048=CARTESIAN_POINT('Ctrl Pts',(1.79473946456196,0.772674740329891,
9.02122484293926));
#281049=CARTESIAN_POINT('Ctrl Pts',(1.82188929464314,0.709612148841472,
9.01731405612572));
#281050=CARTESIAN_POINT('Ctrl Pts',(1.84568577109271,0.645176368338531,
9.01340326931219));
#281051=CARTESIAN_POINT('Ctrl Pts',(1.86601054510086,0.579759127200589,
9.00949248249866));
#281052=CARTESIAN_POINT('Ctrl Pts',(1.88637041373818,0.514228930621264,
9.00557494295996));
#281053=CARTESIAN_POINT('Ctrl Pts',(1.9032464948483,0.447714367617182,9.00165740342125));
#281054=CARTESIAN_POINT('Ctrl Pts',(1.91657125858195,0.380618721002536,
8.99773986388255));
#281055=CARTESIAN_POINT('Ctrl Pts',(1.92286022946874,0.348951175023886,
8.99589087859476));
#281056=CARTESIAN_POINT('Ctrl Pts',(1.92835885313605,0.31715427767523,8.99404189330698));
#281057=CARTESIAN_POINT('Ctrl Pts',(1.9330640536675,0.285270686223748,8.99219290801919));
#281058=CARTESIAN_POINT('Ctrl Pts',(1.94303466914674,0.217707353197879,
8.98827479205196));
#281059=CARTESIAN_POINT('Ctrl Pts',(1.94947863363781,0.149486727575227,
8.98435667608473));
#281060=CARTESIAN_POINT('Ctrl Pts',(1.95232002632467,0.0810093501494835,
8.98043856011751));
#281061=CARTESIAN_POINT('Ctrl Pts',(1.95515714033493,0.0126350885491758,
8.97652634419752));
#281062=CARTESIAN_POINT('Ctrl Pts',(1.95440242879606,-0.0559946700335427,
8.97261412827754));
#281063=CARTESIAN_POINT('Ctrl Pts',(1.95003146360188,-0.124472048921536,
8.96870191235756));
#281064=CARTESIAN_POINT('Ctrl Pts',(1.94566563841341,-0.19286890231836,
8.96479429698032));
#281065=CARTESIAN_POINT('Ctrl Pts',(1.93769203630091,-0.261113243337137,
8.96088668160308));
#281066=CARTESIAN_POINT('Ctrl Pts',(1.92613827731413,-0.328796801482873,
8.95697906622584));
#281067=CARTESIAN_POINT('Ctrl Pts',(1.9145917597799,-0.396437938172902,
8.9530738999919));
#281068=CARTESIAN_POINT('Ctrl Pts',(1.89946961914804,-0.463518505430738,
8.94916873375795));
#281069=CARTESIAN_POINT('Ctrl Pts',(1.88085117725033,-0.529636525398369,
8.94526356752401));
#281070=CARTESIAN_POINT('Ctrl Pts',(1.86223801885084,-0.595735782547756,
8.94135950948908));
#281071=CARTESIAN_POINT('Ctrl Pts',(1.84013066208068,-0.660872561411314,
8.93745545145414));
#281072=CARTESIAN_POINT('Ctrl Pts',(1.81465885824272,-0.724658007753471,
8.93355139341921));
#281073=CARTESIAN_POINT('Ctrl Pts',(1.78918554658959,-0.788447229904536,
8.92964710428176));
#281074=CARTESIAN_POINT('Ctrl Pts',(1.76034757726571,-0.850884504869678,
8.92574281514431));
#281075=CARTESIAN_POINT('Ctrl Pts',(1.72832293633162,-0.911600695343118,
8.92183852600686));
#281076=CARTESIAN_POINT('Ctrl Pts',(1.69626418395759,-0.972381558413157,
8.91793007816784));
#281077=CARTESIAN_POINT('Ctrl Pts',(1.66101221587393,-1.03143724251754,
8.91402163032883));
#281078=CARTESIAN_POINT('Ctrl Pts',(1.62279063585553,-1.08842388442169,
8.91011318248981));
#281079=CARTESIAN_POINT('Ctrl Pts',(1.58454617768734,-1.14544463660933,
8.90620239518563));
#281080=CARTESIAN_POINT('Ctrl Pts',(1.54332886520718,-1.20039348829709,
8.90229160788145));
#281081=CARTESIAN_POINT('Ctrl Pts',(1.49940355228453,-1.25295849388419,
8.89838082057726));
#281082=CARTESIAN_POINT('Ctrl Pts',(1.45540239389377,-1.30561426302401,
8.89446328054956));
#281083=CARTESIAN_POINT('Ctrl Pts',(1.40868423744711,-1.35587761076023,
8.89054574052185));
#281084=CARTESIAN_POINT('Ctrl Pts',(1.3595512142975,-1.40347301210326,8.88662820049415));
#281085=CARTESIAN_POINT('Ctrl Pts',(1.33636165529235,-1.4259368520436,8.88477921950735));
#281086=CARTESIAN_POINT('Ctrl Pts',(1.31263464328404,-1.44780695906798,
8.88293023852055));
#281087=CARTESIAN_POINT('Ctrl Pts',(1.28840434253463,-1.46905760613323,
8.88108125753375));
#281088=CARTESIAN_POINT('Ctrl Pts',(1.23705869622743,-1.51408916472988,
8.87716314175142));
#281089=CARTESIAN_POINT('Ctrl Pts',(1.18324754855695,-1.55651484513038,
8.87324502596909));
#281090=CARTESIAN_POINT('Ctrl Pts',(1.12726617493087,-1.59605356139972,
8.86932691018676));
#281091=CARTESIAN_POINT('Ctrl Pts',(1.07136910020881,-1.63553273875044,
8.86541469445377));
#281092=CARTESIAN_POINT('Ctrl Pts',(1.01330868391549,-1.67213329834028,
8.86150247872078));
#281093=CARTESIAN_POINT('Ctrl Pts',(0.953414300781563,-1.70561342955114,
8.85759026298778));
#281094=CARTESIAN_POINT('Ctrl Pts',(0.893590350061986,-1.73905419001719,
8.8536826477997));
#281095=CARTESIAN_POINT('Ctrl Pts',(0.831937142946086,-1.76938157081715,
8.84977503261162));
#281096=CARTESIAN_POINT('Ctrl Pts',(0.768812623306882,-1.79639726960491,
8.84586741742354));
#281097=CARTESIAN_POINT('Ctrl Pts',(0.705727667714937,-1.82339603598052,
8.84196225137998));
#281098=CARTESIAN_POINT('Ctrl Pts',(0.641173680069429,-1.8470870446482,
8.83805708533643));
#281099=CARTESIAN_POINT('Ctrl Pts',(0.575531368650073,-1.8673188382544,
8.83415191929288));
#281100=CARTESIAN_POINT('Ctrl Pts',(0.509907685070244,-1.88754489052401,
8.83024786144928));
#281101=CARTESIAN_POINT('Ctrl Pts',(0.443196760660883,-1.90431353166343,
8.82634380360568));
#281102=CARTESIAN_POINT('Ctrl Pts',(0.375795639602714,-1.91752278663269,
8.82243974576208));
#281103=CARTESIAN_POINT('Ctrl Pts',(0.308390528715172,-1.93073282352772,
8.81853545681662));
#281104=CARTESIAN_POINT('Ctrl Pts',(0.240295623253851,-1.94038296385983,
8.81463116787115));
#281105=CARTESIAN_POINT('Ctrl Pts',(0.171917574008792,-1.94642244842864,
8.81072687892569));
#281106=CARTESIAN_POINT('Ctrl Pts',(0.103466691034717,-1.9524683660295,
8.80681843127833));
#281107=CARTESIAN_POINT('Ctrl Pts',(0.0347325533016588,-1.9548959092115,
8.80290998363097));
#281108=CARTESIAN_POINT('Ctrl Pts',(-0.0338746698053916,-1.95370635120675,
8.79900153598361));
#281109=CARTESIAN_POINT('Ctrl Pts',(-0.10252295888464,-1.95251608117265,
8.79509074887118));
#281110=CARTESIAN_POINT('Ctrl Pts',(-0.171043691411102,-1.94770443551453,
8.79117996175874));
#281111=CARTESIAN_POINT('Ctrl Pts',(-0.239031129806031,-1.93932465538487,
8.78726917464631));
#281112=CARTESIAN_POINT('Ctrl Pts',(-0.30713596157698,-1.93093040595466,
8.78335163480847));
#281113=CARTESIAN_POINT('Ctrl Pts',(-0.374705177301888,-1.91895581133413,
8.77943409497064));
#281114=CARTESIAN_POINT('Ctrl Pts',(-0.441343409147208,-1.90350518654463,
8.7755165551328));
#281115=CARTESIAN_POINT('Ctrl Pts',(-0.472795019748818,-1.8962128706927,
8.77366757243798));
#281116=CARTESIAN_POINT('Ctrl Pts',(-0.50403946831885,-1.88814695237618,
8.77181858974315));
#281117=CARTESIAN_POINT('Ctrl Pts',(-0.535036607739613,-1.87932217258736,
8.76996960704832));
#281118=CARTESIAN_POINT('Ctrl Pts',(-0.600721581909144,-1.86062188464751,
8.76605149128606));
#281119=CARTESIAN_POINT('Ctrl Pts',(-0.665555182560461,-1.83843670633144,
8.76213337552379));
#281120=CARTESIAN_POINT('Ctrl Pts',(-0.729141090117285,-1.81286217642229,
8.75821525976153));
#281121=CARTESIAN_POINT('Ctrl Pts',(-0.792631247554809,-1.78732615762958,
8.75430304404954));
#281122=CARTESIAN_POINT('Ctrl Pts',(-0.854876988018642,-1.75841109858282,
8.75039082833756));
#281123=CARTESIAN_POINT('Ctrl Pts',(-0.915496483997269,-1.726262490987,
8.74647861262558));
#281124=CARTESIAN_POINT('Ctrl Pts',(-0.976044694849279,-1.69415168835023,
8.7425709974598));
#281125=CARTESIAN_POINT('Ctrl Pts',(-1.03497002672235,-1.65881511829838,
8.73866338229403));
#281126=CARTESIAN_POINT('Ctrl Pts',(-1.09191170032944,-1.6204458765055,
8.73475576712825));
#281127=CARTESIAN_POINT('Ctrl Pts',(-1.14881768505016,-1.5821006831015,
8.7308506011078));
#281128=CARTESIAN_POINT('Ctrl Pts',(-1.20374207078221,-1.54072686271804,
8.72694543508734));
#281129=CARTESIAN_POINT('Ctrl Pts',(-1.25635107871759,-1.49656204916641,
8.72304026906689));
#281130=CARTESIAN_POINT('Ctrl Pts',(-1.30894515736708,-1.45240976862298,
8.71913621124715));
#281131=CARTESIAN_POINT('Ctrl Pts',(-1.35922478603156,-1.40546838332545,
8.7152321534274));
#281132=CARTESIAN_POINT('Ctrl Pts',(-1.40688888954281,-1.35601609595204,
8.71132809560766));
#281133=CARTESIAN_POINT('Ctrl Pts',(-1.45455581453592,-1.30656088124502,
8.70742380668678));
#281134=CARTESIAN_POINT('Ctrl Pts',(-1.4996065674896,-1.25459482530796,
8.70351951776591));
#281135=CARTESIAN_POINT('Ctrl Pts',(-1.54177788401154,-1.20043198739992,
8.69961522884503));
#281136=CARTESIAN_POINT('Ctrl Pts',(-1.58399411982558,-1.14621145728451,
8.6957067812232));
#281137=CARTESIAN_POINT('Ctrl Pts',(-1.62332449552704,-1.08978986428043,
8.69179833360136));
#281138=CARTESIAN_POINT('Ctrl Pts',(-1.65954754646575,-1.03151245315775,
8.68788988597952));
#281139=CARTESIAN_POINT('Ctrl Pts',(-1.69579227929716,-0.973200159148551,
8.68397909889318));
#281140=CARTESIAN_POINT('Ctrl Pts',(-1.72892574844505,-0.913030267195515,
8.68006831180683));
#281141=CARTESIAN_POINT('Ctrl Pts',(-1.7587725482376,-0.851372494015285,
8.67615752472049));
#281142=CARTESIAN_POINT('Ctrl Pts',(-1.78867088426062,-0.789608256851292,
8.67223998490937));
#281143=CARTESIAN_POINT('Ctrl Pts',(-1.8152710338404,-0.726351464104802,
8.66832244509824));
#281144=CARTESIAN_POINT('Ctrl Pts',(-1.8384461208373,-0.661990831340053,
8.66440490528712));
#281145=CARTESIAN_POINT('Ctrl Pts',(-1.84938419468375,-0.631614187917754,
8.66255592237904));
#281146=CARTESIAN_POINT('Ctrl Pts',(-1.8595600260523,-0.600991854473024,
8.66070693947096));
#281147=CARTESIAN_POINT('Ctrl Pts',(-1.86896421628828,-0.570165553356156,
8.65885795656288));
#281148=CARTESIAN_POINT('Ctrl Pts',(-1.89332618263693,-0.490308671304903,
8.65406808542506));
#281149=CARTESIAN_POINT('Ctrl Pts',(-1.91258486915543,-0.408826904120657,
8.64927821428725));
#281150=CARTESIAN_POINT('Ctrl Pts',(-1.92656107311205,-0.326310330160359,
8.64448834314944));
#281151=CARTESIAN_POINT('Ctrl Pts',(-1.94033992247678,-0.244958952760407,
8.63976610862214));
#281152=CARTESIAN_POINT('Ctrl Pts',(-1.94898437599119,-0.162601767940379,
8.63504387409485));
#281153=CARTESIAN_POINT('Ctrl Pts',(-1.95236880609761,-0.0798250898965604,
8.63032163956755));
#281154=CARTESIAN_POINT('Ctrl Pts',(-1.9534323731954,-0.0538122757850696,
8.62883766350265));
#281155=CARTESIAN_POINT('Ctrl Pts',(-1.95397683673528,-0.0277581924780917,
8.62735368743774));
#281156=CARTESIAN_POINT('Ctrl Pts',(-1.95399927652111,-0.00168147404713564,
8.62586971137284));
#281157=CARTESIAN_POINT('',(-1.95392510023955,0.000982308602275455,7.92586964531847));
#281158=CARTESIAN_POINT('Ctrl Pts',(-1.95279013340439,-0.00168009551267251,
8.62586969212423));
#281159=CARTESIAN_POINT('Ctrl Pts',(-1.94903607268958,0.455640131522026,
8.59982856344197));
#281160=CARTESIAN_POINT('Ctrl Pts',(-1.56070656660671,1.56913066960483,
8.53675021793123));
#281161=CARTESIAN_POINT('Ctrl Pts',(0.294270353677477,2.29051751091558,
8.43663465559201));
#281162=CARTESIAN_POINT('Ctrl Pts',(2.08375418707712,0.995506903268704,
8.32552300510657));
#281163=CARTESIAN_POINT('Ctrl Pts',(1.96677879493936,-1.21030850518367,
8.21441135462113));
#281164=CARTESIAN_POINT('Ctrl Pts',(0.050366789813365,-2.30879377455664,
8.1032997041357));
#281165=CARTESIAN_POINT('Ctrl Pts',(-1.64840826021826,-1.43117012984314,
8.00711914997006));
#281166=CARTESIAN_POINT('Ctrl Pts',(-1.94951814111497,-0.387989405753114,
7.94797581263291));
#281167=CARTESIAN_POINT('Ctrl Pts',(-1.95128545551857,0.000980157954364874,
7.92586969212424));
#281168=CARTESIAN_POINT('',(-1.95399967105378,0.00113380850773978,7.22586969217444));
#281169=CARTESIAN_POINT('Ctrl Pts',(-1.95399975305789,0.00098236942558494,
7.92586964399473));
#281170=CARTESIAN_POINT('Ctrl Pts',(-1.95396158680754,0.0768976430830345,
7.92156116990685));
#281171=CARTESIAN_POINT('Ctrl Pts',(-1.94949516076616,0.152661436815141,
7.91725269581898));
#281172=CARTESIAN_POINT('Ctrl Pts',(-1.94067802404546,0.227782367594661,
7.9129442217311));
#281173=CARTESIAN_POINT('Ctrl Pts',(-1.93182936676887,0.303171849670571,
7.90862034519426));
#281174=CARTESIAN_POINT('Ctrl Pts',(-1.91859897376203,0.377913573292325,
7.90429646865743));
#281175=CARTESIAN_POINT('Ctrl Pts',(-1.90111518072707,0.451527484887769,
7.89997259212059));
#281176=CARTESIAN_POINT('Ctrl Pts',(-1.88354776221016,0.525493493927039,
7.89562803435866));
#281177=CARTESIAN_POINT('Ctrl Pts',(-1.86168630271332,0.59832059449387,
7.89128347659673));
#281178=CARTESIAN_POINT('Ctrl Pts',(-1.83570921630156,0.66954288375391,
7.8869389188348));
#281179=CARTESIAN_POINT('Ctrl Pts',(-1.82402478376978,0.701578502392081,
7.88498474694481));
#281180=CARTESIAN_POINT('Ctrl Pts',(-1.81150831947543,0.733289747289453,
7.88303057505482));
#281181=CARTESIAN_POINT('Ctrl Pts',(-1.79817909327187,0.764635827384474,
7.88107640316483));
#281182=CARTESIAN_POINT('Ctrl Pts',(-1.77145398682494,0.827484736574002,
7.8771582873659));
#281183=CARTESIAN_POINT('Ctrl Pts',(-1.74137694789808,0.889055425517929,
7.87324017156697));
#281184=CARTESIAN_POINT('Ctrl Pts',(-1.70809206844313,0.948966535617398,
7.86932205576804));
#281185=CARTESIAN_POINT('Ctrl Pts',(-1.67485731064044,1.00878742926193,
7.86540984001865));
#281186=CARTESIAN_POINT('Ctrl Pts',(-1.63842453608282,1.06695327728761,
7.86149762426926));
#281187=CARTESIAN_POINT('Ctrl Pts',(-1.59898559917462,1.12310331387286,
7.85758540851987));
#281188=CARTESIAN_POINT('Ctrl Pts',(-1.55959304023405,1.17918732117883,
7.85367779331577));
#281189=CARTESIAN_POINT('Ctrl Pts',(-1.51720162104138,1.23325982424866,
7.84977017811167));
#281190=CARTESIAN_POINT('Ctrl Pts',(-1.47204781227257,1.28498686311711,
7.84586256290757));
#281191=CARTESIAN_POINT('Ctrl Pts',(-1.42692230419587,1.33668148144251,
7.84195739684824));
#281192=CARTESIAN_POINT('Ctrl Pts',(-1.37903816375647,1.3860331819478,7.83805223078891));
#281193=CARTESIAN_POINT('Ctrl Pts',(-1.32867269552391,1.43274033522101,
7.83414706472959));
#281194=CARTESIAN_POINT('Ctrl Pts',(-1.27832151990334,1.47943423403155,
7.83024300687048));
#281195=CARTESIAN_POINT('Ctrl Pts',(-1.22549077483517,1.523484741101,7.82633894901138));
#281196=CARTESIAN_POINT('Ctrl Pts',(-1.17049395096475,1.56462772273628,
7.82243489115228));
#281197=CARTESIAN_POINT('Ctrl Pts',(-1.11549387154516,1.60577313983948,
7.81853060219161));
#281198=CARTESIAN_POINT('Ctrl Pts',(-1.05832785415725,1.64401039721329,
7.81462631323094));
#281199=CARTESIAN_POINT('Ctrl Pts',(-0.999340264593367,1.67911733823532,
7.81072202427027));
#281200=CARTESIAN_POINT('Ctrl Pts',(-0.940289843673999,1.71426167384675,
7.80681357660826));
#281201=CARTESIAN_POINT('Ctrl Pts',(-0.879414401895716,1.74626878683899,
7.80290512894625));
#281202=CARTESIAN_POINT('Ctrl Pts',(-0.817084049245728,1.77496187465202,
7.79899668128424));
#281203=CARTESIAN_POINT('Ctrl Pts',(-0.754716387751583,1.80367213717843,
7.79508589415745));
#281204=CARTESIAN_POINT('Ctrl Pts',(-0.690892539313103,1.829064244814,7.79117510703066));
#281205=CARTESIAN_POINT('Ctrl Pts',(-0.626001166910012,1.85101014017409,
7.78726431990388));
#281206=CARTESIAN_POINT('Ctrl Pts',(-0.560997747094305,1.8729939293358,
7.7833467800523));
#281207=CARTESIAN_POINT('Ctrl Pts',(-0.49492359777793,1.89151949716494,
7.77942924020072));
#281208=CARTESIAN_POINT('Ctrl Pts',(-0.42818019704342,1.90650930206487,
7.77551170034915));
#281209=CARTESIAN_POINT('Ctrl Pts',(-0.396678951771866,1.91358412168042,
7.77366271779256));
#281210=CARTESIAN_POINT('Ctrl Pts',(-0.365028733820059,1.91987205894661,
7.77181373523598));
#281211=CARTESIAN_POINT('Ctrl Pts',(-0.333272110538601,1.92536897771236,
7.76996475267939));
#281212=CARTESIAN_POINT('Ctrl Pts',(-0.26597773452622,1.93701731056733,
7.76604663688034));
#281213=CARTESIAN_POINT('Ctrl Pts',(-0.197938535201442,1.9451564360216,
7.7621285210813));
#281214=CARTESIAN_POINT('Ctrl Pts',(-0.129553040639174,1.94970049229648,
7.75821040528225));
#281215=CARTESIAN_POINT('Ctrl Pts',(-0.0612705235860549,1.95423770595657,
7.75429818953274));
#281216=CARTESIAN_POINT('Ctrl Pts',(0.00735676693203037,1.95519056215335,
7.75038597378324));
#281217=CARTESIAN_POINT('Ctrl Pts',(0.0759216882150816,1.9525244933825,
7.74647375803373));
#281218=CARTESIAN_POINT('Ctrl Pts',(0.144405981013923,1.9498615597583,7.74256614282951));
#281219=CARTESIAN_POINT('Ctrl Pts',(0.212827561055752,1.94358817197773,
7.73865852762529));
#281220=CARTESIAN_POINT('Ctrl Pts',(0.28077759711522,1.93372178478658,7.73475091242108));
#281221=CARTESIAN_POINT('Ctrl Pts',(0.34868504467321,1.92386158147214,7.73084574636164));
#281222=CARTESIAN_POINT('Ctrl Pts',(0.41612104883496,1.91041291643297,7.7269405803022));
#281223=CARTESIAN_POINT('Ctrl Pts',(0.482681782852538,1.89344508674065,
7.72303541424276));
#281224=CARTESIAN_POINT('Ctrl Pts',(0.549223628397983,1.87648207214514,
7.71913135638355));
#281225=CARTESIAN_POINT('Ctrl Pts',(0.614890220468014,1.85600199685958,
7.71522729852433));
#281226=CARTESIAN_POINT('Ctrl Pts',(0.679289597316019,1.83212489830203,
7.71132324066511));
#281227=CARTESIAN_POINT('Ctrl Pts',(0.743692786299331,1.80824638633438,
7.70741895170433));
#281228=CARTESIAN_POINT('Ctrl Pts',(0.806828150826173,1.78097062526735,
7.70351466274355));
#281229=CARTESIAN_POINT('Ctrl Pts',(0.868322240017641,1.75046636285612,
7.69961037378277));
#281230=CARTESIAN_POINT('Ctrl Pts',(0.92988183039347,1.71992960845515,7.69570192612065));
#281231=CARTESIAN_POINT('Ctrl Pts',(0.989796215028153,1.68615770877636,
7.69179347845853));
#281232=CARTESIAN_POINT('Ctrl Pts',(1.04771607443799,1.64936564392625,7.68788503079641));
#281233=CARTESIAN_POINT('Ctrl Pts',(1.10567060271965,1.61255155658863,7.68397424366951));
#281234=CARTESIAN_POINT('Ctrl Pts',(1.16162782902405,1.57271399159945,7.68006345654261));
#281235=CARTESIAN_POINT('Ctrl Pts',(1.21526931542516,1.53010996042313,7.67615266941572));
#281236=CARTESIAN_POINT('Ctrl Pts',(1.26900342415086,1.48743236520768,7.67223512956403));
#281237=CARTESIAN_POINT('Ctrl Pts',(1.32041344416103,1.44197909564308,7.66831758971235));
#281238=CARTESIAN_POINT('Ctrl Pts',(1.36921641949976,1.3940453351926,7.66440004986067));
#281239=CARTESIAN_POINT('Ctrl Pts',(1.39225022476467,1.37142177799823,7.6625510673051));
#281240=CARTESIAN_POINT('Ctrl Pts',(1.41470385035661,1.34824616262135,7.66070208474953));
#281241=CARTESIAN_POINT('Ctrl Pts',(1.43655072720674,1.32455200281521,7.65885310219396));
#281242=CARTESIAN_POINT('Ctrl Pts',(1.48284569796856,1.2743425178176,7.65493498639478));
#281243=CARTESIAN_POINT('Ctrl Pts',(1.52659693240248,1.22160346688017,7.6510168705956));
#281244=CARTESIAN_POINT('Ctrl Pts',(1.56751608586576,1.16662304132573,7.64709875479642));
#281245=CARTESIAN_POINT('Ctrl Pts',(1.60837362169326,1.11172540741164,7.64318653904677));
#281246=CARTESIAN_POINT('Ctrl Pts',(1.64640724907164,1.05459348877088,7.63927432329713));
#281247=CARTESIAN_POINT('Ctrl Pts',(1.68136703821542,0.995550542565618,
7.63536210754748));
#281248=CARTESIAN_POINT('Ctrl Pts',(1.71628571661696,0.936577027538358,
7.63145449234313));
#281249=CARTESIAN_POINT('Ctrl Pts',(1.74813748613206,0.875697369287417,
7.62754687713877));
#281250=CARTESIAN_POINT('Ctrl Pts',(1.77671520105431,0.813264467650303,
7.62363926193441));
#281251=CARTESIAN_POINT('Ctrl Pts',(1.80527500455042,0.75087069658433,7.61973409587483));
#281252=CARTESIAN_POINT('Ctrl Pts',(1.83056461981158,0.686926059523024,
7.61582892981525));
#281253=CARTESIAN_POINT('Ctrl Pts',(1.85242316530533,0.621807379049321,
7.61192376375566));
#281254=CARTESIAN_POINT('Ctrl Pts',(1.87427550782471,0.556707177824659,
7.6080197058963));
#281255=CARTESIAN_POINT('Ctrl Pts',(1.89269855700926,0.490434060674127,
7.60411564803694));
#281256=CARTESIAN_POINT('Ctrl Pts',(1.90758049193009,0.423382412019868,
7.60021159017758));
#281257=CARTESIAN_POINT('Ctrl Pts',(1.92246330779034,0.356326794228461,
7.59630730121665));
#281258=CARTESIAN_POINT('Ctrl Pts',(1.93380448915002,0.288493034186758,
7.59240301225573));
#281259=CARTESIAN_POINT('Ctrl Pts',(1.94154317608092,0.220286394072858,
7.5884987232948));
#281260=CARTESIAN_POINT('Ctrl Pts',(1.94929010596925,0.152007102818522,
7.58459027563253));
#281261=CARTESIAN_POINT('Ctrl Pts',(1.95342682792389,0.0833546285307044,
7.58068182797026));
#281262=CARTESIAN_POINT('Ctrl Pts',(1.95394441081184,0.0147390453280266,
7.57677338030799));
#281263=CARTESIAN_POINT('Ctrl Pts',(1.95446230350742,-0.0539176088455757,
7.57286259318095));
#281264=CARTESIAN_POINT('Ctrl Pts',(1.95135676805297,-0.122536836543049,
7.5689518060539));
#281265=CARTESIAN_POINT('Ctrl Pts',(1.94467093540427,-0.190711701250598,
7.56504101892685));
#281266=CARTESIAN_POINT('Ctrl Pts',(1.93797355838192,-0.25900428295056,
7.56112347907502));
#281267=CARTESIAN_POINT('Ctrl Pts',(1.92768361946341,-0.326850484236416,
7.55720593922319));
#281268=CARTESIAN_POINT('Ctrl Pts',(1.91389556563938,-0.393852464542159,
7.55328839937135));
#281269=CARTESIAN_POINT('Ctrl Pts',(1.90738794301336,-0.425475752976507,
7.55143941681707));
#281270=CARTESIAN_POINT('Ctrl Pts',(1.90010180379956,-0.456911188780959,
7.54959043426279));
#281271=CARTESIAN_POINT('Ctrl Pts',(1.89205088566652,-0.488118270553907,
7.54774145170851));
#281272=CARTESIAN_POINT('Ctrl Pts',(1.87499045994153,-0.554248132003628,
7.54382333590944));
#281273=CARTESIAN_POINT('Ctrl Pts',(1.85442504231282,-0.619613578577113,
7.53990522011037));
#281274=CARTESIAN_POINT('Ctrl Pts',(1.83044028258338,-0.683816036588854,
7.5359871043113));
#281275=CARTESIAN_POINT('Ctrl Pts',(1.80649164002804,-0.747921816068889,
7.53207488856176));
#281276=CARTESIAN_POINT('Ctrl Pts',(1.77913404502007,-0.810867625573898,
7.52816267281223));
#281277=CARTESIAN_POINT('Ctrl Pts',(1.74850344534968,-0.872268136297721,
7.52425045706269));
#281278=CARTESIAN_POINT('Ctrl Pts',(1.71790886553865,-0.933596443480497,
7.52034284185845));
#281279=CARTESIAN_POINT('Ctrl Pts',(1.68404914351472,-0.993382622771358,
7.5164352266542));
#281280=CARTESIAN_POINT('Ctrl Pts',(1.64710833992997,-1.05126120280982,
7.51252761144996));
#281281=CARTESIAN_POINT('Ctrl Pts',(1.61019068943766,-1.1091035067529,7.50862244539049));
#281282=CARTESIAN_POINT('Ctrl Pts',(1.57019605212303,-1.16504016945973,
7.50471727933102));
#281283=CARTESIAN_POINT('Ctrl Pts',(1.52735368469385,-1.21873160369793,
7.50081211327155));
#281284=CARTESIAN_POINT('Ctrl Pts',(1.48452347498611,-1.27240780148818,
7.4969080554123));
#281285=CARTESIAN_POINT('Ctrl Pts',(1.43884744607434,-1.32383965135485,
7.49300399755305));
#281286=CARTESIAN_POINT('Ctrl Pts',(1.39059622456031,-1.3727192503344,7.48909993969381));
#281287=CARTESIAN_POINT('Ctrl Pts',(1.34234214680455,-1.4216017427526,7.48519565073299));
#281288=CARTESIAN_POINT('Ctrl Pts',(1.29151292118007,-1.46793133608345,
7.48129136177218));
#281289=CARTESIAN_POINT('Ctrl Pts',(1.23841596040746,-1.51143703441727,
7.47738707281136));
#281290=CARTESIAN_POINT('Ctrl Pts',(1.18526244275497,-1.55498907337999,
7.47347862514921));
#281291=CARTESIAN_POINT('Ctrl Pts',(1.12983675055633,-1.59571090215063,
7.46957017748706));
#281292=CARTESIAN_POINT('Ctrl Pts',(1.07247851226217,-1.63337253580924,
7.46566172982491));
#281293=CARTESIAN_POINT('Ctrl Pts',(1.01508594126359,-1.67105671244992,
7.46175094269797));
#281294=CARTESIAN_POINT('Ctrl Pts',(0.955758946904507,-1.70567680055392,
7.45784015557104));
#281295=CARTESIAN_POINT('Ctrl Pts',(0.894862767837988,-1.73704825112526,
7.45392936844411));
#281296=CARTESIAN_POINT('Ctrl Pts',(0.833861439827212,-1.76847387052884,
7.45001182859239));
#281297=CARTESIAN_POINT('Ctrl Pts',(0.771285967684583,-1.79663945516226,
7.44609428874067));
#281298=CARTESIAN_POINT('Ctrl Pts',(0.707521790321602,-1.82140849789939,
7.44217674888895));
#281299=CARTESIAN_POINT('Ctrl Pts',(0.677426665304581,-1.83309887749109,
7.44032776633366));
#281300=CARTESIAN_POINT('Ctrl Pts',(0.64706696375964,-1.84403336294319,
7.43847878377837));
#281301=CARTESIAN_POINT('Ctrl Pts',(0.616484161285372,-1.85420152057005,
7.43662980122308));
#281302=CARTESIAN_POINT('Ctrl Pts',(0.551677188817107,-1.87574851620365,
7.43271168542399));
#281303=CARTESIAN_POINT('Ctrl Pts',(0.485610740661061,-1.89393649124481,
7.42879356962489));
#281304=CARTESIAN_POINT('Ctrl Pts',(0.418666098724568,-1.90862115093036,
7.4248754538258));
#281305=CARTESIAN_POINT('Ctrl Pts',(0.351822264605887,-1.92328369789031,
7.42096323807624));
#281306=CARTESIAN_POINT('Ctrl Pts',(0.284103337830234,-1.93445329480633,
7.41705102232668));
#281307=CARTESIAN_POINT('Ctrl Pts',(0.215906763008642,-1.94203508456648,
7.41313880657712));
#281308=CARTESIAN_POINT('Ctrl Pts',(0.147790383516518,-1.94960795856906,
7.40923119137285));
#281309=CARTESIAN_POINT('Ctrl Pts',(0.0791979580515704,-1.95360135043905,
7.40532357616858));
#281310=CARTESIAN_POINT('Ctrl Pts',(0.0105363536613027,-1.95397159274426,
7.40141596096431));
#281311=CARTESIAN_POINT('Ctrl Pts',(-0.0580822162435067,-1.95434160299565,
7.39751079490482));
#281312=CARTESIAN_POINT('Ctrl Pts',(-0.126769388294698,-1.95109296568588,
7.39360562884533));
#281313=CARTESIAN_POINT('Ctrl Pts',(-0.19511551808398,-1.94423402259163,
7.38970046278583));
#281314=CARTESIAN_POINT('Ctrl Pts',(-0.263442252745103,-1.93737702591454,
7.38579640492656));
#281315=CARTESIAN_POINT('Ctrl Pts',(-0.331427648077723,-1.92691180640519,
7.38189234706729));
#281316=CARTESIAN_POINT('Ctrl Pts',(-0.398666230450798,-1.91289864778512,
7.37798828920802));
#281317=CARTESIAN_POINT('Ctrl Pts',(-0.46590879302657,-1.89888465965304,
7.37408400024718));
#281318=CARTESIAN_POINT('Ctrl Pts',(-0.532403973866264,-1.88132241831172,
7.37017971128634));
#281319=CARTESIAN_POINT('Ctrl Pts',(-0.597757344296068,-1.86032313250685,
7.3662754223255));
#281320=CARTESIAN_POINT('Ctrl Pts',(-0.663180326671078,-1.83930147905479,
7.36236697466333));
#281321=CARTESIAN_POINT('Ctrl Pts',(-0.727458602252804,-1.81483562565828,
7.35845852700115));
#281322=CARTESIAN_POINT('Ctrl Pts',(-0.79021471437671,-1.78708609338849,
7.35455007933897));
#281323=CARTESIAN_POINT('Ctrl Pts',(-0.853008390190014,-1.7593199511858,
7.35063929221201));
#281324=CARTESIAN_POINT('Ctrl Pts',(-0.914277650453092,-1.72826644080647,
7.34672850508506));
#281325=CARTESIAN_POINT('Ctrl Pts',(-0.973669311359256,-1.69413224752886,
7.3428177179581));
#281326=CARTESIAN_POINT('Ctrl Pts',(-1.03316352337023,-1.65993911501333,
7.33890017810636));
#281327=CARTESIAN_POINT('Ctrl Pts',(-1.0907732527164,-1.62265495005914,
7.33498263825462));
#281328=CARTESIAN_POINT('Ctrl Pts',(-1.14617471264073,-1.58252947148005,
7.33106509840288));
#281329=CARTESIAN_POINT('Ctrl Pts',(-1.17232284049716,-1.56359123148386,
7.3292161158478));
#281330=CARTESIAN_POINT('Ctrl Pts',(-1.1979795396265,-1.54402063518359,
7.32736713329272));
#281331=CARTESIAN_POINT('Ctrl Pts',(-1.22311354317257,-1.52384686255143,
7.32551815073764));
#281332=CARTESIAN_POINT('Ctrl Pts',(-1.27569843014326,-1.48163967690788,
7.32164974439755));
#281333=CARTESIAN_POINT('Ctrl Pts',(-1.32621309543889,-1.43661316524796,
7.31778133805745));
#281334=CARTESIAN_POINT('Ctrl Pts',(-1.3743338022176,-1.38900057598336,
7.31391293171736));
#281335=CARTESIAN_POINT('Ctrl Pts',(-1.4223718768899,-1.34146974629392,
7.31005116814262));
#281336=CARTESIAN_POINT('Ctrl Pts',(-1.4680237975101,-1.29136200687844,
7.30618940456789));
#281337=CARTESIAN_POINT('Ctrl Pts',(-1.51099832301929,-1.23895119671152,
7.30232764099316));
#281338=CARTESIAN_POINT('Ctrl Pts',(-1.5539317360317,-1.18659052646442,
7.29846957185696));
#281339=CARTESIAN_POINT('Ctrl Pts',(-1.59419251060611,-1.13193154021921,
7.29461150272075));
#281340=CARTESIAN_POINT('Ctrl Pts',(-1.6315268499352,-1.07528421263428,
7.29075343358454));
#281341=CARTESIAN_POINT('Ctrl Pts',(-1.6688390587004,-1.01867046371512,
7.28689765138435));
#281342=CARTESIAN_POINT('Ctrl Pts',(-1.70322799382576,-0.960071131503946,
7.28304186918416));
#281343=CARTESIAN_POINT('Ctrl Pts',(-1.73448192833098,-0.899826894626534,
7.27918608698398));
#281344=CARTESIAN_POINT('Ctrl Pts',(-1.76572870765072,-0.839596449890684,
7.27533118751543));
#281345=CARTESIAN_POINT('Ctrl Pts',(-1.79384167895834,-0.777722296975262,
7.27147628804688));
#281346=CARTESIAN_POINT('Ctrl Pts',(-1.81865500239731,-0.71456978823292,
7.26762138857834));
#281347=CARTESIAN_POINT('Ctrl Pts',(-1.8434864034073,-0.651371270177707,
7.26376368065009));
#281348=CARTESIAN_POINT('Ctrl Pts',(-1.86501316883761,-0.586893007186788,
7.25990597272184));
#281349=CARTESIAN_POINT('Ctrl Pts',(-1.88311808384908,-0.521519206051485,
7.2560482647936));
#281350=CARTESIAN_POINT('Ctrl Pts',(-1.90122994604552,-0.456120319800443,
7.2521890765927));
#281351=CARTESIAN_POINT('Ctrl Pts',(-1.91591723290655,-0.389825705105673,
7.2483298883918));
#281352=CARTESIAN_POINT('Ctrl Pts',(-1.92711367637425,-0.32303076994509,
7.2444707001909));
#281353=CARTESIAN_POINT('Ctrl Pts',(-1.9383275135784,-0.256132068485687,
7.24060551671993));
#281354=CARTESIAN_POINT('Ctrl Pts',(-1.94603962377029,-0.188731997572627,
7.23674033324896));
#281355=CARTESIAN_POINT('Ctrl Pts',(-1.95023563501482,-0.121231051790984,
7.23287514977798));
#281356=CARTESIAN_POINT('Ctrl Pts',(-1.95277065731482,-0.0804503215079684,
7.23053999724347));
#281357=CARTESIAN_POINT('Ctrl Pts',(-1.95402332588266,-0.0396328002594552,
7.22820484470895));
#281358=CARTESIAN_POINT('Ctrl Pts',(-1.95399967105378,0.00113380850775126,
7.22586969217444));
#281359=CARTESIAN_POINT('',(-1.95399924719281,-0.00171521716542704,6.52586969212424));
#281360=CARTESIAN_POINT('Ctrl Pts',(-1.95399967105327,0.00113380938422453,
7.22586969212423));
#281361=CARTESIAN_POINT('Ctrl Pts',(-1.9539609640812,0.0678411516748536,
7.22204862816689));
#281362=CARTESIAN_POINT('Ctrl Pts',(-1.9505065413377,0.134447927039275,
7.21822756420955));
#281363=CARTESIAN_POINT('Ctrl Pts',(-1.94366557894286,0.200699071330002,
7.21440650025221));
#281364=CARTESIAN_POINT('Ctrl Pts',(-1.93665086180136,0.268632939501905,
7.2104883844531));
#281365=CARTESIAN_POINT('Ctrl Pts',(-1.92605637388582,0.336333270622923,
7.206570268654));
#281366=CARTESIAN_POINT('Ctrl Pts',(-1.91190740994614,0.403393177672903,
7.20265215285489));
#281367=CARTESIAN_POINT('Ctrl Pts',(-1.89777975206077,0.470352103334573,
7.19873993710531));
#281368=CARTESIAN_POINT('Ctrl Pts',(-1.88010834163168,0.536672041455856,
7.19482772135574));
#281369=CARTESIAN_POINT('Ctrl Pts',(-1.85897018357449,0.601951706186642,
7.19091550560616));
#281370=CARTESIAN_POINT('Ctrl Pts',(-1.83785688280018,0.667154605709812,
7.18700789040187));
#281371=CARTESIAN_POINT('Ctrl Pts',(-1.81328508159823,0.731319195598035,
7.18310027519759));
#281372=CARTESIAN_POINT('Ctrl Pts',(-1.78538231978286,0.794056655539634,
7.1791926599933));
#281373=CARTESIAN_POINT('Ctrl Pts',(-1.75749704635867,0.856754794024498,
7.17528749393379));
#281374=CARTESIAN_POINT('Ctrl Pts',(-1.72628515313261,0.918027128483419,
7.17138232787428));
#281375=CARTESIAN_POINT('Ctrl Pts',(-1.69192272872721,0.977503698211054,
7.16747716181477));
#281376=CARTESIAN_POINT('Ctrl Pts',(-1.65757005562196,1.03696338979655,
7.16357310395548));
#281377=CARTESIAN_POINT('Ctrl Pts',(-1.6200688721345,1.09462790258377,7.15966904609619));
#281378=CARTESIAN_POINT('Ctrl Pts',(-1.57964089664353,1.15015244104911,
7.15576498823691));
#281379=CARTESIAN_POINT('Ctrl Pts',(-1.53921052800964,1.20568026630174,
7.15186069927605));
#281380=CARTESIAN_POINT('Ctrl Pts',(-1.49585331500633,1.25906746960417,
7.1479564103152));
#281381=CARTESIAN_POINT('Ctrl Pts',(-1.44983285152109,1.31000026818708,
7.14405212135435));
#281382=CARTESIAN_POINT('Ctrl Pts',(-1.40376336877392,1.36098731846598,
7.14014367369215));
#281383=CARTESIAN_POINT('Ctrl Pts',(-1.35502530458131,1.40951438094631,
7.13623522602996));
#281384=CARTESIAN_POINT('Ctrl Pts',(-1.30392022058927,1.45530342483567,
7.13232677836777));
#281385=CARTESIAN_POINT('Ctrl Pts',(-1.25278454681981,1.50111987650037,
7.12841599124079));
#281386=CARTESIAN_POINT('Ctrl Pts',(-1.19927941672047,1.5441947393922,7.12450520411382));
#281387=CARTESIAN_POINT('Ctrl Pts',(-1.14373848737084,1.58429109462455,
7.12059441698685));
#281388=CARTESIAN_POINT('Ctrl Pts',(-1.08810165594369,1.62445668391209,
7.11667687713509));
#281389=CARTESIAN_POINT('Ctrl Pts',(-1.03042242271735,1.66163323466832,
7.11275933728333));
#281390=CARTESIAN_POINT('Ctrl Pts',(-0.971061579032576,1.69562832299026,
7.10884179743157));
#281391=CARTESIAN_POINT('Ctrl Pts',(-0.943044719326595,1.71167316940899,
7.10699281487664));
#281392=CARTESIAN_POINT('Ctrl Pts',(-0.91465358830197,1.72700999205061,
7.1051438323217));
#281393=CARTESIAN_POINT('Ctrl Pts',(-0.885927643488578,1.74162229272101,
7.10329484976677));
#281394=CARTESIAN_POINT('Ctrl Pts',(-0.825055474674994,1.77258672013816,
7.09937673396767));
#281395=CARTESIAN_POINT('Ctrl Pts',(-0.762437306951289,1.80041733419865,
7.09545861816858));
#281396=CARTESIAN_POINT('Ctrl Pts',(-0.698428660500115,1.8249146298367,
7.09154050236948));
#281397=CARTESIAN_POINT('Ctrl Pts',(-0.634516400731742,1.84937503650435,
7.08762828661992));
#281398=CARTESIAN_POINT('Ctrl Pts',(-0.569218273449775,1.8705119121578,
7.08371607087036));
#281399=CARTESIAN_POINT('Ctrl Pts',(-0.502913148641049,1.88817222861792,
7.0798038551208));
#281400=CARTESIAN_POINT('Ctrl Pts',(-0.436685994923168,1.90581177754094,
7.07589623991653));
#281401=CARTESIAN_POINT('Ctrl Pts',(-0.369454668522051,1.91998276057471,
7.07198862471225));
#281402=CARTESIAN_POINT('Ctrl Pts',(-0.301614985331262,1.9305813633783,
7.06808100950798));
#281403=CARTESIAN_POINT('Ctrl Pts',(-0.233817821476945,1.94117332338026,
7.06417584344849));
#281404=CARTESIAN_POINT('Ctrl Pts',(-0.165413542095161,1.94819726892558,
7.06027067738899));
#281405=CARTESIAN_POINT('Ctrl Pts',(-0.0968084602488389,1.95160040019064,
7.05636551132949));
#281406=CARTESIAN_POINT('Ctrl Pts',(-0.0282228470155735,1.9550025657219,
7.05246145347022));
#281407=CARTESIAN_POINT('Ctrl Pts',(0.0405629645149766,1.95478593239357,
7.04855739561095));
#281408=CARTESIAN_POINT('Ctrl Pts',(0.109139044682844,1.9509496838529,7.04465333775167));
#281409=CARTESIAN_POINT('Ctrl Pts',(0.177719184226884,1.94711320822464,
7.04074904879083));
#281410=CARTESIAN_POINT('Ctrl Pts',(0.246089076792685,1.93965672202949,
7.03684475982999));
#281411=CARTESIAN_POINT('Ctrl Pts',(0.313842125088751,1.92863141126545,
7.03294047086915));
#281412=CARTESIAN_POINT('Ctrl Pts',(0.381667341376385,1.91759435675624,
7.02903202320697));
#281413=CARTESIAN_POINT('Ctrl Pts',(0.448873915721153,1.90298097046063,
7.02512357554479));
#281414=CARTESIAN_POINT('Ctrl Pts',(0.515064684401739,1.88489372933387,
7.02121512788261));
#281415=CARTESIAN_POINT('Ctrl Pts',(0.581295072641165,1.86679566179539,
7.01730434075565));
#281416=CARTESIAN_POINT('Ctrl Pts',(0.646507978082287,1.84521975569629,
7.01339355362869));
#281417=CARTESIAN_POINT('Ctrl Pts',(0.710323359051366,1.82031775401604,
7.00948276650173));
#281418=CARTESIAN_POINT('Ctrl Pts',(0.774248929527226,1.7953727542491,7.00556522664999));
#281419=CARTESIAN_POINT('Ctrl Pts',(0.836771711459432,1.76709039912909,
7.00164768679825));
#281420=CARTESIAN_POINT('Ctrl Pts',(0.897534318749179,1.73566936559572,
6.9977301469465));
#281421=CARTESIAN_POINT('Ctrl Pts',(0.926212776436969,1.72083940979089,
6.99588116439145));
#281422=CARTESIAN_POINT('Ctrl Pts',(0.954499531921449,1.70531092261739,
6.99403218183639));
#281423=CARTESIAN_POINT('Ctrl Pts',(0.982359318873593,1.68910809856036,
6.99218319928133));
#281424=CARTESIAN_POINT('Ctrl Pts',(1.04139604213431,1.65477324734489,6.98826508348223));
#281425=CARTESIAN_POINT('Ctrl Pts',(1.09874755079015,1.61727148121357,6.98434696768313));
#281426=CARTESIAN_POINT('Ctrl Pts',(1.15405337018907,1.57679320735322,6.98042885188403));
#281427=CARTESIAN_POINT('Ctrl Pts',(1.20927590795705,1.53637588723519,6.97651663613447));
#281428=CARTESIAN_POINT('Ctrl Pts',(1.26245847639234,1.49299124302138,6.9726044203849));
#281429=CARTESIAN_POINT('Ctrl Pts',(1.31326697450054,1.44687451207291,6.96869220463533));
#281430=CARTESIAN_POINT('Ctrl Pts',(1.36401572467772,1.40081201180162,6.96478458943106));
#281431=CARTESIAN_POINT('Ctrl Pts',(1.41239558653464,1.35202413444964,6.96087697422678));
#281432=CARTESIAN_POINT('Ctrl Pts',(1.45810460623655,1.30078705300743,6.95696935902251));
#281433=CARTESIAN_POINT('Ctrl Pts',(1.50378497726122,1.24958208502157,6.95306419296301));
#281434=CARTESIAN_POINT('Ctrl Pts',(1.54679750006817,1.19593132425755,6.9491590269035));
#281435=CARTESIAN_POINT('Ctrl Pts',(1.58687737931631,1.14014743915609,6.945253860844));
#281436=CARTESIAN_POINT('Ctrl Pts',(1.62694588477639,1.08437938429411,6.94134980298473));
#281437=CARTESIAN_POINT('Ctrl Pts',(1.66408311190234,1.02647980606318,6.93744574512545));
#281438=CARTESIAN_POINT('Ctrl Pts',(1.69806597079622,0.966792614175287,
6.93354168726617));
#281439=CARTESIAN_POINT('Ctrl Pts',(1.73205084131295,0.907101889090883,
6.92963739830533));
#281440=CARTESIAN_POINT('Ctrl Pts',(1.7628807317453,0.845623768984775,6.92573310934448));
#281441=CARTESIAN_POINT('Ctrl Pts',(1.79037804360517,0.782727577753921,
6.92182882038364));
#281442=CARTESIAN_POINT('Ctrl Pts',(1.81790464456448,0.719764391872499,
6.91792037272145));
#281443=CARTESIAN_POINT('Ctrl Pts',(1.84209138536074,0.655380571980799,
6.91401192505927));
#281444=CARTESIAN_POINT('Ctrl Pts',(1.86280887148414,0.589965345016128,
6.91010347739709));
#281445=CARTESIAN_POINT('Ctrl Pts',(1.88353875839509,0.524510962705703,
6.90619269027012));
#281446=CARTESIAN_POINT('Ctrl Pts',(1.90079513427067,0.45802442082151,6.90228190314316));
#281447=CARTESIAN_POINT('Ctrl Pts',(1.91449927890125,0.390907292189067,
6.89837111601619));
#281448=CARTESIAN_POINT('Ctrl Pts',(1.92822708636852,0.323674272948614,
6.89445357616445));
#281449=CARTESIAN_POINT('Ctrl Pts',(1.93839034807995,0.255808980028962,
6.8905360363127));
#281450=CARTESIAN_POINT('Ctrl Pts',(1.94496206129787,0.187719418579768,
6.88661849646095));
#281451=CARTESIAN_POINT('Ctrl Pts',(1.94806374846798,0.15558281855454,6.88476951390593));
#281452=CARTESIAN_POINT('Ctrl Pts',(1.95036613437155,0.123396276819736,
6.88292053135091));
#281453=CARTESIAN_POINT('Ctrl Pts',(1.95187040959523,0.0912025446276998,
6.88107154879589));
#281454=CARTESIAN_POINT('Ctrl Pts',(1.95505806785845,0.0229819059899013,
6.87715343299679));
#281455=CARTESIAN_POINT('Ctrl Pts',(1.95467112714343,-0.0455412892431805,
6.87323531719769));
#281456=CARTESIAN_POINT('Ctrl Pts',(1.9506739622135,-0.113960928138913,
6.86931720139859));
#281457=CARTESIAN_POINT('Ctrl Pts',(1.94668281636833,-0.182277538109707,
6.86540498564903));
#281458=CARTESIAN_POINT('Ctrl Pts',(1.93909226412263,-0.250490414134239,
6.86149276989946));
#281459=CARTESIAN_POINT('Ctrl Pts',(1.92791864768824,-0.318191275643976,
6.8575805541499));
#281460=CARTESIAN_POINT('Ctrl Pts',(1.91675817079721,-0.385812524755137,
6.85367293894562));
#281461=CARTESIAN_POINT('Ctrl Pts',(1.90202307747573,-0.452922472114777,
6.84976532374134));
#281462=CARTESIAN_POINT('Ctrl Pts',(1.88378153822363,-0.519117632379996,
6.84585770853707));
#281463=CARTESIAN_POINT('Ctrl Pts',(1.8655514320754,-0.585271304033257,
6.84195254247757));
#281464=CARTESIAN_POINT('Ctrl Pts',(1.84381936993339,-0.650510852804162,
6.83804737641807));
#281465=CARTESIAN_POINT('Ctrl Pts',(1.81870433956832,-0.71444420722359,
6.83414221035857));
#281466=CARTESIAN_POINT('Ctrl Pts',(1.7935964362964,-0.778359418763425,
6.83023815249929));
#281467=CARTESIAN_POINT('Ctrl Pts',(1.76510765035267,-0.84096871418652,
6.82633409464001));
#281468=CARTESIAN_POINT('Ctrl Pts',(1.73340584003042,-0.901898106078744,
6.82243003678074));
#281469=CARTESIAN_POINT('Ctrl Pts',(1.7017021531125,-0.962831104699797,
6.81852574781989));
#281470=CARTESIAN_POINT('Ctrl Pts',(1.66678529352021,-1.02208356719771,
6.81462145885904));
#281471=CARTESIAN_POINT('Ctrl Pts',(1.62886914919724,-1.07930593197363,
6.8107171698982));
#281472=CARTESIAN_POINT('Ctrl Pts',(1.59091261802746,-1.13658924785418,
6.80680872223601));
#281473=CARTESIAN_POINT('Ctrl Pts',(1.54995069865983,-1.1918377397423,6.80290027457383));
#281474=CARTESIAN_POINT('Ctrl Pts',(1.50624015085242,-1.2447315405179,6.79899182691165));
#281475=CARTESIAN_POINT('Ctrl Pts',(1.46250343938723,-1.2976570017364,6.79508103978468));
#281476=CARTESIAN_POINT('Ctrl Pts',(1.41601515810384,-1.34822460463977,
6.79117025265772));
#281477=CARTESIAN_POINT('Ctrl Pts',(1.36706993060505,-1.39615035180151,
6.78725946553075));
#281478=CARTESIAN_POINT('Ctrl Pts',(1.31804018977428,-1.44415885196672,
6.783341925679));
#281479=CARTESIAN_POINT('Ctrl Pts',(1.26654540451618,-1.48951606708082,
6.77942438582726));
#281480=CARTESIAN_POINT('Ctrl Pts',(1.21291366068032,-1.531977954063,6.77550684597551));
#281481=CARTESIAN_POINT('Ctrl Pts',(1.18760079533619,-1.55201892141859,
6.77365786342049));
#281482=CARTESIAN_POINT('Ctrl Pts',(1.16181232286502,-1.57141554837522,
6.77180888086548));
#281483=CARTESIAN_POINT('Ctrl Pts',(1.13558480148282,-1.59014564070126,
6.76995989831046));
#281484=CARTESIAN_POINT('Ctrl Pts',(1.08000695645659,-1.62983593981318,
6.76604178251136));
#281485=CARTESIAN_POINT('Ctrl Pts',(1.02223558446953,-1.66668762344908,
6.76212366671226));
#281486=CARTESIAN_POINT('Ctrl Pts',(0.962592503785318,-1.70045043199039,
6.75820555091316));
#281487=CARTESIAN_POINT('Ctrl Pts',(0.903039235947001,-1.73416239919545,
6.75429333516359));
#281488=CARTESIAN_POINT('Ctrl Pts',(0.841620277728886,-1.76479448221852,
6.75038111941403));
#281489=CARTESIAN_POINT('Ctrl Pts',(0.778687462804387,-1.79213889954748,
6.74646890366446));
#281490=CARTESIAN_POINT('Ctrl Pts',(0.715828653324338,-1.81945116138237,
6.74256128846019));
#281491=CARTESIAN_POINT('Ctrl Pts',(0.651459971661729,-1.84348324058542,
6.73865367325591));
#281492=CARTESIAN_POINT('Ctrl Pts',(0.585957342396771,-1.86407349449836,
6.73474605805164));
#281493=CARTESIAN_POINT('Ctrl Pts',(0.520495767691645,-1.88465084322228,
6.73084089199214));
#281494=CARTESIAN_POINT('Ctrl Pts',(0.453902123407269,-1.9017904986943,
6.72693572593264));
#281495=CARTESIAN_POINT('Ctrl Pts',(0.386570316657824,-1.9153796987227,
6.72303055987314));
#281496=CARTESIAN_POINT('Ctrl Pts',(0.319257617193964,-1.92896504243507,
6.71912650201386));
#281497=CARTESIAN_POINT('Ctrl Pts',(0.251207653039465,-1.93900183358048,
6.71522244415458));
#281498=CARTESIAN_POINT('Ctrl Pts',(0.182825654506691,-1.94542817396433,
6.7113183862953));
#281499=CARTESIAN_POINT('Ctrl Pts',(0.114439608086459,-1.95185489475682,
6.70741409733446));
#281500=CARTESIAN_POINT('Ctrl Pts',(0.045721978226763,-1.95467069700702,
6.70350980837361));
#281501=CARTESIAN_POINT('Ctrl Pts',(-0.0229175501145682,-1.95386560077625,
6.69960551941277));
#281502=CARTESIAN_POINT('Ctrl Pts',(-0.0916301906925765,-1.95305964698735,
6.69569707175059));
#281503=CARTESIAN_POINT('Ctrl Pts',(-0.160264070938615,-1.94862510342967,
6.6917886240884));
#281504=CARTESIAN_POINT('Ctrl Pts',(-0.228411190336413,-1.94060411422039,
6.68788017642622));
#281505=CARTESIAN_POINT('Ctrl Pts',(-0.29659910029851,-1.93257832391784,
6.68396938929926));
#281506=CARTESIAN_POINT('Ctrl Pts',(-0.364299184693671,-1.92096189878078,
6.68005860217229));
#281507=CARTESIAN_POINT('Ctrl Pts',(-0.431113031838807,-1.90584825045929,
6.67614781504533));
#281508=CARTESIAN_POINT('Ctrl Pts',(-0.498042245918241,-1.8907085055224,
6.67223027519358));
#281509=CARTESIAN_POINT('Ctrl Pts',(-0.564081695480184,-1.8720596188736,
6.66831273534183));
#281510=CARTESIAN_POINT('Ctrl Pts',(-0.628848376951741,-1.8500447883241,
6.66439519549009));
#281511=CARTESIAN_POINT('Ctrl Pts',(-0.659416659271667,-1.839654329215,
6.66254621293506));
#281512=CARTESIAN_POINT('Ctrl Pts',(-0.689701714196233,-1.82851476468504,
6.66069723038004));
#281513=CARTESIAN_POINT('Ctrl Pts',(-0.719665063562426,-1.81664476337222,
6.65884824782501));
#281514=CARTESIAN_POINT('Ctrl Pts',(-0.783159374109898,-1.79149144888976,
6.65493013202591));
#281515=CARTESIAN_POINT('Ctrl Pts',(-0.845459247551919,-1.76295544045873,
6.65101201622681));
#281516=CARTESIAN_POINT('Ctrl Pts',(-0.906179858676215,-1.73117129820522,
6.64709390042771));
#281517=CARTESIAN_POINT('Ctrl Pts',(-0.966809034367842,-1.69943501773612,
6.64318168467815));
#281518=CARTESIAN_POINT('Ctrl Pts',(-1.02586323517391,-1.66446053695241,
6.63926946892858));
#281519=CARTESIAN_POINT('Ctrl Pts',(-1.08297703407796,-1.62643067594647,
6.63535725317902));
#281520=CARTESIAN_POINT('Ctrl Pts',(-1.14002367037253,-1.58844553591432,
6.63144963797474));
#281521=CARTESIAN_POINT('Ctrl Pts',(-1.19513402897873,-1.54741242265076,
6.62754202277047));
#281522=CARTESIAN_POINT('Ctrl Pts',(-1.24796837050111,-1.5035594255728,
6.62363440756619));
#281523=CARTESIAN_POINT('Ctrl Pts',(-1.30076959746519,-1.4597339138876,
6.61972924150669));
#281524=CARTESIAN_POINT('Ctrl Pts',(-1.35129725946874,-1.41309233778612,
6.61582407544719));
#281525=CARTESIAN_POINT('Ctrl Pts',(-1.39924292182024,-1.36390441224302,
6.61191890938769));
#281526=CARTESIAN_POINT('Ctrl Pts',(-1.44717497824744,-1.31473044515117,
6.60801485152842));
#281527=CARTESIAN_POINT('Ctrl Pts',(-1.49252614641283,-1.26301191516475,
6.60411079366914));
#281528=CARTESIAN_POINT('Ctrl Pts',(-1.53502457552179,-1.20905564493291,
6.60020673580987));
#281529=CARTESIAN_POINT('Ctrl Pts',(-1.57752552033461,-1.15509618074779,
6.59630244684903));
#281530=CARTESIAN_POINT('Ctrl Pts',(-1.61717308848852,-1.09889910132795,
6.59239815788819));
#281531=CARTESIAN_POINT('Ctrl Pts',(-1.65373662517302,-1.04080313919653,
6.58849386892735));
#281532=CARTESIAN_POINT('Ctrl Pts',(-1.69033910795774,-0.982645295437449,
6.58458542126517));
#281533=CARTESIAN_POINT('Ctrl Pts',(-1.72385074093752,-0.922584949540845,
6.58067697360298));
#281534=CARTESIAN_POINT('Ctrl Pts',(-1.75408556887754,-0.860987698550653,
6.5767685259408));
#281535=CARTESIAN_POINT('Ctrl Pts',(-1.78433849436452,-0.799353577526197,
6.57285773881384));
#281536=CARTESIAN_POINT('Ctrl Pts',(-1.81131051812368,-0.736181172993751,
6.56894695168687));
#281537=CARTESIAN_POINT('Ctrl Pts',(-1.83486395345815,-0.671855841903561,
6.56503616455991));
#281538=CARTESIAN_POINT('Ctrl Pts',(-1.85845805832061,-0.607419440779791,
6.56111862470816));
#281539=CARTESIAN_POINT('Ctrl Pts',(-1.87862164916358,-0.541826609799558,
6.55720108485641));
#281540=CARTESIAN_POINT('Ctrl Pts',(-1.89526722063687,-0.475476773753879,
6.55328354500467));
#281541=CARTESIAN_POINT('Ctrl Pts',(-1.90312352138613,-0.444161281373481,
6.55143456244964));
#281542=CARTESIAN_POINT('Ctrl Pts',(-1.91019688938173,-0.412677286790502,
6.54958557989462));
#281543=CARTESIAN_POINT('Ctrl Pts',(-1.91648213078546,-0.381067241284289,
6.54773659733959));
#281544=CARTESIAN_POINT('Ctrl Pts',(-1.93570543873075,-0.284388434553022,
6.54208151446248));
#281545=CARTESIAN_POINT('Ctrl Pts',(-1.94761790070022,-0.186211271518132,
6.53642643158537));
#281546=CARTESIAN_POINT('Ctrl Pts',(-1.95204230768552,-0.0874461491764296,
6.53077134870826));
#281547=CARTESIAN_POINT('Ctrl Pts',(-1.9533206222037,-0.0589105984917037,
6.52913746318025));
#281548=CARTESIAN_POINT('Ctrl Pts',(-1.95397413257682,-0.0303261369517731,
6.52750357765225));
#281549=CARTESIAN_POINT('Ctrl Pts',(-1.95399924719281,-0.00171521716542704,
6.52586969212424));
#281550=CARTESIAN_POINT('',(-1.95079815420139,-3.45302974047446E-5,5.82586969212423));
#281551=CARTESIAN_POINT('Ctrl Pts',(-1.95470925949157,-0.0017091530386519,
6.52586931036698));
#281552=CARTESIAN_POINT('Ctrl Pts',(-1.94992763104345,0.51940321820411,
6.49612118919603));
#281553=CARTESIAN_POINT('Ctrl Pts',(-1.46756271540364,1.69712511346729,
6.42933585119661));
#281554=CARTESIAN_POINT('Ctrl Pts',(0.521076907609903,2.2497876261868,6.32551329636871));
#281555=CARTESIAN_POINT('Ctrl Pts',(2.17259204728733,0.782885242326123,
6.21440164588327));
#281556=CARTESIAN_POINT('Ctrl Pts',(1.83636881720092,-1.40029106752842,
6.10328999539785));
#281557=CARTESIAN_POINT('Ctrl Pts',(-0.179976902307915,-2.30231922661122,
5.99217834491238));
#281558=CARTESIAN_POINT('Ctrl Pts',(-1.72105200304095,-1.29994935931744,
5.89970491048787));
#281559=CARTESIAN_POINT('Ctrl Pts',(-1.95084923717034,-0.323977343102287,
5.84426869289181));
#281560=CARTESIAN_POINT('Ctrl Pts',(-1.95079815420139,-3.45302974047446E-5,
5.82586969212423));
#281561=CARTESIAN_POINT('',(-1.95399923068592,0.0017339200773292,5.12586969212423));
#281562=CARTESIAN_POINT('Ctrl Pts',(-1.95079815420139,-3.45302974047446E-5,
5.82586969212423));
#281563=CARTESIAN_POINT('Ctrl Pts',(-1.95074640707532,0.328120037045956,
5.80723147606333));
#281564=CARTESIAN_POINT('Ctrl Pts',(-1.71664579075019,1.30844134569539,
5.75155604317396));
#281565=CARTESIAN_POINT('Ctrl Pts',(-0.165142710425363,2.30343078727822,
5.65884339345609));
#281566=CARTESIAN_POINT('Ctrl Pts',(1.84535073495004,1.38843299139978,5.54773174297065));
#281567=CARTESIAN_POINT('Ctrl Pts',(2.16750399418151,-0.796863816342125,
5.43662009248521));
#281568=CARTESIAN_POINT('Ctrl Pts',(0.506574022840454,-2.2530974825717,
5.32550844199979));
#281569=CARTESIAN_POINT('Ctrl Pts',(-1.47389109216557,-1.68893929938375,
5.22192508019049));
#281570=CARTESIAN_POINT('Ctrl Pts',(-1.94982185200388,-0.515279595154487,
5.1553789352097));
#281571=CARTESIAN_POINT('Ctrl Pts',(-1.9545826140287,0.00172892004169586,
5.12587000705737));
#281572=CARTESIAN_POINT('',(-1.95399970461562,-0.00107441242398919,4.42586969212423));
#281573=CARTESIAN_POINT('Ctrl Pts',(-1.95399923068592,0.0017339200773292,
5.12586969212423));
#281574=CARTESIAN_POINT('Ctrl Pts',(-1.95391275218654,0.0991887702010741,
5.12030561986702));
#281575=CARTESIAN_POINT('Ctrl Pts',(-1.94653201774855,0.196330965052306,
5.1147415476098));
#281576=CARTESIAN_POINT('Ctrl Pts',(-1.93201679707086,0.292279140268442,
5.10917747535259));
#281577=CARTESIAN_POINT('Ctrl Pts',(-1.92689293999513,0.326148741523638,
5.10721336391136));
#281578=CARTESIAN_POINT('Ctrl Pts',(-1.92088046947136,0.359869837291548,
5.10524925247014));
#281579=CARTESIAN_POINT('Ctrl Pts',(-1.91398771378947,0.393404412104079,
5.10328514102891));
#281580=CARTESIAN_POINT('Ctrl Pts',(-1.90023767172484,0.460300996804353,
5.09936702522981));
#281581=CARTESIAN_POINT('Ctrl Pts',(-1.88294895453001,0.526608449370511,
5.09544890943072));
#281582=CARTESIAN_POINT('Ctrl Pts',(-1.86218728113428,0.591924429282757,
5.09153079363163));
#281583=CARTESIAN_POINT('Ctrl Pts',(-1.84145687146522,0.657142053879186,
5.08761857788206));
#281584=CARTESIAN_POINT('Ctrl Pts',(-1.81726403252631,0.721370703896118,
5.0837063621325));
#281585=CARTESIAN_POINT('Ctrl Pts',(-1.78972537777022,0.784218765501848,
5.07979414638294));
#281586=CARTESIAN_POINT('Ctrl Pts',(-1.76221910692048,0.846992921328244,
5.07588653117867));
#281587=CARTESIAN_POINT('Ctrl Pts',(-1.7313750306896,0.9083892646335,5.0719789159744));
#281588=CARTESIAN_POINT('Ctrl Pts',(-1.69735880353875,0.968033621342521,
5.06807130077013));
#281589=CARTESIAN_POINT('Ctrl Pts',(-1.66336389646694,1.02764059523439,
5.06416613471064));
#281590=CARTESIAN_POINT('Ctrl Pts',(-1.62620102553603,1.08549733445233,
5.06026096865114));
#281591=CARTESIAN_POINT('Ctrl Pts',(-1.58608227278411,1.14125326898108,
5.05635580259165));
#281592=CARTESIAN_POINT('Ctrl Pts',(-1.54597490485169,1.19699338120212,
5.05245174473238));
#281593=CARTESIAN_POINT('Ctrl Pts',(-1.50291360744137,1.25063347314136,
5.0485476868731));
#281594=CARTESIAN_POINT('Ctrl Pts',(-1.45715335723846,1.30185256211626,
5.04464362901383));
#281595=CARTESIAN_POINT('Ctrl Pts',(-1.41139039824741,1.35307468301649,
5.04073934005299));
#281596=CARTESIAN_POINT('Ctrl Pts',(-1.36292849890078,1.40187515132943,
5.03683505109215));
#281597=CARTESIAN_POINT('Ctrl Pts',(-1.31206121220845,1.44796801602041,
5.0329307621313));
#281598=CARTESIAN_POINT('Ctrl Pts',(-1.261139743601,1.49410997709229,5.02902231446912));
#281599=CARTESIAN_POINT('Ctrl Pts',(-1.2078081396301,1.53753824797739,5.02511386680695));
#281600=CARTESIAN_POINT('Ctrl Pts',(-1.15239416902623,1.57800623547385,
5.02120541914477));
#281601=CARTESIAN_POINT('Ctrl Pts',(-1.09694702949092,1.618498445741,5.01729463201781));
#281602=CARTESIAN_POINT('Ctrl Pts',(-1.03941545472426,1.65602657738826,
5.01338384489085));
#281603=CARTESIAN_POINT('Ctrl Pts',(-0.980155051919915,1.69038814305942,
5.00947305776389));
#281604=CARTESIAN_POINT('Ctrl Pts',(-0.920792324653062,1.72480904057059,
5.00555551791215));
#281605=CARTESIAN_POINT('Ctrl Pts',(-0.859695249169783,1.7560522356547,
5.0016379780604));
#281606=CARTESIAN_POINT('Ctrl Pts',(-0.797241997497702,1.78396221860943,
4.99772043820866));
#281607=CARTESIAN_POINT('Ctrl Pts',(-0.767765597200889,1.79713504480862,
4.9958714556536));
#281608=CARTESIAN_POINT('Ctrl Pts',(-0.737987350060903,1.80956607240149,
4.99402247309853));
#281609=CARTESIAN_POINT('Ctrl Pts',(-0.707948161372474,1.82124281764111,
4.99217349054347));
#281610=CARTESIAN_POINT('Ctrl Pts',(-0.644293142308056,1.84598660977705,
4.98825537474437));
#281611=CARTESIAN_POINT('Ctrl Pts',(-0.579213130476493,1.86743818473269,
4.98433725894526));
#281612=CARTESIAN_POINT('Ctrl Pts',(-0.513081758693453,1.88543446157538,
4.98041914314616));
#281613=CARTESIAN_POINT('Ctrl Pts',(-0.447049970074688,1.90340363893192,
4.97650692739659));
#281614=CARTESIAN_POINT('Ctrl Pts',(-0.379970434354915,1.91792771640892,
4.97259471164702));
#281615=CARTESIAN_POINT('Ctrl Pts',(-0.312235386052087,1.9288921856073,
4.96868249589746));
#281616=CARTESIAN_POINT('Ctrl Pts',(-0.244579990349595,1.93984376120769,
4.96477488069318));
#281617=CARTESIAN_POINT('Ctrl Pts',(-0.17627109623671,1.94724396356192,
4.9608672654889));
#281618=CARTESIAN_POINT('Ctrl Pts',(-0.107712895154416,1.95102894192205,
4.95695965028463));
#281619=CARTESIAN_POINT('Ctrl Pts',(-0.0391976637483059,1.95481154800151,
4.95305448422512));
#281620=CARTESIAN_POINT('Ctrl Pts',(0.0295660746347592,1.95498339782931,
4.94914931816562));
#281621=CARTESIAN_POINT('Ctrl Pts',(0.0981687677183626,1.9515324473461,
4.94524415210612));
#281622=CARTESIAN_POINT('Ctrl Pts',(0.166751992866778,1.94808247616672,
4.94134009424684));
#281623=CARTESIAN_POINT('Ctrl Pts',(0.235173772411825,1.94101177027437,
4.93743603638756));
#281624=CARTESIAN_POINT('Ctrl Pts',(0.303026136125135,1.93036037071451,
4.93353197852828));
#281625=CARTESIAN_POINT('Ctrl Pts',(0.370882516374091,1.9197083406427,4.92962768956744));
#281626=CARTESIAN_POINT('Ctrl Pts',(0.4381689283419,1.90547527490298,4.92572340060659));
#281627=CARTESIAN_POINT('Ctrl Pts',(0.50448590010067,1.88775262590193,4.92181911164575));
#281628=CARTESIAN_POINT('Ctrl Pts',(0.570873510196411,1.87001109940362,
4.91791066398356));
#281629=CARTESIAN_POINT('Ctrl Pts',(0.636289143194882,1.84877269895529,
4.91400221632138));
#281630=CARTESIAN_POINT('Ctrl Pts',(0.700347825399189,1.82417897243078,
4.9100937686592));
#281631=CARTESIAN_POINT('Ctrl Pts',(0.764444850967365,1.79957052493212,
4.90618298153223));
#281632=CARTESIAN_POINT('Ctrl Pts',(0.827182859940686,1.77160295460249,
4.90227219440527));
#281633=CARTESIAN_POINT('Ctrl Pts',(0.888198825250868,1.74046512370199,
4.8983614072783));
#281634=CARTESIAN_POINT('Ctrl Pts',(0.949320146339253,1.70927352735847,
4.89444386742655));
#281635=CARTESIAN_POINT('Ctrl Pts',(1.00871306375764,1.67490099134177,4.89052632757481));
#281636=CARTESIAN_POINT('Ctrl Pts',(1.06604177063362,1.63758082037631,4.88660878772306));
#281637=CARTESIAN_POINT('Ctrl Pts',(1.09309951169722,1.61996661664732,4.88475980516805));
#281638=CARTESIAN_POINT('Ctrl Pts',(1.11969788540273,1.60169639590686,4.88291082261304));
#281639=CARTESIAN_POINT('Ctrl Pts',(1.1458042121979,1.58279774681087,4.88106184005803));
#281640=CARTESIAN_POINT('Ctrl Pts',(1.20112523791307,1.54275026480297,4.87714372425893));
#281641=CARTESIAN_POINT('Ctrl Pts',(1.25445382591107,1.49971958144554,4.87322560845983));
#281642=CARTESIAN_POINT('Ctrl Pts',(1.30545027198386,1.45393108068342,4.86930749266073));
#281643=CARTESIAN_POINT('Ctrl Pts',(1.3563699256459,1.40821153000761,4.86539527691117));
#281644=CARTESIAN_POINT('Ctrl Pts',(1.40496404406613,1.35974272979661,4.8614830611616));
#281645=CARTESIAN_POINT('Ctrl Pts',(1.45092363314304,1.30879204260531,4.85757084541203));
#281646=CARTESIAN_POINT('Ctrl Pts',(1.49682917633276,1.25790127055138,4.85366323020776));
#281647=CARTESIAN_POINT('Ctrl Pts',(1.54010601506789,1.20453477133229,4.84975561500348));
#281648=CARTESIAN_POINT('Ctrl Pts',(1.58048122198482,1.14899743557302,4.84584799979921));
#281649=CARTESIAN_POINT('Ctrl Pts',(1.62083112325575,1.09349490850615,4.84194283373971));
#281650=CARTESIAN_POINT('Ctrl Pts',(1.65828271171005,1.03582464085439,4.8380376676802));
#281651=CARTESIAN_POINT('Ctrl Pts',(1.69260367060217,0.976324133812159,
4.8341325016207));
#281652=CARTESIAN_POINT('Ctrl Pts',(1.72691488996115,0.916840511704942,
4.83022844376143));
#281653=CARTESIAN_POINT('Ctrl Pts',(1.75809699773753,0.855528107148066,
4.82632438590215));
#281654=CARTESIAN_POINT('Ctrl Pts',(1.78596228848867,0.792751350737605,
4.82242032804287));
#281655=CARTESIAN_POINT('Ctrl Pts',(1.81382922873186,0.729970878243186,
4.81851603908202));
#281656=CARTESIAN_POINT('Ctrl Pts',(1.83837876493259,0.66572633241881,4.81461175012118));
#281657=CARTESIAN_POINT('Ctrl Pts',(1.85947098934597,0.60040289787835,4.81070746116033));
#281658=CARTESIAN_POINT('Ctrl Pts',(1.88058568040124,0.535009883279296,
4.80679901349815));
#281659=CARTESIAN_POINT('Ctrl Pts',(1.89823555891359,0.468536155516436,
4.80289056583597));
#281660=CARTESIAN_POINT('Ctrl Pts',(1.91233066466294,0.401381899180544,
4.79898211817378));
#281661=CARTESIAN_POINT('Ctrl Pts',(1.9264342072666,0.334187446574648,4.79507133104682));
#281662=CARTESIAN_POINT('Ctrl Pts',(1.9369786669408,0.266312140827596,4.79116054391985));
#281663=CARTESIAN_POINT('Ctrl Pts',(1.94392573587282,0.198163400786621,
4.78724975679289));
#281664=CARTESIAN_POINT('Ctrl Pts',(1.95088480025308,0.129896988862477,
4.78333221694114));
#281665=CARTESIAN_POINT('Ctrl Pts',(1.95423405256825,0.0613566913681232,
4.77941467708939));
#281666=CARTESIAN_POINT('Ctrl Pts',(1.95398728604934,-0.00704882667864861,
4.77549713723764));
#281667=CARTESIAN_POINT('Ctrl Pts',(1.95387081831553,-0.0393345504547654,
4.77364815468263));
#281668=CARTESIAN_POINT('Ctrl Pts',(1.95295405138724,-0.0715903094458734,
4.77179917212761));
#281669=CARTESIAN_POINT('Ctrl Pts',(1.95124243048703,-0.103773683885063,
4.76995018957259));
#281670=CARTESIAN_POINT('Ctrl Pts',(1.94761539308043,-0.171972373762527,
4.76603207377349));
#281671=CARTESIAN_POINT('Ctrl Pts',(1.94040139983398,-0.240115871687915,
4.76211395797439));
#281672=CARTESIAN_POINT('Ctrl Pts',(1.92960547582867,-0.307796536127403,
4.75819584217529));
#281673=CARTESIAN_POINT('Ctrl Pts',(1.91882580874114,-0.375375284418118,
4.75428362642573));
#281674=CARTESIAN_POINT('Ctrl Pts',(1.90447499255426,-0.442492100594856,
4.75037141067616));
#281675=CARTESIAN_POINT('Ctrl Pts',(1.88660997710864,-0.508742365322707,
4.74645919492659));
#281676=CARTESIAN_POINT('Ctrl Pts',(1.86876596991459,-0.574914723472059,
4.74255157972232));
#281677=CARTESIAN_POINT('Ctrl Pts',(1.84741609813031,-0.640222081285704,
4.73864396451804));
#281678=CARTESIAN_POINT('Ctrl Pts',(1.82266840397388,-0.704269755956704,
4.73473634931377));
#281679=CARTESIAN_POINT('Ctrl Pts',(1.79793622073208,-0.768277287978138,
4.73083118325427));
#281680=CARTESIAN_POINT('Ctrl Pts',(1.76981061650736,-0.831026245226591,
4.72692601719477));
#281681=CARTESIAN_POINT('Ctrl Pts',(1.73844906030112,-0.892138366363726,
4.72302085113527));
#281682=CARTESIAN_POINT('Ctrl Pts',(1.70709640381466,-0.953233145225211,
4.71911679327599));
#281683=CARTESIAN_POINT('Ctrl Pts',(1.67250984278654,-1.01269157266969,
4.71521273541672));
#281684=CARTESIAN_POINT('Ctrl Pts',(1.63489367119866,-1.07015825179015,
4.71130867755744));
#281685=CARTESIAN_POINT('Ctrl Pts',(1.5972752729132,-1.12762833266338,4.7074043885966));
#281686=CARTESIAN_POINT('Ctrl Pts',(1.55662717955417,-1.18310602099055,
4.70350009963575));
#281687=CARTESIAN_POINT('Ctrl Pts',(1.5131970513389,-1.23626481136497,4.69959581067491));
#281688=CARTESIAN_POINT('Ctrl Pts',(1.46972066298917,-1.28948022447783,
4.69568736301272));
#281689=CARTESIAN_POINT('Ctrl Pts',(1.42345663771862,-1.34037142862899,
4.69177891535054));
#281690=CARTESIAN_POINT('Ctrl Pts',(1.37469233479326,-1.38864573763817,
4.68787046768836));
#281691=CARTESIAN_POINT('Ctrl Pts',(1.32589884320296,-1.43694894201848,
4.6839596805614));
#281692=CARTESIAN_POINT('Ctrl Pts',(1.27460246286418,-1.48263180668583,
4.68004889343443));
#281693=CARTESIAN_POINT('Ctrl Pts',(1.22112465363547,-1.5254411100674,4.67613810630747));
#281694=CARTESIAN_POINT('Ctrl Pts',(1.16755450470222,-1.56832433192997,
4.67222056645572));
#281695=CARTESIAN_POINT('Ctrl Pts',(1.11179580870225,-1.60832380307731,
4.66830302660398));
#281696=CARTESIAN_POINT('Ctrl Pts',(1.05419933932767,-1.64522939220071,
4.66438548675223));
#281697=CARTESIAN_POINT('Ctrl Pts',(1.02701522094348,-1.66264792348678,
4.6625365041972));
#281698=CARTESIAN_POINT('Ctrl Pts',(0.999422077750991,-1.67937792344079,
4.66068752164218));
#281699=CARTESIAN_POINT('Ctrl Pts',(0.971458497828496,-1.69540095169161,
4.65883853908715));
#281700=CARTESIAN_POINT('Ctrl Pts',(0.912201830427331,-1.72935480375381,
4.65492042328805));
#281701=CARTESIAN_POINT('Ctrl Pts',(0.851045450939923,-1.76026556654062,
4.65100230748895));
#281702=CARTESIAN_POINT('Ctrl Pts',(0.788334516211265,-1.78791629853021,
4.64708419168985));
#281703=CARTESIAN_POINT('Ctrl Pts',(0.725718014021166,-1.81552539298359,
4.64317197594028));
#281704=CARTESIAN_POINT('Ctrl Pts',(0.661552048916903,-1.83988400257387,
4.63925976019072));
#281705=CARTESIAN_POINT('Ctrl Pts',(0.596207410383258,-1.86082044373015,
4.63534754444115));
#281706=CARTESIAN_POINT('Ctrl Pts',(0.530939613462734,-1.88173226481129,
4.63143992923688));
#281707=CARTESIAN_POINT('Ctrl Pts',(0.464496362042833,-1.89922976036229,
4.6275323140326));
#281708=CARTESIAN_POINT('Ctrl Pts',(0.39726781841187,-1.91318955685376,
4.62362469882833));
#281709=CARTESIAN_POINT('Ctrl Pts',(0.330081411078304,-1.92714060387506,
4.61971953276883));
#281710=CARTESIAN_POINT('Ctrl Pts',(0.262111168410904,-1.93755825046676,
4.61581436670933));
#281711=CARTESIAN_POINT('Ctrl Pts',(0.193760274311138,-1.94436955234823,
4.61190920064983));
#281712=CARTESIAN_POINT('Ctrl Pts',(0.125428776691556,-1.95117892133206,
4.60800514279055));
#281713=CARTESIAN_POINT('Ctrl Pts',(0.0567173313050693,-1.95438392848071,
4.60410108493127));
#281714=CARTESIAN_POINT('Ctrl Pts',(-0.0119646801941463,-1.95396336875282,
4.600197027072));
#281715=CARTESIAN_POINT('Ctrl Pts',(-0.0806507573402421,-1.95354278412979,
4.59629273811115));
#281716=CARTESIAN_POINT('Ctrl Pts',(-0.149306905286468,-1.94949621211857,
4.5923884491503));
#281717=CARTESIAN_POINT('Ctrl Pts',(-0.217524484051122,-1.94185455141169,
4.58848416018946));
#281718=CARTESIAN_POINT('Ctrl Pts',(-0.285814725607615,-1.93420475109606,
4.58457571252727));
#281719=CARTESIAN_POINT('Ctrl Pts',(-0.353664975939816,-1.92295227474412,
4.58066726486509));
#281720=CARTESIAN_POINT('Ctrl Pts',(-0.420673465772656,-1.90817971774014,
4.5767588172029));
#281721=CARTESIAN_POINT('Ctrl Pts',(-0.487722064624607,-1.8933983183824,
4.57284803007594));
#281722=CARTESIAN_POINT('Ctrl Pts',(-0.553927426067727,-1.87509277615426,
4.56893724294897));
#281723=CARTESIAN_POINT('Ctrl Pts',(-0.618902431213532,-1.85339574312611,
4.56502645582201));
#281724=CARTESIAN_POINT('Ctrl Pts',(-0.683989628179872,-1.83166124600495,
4.56110891597026));
#281725=CARTESIAN_POINT('Ctrl Pts',(-0.747841771348525,-1.8065237504166,
4.55719137611851));
#281726=CARTESIAN_POINT('Ctrl Pts',(-0.8100920348914,-1.7781639111751,4.55327383626677));
#281727=CARTESIAN_POINT('Ctrl Pts',(-0.839472629777884,-1.764778763862,
4.55142485371175));
#281728=CARTESIAN_POINT('Ctrl Pts',(-0.868496751906081,-1.75067646673078,
4.54957587115674));
#281729=CARTESIAN_POINT('Ctrl Pts',(-0.897127975177005,-1.73587943018944,
4.54772688860172));
#281730=CARTESIAN_POINT('Ctrl Pts',(-0.957799422801613,-1.70452353529726,
4.54380877280262));
#281731=CARTESIAN_POINT('Ctrl Pts',(-1.01694526252404,-1.66992082367519,
4.53989065700352));
#281732=CARTESIAN_POINT('Ctrl Pts',(-1.07419599511933,-1.63224353699734,
4.53597254120442));
#281733=CARTESIAN_POINT('Ctrl Pts',(-1.1313605173585,-1.59462298622758,
4.53206032545485));
#281734=CARTESIAN_POINT('Ctrl Pts',(-1.18663518852539,-1.55393731717425,
4.52814810970529));
#281735=CARTESIAN_POINT('Ctrl Pts',(-1.23967462057726,-1.51040485800881,
4.52423589395573));
#281736=CARTESIAN_POINT('Ctrl Pts',(-1.29265168124554,-1.46692359056253,
4.52032827875145));
#281737=CARTESIAN_POINT('Ctrl Pts',(-1.3433983446566,-1.42060249210352,
4.51642066354718));
#281738=CARTESIAN_POINT('Ctrl Pts',(-1.39159929401837,-1.37170237474737,
4.5125130483429));
#281739=CARTESIAN_POINT('Ctrl Pts',(-1.43977003285607,-1.32283290612723,
4.5086078822834));
#281740=CARTESIAN_POINT('Ctrl Pts',(-1.48539787819898,-1.27138797461653,
4.5047027162239));
#281741=CARTESIAN_POINT('Ctrl Pts',(-1.52820281048915,-1.21766669085307,
4.5007975501644));
#281742=CARTESIAN_POINT('Ctrl Pts',(-1.57099559568114,-1.1639606520082,
4.49689349230512));
#281743=CARTESIAN_POINT('Ctrl Pts',(-1.61096675172384,-1.10797992780303,
4.49298943444584));
#281744=CARTESIAN_POINT('Ctrl Pts',(-1.64787635895505,-1.05005690588513,
4.48908537658657));
#281745=CARTESIAN_POINT('Ctrl Pts',(-1.68478815105862,-0.992130455201143,
4.48518108762572));
#281746=CARTESIAN_POINT('Ctrl Pts',(-1.71863777238092,-0.932261894735825,
4.48127679866488));
#281747=CARTESIAN_POINT('Ctrl Pts',(-1.74922947427241,-0.870811257584943,
4.47737250970403));
#281748=CARTESIAN_POINT('Ctrl Pts',(-1.77985376129089,-0.80929516553319,
4.47346406204185));
#281749=CARTESIAN_POINT('Ctrl Pts',(-1.80721298377762,-0.746194074899896,
4.46955561437967));
#281750=CARTESIAN_POINT('Ctrl Pts',(-1.83115854742829,-0.681890294827787,
4.46564716671748));
#281751=CARTESIAN_POINT('Ctrl Pts',(-1.85511844408471,-0.617548024684482,
4.46173637959052));
#281752=CARTESIAN_POINT('Ctrl Pts',(-1.87566046823998,-0.552002101823619,
4.45782559246356));
#281753=CARTESIAN_POINT('Ctrl Pts',(-1.89268602308817,-0.485649686509395,
4.45391480533659));
#281754=CARTESIAN_POINT('Ctrl Pts',(-1.90974097582545,-0.419182701011528,
4.44999726548484));
#281755=CARTESIAN_POINT('Ctrl Pts',(-1.9232672438945,-0.351906925699697,
4.4460797256331));
#281756=CARTESIAN_POINT('Ctrl Pts',(-1.93321756400612,-0.284228517602009,
4.44216218578135));
#281757=CARTESIAN_POINT('Ctrl Pts',(-1.93791387061678,-0.252285971856508,
4.44031320322633));
#281758=CARTESIAN_POINT('Ctrl Pts',(-1.94181434939227,-0.220253789367341,
4.43846422067131));
#281759=CARTESIAN_POINT('Ctrl Pts',(-1.94491806301935,-0.188174727689601,
4.43661523811628));
#281760=CARTESIAN_POINT('Ctrl Pts',(-1.95093057648437,-0.126031175333595,
4.43303338945227));
#281761=CARTESIAN_POINT('Ctrl Pts',(-1.95396532753133,-0.0635949222937433,
4.42945154078825));
#281762=CARTESIAN_POINT('Ctrl Pts',(-1.95399970461562,-0.00107441242398919,
4.42586969212423));
#281763=CARTESIAN_POINT('',(-1.95135107115213,-0.00103745302926256,3.72586969212423));
#281764=CARTESIAN_POINT('Ctrl Pts',(-1.95645563342917,-0.00105870546452921,
4.42586871612197));
#281765=CARTESIAN_POINT('Ctrl Pts',(-1.95257657647916,0.583629271897111,
4.3924136732916));
#281766=CARTESIAN_POINT('Ctrl Pts',(-1.36373841242988,1.82237443771501,
4.32192141363275));
#281767=CARTESIAN_POINT('Ctrl Pts',(0.742695215461096,2.18665711155625,
4.21439193714541));
#281768=CARTESIAN_POINT('Ctrl Pts',(2.23979789625715,0.562468568463699,
4.10328028665997));
#281769=CARTESIAN_POINT('Ctrl Pts',(1.68767452724564,-1.57633124585983,
3.99216863617453));
#281770=CARTESIAN_POINT('Ctrl Pts',(-0.408528604769658,-2.272921002955,
3.88105698568911));
#281771=CARTESIAN_POINT('Ctrl Pts',(-1.78456893999856,-1.16809907040787,
3.79229067100566));
#281772=CARTESIAN_POINT('Ctrl Pts',(-1.9525967846073,-0.259527562563923,
3.74056157315071));
#281773=CARTESIAN_POINT('Ctrl Pts',(-1.95135107115213,-0.00103745302926256,
3.72586969212423));
#281774=CARTESIAN_POINT('',(-1.95399929791996,0.00165642032925726,3.02586967147267));
#281775=CARTESIAN_POINT('Ctrl Pts',(-1.95135107115213,-0.00103745302926256,
3.72586969212423));
#281776=CARTESIAN_POINT('Ctrl Pts',(-1.9494564270682,0.392108141373472,
3.70352435632223));
#281777=CARTESIAN_POINT('Ctrl Pts',(-1.64339421395861,1.43960318986175,
3.64414180369176));
#281778=CARTESIAN_POINT('Ctrl Pts',(0.0652379087403862,2.30842143506328,
3.54772203423277));
#281779=CARTESIAN_POINT('Ctrl Pts',(1.97453422882562,1.19761433098204,3.43661038374736));
#281780=CARTESIAN_POINT('Ctrl Pts',(2.07729836817095,-1.00890881459804,
3.32549873326191));
#281781=CARTESIAN_POINT('Ctrl Pts',(0.279509811935439,-2.29236554058799,
3.21438708277647));
#281782=CARTESIAN_POINT('Ctrl Pts',(-1.5663607178597,-1.56079696856402,
3.11451073573059));
#281783=CARTESIAN_POINT('Ctrl Pts',(-1.94902846959061,-0.451530792879088,
3.05167160551317));
#281784=CARTESIAN_POINT('Ctrl Pts',(-1.95267691385146,0.00165493661177622,
3.02586969212423));
#281785=CARTESIAN_POINT('',(-1.95399999957489,4.07595347864031E-5,2.32586969217892));
#281786=CARTESIAN_POINT('Ctrl Pts',(-1.95399929791996,0.00165642032925726,
3.02586967147267));
#281787=CARTESIAN_POINT('Ctrl Pts',(-1.95392951629332,0.0839744449554839,
3.02118607042525));
#281788=CARTESIAN_POINT('Ctrl Pts',(-1.94865405009171,0.166066844841771,
3.01650246937784));
#281789=CARTESIAN_POINT('Ctrl Pts',(-1.93828099351015,0.247351551839267,
3.01181886833043));
#281790=CARTESIAN_POINT('Ctrl Pts',(-1.92776575156035,0.32975044306072,
3.00707106831384));
#281791=CARTESIAN_POINT('Ctrl Pts',(-1.91201229505569,0.411319330749024,
3.00232326829726));
#281792=CARTESIAN_POINT('Ctrl Pts',(-1.89118208470578,0.491473623389805,
2.99757546828068));
#281793=CARTESIAN_POINT('Ctrl Pts',(-1.88326778283756,0.521927721420327,
2.99577157278899));
#281794=CARTESIAN_POINT('Ctrl Pts',(-1.8746211078826,0.552177835310333,
2.9939676772973));
#281795=CARTESIAN_POINT('Ctrl Pts',(-1.86525270256443,0.582192713434385,
2.99216378180561));
#281796=CARTESIAN_POINT('Ctrl Pts',(-1.84490424166246,0.647385940375561,
2.98824566600711));
#281797=CARTESIAN_POINT('Ctrl Pts',(-1.82109343506899,0.711640305956234,
2.98432755020861));
#281798=CARTESIAN_POINT('Ctrl Pts',(-1.79392577154405,0.774562022171296,
2.98040943441011));
#281799=CARTESIAN_POINT('Ctrl Pts',(-1.76679901813221,0.837388988444973,
2.97649721866114));
#281800=CARTESIAN_POINT('Ctrl Pts',(-1.73632563335625,0.898886840098444,
2.97258500291217));
#281801=CARTESIAN_POINT('Ctrl Pts',(-1.70266067811188,0.958677534529514,
2.9686727871632));
#281802=CARTESIAN_POINT('Ctrl Pts',(-1.66903531095797,1.01839791847294,
2.96476517195951));
#281803=CARTESIAN_POINT('Ctrl Pts',(-1.63222606724913,1.07641470557962,
2.96085755675582));
#281804=CARTESIAN_POINT('Ctrl Pts',(-1.59243506670914,1.13237209357837,
2.95694994155213));
#281805=CARTESIAN_POINT('Ctrl Pts',(-1.55266900565673,1.188294409612,2.95304477549321));
#281806=CARTESIAN_POINT('Ctrl Pts',(-1.50992517939374,1.24215948701812,
2.94913960943428));
#281807=CARTESIAN_POINT('Ctrl Pts',(-1.46444955172051,1.2936396370186,2.94523444337536));
#281808=CARTESIAN_POINT('Ctrl Pts',(-1.41898682902996,1.34510517808504,
2.94133038551666));
#281809=CARTESIAN_POINT('Ctrl Pts',(-1.37079416937919,1.39418676681743,
2.93742632765796));
#281810=CARTESIAN_POINT('Ctrl Pts',(-1.32015726901447,1.44059042932689,
2.93352226979925));
#281811=CARTESIAN_POINT('Ctrl Pts',(-1.26951737118713,1.48699683871152,
2.92961798083897));
#281812=CARTESIAN_POINT('Ctrl Pts',(-1.21643330976193,1.53072467672382,
2.92571369187869));
#281813=CARTESIAN_POINT('Ctrl Pts',(-1.16122567402963,1.57151867121407,
2.92180940291841));
#281814=CARTESIAN_POINT('Ctrl Pts',(-1.10595923320594,1.61235611792867,
2.91790095525678));
#281815=CARTESIAN_POINT('Ctrl Pts',(-1.04856510027811,1.6502531916732,2.91399250759515));
#281816=CARTESIAN_POINT('Ctrl Pts',(-0.989393987541334,1.68499719210955,
2.91008405993352));
#281817=CARTESIAN_POINT('Ctrl Pts',(-0.930187456974603,1.7197619891313,
2.9061732728071));
#281818=CARTESIAN_POINT('Ctrl Pts',(-0.869202266529201,1.75136973035253,
2.90226248568068));
#281819=CARTESIAN_POINT('Ctrl Pts',(-0.806812432811743,1.77965437606868,
2.89835169855427));
#281820=CARTESIAN_POINT('Ctrl Pts',(-0.744314871068234,1.80798786065599,
2.89443415870305));
#281821=CARTESIAN_POINT('Ctrl Pts',(-0.680408283207271,1.83298661859123,
2.89051661885183));
#281822=CARTESIAN_POINT('Ctrl Pts',(-0.615484456569281,1.85453360274804,
2.88659907900062));
#281823=CARTESIAN_POINT('Ctrl Pts',(-0.584842005502758,1.86470324988448,
2.88475009644046));
#281824=CARTESIAN_POINT('Ctrl Pts',(-0.553973137488596,1.87410470950349,
2.88290111388031));
#281825=CARTESIAN_POINT('Ctrl Pts',(-0.522919798301886,1.88272963660317,
2.88105213132016));
#281826=CARTESIAN_POINT('Ctrl Pts',(-0.457115727740939,1.90100642506827,
2.87713401552196));
#281827=CARTESIAN_POINT('Ctrl Pts',(-0.390221858888982,1.91586537239888,
2.87321589972376));
#281828=CARTESIAN_POINT('Ctrl Pts',(-0.3226262170164,1.92718144555558,2.86929778392556));
#281829=CARTESIAN_POINT('Ctrl Pts',(-0.255132363262565,1.93848047853386,
2.86538556817691));
#281830=CARTESIAN_POINT('Ctrl Pts',(-0.186939315002833,1.94624714485532,
2.86147335242825));
#281831=CARTESIAN_POINT('Ctrl Pts',(-0.118448765895021,1.95040659603528,
2.8575611366796));
#281832=CARTESIAN_POINT('Ctrl Pts',(-0.0500387578140951,1.95456115593501,
2.85365352147625));
#281833=CARTESIAN_POINT('Ctrl Pts',(0.0186675676677738,1.95511689545972,
2.84974590627289));
#281834=CARTESIAN_POINT('Ctrl Pts',(0.0872616680058097,1.9520505632019,
2.84583829106954));
#281835=CARTESIAN_POINT('Ctrl Pts',(0.155812776167267,1.94898615280466,
2.84193312501097));
#281836=CARTESIAN_POINT('Ctrl Pts',(0.224251308427534,1.94230419585193,
2.8380279589524));
#281837=CARTESIAN_POINT('Ctrl Pts',(0.292168551116957,1.93203352396852,
2.83412279289382));
#281838=CARTESIAN_POINT('Ctrl Pts',(0.360066520386865,1.92176576667587,
2.83021873503548));
#281839=CARTESIAN_POINT('Ctrl Pts',(0.427443007631104,1.90791138966129,
2.82631467717713));
#281840=CARTESIAN_POINT('Ctrl Pts',(0.493896064121049,1.89055089268862,
2.82241061931879));
#281841=CARTESIAN_POINT('Ctrl Pts',(0.56035305431426,1.87318936805752,2.81850633035888));
#281842=CARTESIAN_POINT('Ctrl Pts',(0.625886029970531,1.85232143822732,
2.81460204139897));
#281843=CARTESIAN_POINT('Ctrl Pts',(0.690106621978033,1.82807791144198,
2.81069775243906));
#281844=CARTESIAN_POINT('Ctrl Pts',(0.75439561933792,1.80380856136631,2.80678930477781));
#281845=CARTESIAN_POINT('Ctrl Pts',(0.817368982204935,1.77615661276738,
2.80288085711657));
#281846=CARTESIAN_POINT('Ctrl Pts',(0.878657760003433,1.7453012750771,2.79897240945532));
#281847=CARTESIAN_POINT('Ctrl Pts',(0.939983223194562,1.71442746842368,
2.79506162232929));
#281848=CARTESIAN_POINT('Ctrl Pts',(0.999621667418628,1.68034670070226,
2.79115083520326));
#281849=CARTESIAN_POINT('Ctrl Pts',(1.05723069479197,1.64328307299433,2.78724004807723));
#281850=CARTESIAN_POINT('Ctrl Pts',(1.11493919521126,1.60615544781742,2.78332250822641));
#281851=CARTESIAN_POINT('Ctrl Pts',(1.17061088616287,1.56603497055071,2.77940496837559));
#281852=CARTESIAN_POINT('Ctrl Pts',(1.22393488355458,1.52318725074045,2.77548742852477));
#281853=CARTESIAN_POINT('Ctrl Pts',(1.24910250025779,1.50296417967416,2.77363844596142));
#281854=CARTESIAN_POINT('Ctrl Pts',(1.27374765826116,1.48213413776215,2.77178946339808));
#281855=CARTESIAN_POINT('Ctrl Pts',(1.29784059017172,1.46072783313755,2.76994048083473));
#281856=CARTESIAN_POINT('Ctrl Pts',(1.34889509935635,1.41536646408033,2.76602236503161));
#281857=CARTESIAN_POINT('Ctrl Pts',(1.39766978596067,1.36723531030175,2.76210424922848));
#281858=CARTESIAN_POINT('Ctrl Pts',(1.44384909857897,1.31659248840813,2.75818613342535));
#281859=CARTESIAN_POINT('Ctrl Pts',(1.48995887261158,1.26602592642419,2.75427391767175));
#281860=CARTESIAN_POINT('Ctrl Pts',(1.53348070031946,1.21295556312259,2.75036170191815));
#281861=CARTESIAN_POINT('Ctrl Pts',(1.57413377107873,1.15767822418384,2.74644948616455));
#281862=CARTESIAN_POINT('Ctrl Pts',(1.61473903611734,1.10246588828114,2.74254187095625));
#281863=CARTESIAN_POINT('Ctrl Pts',(1.65248195398085,1.04505212538573,2.73863425574794));
#281864=CARTESIAN_POINT('Ctrl Pts',(1.68712134125316,0.985767508030231,
2.73472664053963));
#281865=CARTESIAN_POINT('Ctrl Pts',(1.72173901787332,0.926520048020952,
2.73082147447611));
#281866=CARTESIAN_POINT('Ctrl Pts',(1.75325677492154,0.865404483324416,
2.72691630841259));
#281867=CARTESIAN_POINT('Ctrl Pts',(1.78147708737339,0.802779787465782,
2.72301114234906));
#281868=CARTESIAN_POINT('Ctrl Pts',(1.80968939152128,0.74017286311841,2.71910708448577));
#281869=CARTESIAN_POINT('Ctrl Pts',(1.83460590669313,0.676058106015654,
2.71520302662248));
#281870=CARTESIAN_POINT('Ctrl Pts',(1.85607618084242,0.610816839084709,
2.71129896875919));
#281871=CARTESIAN_POINT('Ctrl Pts',(1.87754772592922,0.545571710182866,
2.70739467979435));
#281872=CARTESIAN_POINT('Ctrl Pts',(1.89557247365616,0.479200407091641,
2.70349039082952));
#281873=CARTESIAN_POINT('Ctrl Pts',(1.91004960005145,0.412100139945747,
2.69958610186468));
#281874=CARTESIAN_POINT('Ctrl Pts',(1.92454214693551,0.34492840012718,2.69567765419855));
#281875=CARTESIAN_POINT('Ctrl Pts',(1.9354794272508,0.277026628409668,2.69176920653243));
#281876=CARTESIAN_POINT('Ctrl Pts',(1.94281181078051,0.208801982489967,
2.68786075886631));
#281877=CARTESIAN_POINT('Ctrl Pts',(1.95014858322734,0.140536499601684,
2.68394997173543));
#281878=CARTESIAN_POINT('Ctrl Pts',(1.95387613783361,0.0719482491074181,
2.68003918460455));
#281879=CARTESIAN_POINT('Ctrl Pts',(1.95399696060566,0.0034464392987964,
2.67612839747367));
#281880=CARTESIAN_POINT('Ctrl Pts',(1.95411799200142,-0.0651736520342156,
2.67221085761809));
#281881=CARTESIAN_POINT('Ctrl Pts',(1.95061988710443,-0.133706513809952,
2.66829331776251));
#281882=CARTESIAN_POINT('Ctrl Pts',(1.94355709777815,-0.201746890127626,
2.66437577790692));
#281883=CARTESIAN_POINT('Ctrl Pts',(1.9402236348186,-0.233860275325921,
2.66252679538771));
#281884=CARTESIAN_POINT('Ctrl Pts',(1.93609684316677,-0.265864087601263,
2.6606778128685));
#281885=CARTESIAN_POINT('Ctrl Pts',(1.93118636846368,-0.297716661038726,
2.65882883034929));
#281886=CARTESIAN_POINT('Ctrl Pts',(1.92078074899972,-0.365214363028623,
2.65491071455524));
#281887=CARTESIAN_POINT('Ctrl Pts',(1.90681153135665,-0.432299674055665,
2.65099259876119));
#281888=CARTESIAN_POINT('Ctrl Pts',(1.88932434089903,-0.498567482780869,
2.64707448296715));
#281889=CARTESIAN_POINT('Ctrl Pts',(1.87186348332563,-0.564735502889988,
2.64316226722262));
#281890=CARTESIAN_POINT('Ctrl Pts',(1.85089529109169,-0.630087992075255,
2.63925005147809));
#281891=CARTESIAN_POINT('Ctrl Pts',(1.82651675462935,-0.694228020940006,
2.63533783573356));
#281892=CARTESIAN_POINT('Ctrl Pts',(1.80216688595202,-0.758292624745466,
2.63143022053427));
#281893=CARTESIAN_POINT('Ctrl Pts',(1.7744148116385,-0.821147142249368,
2.62752260533498));
#281894=CARTESIAN_POINT('Ctrl Pts',(1.74340736987258,-0.882409622949545,
2.62361499013569));
#281895=CARTESIAN_POINT('Ctrl Pts',(1.71241936239306,-0.943633706654438,
2.61970982408114));
#281896=CARTESIAN_POINT('Ctrl Pts',(1.67818025647906,-1.00326729504705,
2.61580465802659));
#281897=CARTESIAN_POINT('Ctrl Pts',(1.64088443447867,-1.06094970318372,
2.61189949197204));
#281898=CARTESIAN_POINT('Ctrl Pts',(1.60359919621175,-1.11861574232244,
2.60799543411767));
#281899=CARTESIAN_POINT('Ctrl Pts',(1.56325923080096,-1.17433128753308,
2.6040913762633));
#281900=CARTESIAN_POINT('Ctrl Pts',(1.52010323380703,-1.22776307102365,
2.60018731840893));
#281901=CARTESIAN_POINT('Ctrl Pts',(1.47694468218376,-1.28119801742113,
2.59628302945295));
#281902=CARTESIAN_POINT('Ctrl Pts',(1.43097007908696,-1.33234855266104,
2.59237874049696));
#281903=CARTESIAN_POINT('Ctrl Pts',(1.38245839110996,-1.38091447847057,
2.58847445154098));
#281904=CARTESIAN_POINT('Ctrl Pts',(1.33389503031134,-1.42953213487382,
2.58456600388355));
#281905=CARTESIAN_POINT('Ctrl Pts',(1.28278953974889,-1.47555933897962,
2.58065755622612));
#281906=CARTESIAN_POINT('Ctrl Pts',(1.22945701702434,-1.5187334997588,2.57674910856869));
#281907=CARTESIAN_POINT('Ctrl Pts',(1.17609257125198,-1.56193350313323,
2.57283832144643));
#281908=CARTESIAN_POINT('Ctrl Pts',(1.12049883850661,-1.60227677553843,
2.56892753432417));
#281909=CARTESIAN_POINT('Ctrl Pts',(1.06302091419834,-1.63954339252638,
2.56501674720191));
#281910=CARTESIAN_POINT('Ctrl Pts',(1.00544374321688,-1.67687435748447,
2.56109920735473));
#281911=CARTESIAN_POINT('Ctrl Pts',(0.945976313404811,-1.71111781892955,
2.55718166750755));
#281912=CARTESIAN_POINT('Ctrl Pts',(0.884988593721316,-1.74209964955601,
2.55326412766038));
#281913=CARTESIAN_POINT('Ctrl Pts',(0.856203887799534,-1.75672231274344,
2.55141514506154));
#281914=CARTESIAN_POINT('Ctrl Pts',(0.827080811940253,-1.77061910918343,
2.54956616246269));
#281915=CARTESIAN_POINT('Ctrl Pts',(0.797659599874164,-1.78377553597099,
2.54771717986385));
#281916=CARTESIAN_POINT('Ctrl Pts',(0.735314115511668,-1.81165487006191,
2.54379906406891));
#281917=CARTESIAN_POINT('Ctrl Pts',(0.671381648945562,-1.83631694044419,
2.53988094827396));
#281918=CARTESIAN_POINT('Ctrl Pts',(0.606227258951757,-1.85758028373038,
2.53596283247901));
#281919=CARTESIAN_POINT('Ctrl Pts',(0.541170980946729,-1.87881160785565,
2.53205061673367));
#281920=CARTESIAN_POINT('Ctrl Pts',(0.474896895147722,-1.89665421079382,
2.52813840098833));
#281921=CARTESIAN_POINT('Ctrl Pts',(0.407791054982178,-1.9109742163296,
2.52422618524299));
#281922=CARTESIAN_POINT('Ctrl Pts',(0.340764127505167,-1.92527738234539,
2.52031857004302));
#281923=CARTESIAN_POINT('Ctrl Pts',(0.272907866947681,-1.93606607561432,
2.51641095484305));
#281924=CARTESIAN_POINT('Ctrl Pts',(0.204622788546888,-1.94325642013793,
2.51250333964308));
#281925=CARTESIAN_POINT('Ctrl Pts',(0.136380508640256,-1.95044225802664,
2.50859817358794));
#281926=CARTESIAN_POINT('Ctrl Pts',(0.0677104321158824,-1.95403416959126,
2.5046930075328));
#281927=CARTESIAN_POINT('Ctrl Pts',(-0.000978994749919834,-1.95399975475159,
2.50078784147765));
#281928=CARTESIAN_POINT('Ctrl Pts',(-0.0696489290666075,-1.9539653496781,
2.49688378362277));
#281929=CARTESIAN_POINT('Ctrl Pts',(-0.138337711174469,-1.95030666133077,
2.4929797257679));
#281930=CARTESIAN_POINT('Ctrl Pts',(-0.20663588419952,-1.94304338895483,
2.48907566791302));
#281931=CARTESIAN_POINT('Ctrl Pts',(-0.27493810014937,-1.93577968662795,
2.48517137895661));
#281932=CARTESIAN_POINT('Ctrl Pts',(-0.342849172261745,-1.92491103121688,
2.4812670900002));
#281933=CARTESIAN_POINT('Ctrl Pts',(-0.409965574268347,-1.91050889239355,
2.4773628010438));
#281934=CARTESIAN_POINT('Ctrl Pts',(-0.4771534661346,-1.89609141295522,
2.47345435338607));
#281935=CARTESIAN_POINT('Ctrl Pts',(-0.54354451678222,-1.87813304225664,
2.46954590572834));
#281936=CARTESIAN_POINT('Ctrl Pts',(-0.608747188504485,-1.85675600456492,
2.46563745807062));
#281937=CARTESIAN_POINT('Ctrl Pts',(-0.673988888343824,-1.83536617130045,
2.46172667094813));
#281938=CARTESIAN_POINT('Ctrl Pts',(-0.738040334862839,-1.81055377623571,
2.45781588382564));
#281939=CARTESIAN_POINT('Ctrl Pts',(-0.800529556424161,-1.78248939107399,
2.45390509670315));
#281940=CARTESIAN_POINT('Ctrl Pts',(-0.863126677623894,-1.75437654736318,
2.44998755685586));
#281941=CARTESIAN_POINT('Ctrl Pts',(-0.924155752904607,-1.72300073132777,
2.44607001700857));
#281942=CARTESIAN_POINT('Ctrl Pts',(-0.983269786586064,-1.68857825604471,
2.44215247716128));
#281943=CARTESIAN_POINT('Ctrl Pts',(-1.0111701586603,-1.67233169311705,
2.440303494567));
#281944=CARTESIAN_POINT('Ctrl Pts',(-1.03864436191482,-1.65540707644465,
2.43845451197271));
#281945=CARTESIAN_POINT('Ctrl Pts',(-1.06565838499897,-1.6378303350718,
2.43660552937842));
#281946=CARTESIAN_POINT('Ctrl Pts',(-1.12286817424463,-1.60060664327163,
2.43268978886808));
#281947=CARTESIAN_POINT('Ctrl Pts',(-1.1782393626528,-1.56030757388963,
2.42877404835773));
#281948=CARTESIAN_POINT('Ctrl Pts',(-1.23142170315873,-1.51714092588317,
2.42485830784739));
#281949=CARTESIAN_POINT('Ctrl Pts',(-1.28452393606371,-1.47403929902058,
2.42094846554639));
#281950=CARTESIAN_POINT('Ctrl Pts',(-1.33544348490811,-1.42807897357161,
2.4170386232454));
#281951=CARTESIAN_POINT('Ctrl Pts',(-1.38385866196428,-1.37951121913033,
2.41312878094441));
#281952=CARTESIAN_POINT('Ctrl Pts',(-1.43221697663889,-1.33100050626882,
2.40922353065275));
#281953=CARTESIAN_POINT('Ctrl Pts',(-1.47807641473515,-1.27988879327852,
2.40531828036108));
#281954=CARTESIAN_POINT('Ctrl Pts',(-1.52114942784154,-1.22646663965123,
2.40141303006942));
#281955=CARTESIAN_POINT('Ctrl Pts',(-1.56419553052912,-1.17307786220135,
2.3975102196331));
#281956=CARTESIAN_POINT('Ctrl Pts',(-1.60445835293725,-1.11738189000708,
2.39360740919677));
#281957=CARTESIAN_POINT('Ctrl Pts',(-1.64168927749648,-1.05970388135228,
2.38970459876044));
#281958=CARTESIAN_POINT('Ctrl Pts',(-1.67890975389446,-1.00204205894968,
2.38580288357472));
#281959=CARTESIAN_POINT('Ctrl Pts',(-1.71309975449227,-0.942399717911359,
2.38190116838901));
#281960=CARTESIAN_POINT('Ctrl Pts',(-1.74405387701279,-0.881131133303468,
2.37799945320329));
#281961=CARTESIAN_POINT('Ctrl Pts',(-1.77500996482794,-0.819858658718724,
2.37409749029548));
#281962=CARTESIAN_POINT('Ctrl Pts',(-1.80272954693807,-0.756960176404744,
2.37019552738768));
#281963=CARTESIAN_POINT('Ctrl Pts',(-1.82705392995528,-0.692813060670033,
2.36629356447987));
#281964=CARTESIAN_POINT('Ctrl Pts',(-1.85140426136989,-0.628597515045426,
2.36238743909509));
#281965=CARTESIAN_POINT('Ctrl Pts',(-1.87235199103844,-0.563131139338323,
2.35848131371031));
#281966=CARTESIAN_POINT('Ctrl Pts',(-1.88978757097154,-0.496808752541134,
2.35457518832553));
#281967=CARTESIAN_POINT('Ctrl Pts',(-1.90723369128881,-0.430446271669736,
2.35066670155889));
#281968=CARTESIAN_POINT('Ctrl Pts',(-1.92116333674189,-0.363227232231232,
2.34675821479225));
#281969=CARTESIAN_POINT('Ctrl Pts',(-1.93151819040856,-0.29555622159051,
2.34284972802561));
#281970=CARTESIAN_POINT('Ctrl Pts',(-1.94189083526254,-0.227768942032294,
2.33893452589413));
#281971=CARTESIAN_POINT('Ctrl Pts',(-1.94867638232009,-0.159528631298684,
2.33501932376265));
#281972=CARTESIAN_POINT('Ctrl Pts',(-1.95186848814308,-0.0912436572812458,
2.33110412163118));
#281973=CARTESIAN_POINT('Ctrl Pts',(-1.95329105009292,-0.0608124588279669,
2.32935931181376));
#281974=CARTESIAN_POINT('Ctrl Pts',(-1.95400063397863,-0.0303723674190441,
2.32761450199634));
#281975=CARTESIAN_POINT('Ctrl Pts',(-1.95399999957489,4.07595347913703E-5,
2.32586969217892));
#281976=CARTESIAN_POINT('',(-1.9539992755619,-0.00168258835255015,1.62586971130332));
#281977=CARTESIAN_POINT('Ctrl Pts',(-1.95399999957487,4.07604881466012E-5,
2.32586969212423));
#281978=CARTESIAN_POINT('Ctrl Pts',(-1.95399995402589,0.00222431375158761,
2.32574442104715));
#281979=CARTESIAN_POINT('Ctrl Pts',(-1.95399624836735,0.00440786249150779,
2.32561914997006));
#281980=CARTESIAN_POINT('Ctrl Pts',(-1.95398888263491,0.00659139887796774,
2.32549387889298));
#281981=CARTESIAN_POINT('Ctrl Pts',(-1.95375850389951,0.0748860804947652,
2.32157576313438));
#281982=CARTESIAN_POINT('Ctrl Pts',(-1.94994286401812,0.143304051901439,
2.31765764737579));
#281983=CARTESIAN_POINT('Ctrl Pts',(-1.94252670595967,0.211437926194598,
2.31373953161719));
#281984=CARTESIAN_POINT('Ctrl Pts',(-1.93512171543734,0.279469201878615,
2.30982731590804));
#281985=CARTESIAN_POINT('Ctrl Pts',(-1.92412701988573,0.347216744430845,
2.30591510019889));
#281986=CARTESIAN_POINT('Ctrl Pts',(-1.90957937308489,0.414273602693595,
2.30200288448975));
#281987=CARTESIAN_POINT('Ctrl Pts',(-1.89504883349596,0.481251605874107,
2.29809526932556));
#281988=CARTESIAN_POINT('Ctrl Pts',(-1.87697374416079,0.547540059395919,
2.29418765416137));
#281989=CARTESIAN_POINT('Ctrl Pts',(-1.85544238223407,0.612739395020072,
2.29028003899719));
#281990=CARTESIAN_POINT('Ctrl Pts',(-1.83392451534601,0.677897866180661,
2.28637487297755));
#281991=CARTESIAN_POINT('Ctrl Pts',(-1.80895482693705,0.74196810751825,
2.28246970695791));
#281992=CARTESIAN_POINT('Ctrl Pts',(-1.78067177656173,0.804564493472392,
2.27856454093828));
#281993=CARTESIAN_POINT('Ctrl Pts',(-1.75239675229198,0.86714311595353,
2.27466048311858));
#281994=CARTESIAN_POINT('Ctrl Pts',(-1.72081043506945,0.928248265306702,
2.27075642529888));
#281995=CARTESIAN_POINT('Ctrl Pts',(-1.68609918873594,0.987514823050275,
2.26685236747919));
#281996=CARTESIAN_POINT('Ctrl Pts',(-1.6513858876595,1.04678488909601,2.26294807855758));
#281997=CARTESIAN_POINT('Ctrl Pts',(-1.61354754101906,1.10421572431086,
2.25904378963598));
#281998=CARTESIAN_POINT('Ctrl Pts',(-1.57281526226314,1.15946890893724,
2.25513950071438));
#281999=CARTESIAN_POINT('Ctrl Pts',(-1.53203959701168,1.21478094718346,
2.25123105309066));
#282000=CARTESIAN_POINT('Ctrl Pts',(-1.48836414034618,1.26791030904921,
2.24732260546693));
#282001=CARTESIAN_POINT('Ctrl Pts',(-1.44206133777691,1.31855037753173,
2.24341415784321));
#282002=CARTESIAN_POINT('Ctrl Pts',(-1.39573081990885,1.3692207574544,2.23950337075433));
#282003=CARTESIAN_POINT('Ctrl Pts',(-1.34677017694355,1.41739853356051,
2.23559258366544));
#282004=CARTESIAN_POINT('Ctrl Pts',(-1.29548787572475,1.46281480846011,
2.23168179657655));
#282005=CARTESIAN_POINT('Ctrl Pts',(-1.24411702575363,1.50830950328981,
2.22776425676189));
#282006=CARTESIAN_POINT('Ctrl Pts',(-1.19041690134462,1.55103287414906,
2.22384671694722));
#282007=CARTESIAN_POINT('Ctrl Pts',(-1.13472739017928,1.59075760252055,
2.21992917713256));
#282008=CARTESIAN_POINT('Ctrl Pts',(-1.10844330394406,1.60950670202488,
2.21808019422422));
#282009=CARTESIAN_POINT('Ctrl Pts',(-1.08171645180236,1.62758846688301,
2.21623121131588));
#282010=CARTESIAN_POINT('Ctrl Pts',(-1.0545844568764,1.64498256018558,2.21438222840754));
#282011=CARTESIAN_POINT('Ctrl Pts',(-0.997089984035675,1.68184178221119,
2.21046411262223));
#282012=CARTESIAN_POINT('Ctrl Pts',(-0.937546788773812,1.71575617240091,
2.20654599683691));
#282013=CARTESIAN_POINT('Ctrl Pts',(-0.876288810139718,1.74649188982483,
2.2026278810516));
#282014=CARTESIAN_POINT('Ctrl Pts',(-0.815123076134851,1.77718132421884,
2.1987156653163));
#282015=CARTESIAN_POINT('Ctrl Pts',(-0.752248119592166,1.8047013666763,
2.194803449581));
#282016=CARTESIAN_POINT('Ctrl Pts',(-0.688025731581611,1.82886210324387,
2.1908912338457));
#282017=CARTESIAN_POINT('Ctrl Pts',(-0.623878865491443,1.85299442814254,
2.18698361865633));
#282018=CARTESIAN_POINT('Ctrl Pts',(-0.558388172981715,1.87377512024045,
2.18307600346695));
#282019=CARTESIAN_POINT('Ctrl Pts',(-0.491937196864845,1.89106155223482,
2.17916838827758));
#282020=CARTESIAN_POINT('Ctrl Pts',(-0.425527869702247,1.90833714974852,
2.17526322223336));
#282021=CARTESIAN_POINT('Ctrl Pts',(-0.358159927818379,1.92212270800417,
2.17135805618914));
#282022=CARTESIAN_POINT('Ctrl Pts',(-0.290232427847443,1.93232531883888,
2.16745289014492));
#282023=CARTESIAN_POINT('Ctrl Pts',(-0.222324204213047,1.94252503439612,
2.16354883230128));
#282024=CARTESIAN_POINT('Ctrl Pts',(-0.153857223913402,1.9491437479538,
2.15964477445765));
#282025=CARTESIAN_POINT('Ctrl Pts',(-0.085239307148701,1.95213991827349,
2.15574071661401));
#282026=CARTESIAN_POINT('Ctrl Pts',(-0.0166173285370322,1.95513626595189,
2.15183642766913));
#282027=CARTESIAN_POINT('Ctrl Pts',(0.0521551127561943,1.95450962576515,
2.14793213872426));
#282028=CARTESIAN_POINT('Ctrl Pts',(0.120668345670809,1.95027053260646,
2.14402784977938));
#282029=CARTESIAN_POINT('Ctrl Pts',(0.189254556290487,1.94602692412602,
2.14011940213355));
#282030=CARTESIAN_POINT('Ctrl Pts',(0.257580515639657,1.93816321399345,
2.13621095448772));
#282031=CARTESIAN_POINT('Ctrl Pts',(0.325240843492128,1.92674191155031,
2.13230250684189));
#282032=CARTESIAN_POINT('Ctrl Pts',(0.392941670527916,1.9153137727019,2.12839171973152));
#282033=CARTESIAN_POINT('Ctrl Pts',(0.459975593038447,1.90032391089241,
2.12448093262115));
#282034=CARTESIAN_POINT('Ctrl Pts',(0.525949373255067,1.88188555889369,
2.12057014551079));
#282035=CARTESIAN_POINT('Ctrl Pts',(0.592037069866354,1.86341536954115,
2.11665260567583));
#282036=CARTESIAN_POINT('Ctrl Pts',(0.657060504883645,1.84148496292513,
2.11273506584087));
#282037=CARTESIAN_POINT('Ctrl Pts',(0.720644320847418,1.81625652451144,
2.10881752600591));
#282038=CARTESIAN_POINT('Ctrl Pts',(0.750654322105041,1.80434932049974,
2.10696854331131));
#282039=CARTESIAN_POINT('Ctrl Pts',(0.780343962469385,1.79170812344853,
2.1051195606167));
#282040=CARTESIAN_POINT('Ctrl Pts',(0.809675746237423,1.77835350421531,
2.1032705779221));
#282041=CARTESIAN_POINT('Ctrl Pts',(0.871831725778848,1.75005418746022,
2.09935246194773));
#282042=CARTESIAN_POINT('Ctrl Pts',(0.932625480640733,1.71843618955672,
2.09543434597337));
#282043=CARTESIAN_POINT('Ctrl Pts',(0.99167940171878,1.6836531603055,2.091516229999));
#282044=CARTESIAN_POINT('Ctrl Pts',(1.05064439714413,1.64892250866989,2.0876040140735));
#282045=CARTESIAN_POINT('Ctrl Pts',(1.10787433795939,1.61103653218617,2.08369179814801));
#282046=CARTESIAN_POINT('Ctrl Pts',(1.16301340408146,1.5701961093847,2.07977958222251));
#282047=CARTESIAN_POINT('Ctrl Pts',(1.21808762977321,1.52940371261586,2.07587196684218));
#282048=CARTESIAN_POINT('Ctrl Pts',(1.2710754704945,1.48566406084644,2.07196435146185));
#282049=CARTESIAN_POINT('Ctrl Pts',(1.32164902706319,1.43922195969312,2.06805673608152));
#282050=CARTESIAN_POINT('Ctrl Pts',(1.37219088604883,1.39280896668364,2.06415156984599));
#282051=CARTESIAN_POINT('Ctrl Pts',(1.42032110107139,1.34369721618839,2.06024640361046));
#282052=CARTESIAN_POINT('Ctrl Pts',(1.46574512154459,1.29217152060717,2.05634123737493));
#282053=CARTESIAN_POINT('Ctrl Pts',(1.51115625167722,1.24066044688805,2.05243717933991));
#282054=CARTESIAN_POINT('Ctrl Pts',(1.55386238666488,1.18673715677326,2.04853312130489));
#282055=CARTESIAN_POINT('Ctrl Pts',(1.59360737100109,1.13072169303104,2.04462906326987));
#282056=CARTESIAN_POINT('Ctrl Pts',(1.63335470804471,1.07470291344915,2.04072477413383));
#282057=CARTESIAN_POINT('Ctrl Pts',(1.6701402638902,1.01659211700271,2.0368204849978));
#282058=CARTESIAN_POINT('Ctrl Pts',(1.7037506242993,0.956739154733277,2.03291619586177));
#282059=CARTESIAN_POINT('Ctrl Pts',(1.73739678517757,0.896822439379862,
2.02900774802642));
#282060=CARTESIAN_POINT('Ctrl Pts',(1.7678607596992,0.83516028453208,2.02509930019107));
#282061=CARTESIAN_POINT('Ctrl Pts',(1.79497512160515,0.772127135139402,
2.02119085235572));
#282062=CARTESIAN_POINT('Ctrl Pts',(1.82210571324549,0.709056256248384,
2.01728006505649));
#282063=CARTESIAN_POINT('Ctrl Pts',(1.84588253173502,0.644613211141009,
2.01336927775727));
#282064=CARTESIAN_POINT('Ctrl Pts',(1.86618734773961,0.579189764357586,
2.00945849045804));
#282065=CARTESIAN_POINT('Ctrl Pts',(1.88652722388912,0.513653351491413,
2.00554095043722));
#282066=CARTESIAN_POINT('Ctrl Pts',(1.90338301158713,0.447133634847763,
2.0016234104164));
#282067=CARTESIAN_POINT('Ctrl Pts',(1.91668730398203,0.380033917899586,
1.99770587039558));
#282068=CARTESIAN_POINT('Ctrl Pts',(1.9229665975039,0.34836452839387,1.99585688940928));
#282069=CARTESIAN_POINT('Ctrl Pts',(1.92845550807211,0.316566029240909,
1.99400790842298));
#282070=CARTESIAN_POINT('Ctrl Pts',(1.9331509727995,0.284681078339155,1.99215892743667));
#282071=CARTESIAN_POINT('Ctrl Pts',(1.94310097942662,0.217114715647277,
1.98824081194966));
#282072=CARTESIAN_POINT('Ctrl Pts',(1.94952413564899,0.148892135969539,
1.98432269646264));
#282073=CARTESIAN_POINT('Ctrl Pts',(1.95234464277733,0.0804139031428942,
1.98040458097562));
#282074=CARTESIAN_POINT('Ctrl Pts',(1.95516090267743,0.0120387874758331,
1.97649236553776));
#282075=CARTESIAN_POINT('Ctrl Pts',(1.95438526012298,-0.0565907297962358,
1.9725801500999));
#282076=CARTESIAN_POINT('Ctrl Pts',(1.94999341136833,-0.125066764650378,
1.96866793466204));
#282077=CARTESIAN_POINT('Ctrl Pts',(1.94560672717848,-0.193462275575004,
1.96476031976743));
#282078=CARTESIAN_POINT('Ctrl Pts',(1.93761231355979,-0.261704173983213,
1.96085270487283));
#282079=CARTESIAN_POINT('Ctrl Pts',(1.92603791504017,-0.329384197902236,
1.95694508997822));
#282080=CARTESIAN_POINT('Ctrl Pts',(1.91447077091019,-0.397021802574726,
1.95303992422695));
#282081=CARTESIAN_POINT('Ctrl Pts',(1.89932817559024,-0.464097747581249,
1.94913475847568));
#282082=CARTESIAN_POINT('Ctrl Pts',(1.88068957346917,-0.530210079350018,
1.94522959272441));
#282083=CARTESIAN_POINT('Ctrl Pts',(1.86205626056478,-0.596303649923828,
1.94132553517148));
#282084=CARTESIAN_POINT('Ctrl Pts',(1.83992904373194,-0.661433676905025,
1.93742147761854));
#282085=CARTESIAN_POINT('Ctrl Pts',(1.81443779282632,-0.725211345721751,
1.93351742006561));
#282086=CARTESIAN_POINT('Ctrl Pts',(1.78894503294509,-0.788992789910165,
1.92961313140877));
#282087=CARTESIAN_POINT('Ctrl Pts',(1.76008802857329,-0.851421261204326,
1.92570884275193));
#282088=CARTESIAN_POINT('Ctrl Pts',(1.72804487830883,-0.912127676671768,
1.92180455409509));
#282089=CARTESIAN_POINT('Ctrl Pts',(1.69596759684093,-0.972898754414884,
1.91789610673134));
#282090=CARTESIAN_POINT('Ctrl Pts',(1.66069762662193,-1.03194367985739,
1.91398765936759));
#282091=CARTESIAN_POINT('Ctrl Pts',(1.6224586762536,-1.08891865805001,1.91007921200384));
#282092=CARTESIAN_POINT('Ctrl Pts',(1.58419683731237,-1.14592773958304,
1.90616842517257));
#282093=CARTESIAN_POINT('Ctrl Pts',(1.54296277671333,-1.20086401457557,
1.9022576383413));
#282094=CARTESIAN_POINT('Ctrl Pts',(1.49902144341454,-1.25341561829402,
1.89834685151003));
#282095=CARTESIAN_POINT('Ctrl Pts',(1.45500423688004,-1.3060579625503,1.89442931194668));
#282096=CARTESIAN_POINT('Ctrl Pts',(1.40827076263727,-1.35630705747644,
1.89051177238332));
#282097=CARTESIAN_POINT('Ctrl Pts',(1.35912323601593,-1.40388747032004,
1.88659423281997));
#282098=CARTESIAN_POINT('Ctrl Pts',(1.33592677500446,-1.42634429098447,
1.88474524753039));
#282099=CARTESIAN_POINT('Ctrl Pts',(1.3121930395836,-1.44820721209223,1.88289626224081));
#282100=CARTESIAN_POINT('Ctrl Pts',(1.28795620210788,-1.46945051684357,
1.88104727695123));
#282101=CARTESIAN_POINT('Ctrl Pts',(1.2365968232103,-1.51446641212505,1.87712916114264));
#282102=CARTESIAN_POINT('Ctrl Pts',(1.18277273786087,-1.55687567738446,
1.87321104533406));
#282103=CARTESIAN_POINT('Ctrl Pts',(1.12677930717372,-1.59639731674953,
1.86929292952548));
#282104=CARTESIAN_POINT('Ctrl Pts',(1.07087019359426,-1.6358594428774,1.86538071376961));
#282105=CARTESIAN_POINT('Ctrl Pts',(1.01279861651915,-1.67244229158536,
1.86146849801374));
#282106=CARTESIAN_POINT('Ctrl Pts',(0.952894024406714,-1.70590415271491,
1.85755628225787));
#282107=CARTESIAN_POINT('Ctrl Pts',(0.893059876790552,-1.73932666454136,
1.85364866705194));
#282108=CARTESIAN_POINT('Ctrl Pts',(0.831397422435963,-1.76963523894658,
1.84974105184602));
#282109=CARTESIAN_POINT('Ctrl Pts',(0.768264665673746,-1.79663168275448,
1.8458334366401));
#282110=CARTESIAN_POINT('Ctrl Pts',(0.705171478171865,-1.82361120619699,
1.84192827058184));
#282111=CARTESIAN_POINT('Ctrl Pts',(0.640610267537421,-1.84728252404706,
1.83802310452357));
#282112=CARTESIAN_POINT('Ctrl Pts',(0.574961788221266,-1.86749429506101,
1.83411793846531));
#282113=CARTESIAN_POINT('Ctrl Pts',(0.509331938547415,-1.88770033040418,
1.83021388061012));
#282114=CARTESIAN_POINT('Ctrl Pts',(0.442615902587654,-1.90444862317821,
1.82630982275494));
#282115=CARTESIAN_POINT('Ctrl Pts',(0.375210755603282,-1.91763731943233,
1.82240576489975));
#282116=CARTESIAN_POINT('Ctrl Pts',(0.307801618605196,-1.93082679638468,
1.81850147594583));
#282117=CARTESIAN_POINT('Ctrl Pts',(0.23970377281427,-1.94045616655268,
1.8145971869919));
#282118=CARTESIAN_POINT('Ctrl Pts',(0.171323884482255,-1.94647479475228,
1.81069289803798));
#282119=CARTESIAN_POINT('Ctrl Pts',(0.102871160545255,-1.9524998337612,
1.80678445038689));
#282120=CARTESIAN_POINT('Ctrl Pts',(0.0341362854467537,-1.9549064121214,
1.8028760027358));
#282121=CARTESIAN_POINT('Ctrl Pts',(-0.034470571834636,-1.95369592815192,
1.7989675550847));
#282122=CARTESIAN_POINT('Ctrl Pts',(-0.103118494821971,-1.95248471962835,
1.79505676797123));
#282123=CARTESIAN_POINT('Ctrl Pts',(-0.171637756761939,-1.94765217453876,
1.79114598085775));
#282124=CARTESIAN_POINT('Ctrl Pts',(-0.239622636329546,-1.93925165776866,
1.78723519374427));
#282125=CARTESIAN_POINT('Ctrl Pts',(-0.307724904783329,-1.93083663590105,
1.78331765390951));
#282126=CARTESIAN_POINT('Ctrl Pts',(-0.375290465227256,-1.91884143235029,
1.77940011407475));
#282127=CARTESIAN_POINT('Ctrl Pts',(-0.441923981656403,-1.90337048270613,
1.77548257423999));
#282128=CARTESIAN_POINT('Ctrl Pts',(-0.473373364962697,-1.89606857442414,
1.77363359164859));
#282129=CARTESIAN_POINT('Ctrl Pts',(-0.50461535032352,-1.88799312697528,
1.77178460905719));
#282130=CARTESIAN_POINT('Ctrl Pts',(-0.535609795124796,-1.87915889359212,
1.76993562646579));
#282131=CARTESIAN_POINT('Ctrl Pts',(-0.601289082140249,-1.86043856633175,
1.76601750955531));
#282132=CARTESIAN_POINT('Ctrl Pts',(-0.66611593167999,-1.8382336066086,
1.76209939264482));
#282133=CARTESIAN_POINT('Ctrl Pts',(-0.72969405316222,-1.8126396742816,
1.75818127573434));
#282134=CARTESIAN_POINT('Ctrl Pts',(-0.793176436374374,-1.78708428223776,
1.75426905886818));
#282135=CARTESIAN_POINT('Ctrl Pts',(-0.855413370793917,-1.75815022792144,
1.75035684200202));
#282136=CARTESIAN_POINT('Ctrl Pts',(-0.916023073160365,-1.72598311968508,
1.74644462513586));
#282137=CARTESIAN_POINT('Ctrl Pts',(-0.976561501986862,-1.69385383812637,
1.74253700881276));
#282138=CARTESIAN_POINT('Ctrl Pts',(-1.03547606663956,-1.65849928275092,
1.73862939248965));
#282139=CARTESIAN_POINT('Ctrl Pts',(-1.09240604661752,-1.62011265945103,
1.73472177616654));
#282140=CARTESIAN_POINT('Ctrl Pts',(-1.1493003450676,-1.58175009541428,
1.73081660898747));
#282141=CARTESIAN_POINT('Ctrl Pts',(-1.20421211935406,-1.5403595075849,
1.7269114418084));
#282142=CARTESIAN_POINT('Ctrl Pts',(-1.25680766304988,-1.49617863174793,
1.72300627462933));
#282143=CARTESIAN_POINT('Ctrl Pts',(-1.30938828127897,-1.45201029347871,
1.71910221565142));
#282144=CARTESIAN_POINT('Ctrl Pts',(-1.35965359730641,-1.4050535553336,
1.71519815667351));
#282145=CARTESIAN_POINT('Ctrl Pts',(-1.40730262072439,-1.35558671198203,
1.7112940976956));
#282146=CARTESIAN_POINT('Ctrl Pts',(-1.45495446470395,-1.30611694046389,
1.70738980761876));
#282147=CARTESIAN_POINT('Ctrl Pts',(-1.49998936920952,-1.25413712478501,
1.70348551754191));
#282148=CARTESIAN_POINT('Ctrl Pts',(-1.5421441655473,-1.19996140465784,
1.69958122746507));
#282149=CARTESIAN_POINT('Ctrl Pts',(-1.58434386344633,-1.14572797877411,
1.69567277869846));
#282150=CARTESIAN_POINT('Ctrl Pts',(-1.62365702820594,-1.08929436949584,
1.69176432993185));
#282151=CARTESIAN_POINT('Ctrl Pts',(-1.65986230038572,-1.03100588929367,
1.68785588116524));
#282152=CARTESIAN_POINT('Ctrl Pts',(-1.69608924376643,-0.972682519659919,
1.68394509293883));
#282153=CARTESIAN_POINT('Ctrl Pts',(-1.72920435511023,-0.912502500482538,
1.68003430471243));
#282154=CARTESIAN_POINT('Ctrl Pts',(-1.7590323414148,-0.850835602132843,
1.67612351648603));
#282155=CARTESIAN_POINT('Ctrl Pts',(-1.7889118313032,-0.789062224376999,
1.67220597555406));
#282156=CARTESIAN_POINT('Ctrl Pts',(-1.81549267766802,-0.72579729662071,
1.66828843462209));
#282157=CARTESIAN_POINT('Ctrl Pts',(-1.83864812282955,-0.661429573284541,
1.66437089369011));
#282158=CARTESIAN_POINT('Ctrl Pts',(-1.84957686197775,-0.63104976184075,
1.6625219211202));
#282159=CARTESIAN_POINT('Ctrl Pts',(-1.85974329224162,-0.600424495698479,
1.66067294855028));
#282160=CARTESIAN_POINT('Ctrl Pts',(-1.86913802783902,-0.569595499355519,
1.65882397598036));
#282161=CARTESIAN_POINT('Ctrl Pts',(-1.89348479324527,-0.489701144278649,
1.65403230292733));
#282162=CARTESIAN_POINT('Ctrl Pts',(-1.91272391212393,-0.408182349819562,
1.64924062987431));
#282163=CARTESIAN_POINT('Ctrl Pts',(-1.92667621842312,-0.325629773458762,
1.64444895682128));
#282164=CARTESIAN_POINT('Ctrl Pts',(-1.94043089971803,-0.244246498638989,
1.63972515458382));
#282165=CARTESIAN_POINT('Ctrl Pts',(-1.94904743099152,-0.161858499862965,
1.63500135234636));
#282166=CARTESIAN_POINT('Ctrl Pts',(-1.95240023819972,-0.0790525766668212,
1.6302775501089));
#282167=CARTESIAN_POINT('Ctrl Pts',(-1.95344308694579,-0.0532968299717755,
1.62880827050704));
#282168=CARTESIAN_POINT('Ctrl Pts',(-1.95397704349981,-0.0275008065544239,
1.62733899090518));
#282169=CARTESIAN_POINT('Ctrl Pts',(-1.9539992755619,-0.00168258835255015,
1.62586971130332));
#282170=CARTESIAN_POINT('',(-1.95128203910989,0.000979727872364722,0.92586969212423));
#282171=CARTESIAN_POINT('Ctrl Pts',(-1.95279554503994,-0.00168121501241181,
1.62586969212423));
#282172=CARTESIAN_POINT('Ctrl Pts',(-1.94903656010943,0.455834752155161,
1.59981723658113));
#282173=CARTESIAN_POINT('Ctrl Pts',(-1.56043776453642,1.56952521197424,
1.53672756420953));
#282174=CARTESIAN_POINT('Ctrl Pts',(0.294968904732084,2.29042728261437,
1.43660067500948));
#282175=CARTESIAN_POINT('Ctrl Pts',(2.08405785032273,0.994871990457251,
1.32548902452406));
#282176=CARTESIAN_POINT('Ctrl Pts',(1.96640931676784,-1.2109096610648,1.21437737403861));
#282177=CARTESIAN_POINT('Ctrl Pts',(0.049663025814346,-2.30880650358356,
1.10326572355317));
#282178=CARTESIAN_POINT('Ctrl Pts',(-1.64864534346746,-1.43077452179925,
1.00709649624838));
#282179=CARTESIAN_POINT('Ctrl Pts',(-1.94952091996443,-0.387793032173158,
0.947964485772066));
#282180=CARTESIAN_POINT('Ctrl Pts',(-1.95128203910989,0.000979727872364722,
0.92586969212423));
#282181=CARTESIAN_POINT('Ctrl Pts',(-1.95128203910989,0.000979727872364722,
0.92586969212423));
#282182=CARTESIAN_POINT('Ctrl Pts',(-1.9524730612105,0.263901717292074,
0.910927268943587));
#282183=CARTESIAN_POINT('Ctrl Pts',(-1.78055184446198,1.17702392994427,
0.858947628934464));
#282184=CARTESIAN_POINT('Ctrl Pts',(-0.393188016825178,2.2756080016325,
0.769930772096862));
#282185=CARTESIAN_POINT('Ctrl Pts',(1.69827668332872,1.5649425932243,0.658819121611428));
#282186=CARTESIAN_POINT('Ctrl Pts',(2.23594117881619,-0.577629785835539,
0.547707471125989));
#282187=CARTESIAN_POINT('Ctrl Pts',(0.72794696107778,-2.19149774367173,
0.436595820640553));
#282188=CARTESIAN_POINT('Ctrl Pts',(-1.37113779886414,-1.81423119146763,
0.32931688820614));
#282189=CARTESIAN_POINT('Ctrl Pts',(-1.95230360289333,-0.579093481907559,
0.259075172600207));
#282190=CARTESIAN_POINT('Ctrl Pts',(-1.9563354715932,0.00125594757992074,
0.225870673822753));
#282191=CARTESIAN_POINT('Origin',(0.,0.,-1.29405622560369));
#282192=CARTESIAN_POINT('',(-1.55549973622945,-0.00090586429527298,10.9559437744371));
#282193=CARTESIAN_POINT('',(0.499806597877791,1.47301514408978,11.4445));
#282194=CARTESIAN_POINT('Ctrl Pts',(-1.55549973622945,-0.00090586429527298,
10.9559437744371));
#282195=CARTESIAN_POINT('Ctrl Pts',(-1.5554624181148,-0.0649864531813007,
10.9605121932704));
#282196=CARTESIAN_POINT('Ctrl Pts',(-1.55146115138349,-0.128926751081953,
10.9650806121038));
#282197=CARTESIAN_POINT('Ctrl Pts',(-1.54357236633783,-0.192261800361485,
10.9696490309371));
#282198=CARTESIAN_POINT('Ctrl Pts',(-1.53565219727971,-0.255848815940527,
10.9742356243452));
#282199=CARTESIAN_POINT('Ctrl Pts',(-1.52381366620313,-0.318825456507138,
10.9788222177533));
#282200=CARTESIAN_POINT('Ctrl Pts',(-1.50818383456823,-0.380738455041077,
10.9834088111614));
#282201=CARTESIAN_POINT('Ctrl Pts',(-1.49247619331133,-0.442959673594634,
10.9880182378992));
#282202=CARTESIAN_POINT('Ctrl Pts',(-1.47293956753027,-0.504106343920584,
10.992627664637));
#282203=CARTESIAN_POINT('Ctrl Pts',(-1.44975072861387,-0.563740254801405,
10.9972370913749));
#282204=CARTESIAN_POINT('Ctrl Pts',(-1.44502802405396,-0.575885465859958,
10.9981758602693));
#282205=CARTESIAN_POINT('Ctrl Pts',(-1.4401539839899,-0.587968010173575,
10.9991146291638));
#282206=CARTESIAN_POINT('Ctrl Pts',(-1.43513033363107,-0.599984312704903,
11.0000533980582));
#282207=CARTESIAN_POINT('Ctrl Pts',(-1.41288996022962,-0.653182094419901,
11.0042094537666));
#282208=CARTESIAN_POINT('Ctrl Pts',(-1.38764176100762,-0.705251438383512,
11.0083655094749));
#282209=CARTESIAN_POINT('Ctrl Pts',(-1.35952197240883,-0.755830838572767,
11.0125215651832));
#282210=CARTESIAN_POINT('Ctrl Pts',(-1.33145251805152,-0.806319701959642,
11.0166701815784));
#282211=CARTESIAN_POINT('Ctrl Pts',(-1.30052192813529,-0.855323466279215,
11.0208187979737));
#282212=CARTESIAN_POINT('Ctrl Pts',(-1.26691401553271,-0.902501594041128,
11.0249674143689));
#282213=CARTESIAN_POINT('Ctrl Pts',(-1.23333982924824,-0.949632377459965,
11.0291118675315));
#282214=CARTESIAN_POINT('Ctrl Pts',(-1.19709394374559,-0.994940734441594,
11.0332563206942));
#282215=CARTESIAN_POINT('Ctrl Pts',(-1.15840461492088,-1.03811319138618,
11.0374007738569));
#282216=CARTESIAN_POINT('Ctrl Pts',(-1.11973938927939,-1.08125875218987,
11.041542645054));
#282217=CARTESIAN_POINT('Ctrl Pts',(-1.07863408370058,-1.1222706656218,
11.0456845162511));
#282218=CARTESIAN_POINT('Ctrl Pts',(-1.0353571968633,-1.16086852179882,
11.0498263874482));
#282219=CARTESIAN_POINT('Ctrl Pts',(-0.992090804187492,-1.19945701842701,
11.0539672542878));
#282220=CARTESIAN_POINT('Ctrl Pts',(-0.946654262575783,-1.23563227495104,
11.0581081211275));
#282221=CARTESIAN_POINT('Ctrl Pts',(-0.899351290910011,-1.26915227830962,
11.0622489879671));
#282222=CARTESIAN_POINT('Ctrl Pts',(-0.852007614334827,-1.30270112612875,
11.0663934180841));
#282223=CARTESIAN_POINT('Ctrl Pts',(-0.802794721221834,-1.33358985262928,
11.0705378482012));
#282224=CARTESIAN_POINT('Ctrl Pts',(-0.752046543952488,-1.36161897964486,
11.0746822783182));
#282225=CARTESIAN_POINT('Ctrl Pts',(-0.701278443146775,-1.38965911078634,
11.0788283355223));
#282226=CARTESIAN_POINT('Ctrl Pts',(-0.64897432376144,-1.41483717654292,
11.0829743927264));
#282227=CARTESIAN_POINT('Ctrl Pts',(-0.595491192649498,-1.43700051825909,
11.0871204499305));
#282228=CARTESIAN_POINT('Ctrl Pts',(-0.541907029850498,-1.45920572737826,
11.0912743391958));
#282229=CARTESIAN_POINT('Ctrl Pts',(-0.487139895107943,-1.47838465773227,
11.0954282284611));
#282230=CARTESIAN_POINT('Ctrl Pts',(-0.431564295262401,-1.49443384231443,
11.0995821177264));
#282231=CARTESIAN_POINT('Ctrl Pts',(-0.37990761987289,-1.50935131545968,
11.1034430946655));
#282232=CARTESIAN_POINT('Ctrl Pts',(-0.327552956949716,-1.52156533038131,
11.1073040716046));
#282233=CARTESIAN_POINT('Ctrl Pts',(-0.274807223030603,-1.53103273647895,
11.1111650485437));
#282234=CARTESIAN_POINT('Ctrl Pts',(-0.21805856036645,-1.54121863389699,
11.1153190390485));
#282235=CARTESIAN_POINT('Ctrl Pts',(-0.160627328713441,-1.54826587752968,
11.1194730295534));
#282236=CARTESIAN_POINT('Ctrl Pts',(-0.102891144520795,-1.55209331626008,
11.1236270200582));
#282237=CARTESIAN_POINT('Ctrl Pts',(-0.0452553750170186,-1.55591409831451,
11.1277737859487));
#282238=CARTESIAN_POINT('Ctrl Pts',(0.012683780480316,-1.55652615738425,
11.1319205518393));
#282239=CARTESIAN_POINT('Ctrl Pts',(0.0705405746337234,-1.5538996998939,
11.1360673177298));
#282240=CARTESIAN_POINT('Ctrl Pts',(0.128341113208402,-1.55127579617252,
11.1402100516182));
#282241=CARTESIAN_POINT('Ctrl Pts',(0.186058933198519,-1.54541963903664,
11.1443527855066));
#282242=CARTESIAN_POINT('Ctrl Pts',(0.243307004996965,-1.53635345911005,
11.148495519395));
#282243=CARTESIAN_POINT('Ctrl Pts',(0.300521227458064,-1.52729263978641,
11.1526358037896));
#282244=CARTESIAN_POINT('Ctrl Pts',(0.357265740804184,-1.51502564158783,
11.1567760881843));
#282245=CARTESIAN_POINT('Ctrl Pts',(0.413159555535051,-1.49962643070535,
11.1609163725789));
#282246=CARTESIAN_POINT('Ctrl Pts',(0.469041618685836,-1.48423045748094,
11.1650557864857));
#282247=CARTESIAN_POINT('Ctrl Pts',(0.524072838295294,-1.46570371701194,
11.1691952003925));
#282248=CARTESIAN_POINT('Ctrl Pts',(0.577885471001734,-1.44417056901361,
11.1733346142993));
#282249=CARTESIAN_POINT('Ctrl Pts',(0.631747265873237,-1.4226177487539,
11.1774778098935));
#282250=CARTESIAN_POINT('Ctrl Pts',(0.684387765817342,-1.39805322473431,
11.1816210054876));
#282251=CARTESIAN_POINT('Ctrl Pts',(0.735458644606146,-1.37064978461826,
11.1857642010817));
#282252=CARTESIAN_POINT('Ctrl Pts',(0.786551027400648,-1.34323480595527,
11.189909141218));
#282253=CARTESIAN_POINT('Ctrl Pts',(0.836072026975183,-1.31297879814688,
11.1940540813543));
#282254=CARTESIAN_POINT('Ctrl Pts',(0.883700229279736,-1.28009927535756,
11.1981990214906));
#282255=CARTESIAN_POINT('Ctrl Pts',(0.931420843428688,-1.24715595722856,
11.2023520039536));
#282256=CARTESIAN_POINT('Ctrl Pts',(0.977240909000357,-1.21157927010357,
11.2065049864166));
#282257=CARTESIAN_POINT('Ctrl Pts',(1.02087091663919,-1.17362805929317,
11.2106579688796));
#282258=CARTESIAN_POINT('Ctrl Pts',(1.06155856619351,-1.13823623496901,
11.2145308789294));
#282259=CARTESIAN_POINT('Ctrl Pts',(1.10034169991128,-1.1007800021631,11.2184037889793));
#282260=CARTESIAN_POINT('Ctrl Pts',(1.13701614988411,-1.06149636122914,
11.2222766990291));
#282261=CARTESIAN_POINT('Ctrl Pts',(1.17586636956837,-1.01988215620596,
11.2263793755891));
#282262=CARTESIAN_POINT('Ctrl Pts',(1.21252069950925,-0.976033787091652,
11.2304820521491));
#282263=CARTESIAN_POINT('Ctrl Pts',(1.24670795418086,-0.930214774652702,
11.2345847287091));
#282264=CARTESIAN_POINT('Ctrl Pts',(1.28101304438198,-0.8842378347158,11.2387015462426));
#282265=CARTESIAN_POINT('Ctrl Pts',(1.31283360197336,-0.836276988307453,
11.2428183637762));
#282266=CARTESIAN_POINT('Ctrl Pts',(1.34193303162277,-0.786635867882791,
11.2469351813098));
#282267=CARTESIAN_POINT('Ctrl Pts',(1.37085210792835,-0.737302414727498,
11.2510264835045));
#282268=CARTESIAN_POINT('Ctrl Pts',(1.39708339572808,-0.686309906372128,
11.2551177856992));
#282269=CARTESIAN_POINT('Ctrl Pts',(1.4204367528487,-0.633987130119093,
11.2592090878939));
#282270=CARTESIAN_POINT('Ctrl Pts',(1.44377647453577,-0.581694903809472,
11.2632980012809));
#282271=CARTESIAN_POINT('Ctrl Pts',(1.464241376507,-0.528074433640186,11.2673869146679));
#282272=CARTESIAN_POINT('Ctrl Pts',(1.48168787713257,-0.473477860895714,
11.2714758280549));
#282273=CARTESIAN_POINT('Ctrl Pts',(1.49913124686719,-0.4188910858705,11.2755640076591));
#282274=CARTESIAN_POINT('Ctrl Pts',(1.51355712783861,-0.363329063483174,
11.2796521872633));
#282275=CARTESIAN_POINT('Ctrl Pts',(1.52487139541215,-0.307160344858819,
11.2837403668675));
#282276=CARTESIAN_POINT('Ctrl Pts',(1.53632169470053,-0.250316308361276,
11.2878776987548));
#282277=CARTESIAN_POINT('Ctrl Pts',(1.54458491338459,-0.192851429228182,
11.292015030642));
#282278=CARTESIAN_POINT('Ctrl Pts',(1.5496170033841,-0.135156919256407,
11.2961523625293));
#282279=CARTESIAN_POINT('Ctrl Pts',(1.55459709273317,-0.078058613256646,
11.3002469400244));
#282280=CARTESIAN_POINT('Ctrl Pts',(1.5564125824634,-0.0207359431881903,
11.3043415175195));
#282281=CARTESIAN_POINT('Ctrl Pts',(1.5550733198847,0.0364310277481887,
11.3084360950146));
#282282=CARTESIAN_POINT('Ctrl Pts',(1.55371308101812,0.0944933801116644,
11.3125948040979));
#282283=CARTESIAN_POINT('Ctrl Pts',(1.54909845009413,0.152394544073392,
11.3167535131812));
#282284=CARTESIAN_POINT('Ctrl Pts',(1.54129417920738,0.209743898937334,
11.3209122222645));
#282285=CARTESIAN_POINT('Ctrl Pts',(1.53348990832064,0.267093253801277,
11.3250709313479));
#282286=CARTESIAN_POINT('Ctrl Pts',(1.52249618900996,0.323890260715516,
11.3292296404312));
#282287=CARTESIAN_POINT('Ctrl Pts',(1.50843045263315,0.379760213251655,
11.3333883495145));
#282288=CARTESIAN_POINT('Ctrl Pts',(1.49400748347762,0.43704911591291,11.3376526788912));
#282289=CARTESIAN_POINT('Ctrl Pts',(1.47629200845049,0.493613181015604,
11.3419170082678));
#282290=CARTESIAN_POINT('Ctrl Pts',(1.45537425215218,0.549059228291879,
11.3461813376444));
#282291=CARTESIAN_POINT('Ctrl Pts',(1.43450151006181,0.604385957804546,
11.3504364903481));
#282292=CARTESIAN_POINT('Ctrl Pts',(1.41044036062075,0.658599002949918,
11.3546916430517));
#282293=CARTESIAN_POINT('Ctrl Pts',(1.38333089507448,0.711319818880685,
11.3589467957554));
#282294=CARTESIAN_POINT('Ctrl Pts',(1.35625595310978,0.763973495480125,
11.3631965295727));
#282295=CARTESIAN_POINT('Ctrl Pts',(1.32614062312171,0.815138286646112,
11.3674462633901));
#282296=CARTESIAN_POINT('Ctrl Pts',(1.2931727813815,0.864456133932793,11.3716959972074));
#282297=CARTESIAN_POINT('Ctrl Pts',(1.26023691519775,0.913726147769451,
11.3759416092019));
#282298=CARTESIAN_POINT('Ctrl Pts',(1.22445430092607,0.961152373337957,
11.3801872211964));
#282299=CARTESIAN_POINT('Ctrl Pts',(1.18605751251627,1.00640341166141,11.3844328331909));
#282300=CARTESIAN_POINT('Ctrl Pts',(1.14768632431624,1.0516242798555,11.3886756145175));
#282301=CARTESIAN_POINT('Ctrl Pts',(1.10670473881416,1.09467247308709,11.392918395844));
#282302=CARTESIAN_POINT('Ctrl Pts',(1.06338613282229,1.13524895178162,11.3971611771706));
#282303=CARTESIAN_POINT('Ctrl Pts',(1.02007026241049,1.17582286806205,11.4014036905645));
#282304=CARTESIAN_POINT('Ctrl Pts',(0.974418010221406,1.21392503874472,
11.4056462039584));
#282305=CARTESIAN_POINT('Ctrl Pts',(0.926739210629652,1.2492936746344,11.4098887173523));
#282306=CARTESIAN_POINT('Ctrl Pts',(0.87906544940404,1.284658573011,11.4141307824268));
#282307=CARTESIAN_POINT('Ctrl Pts',(0.8293659604616,1.31729022665034,11.4183728475012));
#282308=CARTESIAN_POINT('Ctrl Pts',(0.77798146220205,1.34696885430583,11.4226149125756));
#282309=CARTESIAN_POINT('Ctrl Pts',(0.72655905475185,1.3766693775289,11.4268601072564));
#282310=CARTESIAN_POINT('Ctrl Pts',(0.67344957808929,1.40341228340842,11.4311053019372));
#282311=CARTESIAN_POINT('Ctrl Pts',(0.619019388670748,1.42702321160158,
11.435350496618));
#282312=CARTESIAN_POINT('Ctrl Pts',(0.579915630216658,1.44398578407846,
11.4384003310787));
#282313=CARTESIAN_POINT('Ctrl Pts',(0.540130755853637,1.45933281346944,
11.4414501655393));
#282314=CARTESIAN_POINT('Ctrl Pts',(0.499806597877795,1.47301514408978,
11.4445));
#282315=CARTESIAN_POINT('',(1.55548765964692,0.00619602180124784,11.4445));
#282316=CARTESIAN_POINT('Origin',(0.,0.,11.4445));
#282317=CARTESIAN_POINT('',(-1.55549964551795,-0.00105013977025186,11.0940562256037));
#282318=CARTESIAN_POINT('Ctrl Pts',(-1.55549964551795,-0.00105013977025186,
11.0940562256037));
#282319=CARTESIAN_POINT('Ctrl Pts',(-1.5554467553948,-0.0793926329663125,
11.099684397238));
#282320=CARTESIAN_POINT('Ctrl Pts',(-1.54947416800179,-0.157518393304178,
11.1053125688723));
#282321=CARTESIAN_POINT('Ctrl Pts',(-1.5376858701482,-0.234739035412875,
11.1109407405065));
#282322=CARTESIAN_POINT('Ctrl Pts',(-1.52898608215356,-0.291728027674486,
11.1150943427164));
#282323=CARTESIAN_POINT('Ctrl Pts',(-1.51709613604147,-0.348348961130454,
11.1192479449263));
#282324=CARTESIAN_POINT('Ctrl Pts',(-1.50206118452453,-0.40421831718117,
11.1234015471362));
#282325=CARTESIAN_POINT('Ctrl Pts',(-1.48705242241808,-0.459990354294839,
11.1275479141786));
#282326=CARTESIAN_POINT('Ctrl Pts',(-1.46890966326337,-0.515012915471432,
11.1316942812209));
#282327=CARTESIAN_POINT('Ctrl Pts',(-1.44772929077675,-0.56891137326218,
11.1358406482633));
#282328=CARTESIAN_POINT('Ctrl Pts',(-1.42656954751022,-0.622757335132504,
11.1399829768347));
#282329=CARTESIAN_POINT('Ctrl Pts',(-1.40237824237186,-0.675480882336065,
11.1441253054061));
#282330=CARTESIAN_POINT('Ctrl Pts',(-1.37530140911383,-0.726722976167344,
11.1482676339776));
#282331=CARTESIAN_POINT('Ctrl Pts',(-1.34824062460129,-0.777934698229705,
11.152407507344));
#282332=CARTESIAN_POINT('Ctrl Pts',(-1.3182979446997,-0.827666249677602,
11.1565473807104));
#282333=CARTESIAN_POINT('Ctrl Pts',(-1.285666414579,-0.875581018766156,
11.1606872540768));
#282334=CARTESIAN_POINT('Ctrl Pts',(-1.25304178496714,-0.923485655437193,
11.1648262519944));
#282335=CARTESIAN_POINT('Ctrl Pts',(-1.2177297262288,-0.969573843783421,
11.1689652499121));
#282336=CARTESIAN_POINT('Ctrl Pts',(-1.17996669652475,-1.0135377867117,
11.1731042478297));
#282337=CARTESIAN_POINT('Ctrl Pts',(-1.14216912941584,-1.05754193829136,
11.1772470312023));
#282338=CARTESIAN_POINT('Ctrl Pts',(-1.10191645010097,-1.0994175667123,
11.1813898145749));
#282339=CARTESIAN_POINT('Ctrl Pts',(-1.05948467676934,-1.13889089455091,
11.1855325979474));
#282340=CARTESIAN_POINT('Ctrl Pts',(-1.01703507028913,-1.178380812168,11.1896771224415));
#282341=CARTESIAN_POINT('Ctrl Pts',(-0.972404943244974,-1.2154660829153,
11.1938216469355));
#282342=CARTESIAN_POINT('Ctrl Pts',(-0.925903947025988,-1.24991284931458,
11.1979661714295));
#282343=CARTESIAN_POINT('Ctrl Pts',(-0.879312465587032,-1.28442664488503,
11.2021187606585));
#282344=CARTESIAN_POINT('Ctrl Pts',(-0.83084327445346,-1.31629138864477,
11.2062713498876));
#282345=CARTESIAN_POINT('Ctrl Pts',(-0.780834836710626,-1.34531676856385,
11.2104239391166));
#282346=CARTESIAN_POINT('Ctrl Pts',(-0.733855327658026,-1.37258412903762,
11.2143250128569));
#282347=CARTESIAN_POINT('Ctrl Pts',(-0.68551795147696,-1.3973459328914,
11.2182260865973));
#282348=CARTESIAN_POINT('Ctrl Pts',(-0.636119437584287,-1.41948311406915,
11.2221271603377));
#282349=CARTESIAN_POINT('Ctrl Pts',(-0.584172922826061,-1.44276214248798,
11.2262294534769));
#282350=CARTESIAN_POINT('Ctrl Pts',(-0.530823728255636,-1.46324088760723,
11.230331746616));
#282351=CARTESIAN_POINT('Ctrl Pts',(-0.476408890752611,-1.48074806054638,
11.2344340397552));
#282352=CARTESIAN_POINT('Ctrl Pts',(-0.421759434730541,-1.49833071854027,
11.2385540206058));
#282353=CARTESIAN_POINT('Ctrl Pts',(-0.366035587401732,-1.51291582962675,
11.2426740014564));
#282354=CARTESIAN_POINT('Ctrl Pts',(-0.309602098405575,-1.52437750923545,
11.2467939823069));
#282355=CARTESIAN_POINT('Ctrl Pts',(-0.253566959657262,-1.53575828364062,
11.2508848812166));
#282356=CARTESIAN_POINT('Ctrl Pts',(-0.196832688652311,-1.54405944952486,
11.2549757801262));
#282357=CARTESIAN_POINT('Ctrl Pts',(-0.139771862283216,-1.54920756405134,
11.2590666790359));
#282358=CARTESIAN_POINT('Ctrl Pts',(-0.082744421310311,-1.55435266649661,
11.2631551844246));
#282359=CARTESIAN_POINT('Ctrl Pts',(-0.0253913333222678,-1.55634832320774,
11.2672436898133));
#282360=CARTESIAN_POINT('Ctrl Pts',(0.0319078017594993,-1.55517270493887,
11.2713321952021));
#282361=CARTESIAN_POINT('Ctrl Pts',(0.089196593805501,-1.55399729888021,
11.2754199625769));
#282362=CARTESIAN_POINT('Ctrl Pts',(0.146430919346374,-1.54965176460393,
11.2795077299518));
#282363=CARTESIAN_POINT('Ctrl Pts',(0.203231664787166,-1.54216637897078,
11.2835954973266));
#282364=CARTESIAN_POINT('Ctrl Pts',(0.260802295817886,-1.53457953532876,
11.2877386708968));
#282365=CARTESIAN_POINT('Ctrl Pts',(0.317926943534344,-1.52376712075726,
11.291881844467));
#282366=CARTESIAN_POINT('Ctrl Pts',(0.374219533099056,-1.50981455518455,
11.2960250180372));
#282367=CARTESIAN_POINT('Ctrl Pts',(0.429846320278973,-1.49602701402277,
11.3001191880908));
#282368=CARTESIAN_POINT('Ctrl Pts',(0.48466013278346,-1.47917344225769,
11.3042133581445));
#282369=CARTESIAN_POINT('Ctrl Pts',(0.53830465909531,-1.4593862901906,11.3083075281981));
#282370=CARTESIAN_POINT('Ctrl Pts',(0.592912300176866,-1.43924388662412,
11.3124752035266));
#282371=CARTESIAN_POINT('Ctrl Pts',(0.646307721836913,-1.4160617487065,
11.316642878855));
#282372=CARTESIAN_POINT('Ctrl Pts',(0.698140089099992,-1.39002901624083,
11.3208105541835));
#282373=CARTESIAN_POINT('Ctrl Pts',(0.74997245636307,-1.36399628377517,
11.3249782295119));
#282374=CARTESIAN_POINT('Ctrl Pts',(0.800241316513729,-1.33511331686024,
11.3291459048404));
#282375=CARTESIAN_POINT('Ctrl Pts',(0.848628268415838,-1.30361432641926,
11.3333135801688));
#282376=CARTESIAN_POINT('Ctrl Pts',(0.898135152312619,-1.27138628143345,
11.3375777177203));
#282377=CARTESIAN_POINT('Ctrl Pts',(0.945888563678672,-1.23627928598203,
11.3418418552717));
#282378=CARTESIAN_POINT('Ctrl Pts',(0.991545869198776,-1.19850616989436,
11.3461059928231));
#282379=CARTESIAN_POINT('Ctrl Pts',(1.03710474676417,-1.16081448503697,
11.3503609377529));
#282380=CARTESIAN_POINT('Ctrl Pts',(1.08057613305868,-1.12046841648006,
11.3546158826826));
#282381=CARTESIAN_POINT('Ctrl Pts',(1.1216474100154,-1.07772321938694,11.3588708276123));
#282382=CARTESIAN_POINT('Ctrl Pts',(1.16266629439531,-1.03503255020694,
11.3631203447213));
#282383=CARTESIAN_POINT('Ctrl Pts',(1.20129081374652,-0.989949176777246,
11.3673698618303));
#282384=CARTESIAN_POINT('Ctrl Pts',(1.23724322449347,-0.942766913635077,
11.3716193789393));
#282385=CARTESIAN_POINT('Ctrl Pts',(1.2731606953723,-0.89563050394243,11.375864766212));
#282386=CARTESIAN_POINT('Ctrl Pts',(1.3064109219502,-0.8463996405269,11.3801101534848));
#282387=CARTESIAN_POINT('Ctrl Pts',(1.33675587421288,-0.79540177442433,
11.3843555407576));
#282388=CARTESIAN_POINT('Ctrl Pts',(1.3670805428173,-0.744437997130944,
11.3885980902607));
#282389=CARTESIAN_POINT('Ctrl Pts',(1.39450354811632,-0.691709980582283,
11.3928406397639));
#282390=CARTESIAN_POINT('Ctrl Pts',(1.41883070311814,-0.637573278838822,
11.397083189267));
#282391=CARTESIAN_POINT('Ctrl Pts',(1.44315630177837,-0.583440040517223,
11.401325467351));
#282392=CARTESIAN_POINT('Ctrl Pts',(1.46438623292714,-0.527898733597431,
11.4055677454349));
#282393=CARTESIAN_POINT('Ctrl Pts',(1.48237337026586,-0.471327318459934,
11.4098100235189));
#282394=CARTESIAN_POINT('Ctrl Pts',(1.50035858611496,-0.414761946606878,
11.4140518484183));
#282395=CARTESIAN_POINT('Ctrl Pts',(1.51510155575924,-0.357167150216909,
11.4182936733177));
#282396=CARTESIAN_POINT('Ctrl Pts',(1.52650490708359,-0.298936479289034,
11.422535498217));
#282397=CARTESIAN_POINT('Ctrl Pts',(1.53791669662389,-0.240662719012927,
11.4267804619686));
#282398=CARTESIAN_POINT('Ctrl Pts',(1.54598384210377,-0.181752622457975,
11.4310254257202));
#282399=CARTESIAN_POINT('Ctrl Pts',(1.55066025250447,-0.122609262712029,
11.4352703894718));
#282400=CARTESIAN_POINT('Ctrl Pts',(1.55404948024147,-0.0797451216005902,
11.4383469263145));
#282401=CARTESIAN_POINT('Ctrl Pts',(1.55565876235601,-0.036758661229604,
11.4414234631573));
#282402=CARTESIAN_POINT('Ctrl Pts',(1.55548765964692,0.00619602180124782,
11.4445));
#282403=CARTESIAN_POINT('',(-1.55549927593411,0.00143538631611188,9.6942685916742));
#282404=CARTESIAN_POINT('Ctrl Pts',(-1.55549961664973,-0.00109206342674629,
11.0934258365746));
#282405=CARTESIAN_POINT('Ctrl Pts',(-1.55558866716066,0.125748587234756,
11.084990248375));
#282406=CARTESIAN_POINT('Ctrl Pts',(-1.54016409056307,0.252122806744804,
11.0768042802314));
#282407=CARTESIAN_POINT('Ctrl Pts',(-1.50445838958799,0.395769174174197,
11.0666909871392));
#282408=CARTESIAN_POINT('Ctrl Pts',(-1.49893384134289,0.416203743302519,
11.0652338021612));
#282409=CARTESIAN_POINT('Ctrl Pts',(-1.48805551383009,0.453410142869564,
11.0625418156191));
#282410=CARTESIAN_POINT('Ctrl Pts',(-1.48283063335999,0.470216162081886,
11.0613111268281));
#282411=CARTESIAN_POINT('Ctrl Pts',(-1.47399077411028,0.497035901018334,
11.0593214663562));
#282412=CARTESIAN_POINT('Ctrl Pts',(-1.47055607880628,0.507107777542024,
11.0585683914285));
#282413=CARTESIAN_POINT('Ctrl Pts',(-1.46380312693972,0.526264368494188,
11.0571243754841));
#282414=CARTESIAN_POINT('Ctrl Pts',(-1.46050294052373,0.535354959780714,
11.0564340599115));
#282415=CARTESIAN_POINT('Ctrl Pts',(-1.45278685668432,0.556006975882772,
11.0548538872314));
#282416=CARTESIAN_POINT('Ctrl Pts',(-1.44831736778895,0.567547525712447,
11.0539622813804));
#282417=CARTESIAN_POINT('Ctrl Pts',(-1.43602604252437,0.598193641046168,
11.0515709687516));
#282418=CARTESIAN_POINT('Ctrl Pts',(-1.42796100118238,0.617198291047122,
11.0500632377904));
#282419=CARTESIAN_POINT('Ctrl Pts',(-1.38286882674354,0.717836094444385,
11.0419420526536));
#282420=CARTESIAN_POINT('Ctrl Pts',(-1.33922142003083,0.796301379393232,
11.0351076367119));
#282421=CARTESIAN_POINT('Ctrl Pts',(-1.24506436575965,0.935723017831827,
11.0220893419264));
#282422=CARTESIAN_POINT('Ctrl Pts',(-1.19617983212511,0.997455414915479,
11.0159501097808));
#282423=CARTESIAN_POINT('Ctrl Pts',(-1.12645278358293,1.07297139348107,
11.0081129558573));
#282424=CARTESIAN_POINT('Ctrl Pts',(-1.10965763162062,1.09033185827539,
11.0062866658612));
#282425=CARTESIAN_POINT('Ctrl Pts',(-1.08073608653073,1.11886602995056,
11.0032522375993));
#282426=CARTESIAN_POINT('Ctrl Pts',(-1.06882437267497,1.13025050297403,
11.0020323321105));
#282427=CARTESIAN_POINT('Ctrl Pts',(-1.05162008069498,1.14617800160931,
11.0003150233465));
#282428=CARTESIAN_POINT('Ctrl Pts',(-1.04647486765018,1.15087756161206,
10.9998069618623));
#282429=CARTESIAN_POINT('Ctrl Pts',(-1.04124875384899,1.15558698808154,
10.999296610716));
#282430=CARTESIAN_POINT('Ctrl Pts',(-1.04119938777156,1.15563146777836,
10.9992917904291));
#282431=CARTESIAN_POINT('Ctrl Pts',(-1.04110048648618,1.15572056807992,
10.999282134363));
#282432=CARTESIAN_POINT('Ctrl Pts',(-1.0410509512563,1.15576518866641,10.9992772985851));
#282433=CARTESIAN_POINT('Ctrl Pts',(-1.04095169794807,1.15585458298854,
10.9992676102082));
#282434=CARTESIAN_POINT('Ctrl Pts',(-1.04090197985061,1.15589935670008,
10.9992627576112));
#282435=CARTESIAN_POINT('Ctrl Pts',(-1.04080234683531,1.1559890697291,10.9992530342439));
#282436=CARTESIAN_POINT('Ctrl Pts',(-1.04075243189458,1.15603400902247,
10.9992481634755));
#282437=CARTESIAN_POINT('Ctrl Pts',(-1.04067599346052,1.15610281891718,
10.9992407053068));
#282438=CARTESIAN_POINT('Ctrl Pts',(-1.04064947206665,1.15612669182953,
10.9992381177371));
#282439=CARTESIAN_POINT('Ctrl Pts',(-1.04059561844122,1.15617516416549,
10.9992328637869));
#282440=CARTESIAN_POINT('Ctrl Pts',(-1.04056828616208,1.1561997635296,10.9992301974109));
#282441=CARTESIAN_POINT('Ctrl Pts',(-1.04051277163853,1.15624972367327,
10.999224782059));
#282442=CARTESIAN_POINT('Ctrl Pts',(-1.04048458933168,1.15627508439848,
10.9992220330867));
#282443=CARTESIAN_POINT('Ctrl Pts',(-1.04042733301478,1.1563266044874,10.9992164485009));
#282444=CARTESIAN_POINT('Ctrl Pts',(-1.04039825894877,1.15635276378188,
10.9992136128926));
#282445=CARTESIAN_POINT('Ctrl Pts',(-1.04033917455867,1.15640592073375,
10.9992078507218));
#282446=CARTESIAN_POINT('Ctrl Pts',(-1.04030916416629,1.15643291832303,
10.9992049241642));
#282447=CARTESIAN_POINT('Ctrl Pts',(-1.04024815949679,1.15648779431579,
10.9991989754854));
#282448=CARTESIAN_POINT('Ctrl Pts',(-1.04021716515519,1.15651567263671,
10.9991959533705));
#282449=CARTESIAN_POINT('Ctrl Pts',(-1.04015414162699,1.15657235550215,
10.9991898086465));
#282450=CARTESIAN_POINT('Ctrl Pts',(-1.04012211236437,1.15660115996235,
10.9991866860436));
#282451=CARTESIAN_POINT('Ctrl Pts',(-1.04005696440284,1.15665974373659,
10.9991803350628));
#282452=CARTESIAN_POINT('Ctrl Pts',(-1.04002384561216,1.15668952296706,
10.9991771066909));
#282453=CARTESIAN_POINT('Ctrl Pts',(-1.03995646001558,1.15675010844828,
10.999170538507));
#282454=CARTESIAN_POINT('Ctrl Pts',(-1.03992219312673,1.15678091459261,
10.9991671987032));
#282455=CARTESIAN_POINT('Ctrl Pts',(-1.03985244841962,1.15684360991074,
10.9991604015729));
#282456=CARTESIAN_POINT('Ctrl Pts',(-1.03981697050171,1.15687549897655,
10.9991569442544));
#282457=CARTESIAN_POINT('Ctrl Pts',(-1.03974473606801,1.15694042035925,
10.9991499055544));
#282458=CARTESIAN_POINT('Ctrl Pts',(-1.03970797944307,1.15697345255826,
10.9991463241815));
#282459=CARTESIAN_POINT('Ctrl Pts',(-1.03963311470619,1.1570407250529,10.9991390303295));
#282460=CARTESIAN_POINT('Ctrl Pts',(-1.03959500647224,1.15707496522162,
10.9991353178596));
#282461=CARTESIAN_POINT('Ctrl Pts',(-1.03951735988305,1.15714472358759,
10.9991277542177));
#282462=CARTESIAN_POINT('Ctrl Pts',(-1.03947782140505,1.1571802416356,10.9991239030569));
#282463=CARTESIAN_POINT('Ctrl Pts',(-1.03939722938415,1.15725263127524,
10.99911605383));
#282464=CARTESIAN_POINT('Ctrl Pts',(-1.0393561756972,1.15728950271097,10.9991120557755));
#282465=CARTESIAN_POINT('Ctrl Pts',(-1.03927246134575,1.15736468080535,
10.9991039038881));
#282466=CARTESIAN_POINT('Ctrl Pts',(-1.03922980052158,1.1574029872932,10.9990997500677));
#282467=CARTESIAN_POINT('Ctrl Pts',(-1.0391427722718,1.15748112398872,10.9990912770342));
#282468=CARTESIAN_POINT('Ctrl Pts',(-1.03909840467282,1.15752095400529,
10.9990869578352));
#282469=CARTESIAN_POINT('Ctrl Pts',(-1.03900785470889,1.15760223380232,
10.9990781436092));
#282470=CARTESIAN_POINT('Ctrl Pts',(-1.03896167215727,1.1576436833668,10.9990736485984));
#282471=CARTESIAN_POINT('Ctrl Pts',(-1.0388673746507,1.15772830667017,10.999064471404));
#282472=CARTESIAN_POINT('Ctrl Pts',(-1.03881925948244,1.15777148017534,
10.9990597892376));
#282473=CARTESIAN_POINT('Ctrl Pts',(-1.03872096855693,1.15785966508199,
10.9990502253743));
#282474=CARTESIAN_POINT('Ctrl Pts',(-1.03867079256195,1.15790467622442,
10.9990453436965));
#282475=CARTESIAN_POINT('Ctrl Pts',(-1.03856824002864,1.15799666051055,
10.9990353673234));
#282476=CARTESIAN_POINT('Ctrl Pts',(-1.03851586322621,1.15804363336504,
10.9990302726495));
#282477=CARTESIAN_POINT('Ctrl Pts',(-1.03840875596478,1.158139676783,10.9990198555351));
#282478=CARTESIAN_POINT('Ctrl Pts',(-1.03835402521412,1.15818874702053,
10.9990145331187));
#282479=CARTESIAN_POINT('Ctrl Pts',(-1.0382420421965,1.15828913390693,10.9990036443566));
#282480=CARTESIAN_POINT('Ctrl Pts',(-1.03818478960058,1.15834045019296,
10.9989980780377));
#282481=CARTESIAN_POINT('Ctrl Pts',(-1.03806757845309,1.15844549247949,
10.9989866837189));
#282482=CARTESIAN_POINT('Ctrl Pts',(-1.03800761953384,1.15849921807104,
10.9989808557495));
#282483=CARTESIAN_POINT('Ctrl Pts',(-1.03788479261365,1.15860925871714,
10.9989689185889));
#282484=CARTESIAN_POINT('Ctrl Pts',(-1.03782192419709,1.15866557331252,
10.9989628094317));
#282485=CARTESIAN_POINT('Ctrl Pts',(-1.03769305403018,1.15878099029404,
10.9989502883328));
#282486=CARTESIAN_POINT('Ctrl Pts',(-1.03762705181061,1.15884009216119,
10.9989438764296));
#282487=CARTESIAN_POINT('Ctrl Pts',(-1.03356816846198,1.1624740055239,10.9985496249519));
#282488=CARTESIAN_POINT('Ctrl Pts',(-1.02955685226786,1.16602815711852,
10.9981633425255));
#282489=CARTESIAN_POINT('Ctrl Pts',(-1.0205100596288,1.17396081304609,10.9972996411769));
#282490=CARTESIAN_POINT('Ctrl Pts',(-1.01546470226551,1.17832771980069,
10.9968230691489));
#282491=CARTESIAN_POINT('Ctrl Pts',(-1.00005785387537,1.19149035075042,
10.9953826388546));
#282492=CARTESIAN_POINT('Ctrl Pts',(-0.989608705185513,1.20018315725476,
10.9944259087285));
#282493=CARTESIAN_POINT('Ctrl Pts',(-0.897424173241232,1.27485022514023,
10.9861458830792));
#282494=CARTESIAN_POINT('Ctrl Pts',(-0.809302212751961,1.33253517950121,
10.9793045699599));
#282495=CARTESIAN_POINT('Ctrl Pts',(-0.641516429719631,1.41953553188741,
10.9668683898685));
#282496=CARTESIAN_POINT('Ctrl Pts',(-0.564010858420602,1.45207232399123,
10.9613211039638));
#282497=CARTESIAN_POINT('Ctrl Pts',(-0.45829848584594,1.48670418611114,
10.9536987008877));
#282498=CARTESIAN_POINT('Ctrl Pts',(-0.432114423602015,1.49452460934193,
10.9518072779189));
#282499=CARTESIAN_POINT('Ctrl Pts',(-0.393703126391878,1.5049031676973,
10.9490202284223));
#282500=CARTESIAN_POINT('Ctrl Pts',(-0.38162860725155,1.50801037324325,
10.9481423874465));
#282501=CARTESIAN_POINT('Ctrl Pts',(-0.360238039427589,1.51324158019046,
10.946583522485));
#282502=CARTESIAN_POINT('Ctrl Pts',(-0.350937212327386,1.51542554768599,
10.9459044780075));
#282503=CARTESIAN_POINT('Ctrl Pts',(-0.331390167504047,1.51982587691099,
10.9444744812599));
#282504=CARTESIAN_POINT('Ctrl Pts',(-0.321140518890845,1.52202460437777,
10.9437229973442));
#282505=CARTESIAN_POINT('Ctrl Pts',(-0.293960466217599,1.52756843058981,
10.9417254268116));
#282506=CARTESIAN_POINT('Ctrl Pts',(-0.276995715133783,1.53073557307638,
10.9404737175396));
#282507=CARTESIAN_POINT('Ctrl Pts',(-0.194354385396315,1.54474510341847,
10.9343500417885));
#282508=CARTESIAN_POINT('Ctrl Pts',(-0.128089580697416,1.55164487114233,
10.9293555918289));
#282509=CARTESIAN_POINT('Ctrl Pts',(0.0436706834585422,1.55845158738,10.9162118709234));
#282510=CARTESIAN_POINT('Ctrl Pts',(0.149079943992258,1.55191874261404,
10.90793949041));
#282511=CARTESIAN_POINT('Ctrl Pts',(0.280210361831377,1.53030128256928,
10.8977661398102));
#282512=CARTESIAN_POINT('Ctrl Pts',(0.307282176764719,1.52509596928942,
10.895673952158));
#282513=CARTESIAN_POINT('Ctrl Pts',(0.352199895423476,1.51521452228139,
10.8922302855463));
#282514=CARTESIAN_POINT('Ctrl Pts',(0.370126141399257,1.51093564849712,
10.8908634358028));
#282515=CARTESIAN_POINT('Ctrl Pts',(0.395251312297537,1.50446440173053,
10.8889621362731));
#282516=CARTESIAN_POINT('Ctrl Pts',(0.402516015508042,1.50253705427318,
10.8884141109401));
#282517=CARTESIAN_POINT('Ctrl Pts',(0.414994956898455,1.49912935039154,
10.8874760344921));
#282518=CARTESIAN_POINT('Ctrl Pts',(0.420215827152018,1.49767429228163,
10.8870845765022));
#282519=CARTESIAN_POINT('Ctrl Pts',(0.431278512647751,1.4945287132472,10.8862573136989));
#282520=CARTESIAN_POINT('Ctrl Pts',(0.437118115670375,1.49283119827138,
10.8858219121576));
#282521=CARTESIAN_POINT('Ctrl Pts',(0.453115430075007,1.48807901731567,
10.8846322847013));
#282522=CARTESIAN_POINT('Ctrl Pts',(0.463252323852146,1.48495456346796,
10.8838819431429));
#282523=CARTESIAN_POINT('Ctrl Pts',(0.517000695679873,1.46778394658538,
10.8799180208293));
#282524=CARTESIAN_POINT('Ctrl Pts',(0.560012158111801,1.45191829482634,
10.8767970031312));
#282525=CARTESIAN_POINT('Ctrl Pts',(0.690153591675974,1.397266950416,10.8673308588443));
#282526=CARTESIAN_POINT('Ctrl Pts',(0.774466623102506,1.35235717699037,
10.8611546890569));
#282527=CARTESIAN_POINT('Ctrl Pts',(0.912717935259911,1.26152240260745,
10.8501735948664));
#282528=CARTESIAN_POINT('Ctrl Pts',(0.968620024274432,1.21912515011395,
10.845454042871));
#282529=CARTESIAN_POINT('Ctrl Pts',(1.03438778115328,1.16185868343569,10.8393957405231));
#282530=CARTESIAN_POINT('Ctrl Pts',(1.04711940035235,1.1503975847477,10.8381975466709));
#282531=CARTESIAN_POINT('Ctrl Pts',(1.06736293224256,1.1315597084454,10.836249041304));
#282532=CARTESIAN_POINT('Ctrl Pts',(1.07499400817569,1.12431262355043,10.8355042376461));
#282533=CARTESIAN_POINT('Ctrl Pts',(1.08949589146341,1.11025784971075,10.8340685067181));
#282534=CARTESIAN_POINT('Ctrl Pts',(1.09637791311915,1.10346239365883,10.8333781311068));
#282535=CARTESIAN_POINT('Ctrl Pts',(1.11202725631845,1.08771896865687,10.8317870207963));
#282536=CARTESIAN_POINT('Ctrl Pts',(1.12075064359249,1.07872848828154,10.8308844220105));
#282537=CARTESIAN_POINT('Ctrl Pts',(1.14863268075869,1.04928946500994,10.827947411693));
#282538=CARTESIAN_POINT('Ctrl Pts',(1.16734662431439,1.02842942774217,10.8258944741035));
#282539=CARTESIAN_POINT('Ctrl Pts',(1.26298756999246,0.915845142358684,
10.814952418841));
#282540=CARTESIAN_POINT('Ctrl Pts',(1.3296870433578,0.815985659815655,10.8056690057718));
#282541=CARTESIAN_POINT('Ctrl Pts',(1.41405871655401,0.651370685682743,
10.7913494688679));
#282542=CARTESIAN_POINT('Ctrl Pts',(1.44016148466121,0.591424110158831,
10.7863232048708));
#282543=CARTESIAN_POINT('Ctrl Pts',(1.46750209729009,0.5159848187844,10.7803499922913));
#282544=CARTESIAN_POINT('Ctrl Pts',(1.47238274840529,0.50188825871935,10.7792485677161));
#282545=CARTESIAN_POINT('Ctrl Pts',(1.47924470494201,0.481106950246127,
10.7776484783731));
#282546=CARTESIAN_POINT('Ctrl Pts',(1.48138489519147,0.474476123689844,
10.7771414270284));
#282547=CARTESIAN_POINT('Ctrl Pts',(1.48494939811085,0.463173172550702,
10.7762833042304));
#282548=CARTESIAN_POINT('Ctrl Pts',(1.48639635697944,0.458508424514052,
10.7759309514881));
#282549=CARTESIAN_POINT('Ctrl Pts',(1.48964971023554,0.4478428961885,10.775129473958));
#282550=CARTESIAN_POINT('Ctrl Pts',(1.49144184304489,0.441837924318492,
10.7746811749112));
#282551=CARTESIAN_POINT('Ctrl Pts',(1.49631963863644,0.425125801893591,
10.7734412989697));
#282552=CARTESIAN_POINT('Ctrl Pts',(1.49932669364301,0.414395816687696,
10.7726540559111));
#282553=CARTESIAN_POINT('Ctrl Pts',(1.51893460664779,0.341420391927617,
10.7673536691209));
#282554=CARTESIAN_POINT('Ctrl Pts',(1.53177224071184,0.278219744739171,
10.7630260166086));
#282555=CARTESIAN_POINT('Ctrl Pts',(1.54297133573613,0.197743356954738,
10.757637767271));
#282556=CARTESIAN_POINT('Ctrl Pts',(1.5450187499334,0.181052628470811,10.7565268815939));
#282557=CARTESIAN_POINT('Ctrl Pts',(1.55369601227163,0.0993767274136418,
10.7511102128562));
#282558=CARTESIAN_POINT('Ctrl Pts',(1.55649837239951,0.0340529898274769,
10.7468349833151));
#282559=CARTESIAN_POINT('Ctrl Pts',(1.55433318553348,-0.0736907103521706,
10.7396583767273));
#282560=CARTESIAN_POINT('Ctrl Pts',(1.55174370631422,-0.116073358986913,
10.7368040125552));
#282561=CARTESIAN_POINT('Ctrl Pts',(1.54439432932295,-0.187917833713793,
10.7318664862688));
#282562=CARTESIAN_POINT('Ctrl Pts',(1.54051420598669,-0.21744594718336,
10.7298085794043));
#282563=CARTESIAN_POINT('Ctrl Pts',(1.53373520605703,-0.259623029228178,
10.7268183001497));
#282564=CARTESIAN_POINT('Ctrl Pts',(1.5315217151264,-0.272376610145237,
10.7259073961001));
#282565=CARTESIAN_POINT('Ctrl Pts',(1.52737454149724,-0.294620143452055,
10.7243062061328));
#282566=CARTESIAN_POINT('Ctrl Pts',(1.52551089189618,-0.304122557384738,
10.7236181756145));
#282567=CARTESIAN_POINT('Ctrl Pts',(1.52146151743582,-0.323795155115286,
10.7221851323312));
#282568=CARTESIAN_POINT('Ctrl Pts',(1.51926225801547,-0.333962023513264,
10.7214397185577));
#282569=CARTESIAN_POINT('Ctrl Pts',(1.51328258567308,-0.360322898597827,
10.7194940607842));
#282570=CARTESIAN_POINT('Ctrl Pts',(1.50934425021789,-0.376479308543374,
10.7182888199874));
#282571=CARTESIAN_POINT('Ctrl Pts',(1.49100580577201,-0.446790707899251,
10.7129857514901));
#282572=CARTESIAN_POINT('Ctrl Pts',(1.47394602061114,-0.500201929933816,
10.7088039518584));
#282573=CARTESIAN_POINT('Ctrl Pts',(1.41944362415481,-0.643620434648861,
10.6971509738672));
#282574=CARTESIAN_POINT('Ctrl Pts',(1.37636878239441,-0.73121376627802,
10.6895436084874));
#282575=CARTESIAN_POINT('Ctrl Pts',(1.30470121076244,-0.847878380833579,
10.6789745496787));
#282576=CARTESIAN_POINT('Ctrl Pts',(1.28273120023684,-0.880763354928661,
10.6759440892604));
#282577=CARTESIAN_POINT('Ctrl Pts',(1.25005071238283,-0.925858766696184,
10.6717471414629));
#282578=CARTESIAN_POINT('Ctrl Pts',(1.24036709889929,-0.938792174621642,
10.6705384855767));
#282579=CARTESIAN_POINT('Ctrl Pts',(1.22291440399567,-0.96136033410246,
10.6684237315943));
#282580=CARTESIAN_POINT('Ctrl Pts',(1.21522866596205,-0.971057488813742,
10.6675131415356));
#282581=CARTESIAN_POINT('Ctrl Pts',(1.20336017080253,-0.985670419329448,
10.666139282267));
#282582=CARTESIAN_POINT('Ctrl Pts',(1.1992614023299,-0.99065330419979,10.6656705082037));
#282583=CARTESIAN_POINT('Ctrl Pts',(1.19168908197599,-0.999743122211864,
10.6648150378832));
#282584=CARTESIAN_POINT('Ctrl Pts',(1.18822517346333,-1.00385761812722,
10.664427709035));
#282585=CARTESIAN_POINT('Ctrl Pts',(1.18023073253259,-1.01325420753702,
10.6635428232858));
#282586=CARTESIAN_POINT('Ctrl Pts',(1.17568602174884,-1.01852395864091,
10.6630463078011));
#282587=CARTESIAN_POINT('Ctrl Pts',(1.1615883998763,-1.03465054909685,10.6615254089667));
#282588=CARTESIAN_POINT('Ctrl Pts',(1.15191900523431,-1.04540519137823,
10.6605090877456));
#282589=CARTESIAN_POINT('Ctrl Pts',(1.08021910309249,-1.12294936306196,
10.6531520381283));
#282590=CARTESIAN_POINT('Ctrl Pts',(1.01256557898478,-1.18431594147996,
10.6471632063603));
#282591=CARTESIAN_POINT('Ctrl Pts',(0.880402876411588,-1.28454272709726,
10.6362486238223));
#282592=CARTESIAN_POINT('Ctrl Pts',(0.817718773075237,-1.32532796554308,
10.6313409701965));
#282593=CARTESIAN_POINT('Ctrl Pts',(0.714525528822122,-1.38235347069619,
10.6233812337839));
#282594=CARTESIAN_POINT('Ctrl Pts',(0.675849522873213,-1.4016685465521,
10.6204235424133));
#282595=CARTESIAN_POINT('Ctrl Pts',(0.622909599836934,-1.42540632313544,
10.6163776182191));
#282596=CARTESIAN_POINT('Ctrl Pts',(0.609311445655792,-1.43127184392235,
10.6153386834402));
#282597=CARTESIAN_POINT('Ctrl Pts',(0.586383345584795,-1.44077585255483,
10.6135862902054));
#282598=CARTESIAN_POINT('Ctrl Pts',(0.577098073983648,-1.44452008977695,
10.6128764505064));
#282599=CARTESIAN_POINT('Ctrl Pts',(0.558682321998663,-1.45174024912831,
10.6114679334567));
#282600=CARTESIAN_POINT('Ctrl Pts',(0.549553950336764,-1.45522030478902,
10.6107694336516));
#282601=CARTESIAN_POINT('Ctrl Pts',(0.527196992078277,-1.46350320650752,
10.6090575740427));
#282602=CARTESIAN_POINT('Ctrl Pts',(0.513935066904985,-1.4682128683091,
10.6080411679831));
#282603=CARTESIAN_POINT('Ctrl Pts',(0.467814940902906,-1.4838899297717,
10.6045021427266));
#282604=CARTESIAN_POINT('Ctrl Pts',(0.434657790014992,-1.49393855205032,
10.6019499874408));
#282605=CARTESIAN_POINT('Ctrl Pts',(0.29202626562788,-1.53201438527138,
10.5909310248924));
#282606=CARTESIAN_POINT('Ctrl Pts',(0.180020315406287,-1.54917163311738,
10.5821444849164));
#282607=CARTESIAN_POINT('Ctrl Pts',(0.00402761114676129,-1.55677807437264,
10.5685053928937));
#282608=CARTESIAN_POINT('Ctrl Pts',(-0.0592256624206096,-1.55565683545488,
10.5636452995368));
#282609=CARTESIAN_POINT('Ctrl Pts',(-0.136867693395798,-1.54953630220077,
10.5578485657119));
#282610=CARTESIAN_POINT('Ctrl Pts',(-0.151477981002337,-1.5481763401527,
10.556765306983));
#282611=CARTESIAN_POINT('Ctrl Pts',(-0.172927099247937,-1.54587323690691,
10.5551881468075));
#282612=CARTESIAN_POINT('Ctrl Pts',(-0.179781872361547,-1.54509104245646,
10.5546860947671));
#282613=CARTESIAN_POINT('Ctrl Pts',(-0.191456060092176,-1.54368016263172,
10.5538346968666));
#282614=CARTESIAN_POINT('Ctrl Pts',(-0.19627800046861,-1.54307446884621,
10.5534841028645));
#282615=CARTESIAN_POINT('Ctrl Pts',(-0.207317806202073,-1.54163514826792,
10.5526839009365));
#282616=CARTESIAN_POINT('Ctrl Pts',(-0.213533552442724,-1.54078649683234,
10.5522351381241));
#282617=CARTESIAN_POINT('Ctrl Pts',(-0.230827036101754,-1.53831871250283,
10.5509911023957));
#282618=CARTESIAN_POINT('Ctrl Pts',(-0.241892957051312,-1.53661751851175,
10.5502002241428));
#282619=CARTESIAN_POINT('Ctrl Pts',(-0.324529278761555,-1.52299876042578,
10.5443263422957));
#282620=CARTESIAN_POINT('Ctrl Pts',(-0.395216003340494,-1.50620442150986,
10.5394804033611));
#282621=CARTESIAN_POINT('Ctrl Pts',(-0.471143182596088,-1.48244834337477,
10.5342219939404));
#282622=CARTESIAN_POINT('Ctrl Pts',(-0.477791942356082,-1.48031883388497,
10.5337610927843));
#282623=CARTESIAN_POINT('Ctrl Pts',(-0.594167636441013,-1.44217951342381,
10.5256828403769));
#282624=CARTESIAN_POINT('Ctrl Pts',(-0.699551572562077,-1.39410963233642,
10.5181636623792));
#282625=CARTESIAN_POINT('Ctrl Pts',(-0.820807408283012,-1.32156068433765,
10.5084611466662));
#282626=CARTESIAN_POINT('Ctrl Pts',(-0.842638061758683,-1.30774936762469,
10.5066702783925));
#282627=CARTESIAN_POINT('Ctrl Pts',(-0.874305903834928,-1.28659227587884,
10.5040002592941));
#282628=CARTESIAN_POINT('Ctrl Pts',(-0.884416981160518,-1.27966287980456,
10.5031365743692));
#282629=CARTESIAN_POINT('Ctrl Pts',(-0.902292720529272,-1.26709909218653,
10.5015889021219));
#282630=CARTESIAN_POINT('Ctrl Pts',(-0.910089229686228,-1.26151093907696,
10.5009067032456));
#282631=CARTESIAN_POINT('Ctrl Pts',(-0.926497827399249,-1.24951878614979,
10.4994553240668));
#282632=CARTESIAN_POINT('Ctrl Pts',(-0.935096284482033,-1.24309707954092,
10.4986854804122));
#282633=CARTESIAN_POINT('Ctrl Pts',(-0.958077735723065,-1.22556016042067,
10.4966022283066));
#282634=CARTESIAN_POINT('Ctrl Pts',(-0.972333071261647,-1.21428126929477,
10.4952824313227));
#282635=CARTESIAN_POINT('Ctrl Pts',(-1.05483313371558,-1.14662248259357,
10.4874771233534));
#282636=CARTESIAN_POINT('Ctrl Pts',(-1.11835065451292,-1.08475933374101,
10.480768445215));
#282637=CARTESIAN_POINT('Ctrl Pts',(-1.23177437772815,-0.953682870696902,
10.4673943728585));
#282638=CARTESIAN_POINT('Ctrl Pts',(-1.28195110414912,-0.885088037894109,
10.4607627246729));
#282639=CARTESIAN_POINT('Ctrl Pts',(-1.33936430480862,-0.791397640484429,
10.452378617557));
#282640=CARTESIAN_POINT('Ctrl Pts',(-1.35192822332241,-0.769738392572532,
10.4504841463116));
#282641=CARTESIAN_POINT('Ctrl Pts',(-1.3722360572939,-0.732696731035967,
10.4473277611513));
#282642=CARTESIAN_POINT('Ctrl Pts',(-1.3802571565989,-0.717472329251631,
10.4460535485327));
#282643=CARTESIAN_POINT('Ctrl Pts',(-1.39134474642483,-0.695553130718436,
10.4442548646842));
#282644=CARTESIAN_POINT('Ctrl Pts',(-1.39461857256909,-0.688965459174152,
10.4437188340359));
#282645=CARTESIAN_POINT('Ctrl Pts',(-1.40022480099366,-0.677480753865958,
10.4427925313469));
#282646=CARTESIAN_POINT('Ctrl Pts',(-1.40257850835641,-0.672594377674542,
10.4424009840639));
#282647=CARTESIAN_POINT('Ctrl Pts',(-1.40756918015765,-0.662093441665002,
10.4415651057953));
#282648=CARTESIAN_POINT('Ctrl Pts',(-1.4101981712845,-0.656475318433295,
10.4411212551461));
#282649=CARTESIAN_POINT('Ctrl Pts',(-1.41734560170118,-0.640960260255658,
10.4399043109389));
#282650=CARTESIAN_POINT('Ctrl Pts',(-1.42179403473055,-0.631031180089095,
10.4391353100348));
#282651=CARTESIAN_POINT('Ctrl Pts',(-1.44736783293577,-0.572305759501093,
10.4346397161898));
#282652=CARTESIAN_POINT('Ctrl Pts',(-1.46608657013888,-0.522493105784168,
10.4310385650746));
#282653=CARTESIAN_POINT('Ctrl Pts',(-1.51487353493543,-0.369227272879561,
10.4203083446149));
#282654=CARTESIAN_POINT('Ctrl Pts',(-1.53679023186072,-0.263528494897026,
10.4133551911491));
#282655=CARTESIAN_POINT('Ctrl Pts',(-1.55285780976403,-0.10454766141402,
10.4026385412856));
#282656=CARTESIAN_POINT('Ctrl Pts',(-1.55548860999734,-0.0524581471936984,
10.39909089029));
#282657=CARTESIAN_POINT('Ctrl Pts',(-1.55550339476856,0.0154151398900086,
10.3943653259887));
#282658=CARTESIAN_POINT('Ctrl Pts',(-1.55526749419952,0.0311677294658214,
10.3932614955591));
#282659=CARTESIAN_POINT('Ctrl Pts',(-1.55448434391733,0.0571226334950191,
10.3914297220558));
#282660=CARTESIAN_POINT('Ctrl Pts',(-1.55407576101648,0.0673282314157227,
10.3907061367901));
#282661=CARTESIAN_POINT('Ctrl Pts',(-1.55308009122629,0.0872800231357074,
10.3892846722555));
#282662=CARTESIAN_POINT('Ctrl Pts',(-1.55250168526127,0.0970261894663112,
10.3885870978017));
#282663=CARTESIAN_POINT('Ctrl Pts',(-1.55090798799796,0.120190382918794,
10.3869211766082));
#282664=CARTESIAN_POINT('Ctrl Pts',(-1.54981026824769,0.133601746397285,
10.3859502916934));
#282665=CARTESIAN_POINT('Ctrl Pts',(-1.54541734539986,0.179879020995319,
10.3825771761104));
#282666=CARTESIAN_POINT('Ctrl Pts',(-1.54124965030803,0.212650989996383,
10.3801480862077));
#282667=CARTESIAN_POINT('Ctrl Pts',(-1.52829064496567,0.293811040400294,
10.3740273609555));
#282668=CARTESIAN_POINT('Ctrl Pts',(-1.5182424458844,0.341959457437992,
10.3703014584866));
#282669=CARTESIAN_POINT('Ctrl Pts',(-1.4911687327985,0.446622424415674,
10.3620102574895));
#282670=CARTESIAN_POINT('Ctrl Pts',(-1.47317256477927,0.502809950775666,
10.357431445426));
#282671=CARTESIAN_POINT('Ctrl Pts',(-1.42464954658911,0.629113615484411,
10.3469431409563));
#282672=CARTESIAN_POINT('Ctrl Pts',(-1.39205275426318,0.698285161738727,
10.3410517378102));
#282673=CARTESIAN_POINT('Ctrl Pts',(-1.34897241668961,0.774583881645573,
10.3345696878018));
#282674=CARTESIAN_POINT('Ctrl Pts',(-1.34333577373525,0.784318678359529,
10.3337430898461));
#282675=CARTESIAN_POINT('Ctrl Pts',(-1.33438609337416,0.799395706152846,
10.3324645422152));
#282676=CARTESIAN_POINT('Ctrl Pts',(-1.33114558091394,0.80478021058844,
10.3320082671268));
#282677=CARTESIAN_POINT('Ctrl Pts',(-1.32534085038746,0.814294484233974,
10.3312028404795));
#282678=CARTESIAN_POINT('Ctrl Pts',(-1.32278987113353,0.818431936525194,
10.3308528751958));
#282679=CARTESIAN_POINT('Ctrl Pts',(-1.31657658190223,0.82840437567501,
10.3300099791922));
#282680=CARTESIAN_POINT('Ctrl Pts',(-1.3128948479954,0.834227084533779,
10.3295183238861));
#282681=CARTESIAN_POINT('Ctrl Pts',(-1.30129188637797,0.852310231800497,
10.3279923347766));
#282682=CARTESIAN_POINT('Ctrl Pts',(-1.29323641070349,0.86448419954538,
10.3269663170907));
#282683=CARTESIAN_POINT('Ctrl Pts',(-1.24982904115684,0.928119282113831,
10.3215998339502));
#282684=CARTESIAN_POINT('Ctrl Pts',(-1.21157009261602,0.977536602587193,
10.3174195330472));
#282685=CARTESIAN_POINT('Ctrl Pts',(-1.09744379398282,1.10791693402874,
10.3059468231119));
#282686=CARTESIAN_POINT('Ctrl Pts',(-1.01574965047762,1.18326431312146,
10.2987650513598));
#282687=CARTESIAN_POINT('Ctrl Pts',(-0.897145009003289,1.27124712461845,
10.2887457100352));
#282688=CARTESIAN_POINT('Ctrl Pts',(-0.866777678880776,1.29214338084181,
10.2862141245161));
#282689=CARTESIAN_POINT('Ctrl Pts',(-0.82356489223676,1.31966969156601,
10.2826382766307));
#282690=CARTESIAN_POINT('Ctrl Pts',(-0.81132459788647,1.32723004750484,
10.2816282983451));
#282691=CARTESIAN_POINT('Ctrl Pts',(-0.791309710654248,1.33921213514567,
10.2799804937974));
#282692=CARTESIAN_POINT('Ctrl Pts',(-0.783598559486943,1.34373862510608,
10.2793465135684));
#282693=CARTESIAN_POINT('Ctrl Pts',(-0.767347913949675,1.35309039954303,
10.2780120075182));
#282694=CARTESIAN_POINT('Ctrl Pts',(-0.758800976236422,1.35790188183994,
10.2773110203419));
#282695=CARTESIAN_POINT('Ctrl Pts',(-0.738192999311206,1.36924778767238,
10.2756226222257));
#282696=CARTESIAN_POINT('Ctrl Pts',(-0.726090100142797,1.37570402060775,
10.2746324871337));
#282697=CARTESIAN_POINT('Ctrl Pts',(-0.682987747595944,1.39796954154876,
10.2711103458631));
#282698=CARTESIAN_POINT('Ctrl Pts',(-0.651547022361764,1.41289674927607,
10.268548168706));
#282699=CARTESIAN_POINT('Ctrl Pts',(-0.570968344893476,1.44789174332572,
10.2619944177055));
#282700=CARTESIAN_POINT('Ctrl Pts',(-0.521257455203041,1.46652139839682,
10.2579618043999));
#282701=CARTESIAN_POINT('Ctrl Pts',(-0.433556354551367,1.49436527048542,
10.2508863759753));
#282702=CARTESIAN_POINT('Ctrl Pts',(-0.395987329333671,1.50475663933873,
10.2478678521476));
#282703=CARTESIAN_POINT('Ctrl Pts',(-0.276000358155853,1.53313931874455,
10.2383051808145));
#282704=CARTESIAN_POINT('Ctrl Pts',(-0.192480951828211,1.54584805374588,
10.2317562760017));
#282705=CARTESIAN_POINT('Ctrl Pts',(-0.0934648524612849,1.55276102561773,
10.2243660206077));
#282706=CARTESIAN_POINT('Ctrl Pts',(-0.0785787314062581,1.5535855006278,
10.2232650681283));
#282707=CARTESIAN_POINT('Ctrl Pts',(-0.0567413935722078,1.5544802739144,
10.2216669549433));
#282708=CARTESIAN_POINT('Ctrl Pts',(-0.0497984322582944,1.5547181830929,
10.221161358905));
#282709=CARTESIAN_POINT('Ctrl Pts',(-0.0374754372895732,1.55505780979167,
10.2202687006766));
#282710=CARTESIAN_POINT('Ctrl Pts',(-0.0320962008876879,1.55517813678579,
10.219880649342));
#282711=CARTESIAN_POINT('Ctrl Pts',(-0.02024921028454,1.5553816423701,10.2190295900416));
#282712=CARTESIAN_POINT('Ctrl Pts',(-0.0137814626568731,1.55545239697449,
10.2185672685518));
#282713=CARTESIAN_POINT('Ctrl Pts',(0.00513299666084232,1.55554132578864,
10.2172214876871));
#282714=CARTESIAN_POINT('Ctrl Pts',(0.0175800728929955,1.55545045909689,
10.2163437735013));
#282715=CARTESIAN_POINT('Ctrl Pts',(0.0463027814650971,1.55489593216534,
10.2143338214371));
#282716=CARTESIAN_POINT('Ctrl Pts',(0.0625751415140964,1.55432612642567,
10.2132065688345));
#282717=CARTESIAN_POINT('Ctrl Pts',(0.11879977693695,1.55147286698851,10.2093419542077));
#282718=CARTESIAN_POINT('Ctrl Pts',(0.158673144433685,1.54790333809282,
10.2066540108054));
#282719=CARTESIAN_POINT('Ctrl Pts',(0.326973655330104,1.52626391728274,
10.1953693837633));
#282720=CARTESIAN_POINT('Ctrl Pts',(0.453000507836864,1.49371462508195,
10.1870239642509));
#282721=CARTESIAN_POINT('Ctrl Pts',(0.601465998060656,1.43482480330409,
10.1761157768921));
#282722=CARTESIAN_POINT('Ctrl Pts',(0.629074870052894,1.42293645980539,
10.174040828878));
#282723=CARTESIAN_POINT('Ctrl Pts',(0.667224960076323,1.40518175370018,
10.1710980222386));
#282724=CARTESIAN_POINT('Ctrl Pts',(0.678069805025433,1.3999807975309,10.1702527343258));
#282725=CARTESIAN_POINT('Ctrl Pts',(0.696860472864829,1.39069964189242,
10.1687721919811));
#282726=CARTESIAN_POINT('Ctrl Pts',(0.70483359537619,1.38667574053434,10.1681389110086));
#282727=CARTESIAN_POINT('Ctrl Pts',(0.72150164302638,1.37808276288746,10.1668040745716));
#282728=CARTESIAN_POINT('Ctrl Pts',(0.730188795982824,1.3734995581754,10.1661020439717));
#282729=CARTESIAN_POINT('Ctrl Pts',(0.750962387331102,1.36228696114578,
10.1644076516162));
#282730=CARTESIAN_POINT('Ctrl Pts',(0.763005045205246,1.35557867714106,
10.163412518788));
#282731=CARTESIAN_POINT('Ctrl Pts',(0.805525017865236,1.33114711006379,
10.1598517373085));
#282732=CARTESIAN_POINT('Ctrl Pts',(0.835484987815926,1.31255005556845,
10.1572550385398));
#282733=CARTESIAN_POINT('Ctrl Pts',(0.909749626136563,1.26287850474203,
10.1505868326479));
#282734=CARTESIAN_POINT('Ctrl Pts',(0.953110155757862,1.23048221314794,
10.1464723909431));
#282735=CARTESIAN_POINT('Ctrl Pts',(1.08296112726762,1.12247814855842,10.1334771471873));
#282736=CARTESIAN_POINT('Ctrl Pts',(1.16283087267265,1.03951312353195,10.1244443299217));
#282737=CARTESIAN_POINT('Ctrl Pts',(1.24465143092602,0.933165587419026,
10.1143828479651));
#282738=CARTESIAN_POINT('Ctrl Pts',(1.25617207246346,0.917598502778497,
10.1129446084986));
#282739=CARTESIAN_POINT('Ctrl Pts',(1.27198588404965,0.895374076450525,
10.1109437433006));
#282740=CARTESIAN_POINT('Ctrl Pts',(1.2765229881443,0.888893634761648,10.1103664405932));
#282741=CARTESIAN_POINT('Ctrl Pts',(1.28410432545275,0.877887279353,10.1093966335496));
#282742=CARTESIAN_POINT('Ctrl Pts',(1.28717451057306,0.873379514953184,
10.1090024318707));
#282743=CARTESIAN_POINT('Ctrl Pts',(1.29353197199915,0.86393889998516,10.1081832101091));
#282744=CARTESIAN_POINT('Ctrl Pts',(1.29681485004551,0.859003279009716,
10.1077584764241));
#282745=CARTESIAN_POINT('Ctrl Pts',(1.30550938150789,0.845768093985171,
10.106628653724));
#282746=CARTESIAN_POINT('Ctrl Pts',(1.31087020173034,0.837435216430967,
10.1059268262796));
#282747=CARTESIAN_POINT('Ctrl Pts',(1.33761554398154,0.794975949417039,
10.1023955066197));
#282748=CARTESIAN_POINT('Ctrl Pts',(1.35775067780397,0.760076220453683,
10.0996379220186));
#282749=CARTESIAN_POINT('Ctrl Pts',(1.4117830855697,0.657407811024459,10.0918171268182));
#282750=CARTESIAN_POINT('Ctrl Pts',(1.44211591904419,0.587894183250133,
10.0868684680191));
#282751=CARTESIAN_POINT('Ctrl Pts',(1.49856949249769,0.427504291966573,
10.0756667832826));
#282752=CARTESIAN_POINT('Ctrl Pts',(1.52171870499869,0.335915333446381,
10.0694067945121));
#282753=CARTESIAN_POINT('Ctrl Pts',(1.53926479428324,0.224884800995694,
10.0616103018775));
#282754=CARTESIAN_POINT('Ctrl Pts',(1.54178245938857,0.206920469491736,
10.0603431044049));
#282755=CARTESIAN_POINT('Ctrl Pts',(1.54528735785166,0.17827553037528,10.058311273358));
#282756=CARTESIAN_POINT('Ctrl Pts',(1.54647931767233,0.167621277595261,
10.0575530960274));
#282757=CARTESIAN_POINT('Ctrl Pts',(1.54852860141261,0.147415641208562,
10.0561101577074));
#282758=CARTESIAN_POINT('Ctrl Pts',(1.54940791830335,0.137866949577216,
10.0554261233956));
#282759=CARTESIAN_POINT('Ctrl Pts',(1.55121038825255,0.11609026347054,10.0538609479578));
#282760=CARTESIAN_POINT('Ctrl Pts',(1.55207732900648,0.103858397179467,
10.0529780856248));
#282761=CARTESIAN_POINT('Ctrl Pts',(1.55432356288825,0.0657877608959347,
10.0502180268214));
#282762=CARTESIAN_POINT('Ctrl Pts',(1.55520275199466,0.0399251678423884,
10.0483254570714));
#282763=CARTESIAN_POINT('Ctrl Pts',(1.55629952202834,-0.0814601183507938,
10.0393549435886));
#282764=CARTESIAN_POINT('Ctrl Pts',(1.54836288114979,-0.176835265194943,
10.0320336144696));
#282765=CARTESIAN_POINT('Ctrl Pts',(1.51534653778634,-0.363541902773961,
10.0173396684373));
#282766=CARTESIAN_POINT('Ctrl Pts',(1.49057942071121,-0.454548072093131,
10.0100020859026));
#282767=CARTESIAN_POINT('Ctrl Pts',(1.45313966025916,-0.55510246454981,
10.0020173604628));
#282768=CARTESIAN_POINT('Ctrl Pts',(1.44838860799548,-0.56738354612946,
10.0010445834244));
#282769=CARTESIAN_POINT('Ctrl Pts',(1.44098841786745,-0.585813462746825,
9.9995899563391));
#282770=CARTESIAN_POINT('Ctrl Pts',(1.43845474479215,-0.592007588736285,
9.99910196428355));
#282771=CARTESIAN_POINT('Ctrl Pts',(1.43378124046212,-0.603225845657192,
9.99822003104053));
#282772=CARTESIAN_POINT('Ctrl Pts',(1.43165478088288,-0.608255422204919,
9.99782531888312));
#282773=CARTESIAN_POINT('Ctrl Pts',(1.42717082773411,-0.618707227318865,
9.99700665963995));
#282774=CARTESIAN_POINT('Ctrl Pts',(1.42480884527055,-0.624127360596184,
9.99658298562653));
#282775=CARTESIAN_POINT('Ctrl Pts',(1.41843407464344,-0.638530991334191,
9.99545907575346));
#282776=CARTESIAN_POINT('Ctrl Pts',(1.41436677873941,-0.647490292925158,
9.99476204235993));
#282777=CARTESIAN_POINT('Ctrl Pts',(1.3936234462841,-0.692054694941648,
9.99130225993986));
#282778=CARTESIAN_POINT('Ctrl Pts',(1.37568515912833,-0.727060501835112,
9.98860797429469));
#282779=CARTESIAN_POINT('Ctrl Pts',(1.31899441143588,-0.828061687075055,
9.98079349592539));
#282780=CARTESIAN_POINT('Ctrl Pts',(1.27667870295967,-0.891922289692205,
9.97579523617957));
#282781=CARTESIAN_POINT('Ctrl Pts',(1.1718978683036,-1.02722382843487,9.96452203847612));
#282782=CARTESIAN_POINT('Ctrl Pts',(1.1072657507728,-1.09658215736149,9.95824108126202));
#282783=CARTESIAN_POINT('Ctrl Pts',(1.0232169401654,-1.17172366078031,9.95042154537807));
#282784=CARTESIAN_POINT('Ctrl Pts',(1.00948491285748,-1.18357484204755,
9.94915441897439));
#282785=CARTESIAN_POINT('Ctrl Pts',(0.987312195378336,-1.20204401123956,
9.94712268312834));
#282786=CARTESIAN_POINT('Ctrl Pts',(0.979004589510791,-1.20881974646406,
9.94636452916766));
#282787=CARTESIAN_POINT('Ctrl Pts',(0.963134725257411,-1.22149240653079,
9.94492162386247));
#282788=CARTESIAN_POINT('Ctrl Pts',(0.955586645869443,-1.22740635197405,
9.94423759906924));
#282789=CARTESIAN_POINT('Ctrl Pts',(0.938262409294526,-1.24072328527305,
9.94267242953202));
#282790=CARTESIAN_POINT('Ctrl Pts',(0.928452530916719,-1.24808112762479,
9.9417895634403));
#282791=CARTESIAN_POINT('Ctrl Pts',(0.897674430386662,-1.27060239093662,
9.93902942994074));
#282792=CARTESIAN_POINT('Ctrl Pts',(0.876415121155238,-1.2853583957102,
9.93713678764556));
#282793=CARTESIAN_POINT('Ctrl Pts',(0.774372103184238,-1.35247737553135,
9.92811099901745));
#282794=CARTESIAN_POINT('Ctrl Pts',(0.689221375689425,-1.39778945210965,
9.92073015488553));
#282795=CARTESIAN_POINT('Ctrl Pts',(0.514444930658023,-1.47092410606182,
9.90604592201314));
#282796=CARTESIAN_POINT('Ctrl Pts',(0.425376326242168,-1.49910952664903,
9.89878002623605));
#282797=CARTESIAN_POINT('Ctrl Pts',(0.320155797276616,-1.52226497239393,
9.89076139865152));
#282798=CARTESIAN_POINT('Ctrl Pts',(0.305955122657982,-1.52518257387742,
9.88969105442227));
#282799=CARTESIAN_POINT('Ctrl Pts',(0.284941972115323,-1.52919451663653,
9.88812666765382));
#282800=CARTESIAN_POINT('Ctrl Pts',(0.278160171186423,-1.53044265531156,
9.88762474804067));
#282801=CARTESIAN_POINT('Ctrl Pts',(0.266067371948872,-1.53258520332481,
9.88673531383142));
#282802=CARTESIAN_POINT('Ctrl Pts',(0.260759754289792,-1.53349718148213,
9.88634684936271));
#282803=CARTESIAN_POINT('Ctrl Pts',(0.24911530135477,-1.53543577569523,
9.88549881506956));
#282804=CARTESIAN_POINT('Ctrl Pts',(0.242776749469522,-1.53645075043548,
9.88503989501997));
#282805=CARTESIAN_POINT('Ctrl Pts',(0.224364657230055,-1.53928223982984,
9.88371417741561));
#282806=CARTESIAN_POINT('Ctrl Pts',(0.212275444038127,-1.54099593560062,
9.88285286803188));
#282807=CARTESIAN_POINT('Ctrl Pts',(0.118909473050545,-1.55311130366237,
9.87626247241841));
#282808=CARTESIAN_POINT('Ctrl Pts',(0.0369335631088823,-1.55721996121098,
9.87083135443084));
#282809=CARTESIAN_POINT('Ctrl Pts',(-0.163081408808733,-1.55143187887351,
9.85764352626439));
#282810=CARTESIAN_POINT('Ctrl Pts',(-0.280380362293359,-1.5345747329513,
9.84993633759345));
#282811=CARTESIAN_POINT('Ctrl Pts',(-0.413536328731252,-1.499649870811,
9.84043569419926));
#282812=CARTESIAN_POINT('Ctrl Pts',(-0.432340398125268,-1.49433722832845,
9.83907694735778));
#282813=CARTESIAN_POINT('Ctrl Pts',(-0.462673681735902,-1.48514683230853,
9.83685441804291));
#282814=CARTESIAN_POINT('Ctrl Pts',(-0.474266618038531,-1.48148547388834,
9.8359976382229));
#282815=CARTESIAN_POINT('Ctrl Pts',(-0.494914188618812,-1.47469723573101,
9.83445784658707));
#282816=CARTESIAN_POINT('Ctrl Pts',(-0.503985202632711,-1.47162186012096,
9.83377655828964));
#282817=CARTESIAN_POINT('Ctrl Pts',(-0.523206752306553,-1.46490655629693,
9.83232232789581));
#282818=CARTESIAN_POINT('Ctrl Pts',(-0.533348950617583,-1.46124447316452,
9.83154868078896));
#282819=CARTESIAN_POINT('Ctrl Pts',(-0.560722597449305,-1.4510376154008,
9.82944296332982));
#282820=CARTESIAN_POINT('Ctrl Pts',(-0.577876622449098,-1.44429171136471,
9.82810425701056));
#282821=CARTESIAN_POINT('Ctrl Pts',(-0.615675052637151,-1.42864611932829,
9.82511043111805));
#282822=CARTESIAN_POINT('Ctrl Pts',(-0.6362542261378,-1.41960063724869,
9.82345072033123));
#282823=CARTESIAN_POINT('Ctrl Pts',(-0.700991367835165,-1.38945531904745,
9.8181331384355));
#282824=CARTESIAN_POINT('Ctrl Pts',(-0.744349818166054,-1.36671778785252,
9.81442509219411));
#282825=CARTESIAN_POINT('Ctrl Pts',(-0.862133414366616,-1.29768231610186,
9.80395639880612));
#282826=CARTESIAN_POINT('Ctrl Pts',(-0.933825305300214,-1.24708571469065,
9.79710913659752));
#282827=CARTESIAN_POINT('Ctrl Pts',(-1.03849206906034,-1.15910706510403,
9.78659477604931));
#282828=CARTESIAN_POINT('Ctrl Pts',(-1.07459313835133,-1.12572004079051,
9.78285954456732));
#282829=CARTESIAN_POINT('Ctrl Pts',(-1.11660324698712,-1.08300198079821,
9.7784329799257));
#282830=CARTESIAN_POINT('Ctrl Pts',(-1.12407071720228,-1.07524933926586,
9.77764288208148));
#282831=CARTESIAN_POINT('Ctrl Pts',(-1.13565271219798,-1.06297250389569,
9.77641315521438));
#282832=CARTESIAN_POINT('Ctrl Pts',(-1.13982188411757,-1.05850068620871,
9.77596959824826));
#282833=CARTESIAN_POINT('Ctrl Pts',(-1.14765327146813,-1.0500008817041,
9.77513491876846));
#282834=CARTESIAN_POINT('Ctrl Pts',(-1.1513207249061,-1.04597823713344,
9.77474342841113));
#282835=CARTESIAN_POINT('Ctrl Pts',(-1.16000253613381,-1.03635460913824,
9.7738150371947));
#282836=CARTESIAN_POINT('Ctrl Pts',(-1.16499753073584,-1.0307363965914,
9.77327956561259));
#282837=CARTESIAN_POINT('Ctrl Pts',(-1.18124948554556,-1.01218763466873,
9.77153204968764));
#282838=CARTESIAN_POINT('Ctrl Pts',(-1.19233390553272,-0.999106638871684,
9.7703317402204));
#282839=CARTESIAN_POINT('Ctrl Pts',(-1.22918603261601,-0.954129465201075,
9.76630117487401));
#282840=CARTESIAN_POINT('Ctrl Pts',(-1.2539098806154,-0.921396726955455,
9.76352824382719));
#282841=CARTESIAN_POINT('Ctrl Pts',(-1.33408675807152,-0.806032994620876,
9.7541438788558));
#282842=CARTESIAN_POINT('Ctrl Pts',(-1.38289360906679,-0.719084850558077,
9.7477059230512));
#282843=CARTESIAN_POINT('Ctrl Pts',(-1.44730803479187,-0.573136206360701,
9.73706603456093));
#282844=CARTESIAN_POINT('Ctrl Pts',(-1.46834896484791,-0.516851690831509,
9.73300223399403));
#282845=CARTESIAN_POINT('Ctrl Pts',(-1.49108675389529,-0.443314167285405,
9.72765361427503));
#282846=CARTESIAN_POINT('Ctrl Pts',(-1.49582553401014,-0.427051625814905,
9.72646861026317));
#282847=CARTESIAN_POINT('Ctrl Pts',(-1.50306070278807,-0.400622364920187,
9.7245375812482));
#282848=CARTESIAN_POINT('Ctrl Pts',(-1.50572177123269,-0.390501848271013,
9.72379691693128));
#282849=CARTESIAN_POINT('Ctrl Pts',(-1.51064123726892,-0.370993953502119,
9.72236651387515));
#282850=CARTESIAN_POINT('Ctrl Pts',(-1.51291475001934,-0.36161085810754,
9.72167730004506));
#282851=CARTESIAN_POINT('Ctrl Pts',(-1.51723977373337,-0.343005778881625,
9.72030806124122));
#282852=CARTESIAN_POINT('Ctrl Pts',(-1.51929491002878,-0.333785057158363,
9.71962818588105));
#282853=CARTESIAN_POINT('Ctrl Pts',(-1.52385847318596,-0.312393990993489,
9.71804775800513));
#282854=CARTESIAN_POINT('Ctrl Pts',(-1.52630527757912,-0.300211317062768,
9.71714528760685));
#282855=CARTESIAN_POINT('Ctrl Pts',(-1.53425832795198,-0.257999377946727,
9.71400947844671));
#282856=CARTESIAN_POINT('Ctrl Pts',(-1.53902599631828,-0.227839945848046,
9.71175346709022));
#282857=CARTESIAN_POINT('Ctrl Pts',(-1.55135442567432,-0.131558234917276,
9.70449938697087));
#282858=CARTESIAN_POINT('Ctrl Pts',(-1.55556075073686,-0.0650894167034694,
9.69941056741366));
#282859=CARTESIAN_POINT('Ctrl Pts',(-1.55549933718348,0.00143597414997556,
9.69426865344254));
#282860=CARTESIAN_POINT('',(-1.55403083159801,-0.00119596074553188,8.29405622560371));
#282861=CARTESIAN_POINT('Ctrl Pts',(-1.55549933771838,0.00143539460917734,
9.6942686982367));
#282862=CARTESIAN_POINT('Ctrl Pts',(-1.55541261527942,0.0954142179250701,
9.6870048401175));
#282863=CARTESIAN_POINT('Ctrl Pts',(-1.54680933472033,0.189197638033392,
9.67965256375285));
#282864=CARTESIAN_POINT('Ctrl Pts',(-1.52603212362729,0.302055032806816,
9.67099562326331));
#282865=CARTESIAN_POINT('Ctrl Pts',(-1.52186445503809,0.322397221263767,
9.66944363960071));
#282866=CARTESIAN_POINT('Ctrl Pts',(-1.515606086761,0.350109855788246,9.66734610604476));
#282867=CARTESIAN_POINT('Ctrl Pts',(-1.51386663274056,0.357556353250518,
9.66678416235489));
#282868=CARTESIAN_POINT('Ctrl Pts',(-1.5104498734183,0.371711229618512,
9.66571954545384));
#282869=CARTESIAN_POINT('Ctrl Pts',(-1.50878261662827,0.378421826788227,
9.66521636292153));
#282870=CARTESIAN_POINT('Ctrl Pts',(-1.50586638380403,0.389833736125145,
9.66436353523265));
#282871=CARTESIAN_POINT('Ctrl Pts',(-1.50464003687192,0.394540580464178,
9.66401263320883));
#282872=CARTESIAN_POINT('Ctrl Pts',(-1.50178287494478,0.405299556831327,
9.66321251175281));
#282873=CARTESIAN_POINT('Ctrl Pts',(-1.50013753783908,0.41134766985951,
9.66276413143113));
#282874=CARTESIAN_POINT('Ctrl Pts',(-1.49545766258339,0.428148876994693,
9.66152204775521));
#282875=CARTESIAN_POINT('Ctrl Pts',(-1.49234368629004,0.438879735660125,
9.66073271841768));
#282876=CARTESIAN_POINT('Ctrl Pts',(-1.46960795494937,0.514186385958228,
9.65521534575491));
#282877=CARTESIAN_POINT('Ctrl Pts',(-1.44591458703667,0.577467459906825,
9.65069171557042));
#282878=CARTESIAN_POINT('Ctrl Pts',(-1.38466379563751,0.713402505763742,
9.64081856058279));
#282879=CARTESIAN_POINT('Ctrl Pts',(-1.34534631802599,0.785035170571468,
9.63550513473516));
#282880=CARTESIAN_POINT('Ctrl Pts',(-1.27806998315163,0.887582733140757,
9.62732897832204));
#282881=CARTESIAN_POINT('Ctrl Pts',(-1.25419928031693,0.921004760109985,
9.62456484454457));
#282882=CARTESIAN_POINT('Ctrl Pts',(-1.21135611861394,0.976231820141588,
9.61978282878352));
#282883=CARTESIAN_POINT('Ctrl Pts',(-1.1930469349765,0.998524432871331,
9.61778860776198));
#282884=CARTESIAN_POINT('Ctrl Pts',(-1.16685068066535,1.02867044556686,
9.61499290463235));
#282885=CARTESIAN_POINT('Ctrl Pts',(-1.15948251156927,1.03696850994968,
9.61421253971716));
#282886=CARTESIAN_POINT('Ctrl Pts',(-1.15173553693241,1.04550738413894,
9.61339790587471));
#282887=CARTESIAN_POINT('Ctrl Pts',(-1.15144458739381,1.04582780584705,
9.61336731951908));
#282888=CARTESIAN_POINT('Ctrl Pts',(-1.14454217049321,1.05342304151219,
9.61264189658121));
#282889=CARTESIAN_POINT('Ctrl Pts',(-1.13786216393447,1.06063498539061,
9.61194420402022));
#282890=CARTESIAN_POINT('Ctrl Pts',(-1.12499044511659,1.07427014027379,
9.6106077342234));
#282891=CARTESIAN_POINT('Ctrl Pts',(-1.11881093037791,1.08070436837419,
9.60996949932306));
#282892=CARTESIAN_POINT('Ctrl Pts',(-1.10260748948733,1.09728777135311,
9.60830442022423));
#282893=CARTESIAN_POINT('Ctrl Pts',(-1.0924988964974,1.10735263803247,9.60727388724269));
#282894=CARTESIAN_POINT('Ctrl Pts',(-1.05637096302315,1.14234807365739,
9.6036182849624));
#282895=CARTESIAN_POINT('Ctrl Pts',(-1.02962706589937,1.16651037057111,
9.60096098141674));
#282896=CARTESIAN_POINT('Ctrl Pts',(-0.916655297339226,1.26166351431942,
9.58992208712454));
#282897=CARTESIAN_POINT('Ctrl Pts',(-0.823750934930763,1.32419002778414,
9.58123575563827));
#282898=CARTESIAN_POINT('Ctrl Pts',(-0.669537667954223,1.40542715193257,
9.56774325129167));
#282899=CARTESIAN_POINT('Ctrl Pts',(-0.612382004872291,1.43125682270425,
9.56292653527625));
#282900=CARTESIAN_POINT('Ctrl Pts',(-0.540155656371165,1.45877547520327,
9.55717452124298));
#282901=CARTESIAN_POINT('Ctrl Pts',(-0.526419481355658,1.4637884379101,
9.55609513219524));
#282902=CARTESIAN_POINT('Ctrl Pts',(-0.506105159175053,1.4708791060606,
9.55452215219244));
#282903=CARTESIAN_POINT('Ctrl Pts',(-0.499581101063407,1.47310777104194,
9.55402048680705));
#282904=CARTESIAN_POINT('Ctrl Pts',(-0.488431256707352,1.47683404404708,
9.55316934149036));
#282905=CARTESIAN_POINT('Ctrl Pts',(-0.483813007196752,1.47835342956835,
9.55281861848711));
#282906=CARTESIAN_POINT('Ctrl Pts',(-0.47321102610221,1.48178643472266,
9.55201767192329));
#282907=CARTESIAN_POINT('Ctrl Pts',(-0.467222743311001,1.48368548729067,
9.5515682981928));
#282908=CARTESIAN_POINT('Ctrl Pts',(-0.450491604099716,1.48888005829092,
9.55032073447491));
#282909=CARTESIAN_POINT('Ctrl Pts',(-0.439724031649438,1.49209560972842,
9.54952698047757));
#282910=CARTESIAN_POINT('Ctrl Pts',(-0.356069857420918,1.51609324539627,
9.54342383579048));
#282911=CARTESIAN_POINT('Ctrl Pts',(-0.281776512864256,1.53164283609062,
9.53837347447603));
#282912=CARTESIAN_POINT('Ctrl Pts',(-0.152499314782979,1.54896986194807,
9.52976127771568));
#282913=CARTESIAN_POINT('Ctrl Pts',(-0.0980182946931811,1.55336926948925,
9.52618450954415));
#282914=CARTESIAN_POINT('Ctrl Pts',(0.00872002605207692,1.55634983009207,
9.51912048744014));
#282915=CARTESIAN_POINT('Ctrl Pts',(0.0608954394185542,1.55518228058939,
9.51564107047954));
#282916=CARTESIAN_POINT('Ctrl Pts',(0.147217570034247,1.54889974658509,
9.50975168036049));
#282917=CARTESIAN_POINT('Ctrl Pts',(0.181429699616682,1.54526580399858,
9.50738296166406));
#282918=CARTESIAN_POINT('Ctrl Pts',(0.229019439911564,1.53860876744828,
9.50402443818687));
#282919=CARTESIAN_POINT('Ctrl Pts',(0.242521725054139,1.53653832851592,
9.50306437970104));
#282920=CARTESIAN_POINT('Ctrl Pts',(0.265659963395845,1.53267773956426,
9.5014059562192));
#282921=CARTESIAN_POINT('Ctrl Pts',(0.275309645762535,1.5309738274878,9.50071035225121));
#282922=CARTESIAN_POINT('Ctrl Pts',(0.293745453317072,1.52753855706686,
9.49937348686464));
#282923=CARTESIAN_POINT('Ctrl Pts',(0.302534016375152,1.52582226927122,
9.4987327312353));
#282924=CARTESIAN_POINT('Ctrl Pts',(0.323188960730375,1.52160317257602,
9.49721843208111));
#282925=CARTESIAN_POINT('Ctrl Pts',(0.33504170523239,1.51903731336022,9.49634290748647));
#282926=CARTESIAN_POINT('Ctrl Pts',(0.376762366055451,1.50949366508533,
9.49323725354306));
#282927=CARTESIAN_POINT('Ctrl Pts',(0.406450867280551,1.50177177114491,
9.49098368268089));
#282928=CARTESIAN_POINT('Ctrl Pts',(0.548039896804091,1.4604389700368,9.48001792271427));
#282929=CARTESIAN_POINT('Ctrl Pts',(0.656128923529045,1.41517345486148,
9.47094319001451));
#282930=CARTESIAN_POINT('Ctrl Pts',(0.814419730375271,1.32682288940417,
9.45690475588576));
#282931=CARTESIAN_POINT('Ctrl Pts',(0.868724292907427,1.29192039808412,
9.45194245481959));
#282932=CARTESIAN_POINT('Ctrl Pts',(0.932648220136336,1.24497667928835,
9.44603837431956));
#282933=CARTESIAN_POINT('Ctrl Pts',(0.944461258362085,1.23603908054164,
9.44494463342849));
#282934=CARTESIAN_POINT('Ctrl Pts',(0.961611249896628,1.2226741484721,9.44335488925641));
#282935=CARTESIAN_POINT('Ctrl Pts',(0.967048730602531,1.21837803116929,
9.44285057318998));
#282936=CARTESIAN_POINT('Ctrl Pts',(0.976255024574355,1.21100373719569,
9.44199648321511));
#282937=CARTESIAN_POINT('Ctrl Pts',(0.980038329870864,1.20794403803168,
9.44164544216235));
#282938=CARTESIAN_POINT('Ctrl Pts',(0.988654201724353,1.20090893632097,
9.44084591372869));
#282939=CARTESIAN_POINT('Ctrl Pts',(0.993477207236447,1.19692207193909,
9.44039825758991));
#282940=CARTESIAN_POINT('Ctrl Pts',(1.00680875787069,1.18576564593097,9.43916017138388));
#282941=CARTESIAN_POINT('Ctrl Pts',(1.01526484605332,1.17853356043519,9.43837407030936));
#282942=CARTESIAN_POINT('Ctrl Pts',(1.0718598416443,1.12906932033044,9.43310157432554));
#282943=CARTESIAN_POINT('Ctrl Pts',(1.11743504326533,1.08398438501318,9.42879878823887));
#282944=CARTESIAN_POINT('Ctrl Pts',(1.17157330468898,1.02337314183482,9.42340912187704));
#282945=CARTESIAN_POINT('Ctrl Pts',(1.18282727300556,1.01034462086366,9.4222719093559));
#282946=CARTESIAN_POINT('Ctrl Pts',(1.2356469809701,0.947103750910749,9.41683878014942));
#282947=CARTESIAN_POINT('Ctrl Pts',(1.27424434055381,0.894499915408819,
9.41257332816262));
#282948=CARTESIAN_POINT('Ctrl Pts',(1.3324343652881,0.803750945944138,9.40539605776084));
#282949=CARTESIAN_POINT('Ctrl Pts',(1.35395523379599,0.76694310312271,9.40253056913712));
#282950=CARTESIAN_POINT('Ctrl Pts',(1.38793981918345,0.702919165803043,
9.39757570585457));
#282951=CARTESIAN_POINT('Ctrl Pts',(1.40117953690822,0.67614199760791,9.3955118659821));
#282952=CARTESIAN_POINT('Ctrl Pts',(1.41904492390152,0.637228053124277,
9.39251476415147));
#282953=CARTESIAN_POINT('Ctrl Pts',(1.42430278518711,0.625387596491295,
9.39160313656666));
#282954=CARTESIAN_POINT('Ctrl Pts',(1.43323026758176,0.604586617193399,
9.39000140176424));
#282955=CARTESIAN_POINT('Ctrl Pts',(1.43696531438743,0.595654812045977,
9.38931356106387));
#282956=CARTESIAN_POINT('Ctrl Pts',(1.44453536817917,0.577066518368343,
9.38788162286825));
#282957=CARTESIAN_POINT('Ctrl Pts',(1.44835747433914,0.567405334275767,
9.38713713054527));
#282958=CARTESIAN_POINT('Ctrl Pts',(1.45802967326584,0.542222155424631,
9.38519546708523));
#282959=CARTESIAN_POINT('Ctrl Pts',(1.46372862933815,0.526643953706327,
9.38399333097552));
#282960=CARTESIAN_POINT('Ctrl Pts',(1.48746120477969,0.458407457258115,
9.37872122848307));
#282961=CARTESIAN_POINT('Ctrl Pts',(1.50290816632667,0.404899859479817,
9.37456847200837));
#282962=CARTESIAN_POINT('Ctrl Pts',(1.53744141220164,0.255667694278585,
9.36293798832377));
#282963=CARTESIAN_POINT('Ctrl Pts',(1.55044266502748,0.158797677873854,
9.35532195431415));
#282964=CARTESIAN_POINT('Ctrl Pts',(1.55585038860724,0.0218163286373182,
9.3447405974511));
#282965=CARTESIAN_POINT('Ctrl Pts',(1.55590193998971,-0.0177752250028949,
9.34170697923197));
#282966=CARTESIAN_POINT('Ctrl Pts',(1.55384744497674,-0.0734825912149364,
9.33750617347099));
#282967=CARTESIAN_POINT('Ctrl Pts',(1.55299984398444,-0.0896275954189802,
9.33629678041485));
#282968=CARTESIAN_POINT('Ctrl Pts',(1.55105904912001,-0.118107186202107,
9.33418087119469));
#282969=CARTESIAN_POINT('Ctrl Pts',(1.55007000606673,-0.130447243253486,
9.33326985927595));
#282970=CARTESIAN_POINT('Ctrl Pts',(1.54834132435507,-0.149201361909723,
9.33189544113855));
#282971=CARTESIAN_POINT('Ctrl Pts',(1.54770893220955,-0.155624446302966,
9.33142652715709));
#282972=CARTESIAN_POINT('Ctrl Pts',(1.54647587991665,-0.167396447338708,
9.33057066296337));
#282973=CARTESIAN_POINT('Ctrl Pts',(1.54588742921287,-0.172746275550064,
9.33018308160653));
#282974=CARTESIAN_POINT('Ctrl Pts',(1.54447368052406,-0.185013026508508,
9.32929744618728));
#282975=CARTESIAN_POINT('Ctrl Pts',(1.54362967677005,-0.191927579489049,
9.3288004358046));
#282976=CARTESIAN_POINT('Ctrl Pts',(1.54088858052762,-0.213195298012295,
9.32727787986429));
#282977=CARTESIAN_POINT('Ctrl Pts',(1.53883746737255,-0.227528330313268,
9.32626040585883));
#282978=CARTESIAN_POINT('Ctrl Pts',(1.5224470930103,-0.331672115356008,
9.31891649308499));
#282979=CARTESIAN_POINT('Ctrl Pts',(1.50045367450651,-0.420113078326266,
9.31293983805421));
#282980=CARTESIAN_POINT('Ctrl Pts',(1.4387856521834,-0.599323345085008,
9.30046748363324));
#282981=CARTESIAN_POINT('Ctrl Pts',(1.39793909118043,-0.689243129115332,
9.29399088359443));
#282982=CARTESIAN_POINT('Ctrl Pts',(1.33597429279144,-0.797134128920556,
9.28544828544408));
#282983=CARTESIAN_POINT('Ctrl Pts',(1.32252670961643,-0.819251548559116,
9.28365391706747));
#282984=CARTESIAN_POINT('Ctrl Pts',(1.30190355871589,-0.851338812491502,
9.28097990413411));
#282985=CARTESIAN_POINT('Ctrl Pts',(1.2951512320459,-0.8615764160173,9.28011580559167));
#282986=CARTESIAN_POINT('Ctrl Pts',(1.28290472339639,-0.879674754913353,
9.27856794725283));
#282987=CARTESIAN_POINT('Ctrl Pts',(1.2774575060969,-0.887566626416058,
9.27788598286488));
#282988=CARTESIAN_POINT('Ctrl Pts',(1.26576693508939,-0.904173232263594,
9.2764356982702));
#282989=CARTESIAN_POINT('Ctrl Pts',(1.25950578762102,-0.912874760405781,
9.27566672020235));
#282990=CARTESIAN_POINT('Ctrl Pts',(1.24241129767076,-0.936121426890868,
9.27358734413671));
#282991=CARTESIAN_POINT('Ctrl Pts',(1.23141299239173,-0.950542555011112,
9.27227059129783));
#282992=CARTESIAN_POINT('Ctrl Pts',(1.16564130568487,-1.03372564150277,
9.26451335266591));
#282993=CARTESIAN_POINT('Ctrl Pts',(1.10537936776099,-1.09792524279161,
9.25785280434918));
#282994=CARTESIAN_POINT('Ctrl Pts',(0.976446959897203,-1.21385454430315,
9.2444769008393));
#282995=CARTESIAN_POINT('Ctrl Pts',(0.908258424841598,-1.26568497329169,
9.23779206644919));
#282996=CARTESIAN_POINT('Ctrl Pts',(0.814966809207347,-1.32515688140037,
9.22934916371899));
#282997=CARTESIAN_POINT('Ctrl Pts',(0.79345265834494,-1.33814972577921,
9.22744733510685));
#282998=CARTESIAN_POINT('Ctrl Pts',(0.756652724214756,-1.35917420491084,
9.22428024117004));
#282999=CARTESIAN_POINT('Ctrl Pts',(0.741531341786931,-1.3674827966096,
9.22300256128633));
#283000=CARTESIAN_POINT('Ctrl Pts',(0.719764963415035,-1.37897528145857,
9.22120013134219));
#283001=CARTESIAN_POINT('Ctrl Pts',(0.713231388888479,-1.38236587819077,
9.22066374335529));
#283002=CARTESIAN_POINT('Ctrl Pts',(0.701843830769808,-1.38817321798784,
9.21973720611938));
#283003=CARTESIAN_POINT('Ctrl Pts',(0.697000915441982,-1.39061115111239,
9.21934577644969));
#283004=CARTESIAN_POINT('Ctrl Pts',(0.68659683077379,-1.39578057917449,
9.21851052049622));
#283005=CARTESIAN_POINT('Ctrl Pts',(0.68103198981634,-1.39850422439332,
9.21806717096572));
#283006=CARTESIAN_POINT('Ctrl Pts',(0.665676807117687,-1.40590624536577,
9.2168527553031));
#283007=CARTESIAN_POINT('Ctrl Pts',(0.655853325281988,-1.41051565586234,
9.21608575601693));
#283008=CARTESIAN_POINT('Ctrl Pts',(0.598063277363678,-1.43689781257183,
9.21162672168504));
#283009=CARTESIAN_POINT('Ctrl Pts',(0.5490583116362,-1.4563280183136,9.20805781054925));
#283010=CARTESIAN_POINT('Ctrl Pts',(0.396758994107716,-1.50792951689121,
9.19732686657952));
#283011=CARTESIAN_POINT('Ctrl Pts',(0.291024272551362,-1.53185343434322,
9.19034589876855));
#283012=CARTESIAN_POINT('Ctrl Pts',(0.149056984662356,-1.54873388250611,
9.18075828882264));
#283013=CARTESIAN_POINT('Ctrl Pts',(0.114326432214122,-1.5516841917049,
9.1783983720849));
#283014=CARTESIAN_POINT('Ctrl Pts',(0.0537856195760443,-1.55478350810153,
9.17423568986938));
#283015=CARTESIAN_POINT('Ctrl Pts',(0.0280159601910262,-1.55546122562967,
9.17244851232786));
#283016=CARTESIAN_POINT('Ctrl Pts',(-0.0100017909861832,-1.55551603628207,
9.16978317089332));
#283017=CARTESIAN_POINT('Ctrl Pts',(-0.022245622267092,-1.5553891127206,
9.16892040417147));
#283018=CARTESIAN_POINT('Ctrl Pts',(-0.0440711660815885,-1.55490510827681,
9.16737402000975));
#283019=CARTESIAN_POINT('Ctrl Pts',(-0.0536535873069272,-1.55460395228654,
9.16669218489843));
#283020=CARTESIAN_POINT('Ctrl Pts',(-0.0739546926465336,-1.55377801209777,
9.16524121130815));
#283021=CARTESIAN_POINT('Ctrl Pts',(-0.0846719084071793,-1.55323084719081,
9.16447140655637));
#283022=CARTESIAN_POINT('Ctrl Pts',(-0.113536410014844,-1.55145755565736,
9.1623873677794));
#283023=CARTESIAN_POINT('Ctrl Pts',(-0.13166875170482,-1.55002398401965,
9.16106672949627));
#283024=CARTESIAN_POINT('Ctrl Pts',(-0.241851712891964,-1.53936551224644,
9.15296846430122));
#283025=CARTESIAN_POINT('Ctrl Pts',(-0.332937201156362,-1.52226329235696,
9.14594519050845));
#283026=CARTESIAN_POINT('Ctrl Pts',(-0.488668556344432,-1.47837354284257,
9.13344609047336));
#283027=CARTESIAN_POINT('Ctrl Pts',(-0.5540562156469,-1.4551313005362,9.1280414700007));
#283028=CARTESIAN_POINT('Ctrl Pts',(-0.647096312465075,-1.41487603998816,
9.12025453399286));
#283029=CARTESIAN_POINT('Ctrl Pts',(-0.676118226376044,-1.40123954303452,
9.11781184211173));
#283030=CARTESIAN_POINT('Ctrl Pts',(-0.723018097801362,-1.37740600453737,
9.11386277472675));
#283031=CARTESIAN_POINT('Ctrl Pts',(-0.741151409537471,-1.36773431846762,
9.11233553912384));
#283032=CARTESIAN_POINT('Ctrl Pts',(-0.765964445595221,-1.35386142911248,
9.11025040920396));
#283033=CARTESIAN_POINT('Ctrl Pts',(-0.772810942209479,-1.34996502023214,
9.10967557920964));
#283034=CARTESIAN_POINT('Ctrl Pts',(-0.784388675087898,-1.34325906928833,
9.10870475384096));
#283035=CARTESIAN_POINT('Ctrl Pts',(-0.789135081865346,-1.34047616445362,
9.10830711579856));
#283036=CARTESIAN_POINT('Ctrl Pts',(-0.798989823039099,-1.33462766408329,
9.10748240392973));
#283037=CARTESIAN_POINT('Ctrl Pts',(-0.804095444365979,-1.33155783149172,
9.10705560587412));
#283038=CARTESIAN_POINT('Ctrl Pts',(-0.817761534728267,-1.32323361792594,
9.10591412908604));
#283039=CARTESIAN_POINT('Ctrl Pts',(-0.826289140072323,-1.31792541758583,
9.10520283061206));
#283040=CARTESIAN_POINT('Ctrl Pts',(-0.866290590997002,-1.29248471153181,
9.10186789965414));
#283041=CARTESIAN_POINT('Ctrl Pts',(-0.897086646369665,-1.27130334785427,
9.09930517877944));
#283042=CARTESIAN_POINT('Ctrl Pts',(-0.995957652585755,-1.19791641071497,
9.09098695436034));
#283043=CARTESIAN_POINT('Ctrl Pts',(-1.06048172434973,-1.14119053771222,
9.08540321815311));
#283044=CARTESIAN_POINT('Ctrl Pts',(-1.18066343200416,-1.016491569491,9.07397747411122));
#283045=CARTESIAN_POINT('Ctrl Pts',(-1.23590172778775,-0.948559482264268,
9.06815035866291));
#283046=CARTESIAN_POINT('Ctrl Pts',(-1.295210552105,-0.861585414671342,
9.06084599375461));
#283047=CARTESIAN_POINT('Ctrl Pts',(-1.3050260038456,-0.84664448528441,
9.05959680300931));
#283048=CARTESIAN_POINT('Ctrl Pts',(-1.32028253861523,-0.822525380934137,
9.05758706232532));
#283049=CARTESIAN_POINT('Ctrl Pts',(-1.32589065137397,-0.813454334571488,
9.0568327215374));
#283050=CARTESIAN_POINT('Ctrl Pts',(-1.33636922023038,-0.796109117826926,
9.05539274261717));
#283051=CARTESIAN_POINT('Ctrl Pts',(-1.34125722957913,-0.787846086973782,
9.05470778836685));
#283052=CARTESIAN_POINT('Ctrl Pts',(-1.35226414062597,-0.76883990018957,
9.05313433396118));
#283053=CARTESIAN_POINT('Ctrl Pts',(-1.35833200299605,-0.758068104703732,
9.05224404494274));
#283054=CARTESIAN_POINT('Ctrl Pts',(-1.37399971066364,-0.729462286875039,
9.04988302049727));
#283055=CARTESIAN_POINT('Ctrl Pts',(-1.38338046545114,-0.711511664727011,
9.04840469478335));
#283056=CARTESIAN_POINT('Ctrl Pts',(-1.43960842240988,-0.598598379633111,
9.03912191484671));
#283057=CARTESIAN_POINT('Ctrl Pts',(-1.47699898341463,-0.499258091135512,
9.03099711720682));
#283058=CARTESIAN_POINT('Ctrl Pts',(-1.52075801335195,-0.333442806431975,
9.01769997538751));
#283059=CARTESIAN_POINT('Ctrl Pts',(-1.53347397599849,-0.268974783384797,
9.01259861280046));
#283060=CARTESIAN_POINT('Ctrl Pts',(-1.54495143942652,-0.182168902652506,
9.00594244176158));
#283061=CARTESIAN_POINT('Ctrl Pts',(-1.54736462498052,-0.160384794890064,
9.00429001532586));
#283062=CARTESIAN_POINT('Ctrl Pts',(-1.55070557308965,-0.123026660219925,
9.0014943157176));
#283063=CARTESIAN_POINT('Ctrl Pts',(-1.55186086443734,-0.107476696433552,
9.00034188241117));
#283064=CARTESIAN_POINT('Ctrl Pts',(-1.55320008487744,-0.0848514107250055,
8.99868384497252));
#283065=CARTESIAN_POINT('Ctrl Pts',(-1.5535698237821,-0.0777886458206365,
8.99816892123592));
#283066=CARTESIAN_POINT('Ctrl Pts',(-1.5541364674814,-0.0653387001870624,
8.99726619183106));
#283067=CARTESIAN_POINT('Ctrl Pts',(-1.55435355759496,-0.0599527031948444,
8.9968773084294));
#283068=CARTESIAN_POINT('Ctrl Pts',(-1.5547663019573,-0.0481938131891931,
8.99603192179196));
#283069=CARTESIAN_POINT('Ctrl Pts',(-1.55495077944821,-0.0418207447728264,
8.99557603543462));
#283070=CARTESIAN_POINT('Ctrl Pts',(-1.55536175492209,-0.0237906130767371,
8.99429231133739));
#283071=CARTESIAN_POINT('Ctrl Pts',(-1.55549639283714,-0.0121315776499224,
8.99346932872659));
#283072=CARTESIAN_POINT('Ctrl Pts',(-1.55550453399548,0.014716419385246,
8.9915883067397));
#283073=CARTESIAN_POINT('Ctrl Pts',(-1.55528669166902,0.0299044307063782,
8.99053460238978));
#283074=CARTESIAN_POINT('Ctrl Pts',(-1.55380491416704,0.0810037025495659,
8.98701709161293));
#283075=CARTESIAN_POINT('Ctrl Pts',(-1.55151917532882,0.116875672101914,
8.98459360696074));
#283076=CARTESIAN_POINT('Ctrl Pts',(-1.54151446519784,0.218338976173929,
8.97778925269326));
#283077=CARTESIAN_POINT('Ctrl Pts',(-1.53085981341632,0.283562283574093,
8.9734731750866));
#283078=CARTESIAN_POINT('Ctrl Pts',(-1.49606737764417,0.43517648713866,
8.96321704143038));
#283079=CARTESIAN_POINT('Ctrl Pts',(-1.46854858228056,0.520536306685438,
8.95725838292891));
#283080=CARTESIAN_POINT('Ctrl Pts',(-1.42676383913642,0.619886133613938,
8.94978437978776));
#283081=CARTESIAN_POINT('Ctrl Pts',(-1.41938685814121,0.636596237355085,
8.94850855838314));
#283082=CARTESIAN_POINT('Ctrl Pts',(-1.40720460203217,0.662926064889994,
8.94646614617283));
#283083=CARTESIAN_POINT('Ctrl Pts',(-1.40259072567251,0.672632890436565,
8.94570613140406));
#283084=CARTESIAN_POINT('Ctrl Pts',(-1.39367282829553,0.690903867076421,
8.94426173690647));
#283085=CARTESIAN_POINT('Ctrl Pts',(-1.38938949806302,0.699477605771842,
8.94357810410327));
#283086=CARTESIAN_POINT('Ctrl Pts',(-1.37946685483058,0.718888506099295,
8.94201670420766));
#283087=CARTESIAN_POINT('Ctrl Pts',(-1.37377861601712,0.729699791776197,
8.9411372469085));
#283088=CARTESIAN_POINT('Ctrl Pts',(-1.35576693677747,0.762976270179126,
8.93839909071579));
#283089=CARTESIAN_POINT('Ctrl Pts',(-1.34301590557419,0.785203736968609,
8.93652536815863));
#283090=CARTESIAN_POINT('Ctrl Pts',(-1.28718305678799,0.877189529036339,
8.92857596715251));
#283091=CARTESIAN_POINT('Ctrl Pts',(-1.23917598206827,0.943790674013836,
8.92232767094507));
#283092=CARTESIAN_POINT('Ctrl Pts',(-1.12256427387416,1.08124530357311,
8.9083957359416));
#283093=CARTESIAN_POINT('Ctrl Pts',(-1.05201175014948,1.15000656187652,
8.90070100471601));
#283094=CARTESIAN_POINT('Ctrl Pts',(-0.959015197773904,1.22487331626991,
8.89172853260304));
#283095=CARTESIAN_POINT('Ctrl Pts',(-0.94232358531721,1.23776054422312,
8.89015968218849));
#283096=CARTESIAN_POINT('Ctrl Pts',(-0.918792134835602,1.25517660729986,
8.88801041460191));
#283097=CARTESIAN_POINT('Ctrl Pts',(-0.912171638745465,1.25999611584328,
8.88741240935707));
#283098=CARTESIAN_POINT('Ctrl Pts',(-0.901037459372307,1.26796768389156,
8.8864182273099));
#283099=CARTESIAN_POINT('Ctrl Pts',(-0.896544614606635,1.27114842103992,
8.88602015547349));
#283100=CARTESIAN_POINT('Ctrl Pts',(-0.887256057518737,1.27765056474512,
8.8852036837903));
#283101=CARTESIAN_POINT('Ctrl Pts',(-0.882458397051673,1.28096895266434,
8.88478548329487));
#283102=CARTESIAN_POINT('Ctrl Pts',(-0.869816893373977,1.28960794519267,
8.88369242378091));
#283103=CARTESIAN_POINT('Ctrl Pts',(-0.861942739238357,1.29488408997649,
8.88302046359562));
#283104=CARTESIAN_POINT('Ctrl Pts',(-0.824966977442682,1.3191732607118,
8.87990376746175));
#283105=CARTESIAN_POINT('Ctrl Pts',(-0.795279038712062,1.33728093606542,
8.87751220863644));
#283106=CARTESIAN_POINT('Ctrl Pts',(-0.700346326529784,1.3909026278456,
8.87012317284857));
#283107=CARTESIAN_POINT('Ctrl Pts',(-0.633148845896649,1.42275059406023,
8.86525822716369));
#283108=CARTESIAN_POINT('Ctrl Pts',(-0.476154234957481,1.48382196533134,
8.85417060336886));
#283109=CARTESIAN_POINT('Ctrl Pts',(-0.385470915928925,1.50992040752033,
8.847948801096));
#283110=CARTESIAN_POINT('Ctrl Pts',(-0.272882538937654,1.53151381811522,
8.84004741826831));
#283111=CARTESIAN_POINT('Ctrl Pts',(-0.252701186237536,1.53497280068752,
8.83862510272286));
#283112=CARTESIAN_POINT('Ctrl Pts',(-0.220302834195804,1.5398694879157,
8.83632891608207));
#283113=CARTESIAN_POINT('Ctrl Pts',(-0.20812641744825,1.54156244034849,
8.83546305146916));
#283114=CARTESIAN_POINT('Ctrl Pts',(-0.186390635655043,1.54432227107116,
8.83391165581686));
#283115=CARTESIAN_POINT('Ctrl Pts',(-0.176838923979664,1.54544515702029,
8.83322792501212));
#283116=CARTESIAN_POINT('Ctrl Pts',(-0.156746666562503,1.54761847067169,
8.83178522824136));
#283117=CARTESIAN_POINT('Ctrl Pts',(-0.14620461420192,1.54864994389906,
8.83102570248735));
#283118=CARTESIAN_POINT('Ctrl Pts',(-0.118182496283963,1.55110306176721,
8.82899954667409));
#283119=CARTESIAN_POINT('Ctrl Pts',(-0.100687985346372,1.55233684921951,
8.82772711476697));
#283120=CARTESIAN_POINT('Ctrl Pts',(-0.00466047315678961,1.55747906990809,
8.82069894643226));
#283121=CARTESIAN_POINT('Ctrl Pts',(0.0740487578902953,1.55572359070942,
8.81476931788498));
#283122=CARTESIAN_POINT('Ctrl Pts',(0.204583550436572,1.54288310636638,
8.80468822127711));
#283123=CARTESIAN_POINT('Ctrl Pts',(0.256594318855368,1.53509013777173,
8.80060719742788));
#283124=CARTESIAN_POINT('Ctrl Pts',(0.378404094436337,1.51047469129441,
8.7909729954601));
#283125=CARTESIAN_POINT('Ctrl Pts',(0.447640226323751,1.491423414164,8.78543470018244));
#283126=CARTESIAN_POINT('Ctrl Pts',(0.52949269659049,1.46268361212338,8.77897439549032));
#283127=CARTESIAN_POINT('Ctrl Pts',(0.543592849415666,1.45750222070904,
8.77786493619048));
#283128=CARTESIAN_POINT('Ctrl Pts',(0.564052721661734,1.44964558148286,
8.77626225205672));
#283129=CARTESIAN_POINT('Ctrl Pts',(0.570472696030038,1.44713119400306,
8.77576039979605));
#283130=CARTESIAN_POINT('Ctrl Pts',(0.581877167836612,1.44257693487669,
8.77487103583091));
#283131=CARTESIAN_POINT('Ctrl Pts',(0.586868050399299,1.4405537637008,8.77448257489776));
#283132=CARTESIAN_POINT('Ctrl Pts',(0.59778555683228,1.43606193891327,8.77363449099096));
#283133=CARTESIAN_POINT('Ctrl Pts',(0.60370749847943,1.43358247916766,8.77317551833257));
#283134=CARTESIAN_POINT('Ctrl Pts',(0.62084999349932,1.42628001840185,8.77184948339305));
#283135=CARTESIAN_POINT('Ctrl Pts',(0.632029628093104,1.42136131189933,
8.77098791338006));
#283136=CARTESIAN_POINT('Ctrl Pts',(0.717871076729631,1.38238048649732,
8.76438855391378));
#283137=CARTESIAN_POINT('Ctrl Pts',(0.789800662666339,1.34258464573992,
8.75894963942185));
#283138=CARTESIAN_POINT('Ctrl Pts',(0.956647802313687,1.23220198194696,
8.74576498344532));
#283139=CARTESIAN_POINT('Ctrl Pts',(1.04729850226476,1.15613966665648,8.73806815100407));
#283140=CARTESIAN_POINT('Ctrl Pts',(1.14194019261586,1.05637842939796,8.72857803792099));
#283141=CARTESIAN_POINT('Ctrl Pts',(1.15513198711733,1.04193705347085,8.72721797062166));
#283142=CARTESIAN_POINT('Ctrl Pts',(1.17607983527599,1.01811807066989,8.72499371985817));
#283143=CARTESIAN_POINT('Ctrl Pts',(1.18400456144084,1.0088911577942,8.72413655752578));
#283144=CARTESIAN_POINT('Ctrl Pts',(1.19797534937191,0.992233370933975,
8.72259635260833));
#283145=CARTESIAN_POINT('Ctrl Pts',(1.20406257469083,0.984837706840746,
8.721915037366));
#283146=CARTESIAN_POINT('Ctrl Pts',(1.21685417764382,0.96900070029912,8.72046104330277));
#283147=CARTESIAN_POINT('Ctrl Pts',(1.22353985623163,0.960544978744238,
8.7196876620603));
#283148=CARTESIAN_POINT('Ctrl Pts',(1.24140791579854,0.937457075658295,
8.71758342245968));
#283149=CARTESIAN_POINT('Ctrl Pts',(1.25241888648092,0.922695107135296,
8.716245943866));
#283150=CARTESIAN_POINT('Ctrl Pts',(1.27626706213399,0.88950926273484,8.71325529647892));
#283151=CARTESIAN_POINT('Ctrl Pts',(1.28897242150136,0.870996179180301,
8.71159755147405));
#283152=CARTESIAN_POINT('Ctrl Pts',(1.32803481203978,0.811350700535255,
8.70628863026741));
#283153=CARTESIAN_POINT('Ctrl Pts',(1.35285524483083,0.769251775135271,
8.70258746150893));
#283154=CARTESIAN_POINT('Ctrl Pts',(1.40330163517241,0.673671757338233,
8.69430071706258));
#283155=CARTESIAN_POINT('Ctrl Pts',(1.42793496886137,0.619750189310015,
8.68970032265194));
#283156=CARTESIAN_POINT('Ctrl Pts',(1.47721062546711,0.49324106339723,8.67917612223003));
#283157=CARTESIAN_POINT('Ctrl Pts',(1.49969074285008,0.41996241578308,8.673270266773));
#283158=CARTESIAN_POINT('Ctrl Pts',(1.51918370425405,0.334346747659238,
8.66677445184284));
#283159=CARTESIAN_POINT('Ctrl Pts',(1.5215627676986,0.323347550540598,8.66594751241917));
#283160=CARTESIAN_POINT('Ctrl Pts',(1.52508440065415,0.306165525858772,
8.66466852824798));
#283161=CARTESIAN_POINT('Ctrl Pts',(1.52630915182963,0.300000225202333,
8.66421215452712));
#283162=CARTESIAN_POINT('Ctrl Pts',(1.5284147969853,0.289053784238507,8.66340659259172));
#283163=CARTESIAN_POINT('Ctrl Pts',(1.52931066636584,0.284275867254841,
8.6630565901419));
#283164=CARTESIAN_POINT('Ctrl Pts',(1.53142196672912,0.272716825319416,
8.66221365044807));
#283165=CARTESIAN_POINT('Ctrl Pts',(1.53261476978038,0.265931719159262,
8.66172198822169));
#283166=CARTESIAN_POINT('Ctrl Pts',(1.53619374830058,0.24474884634744,8.66019617291562));
#283167=CARTESIAN_POINT('Ctrl Pts',(1.53842249519941,0.230324763739226,
8.65917033082048));
#283168=CARTESIAN_POINT('Ctrl Pts',(1.54910786158019,0.15407427801638,8.65380621236334));
#283169=CARTESIAN_POINT('Ctrl Pts',(1.55404239431084,0.0918049495432833,
8.64962791033114));
#283170=CARTESIAN_POINT('Ctrl Pts',(1.55731521264481,-0.0813178561447185,
8.63816285679161));
#283171=CARTESIAN_POINT('Ctrl Pts',(1.54757952973813,-0.19193708977623,
8.63098668011777));
#283172=CARTESIAN_POINT('Ctrl Pts',(1.51904261045954,-0.336830157699059,
8.62096800089076));
#283173=CARTESIAN_POINT('Ctrl Pts',(1.51061538381273,-0.372808006338527,
8.61843042713718));
#283174=CARTESIAN_POINT('Ctrl Pts',(1.49713461636587,-0.422345335360386,
8.61484741450703));
#283175=CARTESIAN_POINT('Ctrl Pts',(1.4931604395783,-0.436187481484764,
8.61383643916304));
#283176=CARTESIAN_POINT('Ctrl Pts',(1.48640717639769,-0.458534588154003,
8.61218738954287));
#283177=CARTESIAN_POINT('Ctrl Pts',(1.48374583073281,-0.467074476172627,
8.61155317141504));
#283178=CARTESIAN_POINT('Ctrl Pts',(1.47801237918626,-0.484928701690103,
8.61021847385942));
#283179=CARTESIAN_POINT('Ctrl Pts',(1.47492554808371,-0.494237855922309,
8.60951753535851));
#283180=CARTESIAN_POINT('Ctrl Pts',(1.46731364088471,-0.516487018545973,
8.60782984324266));
#283181=CARTESIAN_POINT('Ctrl Pts',(1.46270520652701,-0.529397409762017,
8.60684037288728));
#283182=CARTESIAN_POINT('Ctrl Pts',(1.44582090851226,-0.574794010099215,
8.60332401463399));
#283183=CARTESIAN_POINT('Ctrl Pts',(1.43262928185464,-0.606926058466518,
8.60076709493563));
#283184=CARTESIAN_POINT('Ctrl Pts',(1.39665754883184,-0.686823306391604,
8.59423082306606));
#283185=CARTESIAN_POINT('Ctrl Pts',(1.37249630289784,-0.733915161615298,
8.59021072725486));
#283186=CARTESIAN_POINT('Ctrl Pts',(1.32463762484317,-0.816534981265038,
8.58286962174845));
#283187=CARTESIAN_POINT('Ctrl Pts',(1.30178541067507,-0.852495602410623,
8.57956835278858));
#283188=CARTESIAN_POINT('Ctrl Pts',(1.23146495878533,-0.953719605307711,
8.57000878788607));
#283189=CARTESIAN_POINT('Ctrl Pts',(1.18035465007434,-1.01629351016106,
8.56375411521788));
#283190=CARTESIAN_POINT('Ctrl Pts',(1.11418764694089,-1.08553857422275,
8.55662092402964));
#283191=CARTESIAN_POINT('Ctrl Pts',(1.10360036379093,-1.09630031961206,
8.555505855995));
#283192=CARTESIAN_POINT('Ctrl Pts',(1.08794173763039,-1.11176020212923,
8.55389665161676));
#283193=CARTESIAN_POINT('Ctrl Pts',(1.08299348962191,-1.1165809768333,8.55339379233873));
#283194=CARTESIAN_POINT('Ctrl Pts',(1.07413009094452,-1.12510168911008,
8.55250333858883));
#283195=CARTESIAN_POINT('Ctrl Pts',(1.07022763570326,-1.12881445513501,
8.55211478547125));
#283196=CARTESIAN_POINT('Ctrl Pts',(1.06163922380611,-1.13690082695788,
8.55126733643126));
#283197=CARTESIAN_POINT('Ctrl Pts',(1.05694544947106,-1.14126581155748,
8.55080908306239));
#283198=CARTESIAN_POINT('Ctrl Pts',(1.04326693419189,-1.15382940244655,
8.54948728025355));
#283199=CARTESIAN_POINT('Ctrl Pts',(1.03421259268092,-1.16195203137534,
8.54862916949874));
#283200=CARTESIAN_POINT('Ctrl Pts',(0.964554830216818,-1.22298244911397,
8.54214573279246));
#283201=CARTESIAN_POINT('Ctrl Pts',(0.90001533547242,-1.27123099095198,
8.53680769466613));
#283202=CARTESIAN_POINT('Ctrl Pts',(0.730608942529068,-1.37847659179953,
8.52358920964173));
#283203=CARTESIAN_POINT('Ctrl Pts',(0.622116615679721,-1.43071813914803,
8.51576600351762));
#283204=CARTESIAN_POINT('Ctrl Pts',(0.4904019445847,-1.47629983373049,8.50614430196203));
#283205=CARTESIAN_POINT('Ctrl Pts',(0.47198552105932,-1.48229041598798,
8.5047973810919));
#283206=CARTESIAN_POINT('Ctrl Pts',(0.441881987335005,-1.49146475968523,
8.50259032314108));
#283207=CARTESIAN_POINT('Ctrl Pts',(0.430260727185607,-1.49485869297977,
8.50173702534028));
#283208=CARTESIAN_POINT('Ctrl Pts',(0.409381385741014,-1.50069276507158,
8.50020105589772));
#283209=CARTESIAN_POINT('Ctrl Pts',(0.400138057161781,-1.50318376183369,
8.49952007370882));
#283210=CARTESIAN_POINT('Ctrl Pts',(0.380405361539547,-1.50830665201224,
8.49806387251919));
#283211=CARTESIAN_POINT('Ctrl Pts',(0.369910411189195,-1.51091477996902,
8.49728792541088));
#283212=CARTESIAN_POINT('Ctrl Pts',(0.341313139977844,-1.51770575746221,
8.49516916887761));
#283213=CARTESIAN_POINT('Ctrl Pts',(0.323162227913809,-1.52167392847343,
8.49381958215409));
#283214=CARTESIAN_POINT('Ctrl Pts',(0.282678070552662,-1.5297676314339,
8.49079752538049));
#283215=CARTESIAN_POINT('Ctrl Pts',(0.260317138806538,-1.53373100216327,
8.48912032865965));
#283216=CARTESIAN_POINT('Ctrl Pts',(0.188744108469357,-1.54480675543285,
8.48372533547588));
#283217=CARTESIAN_POINT('Ctrl Pts',(0.139278054395994,-1.55004936104529,
8.47995570720505));
#283218=CARTESIAN_POINT('Ctrl Pts',(0.0517823189612252,-1.55510050637035,
8.47323157860403));
#283219=CARTESIAN_POINT('Ctrl Pts',(0.0138485648366963,-1.5559007118011,
8.47029814223206));
#283220=CARTESIAN_POINT('Ctrl Pts',(-0.115224157113838,-1.55390275238441,
8.46029082029016));
#283221=CARTESIAN_POINT('Ctrl Pts',(-0.206080788660965,-1.54448182623148,
8.45319223883484));
#283222=CARTESIAN_POINT('Ctrl Pts',(-0.309797628089965,-1.52440641784076,
8.44533004770716));
#283223=CARTESIAN_POINT('Ctrl Pts',(-0.323961062875571,-1.52145941998455,
8.44426199951609));
#283224=CARTESIAN_POINT('Ctrl Pts',(-0.344878705185536,-1.5168017057636,
8.4426949260062));
#283225=CARTESIAN_POINT('Ctrl Pts',(-0.351665366294208,-1.51524262448,8.44218811089947));
#283226=CARTESIAN_POINT('Ctrl Pts',(-0.363678589498723,-1.51239779776459,
8.44129412821897));
#283227=CARTESIAN_POINT('Ctrl Pts',(-0.368909217540298,-1.51113044025227,
8.44090596002896));
#283228=CARTESIAN_POINT('Ctrl Pts',(-0.380399718183411,-1.50828312390999,
8.44005563658089));
#283229=CARTESIAN_POINT('Ctrl Pts',(-0.386656429714188,-1.50669132101865,
8.43959415853569));
#283230=CARTESIAN_POINT('Ctrl Pts',(-0.404889362571955,-1.50193152743612,
8.4382533341363));
#283231=CARTESIAN_POINT('Ctrl Pts',(-0.416838216721867,-1.49865927933808,
8.43737966925648));
#283232=CARTESIAN_POINT('Ctrl Pts',(-0.444301497302848,-1.49078444382009,
8.43538053052546));
#283233=CARTESIAN_POINT('Ctrl Pts',(-0.459785971089976,-1.48608175637665,
8.43425996696124));
#283234=CARTESIAN_POINT('Ctrl Pts',(-0.512934060640443,-1.46903020469825,
8.43042754499172));
#283235=CARTESIAN_POINT('Ctrl Pts',(-0.550199477749753,-1.45548345378508,
8.42776422616033));
#283236=CARTESIAN_POINT('Ctrl Pts',(-0.703801093245219,-1.39290204990904,
8.41673063309731));
#283237=CARTESIAN_POINT('Ctrl Pts',(-0.814456139149638,-1.33122990865694,
8.4086032707209));
#283238=CARTESIAN_POINT('Ctrl Pts',(-0.943100813555837,-1.23742857432828,
8.39776130236525));
#283239=CARTESIAN_POINT('Ctrl Pts',(-0.969130710557461,-1.21714995954985,
8.39548863362209));
#283240=CARTESIAN_POINT('Ctrl Pts',(-1.00510288130866,-1.18723998350902,
8.39221980125609));
#283241=CARTESIAN_POINT('Ctrl Pts',(-1.01559284587807,-1.17827913935506,
8.39125038982909));
#283242=CARTESIAN_POINT('Ctrl Pts',(-1.03327234372118,-1.16276528449421,
8.38958777881137));
#283243=CARTESIAN_POINT('Ctrl Pts',(-1.04052226450031,-1.15628208166506,
8.38889749436198));
#283244=CARTESIAN_POINT('Ctrl Pts',(-1.05475818371208,-1.14330937765328,
8.3875247958195));
#283245=CARTESIAN_POINT('Ctrl Pts',(-1.06174625884392,-1.13682278015591,
8.38684252314824));
#283246=CARTESIAN_POINT('Ctrl Pts',(-1.07893304627083,-1.12057265003051,
8.38514307297146));
#283247=CARTESIAN_POINT('Ctrl Pts',(-1.08905911230751,-1.11073390502356,
8.38412267622768));
#283248=CARTESIAN_POINT('Ctrl Pts',(-1.11070158572051,-1.08912504151811,
8.38189916245897));
#283249=CARTESIAN_POINT('Ctrl Pts',(-1.12216773352817,-1.07730724868828,
8.38069402016327));
#283250=CARTESIAN_POINT('Ctrl Pts',(-1.15438549652802,-1.04302894579015,
8.37722821191461));
#283251=CARTESIAN_POINT('Ctrl Pts',(-1.17466433624008,-1.02013662046442,
8.37494889018055));
#283252=CARTESIAN_POINT('Ctrl Pts',(-1.24688415098179,-0.933599020729825,
8.36645935863183));
#283253=CARTESIAN_POINT('Ctrl Pts',(-1.29443092338352,-0.866471641405444,
8.36010711756891));
#283254=CARTESIAN_POINT('Ctrl Pts',(-1.37745440430075,-0.727063345021788,
8.34752235414539));
#283255=CARTESIAN_POINT('Ctrl Pts',(-1.41307971193189,-0.655141225759011,
8.34131062410142));
#283256=CARTESIAN_POINT('Ctrl Pts',(-1.44860842836483,-0.566867727648813,
8.33422467849016));
#283257=CARTESIAN_POINT('Ctrl Pts',(-1.45400951060219,-0.552866879750471,
8.33311638626311));
#283258=CARTESIAN_POINT('Ctrl Pts',(-1.46162005078161,-0.532255196108869,
8.33150967241274));
#283259=CARTESIAN_POINT('Ctrl Pts',(-1.46398884688373,-0.525704696412887,
8.33100269313486));
#283260=CARTESIAN_POINT('Ctrl Pts',(-1.46810985449827,-0.514064851791627,
8.33010853495586));
#283261=CARTESIAN_POINT('Ctrl Pts',(-1.46987974930401,-0.508982064923382,
8.32972035387279));
#283262=CARTESIAN_POINT('Ctrl Pts',(-1.4737140643189,-0.497783850785474,
8.32887013746383));
#283263=CARTESIAN_POINT('Ctrl Pts',(-1.47576683918818,-0.491664668071929,
8.32840877808154));
#283264=CARTESIAN_POINT('Ctrl Pts',(-1.48164565987713,-0.47377171904175,
8.32706865587837));
#283265=CARTESIAN_POINT('Ctrl Pts',(-1.48536942503124,-0.461964500547456,
8.32619556547948));
#283266=CARTESIAN_POINT('Ctrl Pts',(-1.49363020984236,-0.434638261245243,
8.32419796099838));
#283267=CARTESIAN_POINT('Ctrl Pts',(-1.49806710552977,-0.419090224791675,
8.32307834657289));
#283268=CARTESIAN_POINT('Ctrl Pts',(-1.53749936982175,-0.27227188369062,
8.31264006489354));
#283269=CARTESIAN_POINT('Ctrl Pts',(-1.55539994923164,-0.13701189508263,
8.30398048290367));
#283270=CARTESIAN_POINT('Ctrl Pts',(-1.55549958179694,-0.00114062682748519,
8.2949012130171));
#283271=CARTESIAN_POINT('',(-1.55363820104426,0.00100737127591942,7.59405622560371));
#283272=CARTESIAN_POINT('Ctrl Pts',(-1.55363820104426,0.00100737127591942,
7.59405622560371));
#283273=CARTESIAN_POINT('Ctrl Pts',(-1.55169765832855,-0.326159426902871,
7.6174247256493));
#283274=CARTESIAN_POINT('Ctrl Pts',(-1.29071878250434,-1.17503987929593,
7.67785536563862));
#283275=CARTESIAN_POINT('Ctrl Pts',(0.103792628149562,-1.8358593744105,
7.77534814557165));
#283276=CARTESIAN_POINT('Ctrl Pts',(1.59909575810308,-0.907769413831382,
7.8865345654028));
#283277=CARTESIAN_POINT('Ctrl Pts',(1.62955779866738,0.851876712390422,
7.99772098523398));
#283278=CARTESIAN_POINT('Ctrl Pts',(0.167274199086701,1.83116681231986,
8.10890740506512));
#283279=CARTESIAN_POINT('Ctrl Pts',(-1.26795424285233,1.21093838634352,
8.20768581852172));
#283280=CARTESIAN_POINT('Ctrl Pts',(-1.55156054962447,0.343750973057136,
8.26940209203457));
#283281=CARTESIAN_POINT('Ctrl Pts',(-1.55403083159801,-0.00119596074553188,
8.29405622560371));
#283282=CARTESIAN_POINT('',(-1.5556705629256,-0.00141387709470033,6.19405610964826));
#283283=CARTESIAN_POINT('Ctrl Pts',(-1.55549961880975,0.00108898242830498,
7.59512619280739));
#283284=CARTESIAN_POINT('Ctrl Pts',(-1.55542780661911,0.103665325493169,
7.58741794628577));
#283285=CARTESIAN_POINT('Ctrl Pts',(-1.54520952791527,0.205976189459901,
7.57943937593693));
#283286=CARTESIAN_POINT('Ctrl Pts',(-1.51246140664302,0.368902331225778,
7.56657226291381));
#283287=CARTESIAN_POINT('Ctrl Pts',(-1.49610670180076,0.430458901443685,
7.56167842604611));
#283288=CARTESIAN_POINT('Ctrl Pts',(-1.4713794288958,0.504816380973698,
7.55584579531384));
#283289=CARTESIAN_POINT('Ctrl Pts',(-1.46653533119137,0.518720701921687,
7.55475876047368));
#283290=CARTESIAN_POINT('Ctrl Pts',(-1.45912752412429,0.539050004795983,
7.55317684650052));
#283291=CARTESIAN_POINT('Ctrl Pts',(-1.45671740017356,0.545529522805097,
7.55267376633303));
#283292=CARTESIAN_POINT('Ctrl Pts',(-1.45253811037044,0.556540155140894,
7.55182105128745));
#283293=CARTESIAN_POINT('Ctrl Pts',(-1.45079079298394,0.56107930264104,
7.55147016048475));
#283294=CARTESIAN_POINT('Ctrl Pts',(-1.44674270743863,0.571449984853153,
7.55066998027172));
#283295=CARTESIAN_POINT('Ctrl Pts',(-1.4444279482256,0.577275889665933,
7.55022153070611));
#283296=CARTESIAN_POINT('Ctrl Pts',(-1.43788814092584,0.59344997604703,
7.54897906854654));
#283297=CARTESIAN_POINT('Ctrl Pts',(-1.43358657884975,0.603767107235903,
7.54818943420849));
#283298=CARTESIAN_POINT('Ctrl Pts',(-1.40221127442195,0.676793233376525,
7.54261480746157));
#283299=CARTESIAN_POINT('Ctrl Pts',(-1.37114043650215,0.737714035072817,
7.53803931151013));
#283300=CARTESIAN_POINT('Ctrl Pts',(-1.33014042321069,0.806501676581322,
7.53273819161595));
#283301=CARTESIAN_POINT('Ctrl Pts',(-1.32400607848866,0.816533164272666,
7.53196163448233));
#283302=CARTESIAN_POINT('Ctrl Pts',(-1.2840071852618,0.880307214110137,
7.52699656521615));
#283303=CARTESIAN_POINT('Ctrl Pts',(-1.24699188567161,0.932001233452995,
7.52283984041793));
#283304=CARTESIAN_POINT('Ctrl Pts',(-1.17901055486721,1.01561393170506,
7.51567442521782));
#283305=CARTESIAN_POINT('Ctrl Pts',(-1.14965101778988,1.0487323892171,7.51270426331387));
#283306=CARTESIAN_POINT('Ctrl Pts',(-1.10429504329741,1.09569888510223,
7.50824485195407));
#283307=CARTESIAN_POINT('Ctrl Pts',(-1.08936298922978,1.11054572128396,
7.50679579191809));
#283308=CARTESIAN_POINT('Ctrl Pts',(-1.06170337504077,1.13695276572884,
7.50414091654037));
#283309=CARTESIAN_POINT('Ctrl Pts',(-1.04907660598111,1.14861389596835,
7.50293950593924));
#283310=CARTESIAN_POINT('Ctrl Pts',(-1.02858858986014,1.16691540520328,
7.50100494337827));
#283311=CARTESIAN_POINT('Ctrl Pts',(-1.02084993508036,1.17369137807727,
7.50027750620568));
#283312=CARTESIAN_POINT('Ctrl Pts',(-1.00577755353014,1.18662693197917,
7.49886658949772));
#283313=CARTESIAN_POINT('Ctrl Pts',(-0.998453004049991,1.1927965266716,
7.49818356661102));
#283314=CARTESIAN_POINT('Ctrl Pts',(-0.98171257868298,1.20663504250872,
7.49662810083029));
#283315=CARTESIAN_POINT('Ctrl Pts',(-0.9722630299579,1.21426203843341,7.49575401658594));
#283316=CARTESIAN_POINT('Ctrl Pts',(-0.947415397686373,1.23384125658758,
7.49346519417263));
#283317=CARTESIAN_POINT('Ctrl Pts',(-0.931880672670947,1.2456157233225,
7.49204359639878));
#283318=CARTESIAN_POINT('Ctrl Pts',(-0.820552203385979,1.32674826492543,
7.48191703889393));
#283319=CARTESIAN_POINT('Ctrl Pts',(-0.717360641847691,1.38526170717769,
7.47280087582587));
#283320=CARTESIAN_POINT('Ctrl Pts',(-0.533179306843392,1.46356068592827,
7.45727937821555));
#283321=CARTESIAN_POINT('Ctrl Pts',(-0.455372753775986,1.48960689909923,
7.45093753735175));
#283322=CARTESIAN_POINT('Ctrl Pts',(-0.364022500675698,1.51235475667921,
7.44396181248399));
#283323=CARTESIAN_POINT('Ctrl Pts',(-0.352141223466405,1.51516529609271,
7.44306357367889));
#283324=CARTESIAN_POINT('Ctrl Pts',(-0.333964152894782,1.51923974294616,
7.44170436112457));
#283325=CARTESIAN_POINT('Ctrl Pts',(-0.327691919193283,1.52060496580366,
7.44123805692041));
#283326=CARTESIAN_POINT('Ctrl Pts',(-0.3161419906398,1.52304415409516,7.44038458448527));
#283327=CARTESIAN_POINT('Ctrl Pts',(-0.310867089505607,1.52412955745471,
7.43999681140119));
#283328=CARTESIAN_POINT('Ctrl Pts',(-0.298824969107618,1.5265423151354,
7.43911605114716));
#283329=CARTESIAN_POINT('Ctrl Pts',(-0.292054444104584,1.5278520898811,
7.43862405401858));
#283330=CARTESIAN_POINT('Ctrl Pts',(-0.271023807224473,1.53177560987122,
7.43710508095525));
#283331=CARTESIAN_POINT('Ctrl Pts',(-0.256735206446268,1.5342351502917,
7.43608625225311));
#283332=CARTESIAN_POINT('Ctrl Pts',(-0.150356548579933,1.55101857196858,
7.42858457496211));
#283333=CARTESIAN_POINT('Ctrl Pts',(-0.0571667347852686,1.55724199358747,
7.42246920867134));
#283334=CARTESIAN_POINT('Ctrl Pts',(0.132284669755296,1.55285248151857,
7.4099989402936));
#283335=CARTESIAN_POINT('Ctrl Pts',(0.228112995513905,1.54169120066067,
7.4036639615049));
#283336=CARTESIAN_POINT('Ctrl Pts',(0.347604070680503,1.51638426194872,
7.39527767871498));
#283337=CARTESIAN_POINT('Ctrl Pts',(0.372779537857112,1.51039236725372,
7.3934837170917));
#283338=CARTESIAN_POINT('Ctrl Pts',(0.409647561381616,1.50063969642914,
7.39081019446447));
#283339=CARTESIAN_POINT('Ctrl Pts',(0.421464655097816,1.49736373410331,
7.38994617103066));
#283340=CARTESIAN_POINT('Ctrl Pts',(0.442451176120609,1.49127769320319,
7.38839839572937));
#283341=CARTESIAN_POINT('Ctrl Pts',(0.451635778851122,1.48852185648178,
7.38771643853079));
#283342=CARTESIAN_POINT('Ctrl Pts',(0.471033542818532,1.48250550858444,
7.38626611485995));
#283343=CARTESIAN_POINT('Ctrl Pts',(0.481239606246189,1.47922398985099,
7.38549709005231));
#283344=CARTESIAN_POINT('Ctrl Pts',(0.508620539673677,1.47010693907525,
7.3834174510128));
#283345=CARTESIAN_POINT('Ctrl Pts',(0.525728118581261,1.46407621360948,
7.38210047916107));
#283346=CARTESIAN_POINT('Ctrl Pts',(0.631405474406174,1.42473209069745,
7.37385165039303));
#283347=CARTESIAN_POINT('Ctrl Pts',(0.716871104826995,1.38369943643787,
7.366661701593));
#283348=CARTESIAN_POINT('Ctrl Pts',(0.8632503348941,1.29620451306948,7.35348057692364));
#283349=CARTESIAN_POINT('Ctrl Pts',(0.925494281651514,1.2525206614627,7.34755482009907));
#283350=CARTESIAN_POINT('Ctrl Pts',(1.01512422278765,1.17927426297062,7.33870564676653));
#283351=CARTESIAN_POINT('Ctrl Pts',(1.04497389381006,1.15290726741355,7.33569966005672));
#283352=CARTESIAN_POINT('Ctrl Pts',(1.08092595453072,1.11860486232567,7.3320356796895));
#283353=CARTESIAN_POINT('Ctrl Pts',(1.08800549624715,1.11172020348813,7.33131198262281));
#283354=CARTESIAN_POINT('Ctrl Pts',(1.09922393860948,1.10060075921631,7.33016232940926));
#283355=CARTESIAN_POINT('Ctrl Pts',(1.10340490984098,1.09640909632196,7.32973321926855));
#283356=CARTESIAN_POINT('Ctrl Pts',(1.11139347168942,1.08830812658672,7.32891224795363));
#283357=CARTESIAN_POINT('Ctrl Pts',(1.11520454813528,1.08440252870062,7.32852013223706));
#283358=CARTESIAN_POINT('Ctrl Pts',(1.12363257166192,1.07567405280914,7.32765175921664));
#283359=CARTESIAN_POINT('Ctrl Pts',(1.12823923854861,1.07084128090667,7.32717628043901));
#283360=CARTESIAN_POINT('Ctrl Pts',(1.14179439001396,1.05643623416878,7.32577413313436));
#283361=CARTESIAN_POINT('Ctrl Pts',(1.15065346680217,1.04678009835152,7.32485375923614));
#283362=CARTESIAN_POINT('Ctrl Pts',(1.22249597162214,0.966459515250616,
7.31734510667948));
#283363=CARTESIAN_POINT('Ctrl Pts',(1.27903969228235,0.890282555878519,
7.31113884868504));
#283364=CARTESIAN_POINT('Ctrl Pts',(1.38411449234752,0.717849407659683,
7.2978511130844));
#283365=CARTESIAN_POINT('Ctrl Pts',(1.43029137041731,0.620760130953684,
7.29078630242934));
#283366=CARTESIAN_POINT('Ctrl Pts',(1.47230343403155,0.50224097300336,7.28206979952459));
#283367=CARTESIAN_POINT('Ctrl Pts',(1.47817985169342,0.484672747331978,
7.28077627370905));
#283368=CARTESIAN_POINT('Ctrl Pts',(1.48698415086335,0.456700208026272,
7.27871214211918));
#283369=CARTESIAN_POINT('Ctrl Pts',(1.49011987125119,0.446362748921551,
7.27794836117902));
#283370=CARTESIAN_POINT('Ctrl Pts',(1.49583135898371,0.426802617191487,
7.2765009167782));
#283371=CARTESIAN_POINT('Ctrl Pts',(1.49843014412627,0.417587145625668,
7.27581804135102));
#283372=CARTESIAN_POINT('Ctrl Pts',(1.50412673333248,0.396648510546313,
7.27426405430882));
#283373=CARTESIAN_POINT('Ctrl Pts',(1.50717283608429,0.384912064675614,
7.27339131355366));
#283374=CARTESIAN_POINT('Ctrl Pts',(1.51474212945034,0.354279587782037,
7.271108440597));
#283375=CARTESIAN_POINT('Ctrl Pts',(1.51904890519262,0.335332827720239,
7.26969150745333));
#283376=CARTESIAN_POINT('Ctrl Pts',(1.54727603364526,0.199422653324257,
7.25948831497441));
#283377=CARTESIAN_POINT('Ctrl Pts',(1.5580108230103,0.0801494003488005,
7.25028201781071));
#283378=CARTESIAN_POINT('Ctrl Pts',(1.55296950585114,-0.120087058336532,
7.23474828840498));
#283379=CARTESIAN_POINT('Ctrl Pts',(1.54461557454576,-0.200750759176452,
7.22848303382517));
#283380=CARTESIAN_POINT('Ctrl Pts',(1.52782197636782,-0.292384309470848,
7.22158033598628));
#283381=CARTESIAN_POINT('Ctrl Pts',(1.52548581686377,-0.304338007774974,
7.22068429466812));
#283382=CARTESIAN_POINT('Ctrl Pts',(1.52170554939745,-0.322542392923269,
7.21932770010624));
#283383=CARTESIAN_POINT('Ctrl Pts',(1.52036284955179,-0.32881329650326,
7.21886184666224));
#283384=CARTESIAN_POINT('Ctrl Pts',(1.51782112865239,-0.340335542934345,
7.21800878334559));
#283385=CARTESIAN_POINT('Ctrl Pts',(1.51663359999054,-0.345589041214388,
7.21762097317581));
#283386=CARTESIAN_POINT('Ctrl Pts',(1.513861641275,-0.357562361606684,7.21673961826425));
#283387=CARTESIAN_POINT('Ctrl Pts',(1.51225973715551,-0.36427792078236,
7.21624706901489));
#283388=CARTESIAN_POINT('Ctrl Pts',(1.5070187416916,-0.385618849268429,
7.21468685239591));
#283389=CARTESIAN_POINT('Ctrl Pts',(1.5032116533644,-0.400202641381201,
7.2136281750354));
#283390=CARTESIAN_POINT('Ctrl Pts',(1.47779406465255,-0.492083907991147,
7.20699246044574));
#283391=CARTESIAN_POINT('Ctrl Pts',(1.45043725432645,-0.56767691119827,
7.20168335473523));
#283392=CARTESIAN_POINT('Ctrl Pts',(1.39962252184265,-0.680067241926809,
7.19355825593305));
#283393=CARTESIAN_POINT('Ctrl Pts',(1.38025997076975,-0.718552032129711,
7.19073193657411));
#283394=CARTESIAN_POINT('Ctrl Pts',(1.33362123638254,-0.802390469271581,
7.18438754704369));
#283395=CARTESIAN_POINT('Ctrl Pts',(1.30557913243906,-0.847253519688105,
7.1808622675486));
#283396=CARTESIAN_POINT('Ctrl Pts',(1.25543157955849,-0.919063161975205,
7.17490420635523));
#283397=CARTESIAN_POINT('Ctrl Pts',(1.23460822404052,-0.946851506323747,
7.17251401840584));
#283398=CARTESIAN_POINT('Ctrl Pts',(1.20429209114094,-0.984605850325622,
7.16913019528557));
#283399=CARTESIAN_POINT('Ctrl Pts',(1.19556956901294,-0.995179132476199,
7.16816692762145));
#283400=CARTESIAN_POINT('Ctrl Pts',(1.18036823535781,-1.01311759564374,
7.16650470405919));
#283401=CARTESIAN_POINT('Ctrl Pts',(1.17395728540315,-1.02053942484809,
7.16580854263229));
#283402=CARTESIAN_POINT('Ctrl Pts',(1.16156553857085,-1.03461382519181,
7.16447181138535));
#283403=CARTESIAN_POINT('Ctrl Pts',(1.15559667643018,-1.0412764200319,7.16383175732513));
#283404=CARTESIAN_POINT('Ctrl Pts',(1.13986816810754,-1.05853117478588,
7.16215477068272));
#283405=CARTESIAN_POINT('Ctrl Pts',(1.13001849057908,-1.06903969694249,
7.16111404404092));
#283406=CARTESIAN_POINT('Ctrl Pts',(1.09438122711372,-1.10601788561597,
7.15738061368865));
#283407=CARTESIAN_POINT('Ctrl Pts',(1.06779996547506,-1.13170165850278,
7.15465382946555));
#283408=CARTESIAN_POINT('Ctrl Pts',(0.958004442774669,-1.23047584605486,
7.14360667184893));
#283409=CARTESIAN_POINT('Ctrl Pts',(0.868013087295815,-1.295526901914,7.13499161029401));
#283410=CARTESIAN_POINT('Ctrl Pts',(0.717724395757608,-1.38142875619461,
7.12159252315129));
#283411=CARTESIAN_POINT('Ctrl Pts',(0.661731550788853,-1.40910847796491,
7.11679646779261));
#283412=CARTESIAN_POINT('Ctrl Pts',(0.590774283035635,-1.43902014062864,
7.11106607368267));
#283413=CARTESIAN_POINT('Ctrl Pts',(0.57724705142175,-1.44449960234825,
7.10998874856418));
#283414=CARTESIAN_POINT('Ctrl Pts',(0.557223405980756,-1.45228433228898,
7.10841818067837));
#283415=CARTESIAN_POINT('Ctrl Pts',(0.55078606444337,-1.45473792211662,
7.10791689753226));
#283416=CARTESIAN_POINT('Ctrl Pts',(0.539778674204684,-1.45884984276915,
7.10706617531228));
#283417=CARTESIAN_POINT('Ctrl Pts',(0.535216897708497,-1.46052961480979,
7.1067154966414));
#283418=CARTESIAN_POINT('Ctrl Pts',(0.524738559739492,-1.46433234032395,
7.10591433888086));
#283419=CARTESIAN_POINT('Ctrl Pts',(0.518816923776662,-1.46644084855689,
7.10546471234536));
#283420=CARTESIAN_POINT('Ctrl Pts',(0.502258810971588,-1.47222381688967,
7.10421575038247));
#283421=CARTESIAN_POINT('Ctrl Pts',(0.491594735579027,-1.47581893045395,
7.10342086684222));
#283422=CARTESIAN_POINT('Ctrl Pts',(0.40815602703161,-1.5029432954468,7.09726825633693));
#283423=CARTESIAN_POINT('Ctrl Pts',(0.333763929481463,-1.52119522521214,
7.09217432498568));
#283424=CARTESIAN_POINT('Ctrl Pts',(0.199978159481106,-1.54372582978643,
7.0832182231992));
#283425=CARTESIAN_POINT('Ctrl Pts',(0.141122576585364,-1.5502145244609,
7.0793462469842));
#283426=CARTESIAN_POINT('Ctrl Pts',(0.0331888256996731,-1.55591513787441,
7.07218256896104));
#283427=CARTESIAN_POINT('Ctrl Pts',(-0.0157541790486523,-1.55618914267095,
7.0689109721127));
#283428=CARTESIAN_POINT('Ctrl Pts',(-0.087079990629827,-1.55322322138593,
7.06404632122905));
#283429=CARTESIAN_POINT('Ctrl Pts',(-0.109510074288738,-1.55180306816909,
7.06250268124975));
#283430=CARTESIAN_POINT('Ctrl Pts',(-0.150263484479658,-1.54833483817215,
7.05966709063586));
#283431=CARTESIAN_POINT('Ctrl Pts',(-0.168596386309016,-1.54644595582078,
7.05838006082208));
#283432=CARTESIAN_POINT('Ctrl Pts',(-0.197595010881135,-1.54293639571688,
7.05632389811799));
#283433=CARTESIAN_POINT('Ctrl Pts',(-0.208285265924456,-1.54152967762595,
7.05556149831916));
#283434=CARTESIAN_POINT('Ctrl Pts',(-0.228442570044301,-1.53866370043912,
7.0541151827505));
#283435=CARTESIAN_POINT('Ctrl Pts',(-0.23791249022597,-1.53722790447646,
7.0534320400018));
#283436=CARTESIAN_POINT('Ctrl Pts',(-0.259371688826184,-1.5337712982661,
7.05187538565419));
#283437=CARTESIAN_POINT('Ctrl Pts',(-0.271351614735281,-1.53169721352572,
7.05100022290151));
#283438=CARTESIAN_POINT('Ctrl Pts',(-0.302520998521914,-1.52592371758541,
7.04870662050459));
#283439=CARTESIAN_POINT('Ctrl Pts',(-0.321666678644395,-1.52200283503349,
7.04728127395428));
#283440=CARTESIAN_POINT('Ctrl Pts',(-0.456027776501773,-1.49183842022342,
7.03715763558868));
#283441=CARTESIAN_POINT('Ctrl Pts',(-0.567976871852699,-1.45290568242781,
7.02804907891619));
#283442=CARTESIAN_POINT('Ctrl Pts',(-0.74823727744731,-1.36617426775708,
7.01253481434022));
#283443=CARTESIAN_POINT('Ctrl Pts',(-0.819144449963565,-1.32487604242039,
7.00619243317581));
#283444=CARTESIAN_POINT('Ctrl Pts',(-0.896506468557956,-1.27122202934174,
6.99921619344167));
#283445=CARTESIAN_POINT('Ctrl Pts',(-0.906456506120105,-1.26414632193565,
6.99831793928616));
#283446=CARTESIAN_POINT('Ctrl Pts',(-0.921509546417327,-1.25317261714819,
6.99695870844605));
#283447=CARTESIAN_POINT('Ctrl Pts',(-0.926673155743826,-1.24935916329039,
6.99649240109493));
#283448=CARTESIAN_POINT('Ctrl Pts',(-0.936125383095813,-1.24228761591108,
6.99563892579928));
#283449=CARTESIAN_POINT('Ctrl Pts',(-0.940420754945389,-1.23903916760772,
6.99525115296988));
#283450=CARTESIAN_POINT('Ctrl Pts',(-0.950177717820672,-1.23158032862593,
6.99437039684898));
#283451=CARTESIAN_POINT('Ctrl Pts',(-0.955628277676672,-1.22735585753269,
6.9938784035609));
#283452=CARTESIAN_POINT('Ctrl Pts',(-0.972866559172804,-1.21381082612887,
6.99232182112495));
#283453=CARTESIAN_POINT('Ctrl Pts',(-0.984547834386843,-1.20435529196761,
6.99126616318878));
#283454=CARTESIAN_POINT('Ctrl Pts',(-1.05137410780147,-1.14863981421436,
6.98520954450355));
#283455=CARTESIAN_POINT('Ctrl Pts',(-1.10339892469848,-1.09876038533345,
6.98042240366214));
#283456=CARTESIAN_POINT('Ctrl Pts',(-1.18910481683623,-1.00433706512575,
6.97200740413813));
#283457=CARTESIAN_POINT('Ctrl Pts',(-1.22419430813036,-0.96125514872669,
6.96837133426241));
#283458=CARTESIAN_POINT('Ctrl Pts',(-1.3014736129476,-0.855260106560734,
6.95968454271046));
#283459=CARTESIAN_POINT('Ctrl Pts',(-1.34151771764476,-0.790968612270013,
6.95460719821386));
#283460=CARTESIAN_POINT('Ctrl Pts',(-1.38482145531778,-0.708627165604342,
6.94814717705057));
#283461=CARTESIAN_POINT('Ctrl Pts',(-1.39266012375441,-0.693094986441829,
6.94693073397555));
#283462=CARTESIAN_POINT('Ctrl Pts',(-1.40483643939723,-0.667926938325157,
6.94496116228049));
#283463=CARTESIAN_POINT('Ctrl Pts',(-1.40933943749676,-0.658372353898031,
6.94421380365013));
#283464=CARTESIAN_POINT('Ctrl Pts',(-1.41775922882767,-0.640024738036972,
6.94277892189431));
#283465=CARTESIAN_POINT('Ctrl Pts',(-1.42169240509211,-0.631239727724532,
6.94209200289787));
#283466=CARTESIAN_POINT('Ctrl Pts',(-1.43048613728893,-0.611099194584432,
6.94051712659765));
#283467=CARTESIAN_POINT('Ctrl Pts',(-1.43529341588493,-0.599721275714149,
6.93962740334839));
#283468=CARTESIAN_POINT('Ctrl Pts',(-1.44778640637924,-0.569141907463111,
6.9372354819311));
#283469=CARTESIAN_POINT('Ctrl Pts',(-1.45522526810372,-0.549843006834763,
6.93572516617908));
#283470=CARTESIAN_POINT('Ctrl Pts',(-1.50993290878756,-0.39901842398349,
6.92391095591791));
#283471=CARTESIAN_POINT('Ctrl Pts',(-1.5396562697137,-0.261831358016168,
6.91301637011997));
#283472=CARTESIAN_POINT('Ctrl Pts',(-1.55390189278899,-0.0815961280935081,
6.89905084382698));
#283473=CARTESIAN_POINT('Ctrl Pts',(-1.5555153741194,-0.0405141409409373,
6.89589732999719));
#283474=CARTESIAN_POINT('Ctrl Pts',(-1.5554908803994,0.0244996029640861,
6.890994716635));
#283475=CARTESIAN_POINT('Ctrl Pts',(-1.55493041534923,0.0484114879992756,
6.88921047374986));
#283476=CARTESIAN_POINT('Ctrl Pts',(-1.55341906944806,0.0808910828078689,
6.88682065947192));
#283477=CARTESIAN_POINT('Ctrl Pts',(-1.55294821286529,0.0894764207277253,
6.88619217271994));
#283478=CARTESIAN_POINT('Ctrl Pts',(-1.55208573486681,0.103130794934568,
6.88519817977613));
#283479=CARTESIAN_POINT('Ctrl Pts',(-1.55174041928355,0.1082024141101,6.8848302071354));
#283480=CARTESIAN_POINT('Ctrl Pts',(-1.55096220078562,0.118860840851329,
6.88405958326944));
#283481=CARTESIAN_POINT('Ctrl Pts',(-1.55052396086327,0.124447162873384,
6.88365725459886));
#283482=CARTESIAN_POINT('Ctrl Pts',(-1.54935271741437,0.138409150918347,
6.88265537106138));
#283483=CARTESIAN_POINT('Ctrl Pts',(-1.54858196287555,0.146781636239823,
6.88205787651543));
#283484=CARTESIAN_POINT('Ctrl Pts',(-1.54530324996145,0.179489860371456,
6.87973512480338));
#283485=CARTESIAN_POINT('Ctrl Pts',(-1.54228906330299,0.203772816170861,
6.87803546865865));
#283486=CARTESIAN_POINT('Ctrl Pts',(-1.53263884390513,0.268906015058068,
6.87351875437365));
#283487=CARTESIAN_POINT('Ctrl Pts',(-1.52494347479319,0.309580641335146,
6.87074292738709));
#283488=CARTESIAN_POINT('Ctrl Pts',(-1.48361876100428,0.488582298952724,
6.85853843361351));
#283489=CARTESIAN_POINT('Ctrl Pts',(-1.43272581148776,0.622199651486687,
6.84938874875793));
#283490=CARTESIAN_POINT('Ctrl Pts',(-1.3552318240445,0.76373388184176,6.83824423828892));
#283491=CARTESIAN_POINT('Ctrl Pts',(-1.34578273488005,0.780263747382687,
6.83691951175804));
#283492=CARTESIAN_POINT('Ctrl Pts',(-1.32988166621093,0.80693201361782,
6.8347415024283));
#283493=CARTESIAN_POINT('Ctrl Pts',(-1.32361122482553,0.817176744528968,
6.83389475678209));
#283494=CARTESIAN_POINT('Ctrl Pts',(-1.31213576360208,0.83544686575863,
6.83236591795519));
#283495=CARTESIAN_POINT('Ctrl Pts',(-1.30697411724587,0.843498889742677,
6.83168545001259));
#283496=CARTESIAN_POINT('Ctrl Pts',(-1.29578518121467,0.860604028102614,
6.8302252602346));
#283497=CARTESIAN_POINT('Ctrl Pts',(-1.28973657178683,0.869642508902566,
6.82944476522294));
#283498=CARTESIAN_POINT('Ctrl Pts',(-1.27293562726561,0.894187445005131,
6.82730022024248));
#283499=CARTESIAN_POINT('Ctrl Pts',(-1.26199544649055,0.909562385305535,
6.82592911009729));
#283500=CARTESIAN_POINT('Ctrl Pts',(-1.18882132839201,1.00853640372578,
6.81691541667426));
#283501=CARTESIAN_POINT('Ctrl Pts',(-1.11861068834515,1.08588401662907,
6.80895641393999));
#283502=CARTESIAN_POINT('Ctrl Pts',(-0.968808019565662,1.22085596487664,
6.79333606604023));
#283503=CARTESIAN_POINT('Ctrl Pts',(-0.890427777509494,1.2791481036406,
6.78572857171517));
#283504=CARTESIAN_POINT('Ctrl Pts',(-0.794910671248913,1.33712401923343,
6.77741828086715));
#283505=CARTESIAN_POINT('Ctrl Pts',(-0.782618083607044,1.34435582776144,
6.77636597832437));
#283506=CARTESIAN_POINT('Ctrl Pts',(-0.764296813570521,1.35479785375723,
6.77482470319823));
#283507=CARTESIAN_POINT('Ctrl Pts',(-0.758344083417931,1.35813883665999,
6.77432809777702));
#283508=CARTESIAN_POINT('Ctrl Pts',(-0.747665093598823,1.36404033919229,
6.77344488470922));
#283509=CARTESIAN_POINT('Ctrl Pts',(-0.742947359823282,1.36661566010162,
6.77305737425188));
#283510=CARTESIAN_POINT('Ctrl Pts',(-0.732434203477966,1.37228405831541,
6.77219975293653));
#283511=CARTESIAN_POINT('Ctrl Pts',(-0.726632450264999,1.37536492814084,
6.77173040258224));
#283512=CARTESIAN_POINT('Ctrl Pts',(-0.709339975063412,1.38440767944788,
6.7703425916911));
#283513=CARTESIAN_POINT('Ctrl Pts',(-0.697793807767877,1.39026315990409,
6.76943043409407));
#283514=CARTESIAN_POINT('Ctrl Pts',(-0.67079679777614,1.40353323738401,
6.76732791476882));
#283515=CARTESIAN_POINT('Ctrl Pts',(-0.655293609920436,1.41083813118765,
6.76614320903078));
#283516=CARTESIAN_POINT('Ctrl Pts',(-0.600128098628353,1.43572578067155,
6.76199600262839));
#283517=CARTESIAN_POINT('Ctrl Pts',(-0.559851967281369,1.45190515795145,
6.75909098443087));
#283518=CARTESIAN_POINT('Ctrl Pts',(-0.459811327718358,1.48730935270688,
6.7520510288142));
#283519=CARTESIAN_POINT('Ctrl Pts',(-0.399460777930149,1.50464178253863,
6.74795033485527));
#283520=CARTESIAN_POINT('Ctrl Pts',(-0.258176101446387,1.536115762935,6.73838788083788));
#283521=CARTESIAN_POINT('Ctrl Pts',(-0.176850055963499,1.54758776911403,
6.73290588831504));
#283522=CARTESIAN_POINT('Ctrl Pts',(-0.0770456228605368,1.55369494782263,
6.72596912398444));
#283523=CARTESIAN_POINT('Ctrl Pts',(-0.0590686002445035,1.55448218793097,
6.72471188841707));
#283524=CARTESIAN_POINT('Ctrl Pts',(-0.0303966425756174,1.55523971253574,
6.72269227812918));
#283525=CARTESIAN_POINT('Ctrl Pts',(-0.0197083093384715,1.5554118720076,
6.72193622246404));
#283526=CARTESIAN_POINT('Ctrl Pts',(0.000575805544540651,1.55552948777742,
6.72049493303484));
#283527=CARTESIAN_POINT('Ctrl Pts',(0.0101710045791695,1.55549633942618,
6.71981040235859));
#283528=CARTESIAN_POINT('Ctrl Pts',(0.0320815764149997,1.55521790847319,
6.71824071036492));
#283529=CARTESIAN_POINT('Ctrl Pts',(0.0443954310005491,1.55491511017653,
6.71735379090366));
#283530=CARTESIAN_POINT('Ctrl Pts',(0.0828643422337133,1.55351183496251,
6.71456748617977));
#283531=CARTESIAN_POINT('Ctrl Pts',(0.10899478988918,1.55189738783223,6.71265230357558));
#283532=CARTESIAN_POINT('Ctrl Pts',(0.231503063865512,1.54121914133226,
6.70356164677921));
#283533=CARTESIAN_POINT('Ctrl Pts',(0.32692475806529,1.52383217751525,6.6961362696206));
#283534=CARTESIAN_POINT('Ctrl Pts',(0.508943473883406,1.47277681960009,
6.6814827391431));
#283535=CARTESIAN_POINT('Ctrl Pts',(0.595404065838802,1.43999725000418,
6.67429388807202));
#283536=CARTESIAN_POINT('Ctrl Pts',(0.691474943974453,1.39343173770253,
6.66634834023519));
#283537=CARTESIAN_POINT('Ctrl Pts',(0.704407173364741,1.38693914059612,
6.66528000946877));
#283538=CARTESIAN_POINT('Ctrl Pts',(0.723426933632015,1.37705563357825,
6.66371260251421));
#283539=CARTESIAN_POINT('Ctrl Pts',(0.729584872655285,1.37380299346813,
6.66320573197652));
#283540=CARTESIAN_POINT('Ctrl Pts',(0.740462830659614,1.36796345422184,
6.66231169004866));
#283541=CARTESIAN_POINT('Ctrl Pts',(0.745191513135505,1.36539328675944,
6.66192351751357));
#283542=CARTESIAN_POINT('Ctrl Pts',(0.755562535113961,1.35968642545512,
6.661073230242));
#283543=CARTESIAN_POINT('Ctrl Pts',(0.761198777076861,1.35653910589301,
6.66061179228958));
#283544=CARTESIAN_POINT('Ctrl Pts',(0.777590961902547,1.34725125178266,
6.65927120516224));
#283545=CARTESIAN_POINT('Ctrl Pts',(0.78829367093438,1.34101705926748,6.65839773440212));
#283546=CARTESIAN_POINT('Ctrl Pts',(0.812800896700026,1.32634709877763,
6.65639911412947));
#283547=CARTESIAN_POINT('Ctrl Pts',(0.826550764169178,1.31782237260232,
6.65527887131028));
#283548=CARTESIAN_POINT('Ctrl Pts',(0.873505630584418,1.28768690303119,
6.65144799128946));
#283549=CARTESIAN_POINT('Ctrl Pts',(0.906018412731336,1.26502203098795,
6.64878585163898));
#283550=CARTESIAN_POINT('Ctrl Pts',(1.01541097895417,1.18238017439628,6.63966539926443));
#283551=CARTESIAN_POINT('Ctrl Pts',(1.08749347891351,1.11644108779696,6.63334840350399));
#283552=CARTESIAN_POINT('Ctrl Pts',(1.19028244098421,1.00294760313995,6.6231088990313));
#283553=CARTESIAN_POINT('Ctrl Pts',(1.2253901522336,0.959736464880182,6.61933327626673));
#283554=CARTESIAN_POINT('Ctrl Pts',(1.26785887780604,0.901326359025587,
6.61431224592061));
#283555=CARTESIAN_POINT('Ctrl Pts',(1.27739696154372,0.887756895336745,
6.61315139474784));
#283556=CARTESIAN_POINT('Ctrl Pts',(1.2925537505794,0.865443811728671,6.6112499489345));
#283557=CARTESIAN_POINT('Ctrl Pts',(1.29830518456281,0.85679158939647,6.61051440859563));
#283558=CARTESIAN_POINT('Ctrl Pts',(1.30924786038382,0.839966678105984,
6.6090871108953));
#283559=CARTESIAN_POINT('Ctrl Pts',(1.3144503318504,0.831801837899735,6.60839581553785));
#283560=CARTESIAN_POINT('Ctrl Pts',(1.32643599610891,0.81259809182223,6.60677270042734));
#283561=CARTESIAN_POINT('Ctrl Pts',(1.33315806442328,0.801522093876135,
6.60583868945038));
#283562=CARTESIAN_POINT('Ctrl Pts',(1.35491934506289,0.764634677634679,
6.60273424475909));
#283563=CARTESIAN_POINT('Ctrl Pts',(1.36935252725195,0.738475490855844,
6.60054239623207));
#283564=CARTESIAN_POINT('Ctrl Pts',(1.40253533779561,0.674012245818938,
6.59516062961372));
#283565=CARTESIAN_POINT('Ctrl Pts',(1.4204795248445,0.635322934141587,6.59194637432709));
#283566=CARTESIAN_POINT('Ctrl Pts',(1.46177951877084,0.535750096808311,
6.58372230139521));
#283567=CARTESIAN_POINT('Ctrl Pts',(1.48293885205268,0.47404528648415,6.57866753138253));
#283568=CARTESIAN_POINT('Ctrl Pts',(1.50470799049797,0.394625703168508,
6.57228161227169));
#283569=CARTESIAN_POINT('Ctrl Pts',(1.50897600331429,0.377977529916296,
6.57094972042722));
#283570=CARTESIAN_POINT('Ctrl Pts',(1.52784589732106,0.298950291933647,
6.56466634838832));
#283571=CARTESIAN_POINT('Ctrl Pts',(1.53886264440151,0.235771226002317,
6.55975470473817));
#283572=CARTESIAN_POINT('Ctrl Pts',(1.54718261741522,0.161027932277864,
6.55419261756031));
#283573=CARTESIAN_POINT('Ctrl Pts',(1.54829490310943,0.149956522163682,
6.55337513688733));
#283574=CARTESIAN_POINT('Ctrl Pts',(1.54984698521695,0.132641346906011,
6.55210759563121));
#283575=CARTESIAN_POINT('Ctrl Pts',(1.55036803801667,0.126405517607858,
6.55165332418757));
#283576=CARTESIAN_POINT('Ctrl Pts',(1.55122734902196,0.115315380425145,
6.55084955983854));
#283577=CARTESIAN_POINT('Ctrl Pts',(1.55158046788556,0.110462564113963,
6.55049927385853));
#283578=CARTESIAN_POINT('Ctrl Pts',(1.55238129226738,0.0986944348818104,
6.54965319273492));
#283579=CARTESIAN_POINT('Ctrl Pts',(1.55280556777163,0.0917776751041955,
6.54915869984335));
#283580=CARTESIAN_POINT('Ctrl Pts',(1.55399162184719,0.070068975648567,
6.54761480787361));
#283581=CARTESIAN_POINT('Ctrl Pts',(1.5545883948504,0.0552683169444688,
6.54657400337074));
#283582=CARTESIAN_POINT('Ctrl Pts',(1.55665088349847,-0.0239966576722541,
6.54105215008089));
#283583=CARTESIAN_POINT('Ctrl Pts',(1.55431877384013,-0.088504090703835,
6.53674163935358));
#283584=CARTESIAN_POINT('Ctrl Pts',(1.53652231810634,-0.26892959715407,
6.52474814113756));
#283585=CARTESIAN_POINT('Ctrl Pts',(1.51200157123545,-0.383501638794764,
6.51717781213232));
#283586=CARTESIAN_POINT('Ctrl Pts',(1.46514012928999,-0.523341320002035,
6.50711202862732));
#283587=CARTESIAN_POINT('Ctrl Pts',(1.4545325465319,-0.552138200456382,
6.50499476686973));
#283588=CARTESIAN_POINT('Ctrl Pts',(1.43855369778288,-0.591853549419929,
6.50200160706115));
#283589=CARTESIAN_POINT('Ctrl Pts',(1.43389508192174,-0.603052439437859,
6.50114933806971));
#283590=CARTESIAN_POINT('Ctrl Pts',(1.42557015799808,-0.622422820437998,
6.49966013953967));
#283591=CARTESIAN_POINT('Ctrl Pts',(1.42196331053641,-0.630619362352773,
6.49902524417241));
#283592=CARTESIAN_POINT('Ctrl Pts',(1.41426208104662,-0.647718323930799,
6.49769054626426));
#283593=CARTESIAN_POINT('Ctrl Pts',(1.41015396281183,-0.656614083078789,
6.4969902954529));
#283594=CARTESIAN_POINT('Ctrl Pts',(1.40011921105144,-0.677814852349313,
6.49530697992032));
#283595=CARTESIAN_POINT('Ctrl Pts',(1.39411411400355,-0.690081585187227,
6.49432123440742));
#283596=CARTESIAN_POINT('Ctrl Pts',(1.37242595106076,-0.732945679961526,
6.49083399394285));
#283597=CARTESIAN_POINT('Ctrl Pts',(1.35589181071166,-0.763098561733579,
6.48830312735241));
#283598=CARTESIAN_POINT('Ctrl Pts',(1.31181080101408,-0.83752593281818,
6.4818525563301));
#283599=CARTESIAN_POINT('Ctrl Pts',(1.28301313016479,-0.881007158273952,
6.47789349817351));
#283600=CARTESIAN_POINT('Ctrl Pts',(1.21942477724302,-0.967271539143556,
6.46965782177956));
#283601=CARTESIAN_POINT('Ctrl Pts',(1.18443075747874,-1.00981900766067,
6.46538135871984));
#283602=CARTESIAN_POINT('Ctrl Pts',(1.09631582849073,-1.1060570721497,6.45526805932651));
#283603=CARTESIAN_POINT('Ctrl Pts',(1.04138915749959,-1.1579214011463,6.44945048408799));
#283604=CARTESIAN_POINT('Ctrl Pts',(0.974206759339196,-1.21269431851723,
6.44303829705089));
#283605=CARTESIAN_POINT('Ctrl Pts',(0.965427454652025,-1.21969511326993,
6.4422132049179));
#283606=CARTESIAN_POINT('Ctrl Pts',(0.951620589825,-1.23046249119583,6.44093645477913));
#283607=CARTESIAN_POINT('Ctrl Pts',(0.946644939638089,-1.23429455609448,
6.44048049097239));
#283608=CARTESIAN_POINT('Ctrl Pts',(0.937776127773533,-1.24103981569778,
6.43967528196184));
#283609=CARTESIAN_POINT('Ctrl Pts',(0.9338924602303,-1.24396493673252,6.43932522664153));
#283610=CARTESIAN_POINT('Ctrl Pts',(0.924466642400233,-1.25099530039113,
6.43848168511117));
#283611=CARTESIAN_POINT('Ctrl Pts',(0.918910818049202,-1.25508196059468,
6.43798947915095));
#283612=CARTESIAN_POINT('Ctrl Pts',(0.901480895989794,-1.26772498606289,
6.43646020215657));
#283613=CARTESIAN_POINT('Ctrl Pts',(0.889512680547177,-1.27615111880029,
6.43543149604163));
#283614=CARTESIAN_POINT('Ctrl Pts',(0.825576522175744,-1.31982829869947,
6.43003747486217));
#283615=CARTESIAN_POINT('Ctrl Pts',(0.771622498192837,-1.35208133719632,
6.42583411052176));
#283616=CARTESIAN_POINT('Ctrl Pts',(0.616540474983412,-1.43247097659275,
6.41427011325858));
#283617=CARTESIAN_POINT('Ctrl Pts',(0.511963053506555,-1.47308789695883,
6.40702057564269));
#283618=CARTESIAN_POINT('Ctrl Pts',(0.369411508968676,-1.51142100825604,
6.39699502553451));
#283619=CARTESIAN_POINT('Ctrl Pts',(0.334580409405811,-1.51951108846512,
6.39453727680501));
#283620=CARTESIAN_POINT('Ctrl Pts',(0.285540354399109,-1.52913355756688,
6.39104830430307));
#283621=CARTESIAN_POINT('Ctrl Pts',(0.271540524280211,-1.53168157620455,
6.39004910955775));
#283622=CARTESIAN_POINT('Ctrl Pts',(0.248716085110685,-1.5355129556002,
6.38841398324918));
#283623=CARTESIAN_POINT('Ctrl Pts',(0.239911707522368,-1.53691317073847,
6.38778177690101));
#283624=CARTESIAN_POINT('Ctrl Pts',(0.221368715687206,-1.53969896287266,
6.38644694275585));
#283625=CARTESIAN_POINT('Ctrl Pts',(0.211628056039106,-1.54106799403702,
6.38574382267036));
#283626=CARTESIAN_POINT('Ctrl Pts',(0.188126472050311,-1.54414408278291,
6.38404240596493));
#283627=CARTESIAN_POINT('Ctrl Pts',(0.174354655125536,-1.54575966726496,
6.38304127944408));
#283628=CARTESIAN_POINT('Ctrl Pts',(0.124925284018921,-1.55088932014354,
6.37943231262649));
#283629=CARTESIAN_POINT('Ctrl Pts',(0.0891728657577869,-1.55335502129853,
6.37679228843598));
#283630=CARTESIAN_POINT('Ctrl Pts',(-0.00201351927747187,-1.55648550265918,
6.36997886386016));
#283631=CARTESIAN_POINT('Ctrl Pts',(-0.0574533471240208,-1.55542571916719,
6.36576002701786));
#283632=CARTESIAN_POINT('Ctrl Pts',(-0.232606063064412,-1.54270047770986,
6.35223738972163));
#283633=CARTESIAN_POINT('Ctrl Pts',(-0.351086710665847,-1.52012193412441,
6.34277053373473));
#283634=CARTESIAN_POINT('Ctrl Pts',(-0.478299917337154,-1.48019640715587,
6.33284952173644));
#283635=CARTESIAN_POINT('Ctrl Pts',(-0.490762097551915,-1.47611138054362,
6.33188076843525));
#283636=CARTESIAN_POINT('Ctrl Pts',(-0.509491470964639,-1.46970857618049,
6.33043108797992));
#283637=CARTESIAN_POINT('Ctrl Pts',(-0.515797469385821,-1.46750735357876,
6.32994407484161));
#283638=CARTESIAN_POINT('Ctrl Pts',(-0.527230008477916,-1.46343382178655,
6.32906335022191));
#283639=CARTESIAN_POINT('Ctrl Pts',(-0.5323612407226,-1.46157502232004,
6.32866887512415));
#283640=CARTESIAN_POINT('Ctrl Pts',(-0.543037114109334,-1.45764398130796,
6.3278499845026));
#283641=CARTESIAN_POINT('Ctrl Pts',(-0.548579859251683,-1.45556704576282,
6.32742584796264));
#283642=CARTESIAN_POINT('Ctrl Pts',(-0.563332179360345,-1.44994292982204,
6.32629935979313));
#283643=CARTESIAN_POINT('Ctrl Pts',(-0.572520271662161,-1.44633958527201,
6.3256002363331));
#283644=CARTESIAN_POINT('Ctrl Pts',(-0.618520323465517,-1.42779243717715,
6.32210955204408));
#283645=CARTESIAN_POINT('Ctrl Pts',(-0.654787996334789,-1.4115282324559,
6.31938793102255));
#283646=CARTESIAN_POINT('Ctrl Pts',(-0.758472521619566,-1.36017313397632,
6.31158436026833));
#283647=CARTESIAN_POINT('Ctrl Pts',(-0.823991135252997,-1.32151108657096,
6.3066202900587));
#283648=CARTESIAN_POINT('Ctrl Pts',(-0.964229229278627,-1.22425770914935,
6.29537812268854));
#283649=CARTESIAN_POINT('Ctrl Pts',(-1.03693365902289,-1.1633185252147,
6.28909331355653));
#283650=CARTESIAN_POINT('Ctrl Pts',(-1.11642390976572,-1.08328522163345,
6.28126958470426));
#283651=CARTESIAN_POINT('Ctrl Pts',(-1.12897875900211,-1.07019443634102,
6.28000250653059));
#283652=CARTESIAN_POINT('Ctrl Pts',(-1.14858535129763,-1.04902186168229,
6.27797082086458));
#283653=CARTESIAN_POINT('Ctrl Pts',(-1.15578762361226,-1.04108123325357,
6.27721266798382));
#283654=CARTESIAN_POINT('Ctrl Pts',(-1.16927562919944,-1.02589799954425,
6.2757697471697));
#283655=CARTESIAN_POINT('Ctrl Pts',(-1.17557761212984,-1.01867044366101,
6.27508570562997));
#283656=CARTESIAN_POINT('Ctrl Pts',(-1.18978573513569,-1.00206813112445,
6.27352047261503));
#283657=CARTESIAN_POINT('Ctrl Pts',(-1.19764855280994,-0.992657323995823,
6.27263755948484));
#283658=CARTESIAN_POINT('Ctrl Pts',(-1.22130045408711,-0.963658858554,6.26992931278323));
#283659=CARTESIAN_POINT('Ctrl Pts',(-1.23672559484325,-0.94378115102228,
6.26808969298344));
#283660=CARTESIAN_POINT('Ctrl Pts',(-1.29130671686026,-0.869808036496203,
6.26129998372855));
#283661=CARTESIAN_POINT('Ctrl Pts',(-1.32744612453512,-0.813586944268549,
6.25624217308097));
#283662=CARTESIAN_POINT('Ctrl Pts',(-1.3946170124684,-0.692639009887966,
6.24560291173027));
#283663=CARTESIAN_POINT('Ctrl Pts',(-1.42501285501546,-0.627728688854752,
6.24002190928897));
#283664=CARTESIAN_POINT('Ctrl Pts',(-1.47160752256398,-0.50721913081853,
6.23005026678234));
#283665=CARTESIAN_POINT('Ctrl Pts',(-1.48938646004944,-0.452359877992798,
6.2256487107456));
#283666=CARTESIAN_POINT('Ctrl Pts',(-1.50687443407433,-0.386043601632136,
6.2205782026086));
#283667=CARTESIAN_POINT('Ctrl Pts',(-1.50955553405755,-0.375422868412904,
6.21977368128932));
#283668=CARTESIAN_POINT('Ctrl Pts',(-1.5135826029735,-0.358729179364893,
6.21852183329899));
#283669=CARTESIAN_POINT('Ctrl Pts',(-1.51500465785352,-0.352675219515232,
6.21807045542671));
#283670=CARTESIAN_POINT('Ctrl Pts',(-1.51759742241878,-0.341332176713582,
6.21722979922491));
#283671=CARTESIAN_POINT('Ctrl Pts',(-1.51877682081666,-0.336045474830606,
6.21684006969916));
#283672=CARTESIAN_POINT('Ctrl Pts',(-1.52107136114657,-0.325501222267586,
6.21606677300186));
#283673=CARTESIAN_POINT('Ctrl Pts',(-1.52218688824927,-0.320243986555809,
6.21568318647495));
#283674=CARTESIAN_POINT('Ctrl Pts',(-1.52473626775074,-0.30791496720822,
6.2147879981349));
#283675=CARTESIAN_POINT('Ctrl Pts',(-1.52614822035645,-0.30083870741485,
6.21427757032291));
#283676=CARTESIAN_POINT('Ctrl Pts',(-1.52975391864935,-0.282089114927303,
6.21293338783339));
#283677=CARTESIAN_POINT('Ctrl Pts',(-1.53186334017751,-0.270399792678156,
6.21210382229557));
#283678=CARTESIAN_POINT('Ctrl Pts',(-1.54817398109791,-0.173688750447234,
6.20530145682289));
#283679=CARTESIAN_POINT('Ctrl Pts',(-1.55542054432572,-0.0876372136492061,
6.19963183488464));
#283680=CARTESIAN_POINT('Ctrl Pts',(-1.55549935018888,-0.00142181643757374,
6.19395780777199));
#283681=CARTESIAN_POINT('',(-1.55313101942593,0.000158339568030034,5.49415672523128));
#283682=CARTESIAN_POINT('Ctrl Pts',(-1.5529563387483,0.000151106445085633,
5.49405622560371));
#283683=CARTESIAN_POINT('Ctrl Pts',(-1.55272340811799,-0.268780222436924,
5.5132440667186));
#283684=CARTESIAN_POINT('Ctrl Pts',(-1.35831396530156,-1.05747938365068,
5.56949404777722));
#283685=CARTESIAN_POINT('Ctrl Pts',(-0.103102773360761,-1.83589824620028,
5.66280616877956));
#283686=CARTESIAN_POINT('Ctrl Pts',(1.4869956060099,-1.08166382022474,5.77399258861071));
#283687=CARTESIAN_POINT('Ctrl Pts',(1.71494149863546,0.663421591850831,
5.88517900844189));
#283688=CARTESIAN_POINT('Ctrl Pts',(0.371926577693494,1.80078404398782,
5.99636542827304));
#283689=CARTESIAN_POINT('Ctrl Pts',(-1.18720044783918,1.3264536081355,6.0993244620085));
#283690=CARTESIAN_POINT('Ctrl Pts',(-1.55195178408473,0.400947059710162,
6.16522135580024));
#283691=CARTESIAN_POINT('Ctrl Pts',(-1.5556705629256,-0.00141387709470033,
6.19405610964826));
#283692=CARTESIAN_POINT('',(-1.55731595967384,-0.000935870630138446,4.09405524453403));
#283693=CARTESIAN_POINT('Ctrl Pts',(-1.55549997886283,0.000256432700539262,
5.49551966671036));
#283694=CARTESIAN_POINT('Ctrl Pts',(-1.5554991185824,0.00547482406793109,
5.49514503270296));
#283695=CARTESIAN_POINT('Ctrl Pts',(-1.55547199833197,0.010693128598903,
5.49476957764081));
#283696=CARTESIAN_POINT('Ctrl Pts',(-1.55533490000557,0.0240953838132042,
5.49380312031377));
#283697=CARTESIAN_POINT('Ctrl Pts',(-1.55518658709843,0.0322786808451574,
5.49321093089671));
#283698=CARTESIAN_POINT('Ctrl Pts',(-1.55432199513997,0.065506767024369,
5.49079768122473));
#283699=CARTESIAN_POINT('Ctrl Pts',(-1.55306527454723,0.0905324237099038,
5.48896003392764));
#283700=CARTESIAN_POINT('Ctrl Pts',(-1.5421203365499,0.237506956043084,
5.4780438999739));
#283701=CARTESIAN_POINT('Ctrl Pts',(-1.5186779841696,0.357982530041526,
5.46854438678358));
#283702=CARTESIAN_POINT('Ctrl Pts',(-1.46183840961193,0.53545611450869,
5.45411423925923));
#283703=CARTESIAN_POINT('Ctrl Pts',(-1.43854449778955,0.595211079027277,
5.44918523340074));
#283704=CARTESIAN_POINT('Ctrl Pts',(-1.40542540183141,0.666766672759873,
5.44331588692544));
#283705=CARTESIAN_POINT('Ctrl Pts',(-1.39903129167002,0.680080762315757,
5.44222539821618));
#283706=CARTESIAN_POINT('Ctrl Pts',(-1.3893632167977,0.699498398527043,
5.44063945106656));
#283707=CARTESIAN_POINT('Ctrl Pts',(-1.38623681357353,0.705673904389142,
5.44013573410594));
#283708=CARTESIAN_POINT('Ctrl Pts',(-1.38084301210415,0.716153957993286,
5.43928231124514));
#283709=CARTESIAN_POINT('Ctrl Pts',(-1.37859651498946,0.720468991002216,
5.43893134363674));
#283710=CARTESIAN_POINT('Ctrl Pts',(-1.37341160068452,0.730315033294327,
5.43813150187911));
#283711=CARTESIAN_POINT('Ctrl Pts',(-1.37045998417119,0.735838914583601,
5.4376834631261));
#283712=CARTESIAN_POINT('Ctrl Pts',(-1.36216059912738,0.751147849700196,
5.43644326714848));
#283713=CARTESIAN_POINT('Ctrl Pts',(-1.35674072459185,0.760893694930043,
5.4356554626379));
#283714=CARTESIAN_POINT('Ctrl Pts',(-1.31878746532864,0.827444878589895,
5.43028168349018));
#283715=CARTESIAN_POINT('Ctrl Pts',(-1.28279681546386,0.882213144464907,
5.42588774124978));
#283716=CARTESIAN_POINT('Ctrl Pts',(-1.23434786585122,0.946676002542723,
5.42054324604659));
#283717=CARTESIAN_POINT('Ctrl Pts',(-1.22506217965674,0.958661970525544,
5.41954172012888));
#283718=CARTESIAN_POINT('Ctrl Pts',(-1.17100858354432,1.02636623759926,
5.41382839449819));
#283719=CARTESIAN_POINT('Ctrl Pts',(-1.12261913824008,1.07908047166182,
5.40915502094565));
#283720=CARTESIAN_POINT('Ctrl Pts',(-1.02789304292682,1.16897888008542,
5.40043588478306));
#283721=CARTESIAN_POINT('Ctrl Pts',(-0.982727759685129,1.20719534945809,
5.39642931246848));
#283722=CARTESIAN_POINT('Ctrl Pts',(-0.922435306134706,1.25258165788644,
5.39118043073622));
#283723=CARTESIAN_POINT('Ctrl Pts',(-0.909215639357971,1.26221020015493,
5.39003546580615));
#283724=CARTESIAN_POINT('Ctrl Pts',(-0.887969190220278,1.27717807246545,
5.38820307351456));
#283725=CARTESIAN_POINT('Ctrl Pts',(-0.880040094008858,1.28265448853016,
5.38752091576348));
#283726=CARTESIAN_POINT('Ctrl Pts',(-0.864390056963656,1.29325012679417,
5.3861774777026));
#283727=CARTESIAN_POINT('Ctrl Pts',(-0.856673247449613,1.2983747537971,
5.38551643805449));
#283728=CARTESIAN_POINT('Ctrl Pts',(-0.838831670299249,1.30999479896602,
5.38399098751339));
#283729=CARTESIAN_POINT('Ctrl Pts',(-0.828676525033821,1.31644223046614,
5.38312483817094));
#283730=CARTESIAN_POINT('Ctrl Pts',(-0.801499768435247,1.3332575051954,
5.38081189806941));
#283731=CARTESIAN_POINT('Ctrl Pts',(-0.78435244596338,1.34341677307045,
5.37935765259221));
#283732=CARTESIAN_POINT('Ctrl Pts',(-0.646869350932612,1.42134189100549,
5.3677332023205));
#283733=CARTESIAN_POINT('Ctrl Pts',(-0.518208795480751,1.47312477764943,
5.3569845925563));
#283734=CARTESIAN_POINT('Ctrl Pts',(-0.342673207996331,1.51789780885836,
5.34297909981599));
#283735=CARTESIAN_POINT('Ctrl Pts',(-0.300473239542847,1.52681204362755,
5.33966649560503));
#283736=CARTESIAN_POINT('Ctrl Pts',(-0.241123071012958,1.536792515486,5.3351242002023));
#283737=CARTESIAN_POINT('Ctrl Pts',(-0.224245011447707,1.5393459004059,
5.33384552282526));
#283738=CARTESIAN_POINT('Ctrl Pts',(-0.194536987017095,1.54334123531981,
5.3316214340136));
#283739=CARTESIAN_POINT('Ctrl Pts',(-0.181724929709431,1.54490222564149,
5.33067089668175));
#283740=CARTESIAN_POINT('Ctrl Pts',(-0.162372257850548,1.54701601332483,
5.32924955155693));
#283741=CARTESIAN_POINT('Ctrl Pts',(-0.155845529685681,1.54768713592207,
5.32877267177119));
#283742=CARTESIAN_POINT('Ctrl Pts',(-0.143964175303132,1.54883293463854,
5.3279092801111));
#283743=CARTESIAN_POINT('Ctrl Pts',(-0.138611206851933,1.54932116702434,
5.32752205770599));
#283744=CARTESIAN_POINT('Ctrl Pts',(-0.126445675118673,1.55036720112347,
5.32664598008888));
#283745=CARTESIAN_POINT('Ctrl Pts',(-0.11963185606256,1.55090786018908,
5.3261580764442));
#283746=CARTESIAN_POINT('Ctrl Pts',(-0.0985439974603953,1.55244132106271,
5.32465605497674));
#283747=CARTESIAN_POINT('Ctrl Pts',(-0.0842591641910188,1.55328213994008,
5.32364988218428));
#283748=CARTESIAN_POINT('Ctrl Pts',(0.0511940515907608,1.55938079860967,
5.31419848337449));
#283749=CARTESIAN_POINT('Ctrl Pts',(0.172593295299025,1.55064827680406,
5.30638146696615));
#283750=CARTESIAN_POINT('Ctrl Pts',(0.345726188914309,1.51758766040755,
5.29473689372495));
#283751=CARTESIAN_POINT('Ctrl Pts',(0.399105611911333,1.50443108699072,
5.29107946082504));
#283752=CARTESIAN_POINT('Ctrl Pts',(0.485764512200602,1.47813471516828,
5.28492437537136));
#283753=CARTESIAN_POINT('Ctrl Pts',(0.51948679190479,1.4666228359979,5.28247330611433));
#283754=CARTESIAN_POINT('Ctrl Pts',(0.565716048478519,1.44904695172144,
5.27901783739476));
#283755=CARTESIAN_POINT('Ctrl Pts',(0.578583371567505,1.44395740108128,
5.27804560306345));
#283756=CARTESIAN_POINT('Ctrl Pts',(0.600473572911076,1.43495936809009,
5.27637273532666));
#283757=CARTESIAN_POINT('Ctrl Pts',(0.609530586580863,1.43113568740939,
5.27567499028124));
#283758=CARTESIAN_POINT('Ctrl Pts',(0.626735296029037,1.42367927965112,
5.27433852329056));
#283759=CARTESIAN_POINT('Ctrl Pts',(0.634889205355858,1.42006179914445,
5.27370034454408));
#283760=CARTESIAN_POINT('Ctrl Pts',(0.655996175763244,1.41047957148434,
5.272035641227));
#283761=CARTESIAN_POINT('Ctrl Pts',(0.668898862452639,1.40440659739065,
5.27100543121115));
#283762=CARTESIAN_POINT('Ctrl Pts',(0.714079285919814,1.38237745162958,
5.26735228342539));
#283763=CARTESIAN_POINT('Ctrl Pts',(0.745882424011416,1.36548001171883,
5.26469716888098));
#283764=CARTESIAN_POINT('Ctrl Pts',(0.873787305127055,1.29172033589242,
5.25366277875605));
#283765=CARTESIAN_POINT('Ctrl Pts',(0.964208399238657,1.22570017467944,
5.24497881364308));
#283766=CARTESIAN_POINT('Ctrl Pts',(1.09315990116245,1.10838384784354,5.2314838106662));
#283767=CARTESIAN_POINT('Ctrl Pts',(1.13695926116461,1.06340895670286,5.22666255042126));
#283768=CARTESIAN_POINT('Ctrl Pts',(1.18747986338139,1.00483121506877,5.22090578111305));
#283769=CARTESIAN_POINT('Ctrl Pts',(1.19687656078714,0.99362001597432,5.21982593798354));
#283770=CARTESIAN_POINT('Ctrl Pts',(1.21046831982977,0.976931030925822,
5.21825242662576));
#283771=CARTESIAN_POINT('Ctrl Pts',(1.21478700258578,0.971555626664188,
5.21775067649091));
#283772=CARTESIAN_POINT('Ctrl Pts',(1.22208968608591,0.962341252657412,
5.21689943706303));
#283773=CARTESIAN_POINT('Ctrl Pts',(1.22509160501491,0.958516796510098,
5.21654870392902));
#283774=CARTESIAN_POINT('Ctrl Pts',(1.23193071722327,0.949719122310274,
5.21574780342528));
#283775=CARTESIAN_POINT('Ctrl Pts',(1.23575577394762,0.94473666922855,5.21529848528453));
#283776=CARTESIAN_POINT('Ctrl Pts',(1.24633695493368,0.930779580781612,
5.21405122747741));
#283777=CARTESIAN_POINT('Ctrl Pts',(1.25302637014761,0.921754505370562,
5.21325772033959));
#283778=CARTESIAN_POINT('Ctrl Pts',(1.30398779752879,0.851419334673316,
5.20716654632157));
#283779=CARTESIAN_POINT('Ctrl Pts',(1.34383975871665,0.787017822628581,
5.20212675746629));
#283780=CARTESIAN_POINT('Ctrl Pts',(1.40422697131077,0.671366133002683,
5.19351181872391));
#283781=CARTESIAN_POINT('Ctrl Pts',(1.42701500864217,0.621461211563885,
5.189921919155));
#283782=CARTESIAN_POINT('Ctrl Pts',(1.46624283895116,0.521949135579925,
5.18284559768908));
#283783=CARTESIAN_POINT('Ctrl Pts',(1.48291245496679,0.472513451841354,
5.1793673291509));
#283784=CARTESIAN_POINT('Ctrl Pts',(1.50640488548135,0.389239264348815,
5.17347966139198));
#283785=CARTESIAN_POINT('Ctrl Pts',(1.51464123105902,0.355843404174913,
5.17111148346894));
#283786=CARTESIAN_POINT('Ctrl Pts',(1.52459296377786,0.308841553684111,
5.16775359843802));
#283787=CARTESIAN_POINT('Ctrl Pts',(1.52724600301168,0.295442779178589,
5.16679362211836));
#283788=CARTESIAN_POINT('Ctrl Pts',(1.53149868327036,0.272374830360456,
5.16513529680096));
#283789=CARTESIAN_POINT('Ctrl Pts',(1.5331840540612,0.262722122100428,5.16443970798818));
#283790=CARTESIAN_POINT('Ctrl Pts',(1.53623488061118,0.244218816257638,
5.16310284138545));
#283791=CARTESIAN_POINT('Ctrl Pts',(1.53761532795962,0.235371059481809,
5.16246206913289));
#283792=CARTESIAN_POINT('Ctrl Pts',(1.540685381266,0.214513165538916,5.16094768358292));
#283793=CARTESIAN_POINT('Ctrl Pts',(1.54231104448387,0.20249436730432,5.16007208864091));
#283794=CARTESIAN_POINT('Ctrl Pts',(1.54755220045282,0.160011136346541,
5.15696591940551));
#283795=CARTESIAN_POINT('Ctrl Pts',(1.55040664333606,0.129461854421636,
5.15471189334351));
#283796=CARTESIAN_POINT('Ctrl Pts',(1.55977999635251,-0.0177386591366861,
5.14374606308071));
#283797=CARTESIAN_POINT('Ctrl Pts',(1.55404469942018,-0.134776590449723,
5.13467178316308));
#283798=CARTESIAN_POINT('Ctrl Pts',(1.52490562563184,-0.313689423111976,
5.12063397442985));
#283799=CARTESIAN_POINT('Ctrl Pts',(1.51059153591323,-0.376633997131565,
5.11567183068498));
#283800=CARTESIAN_POINT('Ctrl Pts',(1.48823389725521,-0.452724524602937,
5.10976791550134));
#283801=CARTESIAN_POINT('Ctrl Pts',(1.48385541939011,-0.466875534954578,
5.10867419074575));
#283802=CARTESIAN_POINT('Ctrl Pts',(1.4771326414371,-0.487552487624977,
5.10708446609254));
#283803=CARTESIAN_POINT('Ctrl Pts',(1.47494595016069,-0.494128240054058,
5.10658015365321));
#283804=CARTESIAN_POINT('Ctrl Pts',(1.4711491657838,-0.505296008701843,
5.10572606813904));
#283805=CARTESIAN_POINT('Ctrl Pts',(1.4695613814533,-0.509895355010277,
5.10537502794862));
#283806=CARTESIAN_POINT('Ctrl Pts',(1.46588233436924,-0.520392530646494,
5.10457549899203));
#283807=CARTESIAN_POINT('Ctrl Pts',(1.4637770378746,-0.526285275520889,
5.10412784148784));
#283808=CARTESIAN_POINT('Ctrl Pts',(1.45782968462014,-0.542620175335744,
5.10288974745943));
#283809=CARTESIAN_POINT('Ctrl Pts',(1.45391097166605,-0.553034311068582,
5.10210364001836));
#283810=CARTESIAN_POINT('Ctrl Pts',(1.42668445726724,-0.623099602218949,
5.09683080756177));
#283811=CARTESIAN_POINT('Ctrl Pts',(1.39982059615336,-0.681312062502137,
5.09252771901382));
#283812=CARTESIAN_POINT('Ctrl Pts',(1.36128143755865,-0.752853925609075,
5.08713854163707));
#283813=CARTESIAN_POINT('Ctrl Pts',(1.35287209161084,-0.767862816030155,
5.08600211510296));
#283814=CARTESIAN_POINT('Ctrl Pts',(1.31142712917084,-0.839038070531316,
5.08057126968214));
#283815=CARTESIAN_POINT('Ctrl Pts',(1.27513390224327,-0.893229697464711,
5.07630730798694));
#283816=CARTESIAN_POINT('Ctrl Pts',(1.20964565836676,-0.97885432408689,
5.06913049938858));
#283817=CARTESIAN_POINT('Ctrl Pts',(1.18236146377073,-1.01164190938535,
5.06626388311691));
#283818=CARTESIAN_POINT('Ctrl Pts',(1.13372886978653,-1.06542558085201,
5.06130727619341));
#283819=CARTESIAN_POINT('Ctrl Pts',(1.11305822606272,-1.08700230174605,
5.0592428454919));
#283820=CARTESIAN_POINT('Ctrl Pts',(1.08255134915105,-1.11706342776354,
5.05624503902177));
#283821=CARTESIAN_POINT('Ctrl Pts',(1.07320941846039,-1.12604158507372,
5.05533331207533));
#283822=CARTESIAN_POINT('Ctrl Pts',(1.05669297089046,-1.14152264418962,
5.05373146233934));
#283823=CARTESIAN_POINT('Ctrl Pts',(1.04956776480652,-1.1480772976023,5.05304360706241));
#283824=CARTESIAN_POINT('Ctrl Pts',(1.03467065694356,-1.16152693313058,
5.05161169605077));
#283825=CARTESIAN_POINT('Ctrl Pts',(1.02688995582354,-1.16841139743433,
5.05086724597422));
#283826=CARTESIAN_POINT('Ctrl Pts',(1.0065108514817,-1.18608229512629,5.04892582090416));
#283827=CARTESIAN_POINT('Ctrl Pts',(0.993808162465199,-1.19674583833066,
5.04772388323463));
#283828=CARTESIAN_POINT('Ctrl Pts',(0.937763423603453,-1.24228612118081,
5.04245408933417));
#283829=CARTESIAN_POINT('Ctrl Pts',(0.892743471124306,-1.2750226516954,
5.03830353396108));
#283830=CARTESIAN_POINT('Ctrl Pts',(0.764219343336251,-1.35833129091181,
5.02667427013253));
#283831=CARTESIAN_POINT('Ctrl Pts',(0.677561649835615,-1.40356774020954,
5.01905705579641));
#283832=CARTESIAN_POINT('Ctrl Pts',(0.55059301904567,-1.45533317969305,
5.00847350624125));
#283833=CARTESIAN_POINT('Ctrl Pts',(0.513376369089351,-1.46887455625755,
5.0054389396611));
#283834=CARTESIAN_POINT('Ctrl Pts',(0.460287214164724,-1.48592643013444,
5.00123696655656));
#283835=CARTESIAN_POINT('Ctrl Pts',(0.444816265438071,-1.49063081047118,
5.00002733203459));
#283836=CARTESIAN_POINT('Ctrl Pts',(0.417374359606732,-1.49850998367764,
4.99791104438924));
#283837=CARTESIAN_POINT('Ctrl Pts',(0.405433757298075,-1.50178461218087,
4.99699989338688));
#283838=CARTESIAN_POINT('Ctrl Pts',(0.387210422422518,-1.5065490356495,
4.9956253095767));
#283839=CARTESIAN_POINT('Ctrl Pts',(0.380955753739081,-1.50814277366893,
4.99515636706837));
#283840=CARTESIAN_POINT('Ctrl Pts',(0.369467536380055,-1.51099402943458,
4.99430047626529));
#283841=CARTESIAN_POINT('Ctrl Pts',(0.364237291325487,-1.51226334175097,
4.99391289654182));
#283842=CARTESIAN_POINT('Ctrl Pts',(0.352223206372751,-1.51511305714213,
4.9930272970276));
#283843=CARTESIAN_POINT('Ctrl Pts',(0.345435223296114,-1.51667507215613,
4.99253032057237));
#283844=CARTESIAN_POINT('Ctrl Pts',(0.324508790589972,-1.52134277079016,
4.99100797114073));
#283845=CARTESIAN_POINT('Ctrl Pts',(0.310336811589613,-1.52429684909104,
4.98999066658263));
#283846=CARTESIAN_POINT('Ctrl Pts',(0.205564675119994,-1.54461418795323,
4.98255628363391));
#283847=CARTESIAN_POINT('Ctrl Pts',(0.113608213434321,-1.55408746344118,
4.9764992832139));
#283848=CARTESIAN_POINT('Ctrl Pts',(-0.0754535337835974,-1.55668185656689,
4.96405663635709));
#283849=CARTESIAN_POINT('Ctrl Pts',(-0.17215225755354,-1.54897142935768,
4.95769043733825));
#283850=CARTESIAN_POINT('Ctrl Pts',(-0.293288792738089,-1.52782432209277,
4.9492503123365));
#283851=CARTESIAN_POINT('Ctrl Pts',(-0.318956481770425,-1.52267268330145,
4.94743597031639));
#283852=CARTESIAN_POINT('Ctrl Pts',(-0.356492238879651,-1.51414835814987,
4.94473788398835));
#283853=CARTESIAN_POINT('Ctrl Pts',(-0.368470591445589,-1.5112780599773,
4.94387010277791));
#283854=CARTESIAN_POINT('Ctrl Pts',(-0.389717163372071,-1.50591927113162,
4.94231815531697));
#283855=CARTESIAN_POINT('Ctrl Pts',(-0.398998925965467,-1.50348667041789,
4.94163582065248));
#283856=CARTESIAN_POINT('Ctrl Pts',(-0.418572409065049,-1.49816276130777,
4.94018738014775));
#283857=CARTESIAN_POINT('Ctrl Pts',(-0.428857975441933,-1.49525093122185,
4.93942063934572));
#283858=CARTESIAN_POINT('Ctrl Pts',(-0.456374580165599,-1.48715374975951,
4.9373538772618));
#283859=CARTESIAN_POINT('Ctrl Pts',(-0.473546534744002,-1.4817751724637,
4.93604763405927));
#283860=CARTESIAN_POINT('Ctrl Pts',(-0.568453890697525,-1.45023021837367,
4.92873317869972));
#283861=CARTESIAN_POINT('Ctrl Pts',(-0.644105814605085,-1.41824931098287,
4.92253532239577));
#283862=CARTESIAN_POINT('Ctrl Pts',(-0.772547701739792,-1.35154938722656,
4.91139367169342));
#283863=CARTESIAN_POINT('Ctrl Pts',(-0.826420777600485,-1.3192968067106,
4.90650997392966));
#283864=CARTESIAN_POINT('Ctrl Pts',(-0.914003442042359,-1.25938869739363,
4.89830537373349));
#283865=CARTESIAN_POINT('Ctrl Pts',(-0.948771761555057,-1.23340781261568,
4.89497130406377));
#283866=CARTESIAN_POINT('Ctrl Pts',(-0.995696104886528,-1.19518331195752,
4.89040288505791));
#283867=CARTESIAN_POINT('Ctrl Pts',(-1.0088026157071,-1.18414155438375,
4.88911901589027));
#283868=CARTESIAN_POINT('Ctrl Pts',(-1.03148530664532,-1.16438218851592,
4.88688685041603));
#283869=CARTESIAN_POINT('Ctrl Pts',(-1.04113993849472,-1.15575753356495,
4.88593337946689));
#283870=CARTESIAN_POINT('Ctrl Pts',(-1.05552993935691,-1.14257601314418,
4.88450855907068));
#283871=CARTESIAN_POINT('Ctrl Pts',(-1.06034565932528,-1.13810829259536,
4.88403109481396));
#283872=CARTESIAN_POINT('Ctrl Pts',(-1.06905014763623,-1.12992960906528,
4.88316713854138));
#283873=CARTESIAN_POINT('Ctrl Pts',(-1.07294808194658,-1.12622890885256,
4.88277993021587));
#283874=CARTESIAN_POINT('Ctrl Pts',(-1.08175285965471,-1.11778244525903,
4.88190449956577));
#283875=CARTESIAN_POINT('Ctrl Pts',(-1.08664772735254,-1.11302451259086,
4.88141722244139));
#283876=CARTESIAN_POINT('Ctrl Pts',(-1.10167160019875,-1.09822734859344,
4.87991914450417));
#283877=CARTESIAN_POINT('Ctrl Pts',(-1.11169433882965,-1.08808058468585,
4.8789162288712));
#283878=CARTESIAN_POINT('Ctrl Pts',(-1.18910836532124,-1.00752203534501,
4.87112763911835));
#283879=CARTESIAN_POINT('Ctrl Pts',(-1.24989613273275,-0.931044891407583,
4.86474775779634));
#283880=CARTESIAN_POINT('Ctrl Pts',(-1.35968806954421,-0.762598609926195,
4.85151586146143));
#283881=CARTESIAN_POINT('Ctrl Pts',(-1.40742978767123,-0.670407182538903,
4.84468350877883));
#283882=CARTESIAN_POINT('Ctrl Pts',(-1.45274699049436,-0.556305327441571,
4.83618164536551));
#283883=CARTESIAN_POINT('Ctrl Pts',(-1.45950752898951,-0.538318820045125,
4.83484096630898));
#283884=CARTESIAN_POINT('Ctrl Pts',(-1.46959444259906,-0.509894392674305,
4.83271900722765));
#283885=CARTESIAN_POINT('Ctrl Pts',(-1.47314683743284,-0.499538288553856,
4.83194523389503));
#283886=CARTESIAN_POINT('Ctrl Pts',(-1.47959446841543,-0.480074756832254,
4.83048929757246));
#283887=CARTESIAN_POINT('Ctrl Pts',(-1.48251568695909,-0.470976425674157,
4.82980802932932));
#283888=CARTESIAN_POINT('Ctrl Pts',(-1.48888762285446,-0.450483769486474,
4.82827174048569));
#283889=CARTESIAN_POINT('Ctrl Pts',(-1.49229169359224,-0.439075695804738,
4.82741523826182));
#283890=CARTESIAN_POINT('Ctrl Pts',(-1.50069922795543,-0.409671748049369,
4.82520385673177));
#283891=CARTESIAN_POINT('Ctrl Pts',(-1.50550997191583,-0.391623265476998,
4.82384286320593));
#283892=CARTESIAN_POINT('Ctrl Pts',(-1.54033097574258,-0.250845564800252,
4.81319509430448));
#283893=CARTESIAN_POINT('Ctrl Pts',(-1.55560595750119,-0.12498128167098,
4.80342941955489));
#283894=CARTESIAN_POINT('Ctrl Pts',(-1.55543470816142,0.0780745858892366,
4.78768878259148));
#283895=CARTESIAN_POINT('Ctrl Pts',(-1.54968774875899,0.154736691934658,
4.78176471616885));
#283896=CARTESIAN_POINT('Ctrl Pts',(-1.53663215718487,0.241802853964703,
4.77525159579969));
#283897=CARTESIAN_POINT('Ctrl Pts',(-1.53484169064513,0.252918980925539,
4.77442421834414));
#283898=CARTESIAN_POINT('Ctrl Pts',(-1.53186354482938,0.270210759887601,
4.77314470448401));
#283899=CARTESIAN_POINT('Ctrl Pts',(-1.53075889692148,0.276400032510002,
4.77268823360414));
#283900=CARTESIAN_POINT('Ctrl Pts',(-1.52873363468571,0.287362756983758,
4.77188258784134));
#283901=CARTESIAN_POINT('Ctrl Pts',(-1.5278281586583,0.292138663432025,
4.77153259774745));
#283902=CARTESIAN_POINT('Ctrl Pts',(-1.52558567963406,0.303670900382418,
4.77068979992706));
#283903=CARTESIAN_POINT('Ctrl Pts',(-1.52422617478093,0.310422703041895,
4.77019826598363));
#283904=CARTESIAN_POINT('Ctrl Pts',(-1.51984816121821,0.331443073329807,
4.76867326667872));
#283905=CARTESIAN_POINT('Ctrl Pts',(-1.51667369580976,0.345678875258279,
4.76764809961364));
#283906=CARTESIAN_POINT('Ctrl Pts',(-1.49888426204093,0.420486010195662,
4.76229100936725));
#283907=CARTESIAN_POINT('Ctrl Pts',(-1.48083821774806,0.480190112556536,
4.75811859777211));
#283908=CARTESIAN_POINT('Ctrl Pts',(-1.42100032455901,0.642294885730506,
4.74667672843741));
#283909=CARTESIAN_POINT('Ctrl Pts',(-1.37181519404658,0.741556960023045,
4.73951771499704));
#283910=CARTESIAN_POINT('Ctrl Pts',(-1.29255650026169,0.866177413175332,
4.72950071279298));
#283911=CARTESIAN_POINT('Ctrl Pts',(-1.27146247963229,0.896854733330727,
4.72694455947008));
#283912=CARTESIAN_POINT('Ctrl Pts',(-1.24068543774466,0.938343474394788,
4.72333955694567));
#283913=CARTESIAN_POINT('Ctrl Pts',(-1.23192003715069,0.94982199844864,
4.72232574936717));
#283914=CARTESIAN_POINT('Ctrl Pts',(-1.21746455214268,0.968215088153344,
4.72067334693005));
#283915=CARTESIAN_POINT('Ctrl Pts',(-1.21187221873962,0.975205676774685,
4.72003863991375));
#283916=CARTESIAN_POINT('Ctrl Pts',(-1.20003156996824,0.989747715803581,
4.71870394431058));
#283917=CARTESIAN_POINT('Ctrl Pts',(-1.19377162032332,0.997289135733643,
4.71800350446682));
#283918=CARTESIAN_POINT('Ctrl Pts',(-1.17860989500708,1.0152073063702,4.71631898332029));
#283919=CARTESIAN_POINT('Ctrl Pts',(-1.16964190173228,1.02552667396715,
4.71533221132934));
#283920=CARTESIAN_POINT('Ctrl Pts',(-1.1375830092729,1.06144891412006,4.71183696922541));
#283921=CARTESIAN_POINT('Ctrl Pts',(-1.11377967751207,1.08639927457709,
4.70929894684318));
#283922=CARTESIAN_POINT('Ctrl Pts',(-1.05180330860477,1.14718316029612,
4.70282489201629));
#283923=CARTESIAN_POINT('Ctrl Pts',(-1.01261569743052,1.18191703685438,
4.69884912782438));
#283924=CARTESIAN_POINT('Ctrl Pts',(-0.930800458297922,1.24737394213607,
4.69079606667584));
#283925=CARTESIAN_POINT('Ctrl Pts',(-0.888215171316857,1.27804723004451,
4.68672359706146));
#283926=CARTESIAN_POINT('Ctrl Pts',(-0.783849061468839,1.34548037621719,
4.6770905589045));
#283927=CARTESIAN_POINT('Ctrl Pts',(-0.720901861033794,1.3802316567811,
4.67154484035654));
#283928=CARTESIAN_POINT('Ctrl Pts',(-0.642150315273902,1.41684469961363,
4.66507742698801));
#283929=CARTESIAN_POINT('Ctrl Pts',(-0.628436209930061,1.42298064100923,
4.66396780404464));
#283930=CARTESIAN_POINT('Ctrl Pts',(-0.608233146093668,1.43167079038411,
4.66235953953423));
#283931=CARTESIAN_POINT('Ctrl Pts',(-0.601812992457291,1.43438137856049,
4.66185231776431));
#283932=CARTESIAN_POINT('Ctrl Pts',(-0.590402243656272,1.43910889433745,
4.66095790023241));
#283933=CARTESIAN_POINT('Ctrl Pts',(-0.585419140956528,1.44114317525696,
4.66056969997619));
#283934=CARTESIAN_POINT('Ctrl Pts',(-0.574439705093223,1.44555902622311,
4.65971964110002));
#283935=CARTESIAN_POINT('Ctrl Pts',(-0.568439022966637,1.44792919517864,
4.65925845655269));
#283936=CARTESIAN_POINT('Ctrl Pts',(-0.550893031848742,1.45473367588362,
4.65791936863506));
#283937=CARTESIAN_POINT('Ctrl Pts',(-0.539309042475031,1.45906784705516,
4.65704712436573));
#283938=CARTESIAN_POINT('Ctrl Pts',(-0.512485318052329,1.46874087204005,
4.65505177915966));
#283939=CARTESIAN_POINT('Ctrl Pts',(-0.497211466504593,1.47398159931793,
4.65393356224901));
#283940=CARTESIAN_POINT('Ctrl Pts',(-0.444300682815755,1.49122011826231,
4.65011241441144));
#283941=CARTESIAN_POINT('Ctrl Pts',(-0.406287976774585,1.50202232703985,
4.64745771620777));
#283942=CARTESIAN_POINT('Ctrl Pts',(-0.273333380629268,1.53438665325644,
4.63835391132833));
#283943=CARTESIAN_POINT('Ctrl Pts',(-0.176812993004962,1.54848027342748,
4.63204643070765));
#283944=CARTESIAN_POINT('Ctrl Pts',(-0.0237677265155158,1.55632310336705,
4.62180040172741));
#283945=CARTESIAN_POINT('Ctrl Pts',(0.0321798644021726,1.55617154356592,
4.61800696576614));
#283946=CARTESIAN_POINT('Ctrl Pts',(0.10457807900179,1.55206945897277,4.6129654880601));
#283947=CARTESIAN_POINT('Ctrl Pts',(0.121145923620136,1.55086421332858,
4.61180290187226));
#283948=CARTESIAN_POINT('Ctrl Pts',(0.148044719438292,1.54847378486338,
4.60989933189722));
#283949=CARTESIAN_POINT('Ctrl Pts',(0.158388973653528,1.54744991030415,
4.60916342418869));
#283950=CARTESIAN_POINT('Ctrl Pts',(0.17834423159108,1.54527255697801,4.60773591406529));
#283951=CARTESIAN_POINT('Ctrl Pts',(0.187956282181184,1.54413288562611,
4.60704477823766));
#283952=CARTESIAN_POINT('Ctrl Pts',(0.210394636875548,1.54125982785101,
4.60542281116796));
#283953=CARTESIAN_POINT('Ctrl Pts',(0.223211011486352,1.53945593820858,
4.6044897979831));
#283954=CARTESIAN_POINT('Ctrl Pts',(0.265448718359745,1.53297250649127,
4.60139237091659));
#283955=CARTESIAN_POINT('Ctrl Pts',(0.294756472059076,1.52760797470071,
4.59920667574173));
#283956=CARTESIAN_POINT('Ctrl Pts',(0.365430026832402,1.51256236013031,
4.59384357630822));
#283957=CARTESIAN_POINT('Ctrl Pts',(0.406586544321402,1.50202224198938,
4.59064206042419));
#283958=CARTESIAN_POINT('Ctrl Pts',(0.509876328326764,1.47101357215525,
4.58241568951463));
#283959=CARTESIAN_POINT('Ctrl Pts',(0.571244482837634,1.44828642560361,
4.57734486681293));
#283960=CARTESIAN_POINT('Ctrl Pts',(0.646819371954475,1.41474542474863,
4.57093298301966));
#283961=CARTESIAN_POINT('Ctrl Pts',(0.662523777127389,1.40745947407142,
4.5695913439259));
#283962=CARTESIAN_POINT('Ctrl Pts',(0.735711945631024,1.37200787689559,
4.56330237734785));
#283963=CARTESIAN_POINT('Ctrl Pts',(0.791550219056662,1.34056998133494,
4.55839487213495));
#283964=CARTESIAN_POINT('Ctrl Pts',(0.854636903523957,1.29973065930059,
4.5528367330824));
#283965=CARTESIAN_POINT('Ctrl Pts',(0.863911401415862,1.29358460605336,
4.55201932980882));
#283966=CARTESIAN_POINT('Ctrl Pts',(0.878297931622041,1.28382714759781,
4.55075188222789));
#283967=CARTESIAN_POINT('Ctrl Pts',(0.88345524118723,1.2802836568938,4.55029762802103));
#283968=CARTESIAN_POINT('Ctrl Pts',(0.892584828102444,1.27392945265123,
4.54949387828092));
#283969=CARTESIAN_POINT('Ctrl Pts',(0.896565355039005,1.27113118556369,
4.54914358984694));
#283970=CARTESIAN_POINT('Ctrl Pts',(0.906183280616655,1.26430223233624,
4.54829748239341));
#283971=CARTESIAN_POINT('Ctrl Pts',(0.911806966798369,1.26025248777772,
4.54780296585339));
#283972=CARTESIAN_POINT('Ctrl Pts',(0.929366015300521,1.24742874977715,
4.5462589222856));
#283973=CARTESIAN_POINT('Ctrl Pts',(0.941203658042819,1.23852145415787,
4.54521799223183));
#283974=CARTESIAN_POINT('Ctrl Pts',(1.00389023439881,1.18993465799148,4.53969479933298));
#283975=CARTESIAN_POINT('Ctrl Pts',(1.05236732174618,1.14728598289085,4.5353831657249));
#283976=CARTESIAN_POINT('Ctrl Pts',(1.18083093400292,1.01925197264863,4.52338510029554));
#283977=CARTESIAN_POINT('Ctrl Pts',(1.25403558792925,0.927701089906904,
4.51581133747605));
#283978=CARTESIAN_POINT('Ctrl Pts',(1.33261993648512,0.802896461201215,
4.50574488679024));
#283979=CARTESIAN_POINT('Ctrl Pts',(1.34817177344538,0.776499374406902,
4.50363104306515));
#283980=CARTESIAN_POINT('Ctrl Pts',(1.36877501188676,0.739041362634915,
4.50064194397133));
#283981=CARTESIAN_POINT('Ctrl Pts',(1.37449215557495,0.728353258005944,
4.4997902313057));
#283982=CARTESIAN_POINT('Ctrl Pts',(1.38421399716041,0.709656267277678,
4.49830172602355));
#283983=CARTESIAN_POINT('Ctrl Pts',(1.38827558822821,0.701677484791947,
4.49766696275442));
#283984=CARTESIAN_POINT('Ctrl Pts',(1.39663835865834,0.684892393266995,
4.49633226663884));
#283985=CARTESIAN_POINT('Ctrl Pts',(1.40092562704583,0.676079636286962,
4.49563188342889));
#283986=CARTESIAN_POINT('Ctrl Pts',(1.41099180135527,0.654881044255915,
4.49394772327396));
#283987=CARTESIAN_POINT('Ctrl Pts',(1.41669120541793,0.642458599381583,
4.49296125860456));
#283988=CARTESIAN_POINT('Ctrl Pts',(1.43617727533931,0.598466183395161,
4.48946841393429));
#283989=CARTESIAN_POINT('Ctrl Pts',(1.44907729178986,0.566517074492903,
4.48693253584653));
#283990=CARTESIAN_POINT('Ctrl Pts',(1.47885634310482,0.485073881899158,
4.48046552248606));
#283991=CARTESIAN_POINT('Ctrl Pts',(1.49431945571595,0.435110504478843,
4.47649476903844));
#283992=CARTESIAN_POINT('Ctrl Pts',(1.52040815298188,0.332834474915104,
4.46838259730061));
#283993=CARTESIAN_POINT('Ctrl Pts',(1.53091660082822,0.28055972034888,4.46424454314681));
#283994=CARTESIAN_POINT('Ctrl Pts',(1.54998633850925,0.151778018880049,
4.45415253507051));
#283995=CARTESIAN_POINT('Ctrl Pts',(1.55559546020059,0.074965192388891,
4.4482172689654));
#283996=CARTESIAN_POINT('Ctrl Pts',(1.55548461436945,-0.0132175837387635,
4.441693498677));
#283997=CARTESIAN_POINT('Ctrl Pts',(1.55534814308589,-0.0244798580928371,
4.44086584409795));
#283998=CARTESIAN_POINT('Ctrl Pts',(1.55494488341441,-0.0420261186706838,
4.43958599514133));
#283999=CARTESIAN_POINT('Ctrl Pts',(1.55476229708408,-0.048311369406584,
4.43912946280605));
#284000=CARTESIAN_POINT('Ctrl Pts',(1.55437098798986,-0.0594534306405277,
4.43832376399081));
#284001=CARTESIAN_POINT('Ctrl Pts',(1.55417761105585,-0.0643104435871024,
4.43797378168285));
#284002=CARTESIAN_POINT('Ctrl Pts',(1.55365527217932,-0.0760457813590657,
4.43713107346905));
#284003=CARTESIAN_POINT('Ctrl Pts',(1.55330340146001,-0.0829229368217237,
4.43663962056638));
#284004=CARTESIAN_POINT('Ctrl Pts',(1.55206429760475,-0.104351231650944,
4.43511513660698));
#284005=CARTESIAN_POINT('Ctrl Pts',(1.55101814343185,-0.118892903437067,
4.43409039583858));
#284006=CARTESIAN_POINT('Ctrl Pts',(1.54442838942697,-0.195438475024123,
4.42873774019216));
#284007=CARTESIAN_POINT('Ctrl Pts',(1.53537028147,-0.257089863315302,4.42456904527261));
#284008=CARTESIAN_POINT('Ctrl Pts',(1.50008630229764,-0.426015087996794,
4.41314179106502));
#284009=CARTESIAN_POINT('Ctrl Pts',(1.46611335116958,-0.531279998529964,
4.40599359212514));
#284010=CARTESIAN_POINT('Ctrl Pts',(1.40609737281374,-0.666234863082336,
4.39597761722625));
#284011=CARTESIAN_POINT('Ctrl Pts',(1.38967564211849,-0.699842805111789,
4.39340973176953));
#284012=CARTESIAN_POINT('Ctrl Pts',(1.3652437621685,-0.745586380482985,
4.38979084911775));
#284013=CARTESIAN_POINT('Ctrl Pts',(1.35824998157003,-0.758252295503872,
4.38877526115647));
#284014=CARTESIAN_POINT('Ctrl Pts',(1.34664224445713,-0.778598189148943,
4.38712075006774));
#284015=CARTESIAN_POINT('Ctrl Pts',(1.34213671889124,-0.786339301073113,
4.3864857347491));
#284016=CARTESIAN_POINT('Ctrl Pts',(1.33256359596594,-0.802465259621048,
4.38515103450201));
#284017=CARTESIAN_POINT('Ctrl Pts',(1.32748314939306,-0.810841976073724,
4.38445090319791));
#284018=CARTESIAN_POINT('Ctrl Pts',(1.31513619994485,-0.8307727211485,4.38276835089282));
#284019=CARTESIAN_POINT('Ctrl Pts',(1.30779620016053,-0.842280010065659,
4.38178325536281));
#284020=CARTESIAN_POINT('Ctrl Pts',(1.28146944860901,-0.88237990110766,
4.37830107286448));
#284021=CARTESIAN_POINT('Ctrl Pts',(1.2616900172202,-0.910437365310724,
4.37577472813087));
#284022=CARTESIAN_POINT('Ctrl Pts',(1.20965453380994,-0.979295287330299,
4.36933897560383));
#284023=CARTESIAN_POINT('Ctrl Pts',(1.17625191142208,-1.01917311450902,
4.36539045152064));
#284024=CARTESIAN_POINT('Ctrl Pts',(1.10256354103288,-1.09868922755383,
4.35706004555156));
#284025=CARTESIAN_POINT('Ctrl Pts',(1.06198568596299,-1.13795887084703,
4.3526756896223));
#284026=CARTESIAN_POINT('Ctrl Pts',(0.96323964097279,-1.22363023401444,
4.34254483831109));
#284027=CARTESIAN_POINT('Ctrl Pts',(0.903689484415122,-1.26824662566834,
4.33681767072797));
#284028=CARTESIAN_POINT('Ctrl Pts',(0.831741632032371,-1.3145005784754,
4.3304906127914));
#284029=CARTESIAN_POINT('Ctrl Pts',(0.822246535638912,-1.32046074051187,
4.32966687773631));
#284030=CARTESIAN_POINT('Ctrl Pts',(0.807336141228614,-1.32959692896331,
4.32839176902863));
#284031=CARTESIAN_POINT('Ctrl Pts',(0.801964884730938,-1.3328435638973,
4.3279361065657));
#284032=CARTESIAN_POINT('Ctrl Pts',(0.792397286878072,-1.33854788326975,
4.327131156268));
#284033=CARTESIAN_POINT('Ctrl Pts',(0.788209011774074,-1.34101843795417,
4.3267810613468));
#284034=CARTESIAN_POINT('Ctrl Pts',(0.778047435383273,-1.34694843346628,
4.32593707413112));
#284035=CARTESIAN_POINT('Ctrl Pts',(0.77206259851507,-1.35038781205101,
4.32544446595661));
#284036=CARTESIAN_POINT('Ctrl Pts',(0.753290529527033,-1.36101018635478,
4.32391262502627));
#284037=CARTESIAN_POINT('Ctrl Pts',(0.740424020960603,-1.36805250608677,
4.32288179725083));
#284038=CARTESIAN_POINT('Ctrl Pts',(0.671696510136271,-1.40441589329085,
4.31746553649999));
#284039=CARTESIAN_POINT('Ctrl Pts',(0.614183538120879,-1.43050365102664,
4.31324353211598));
#284040=CARTESIAN_POINT('Ctrl Pts',(0.449946670513132,-1.49326268362635,
4.30160561228447));
#284041=CARTESIAN_POINT('Ctrl Pts',(0.340600440525213,-1.52193152330799,
4.29430114203787));
#284042=CARTESIAN_POINT('Ctrl Pts',(0.19466370851215,-1.54366437774777,
4.28427200773025));
#284043=CARTESIAN_POINT('Ctrl Pts',(0.160049236145983,-1.5476361351099,
4.28187573887825));
#284044=CARTESIAN_POINT('Ctrl Pts',(0.111264604276624,-1.55157972466035,
4.27845801689116));
#284045=CARTESIAN_POINT('Ctrl Pts',(0.0971821213163001,-1.55252538347587,
4.27746676305576));
#284046=CARTESIAN_POINT('Ctrl Pts',(0.0733188511735155,-1.55380189449793,
4.27577817582622));
#284047=CARTESIAN_POINT('Ctrl Pts',(0.063544078102719,-1.55423232608985,
4.27508398960464));
#284048=CARTESIAN_POINT('Ctrl Pts',(0.0437556836804373,-1.55491672392505,
4.27367324633951));
#284049=CARTESIAN_POINT('Ctrl Pts',(0.0337423842981061,-1.55516623581518,
4.27295658361185));
#284050=CARTESIAN_POINT('Ctrl Pts',(0.00893333831269328,-1.55554471687107,
4.27117368451881));
#284051=CARTESIAN_POINT('Ctrl Pts',(-0.00586288286008003,-1.55555931072095,
4.27010392993936));
#284052=CARTESIAN_POINT('Ctrl Pts',(-0.0636815657953153,-1.5547914273841,
4.26589722066373));
#284053=CARTESIAN_POINT('Ctrl Pts',(-0.106660067298875,-1.55243508516749,
4.2627122282642));
#284054=CARTESIAN_POINT('Ctrl Pts',(-0.223262499703083,-1.54117760251042,
4.25390780083761));
#284055=CARTESIAN_POINT('Ctrl Pts',(-0.296431787630441,-1.52879055183406,
4.24819956395364));
#284056=CARTESIAN_POINT('Ctrl Pts',(-0.457770527266698,-1.489457014717,
4.23532677917162));
#284057=CARTESIAN_POINT('Ctrl Pts',(-0.545009895248322,-1.45979564473976,
4.22816388178082));
#284058=CARTESIAN_POINT('Ctrl Pts',(-0.642344017658711,-1.41675098988497,
4.22024337093766));
#284059=CARTESIAN_POINT('Ctrl Pts',(-0.655482707524068,-1.41072026433852,
4.21917608446682));
#284060=CARTESIAN_POINT('Ctrl Pts',(-0.674821472912216,-1.40151513998986,
4.21760990985733));
#284061=CARTESIAN_POINT('Ctrl Pts',(-0.681086930064984,-1.39848107123724,
4.21710324422117));
#284062=CARTESIAN_POINT('Ctrl Pts',(-0.692159857057123,-1.39302690067074,
4.21620942126707));
#284063=CARTESIAN_POINT('Ctrl Pts',(-0.696975383947429,-1.3906237920375,
4.21582126475855));
#284064=CARTESIAN_POINT('Ctrl Pts',(-0.707541417526832,-1.38528231419232,
4.21497084359791));
#284065=CARTESIAN_POINT('Ctrl Pts',(-0.713286189218603,-1.3823330871426,
4.21450925731602));
#284066=CARTESIAN_POINT('Ctrl Pts',(-0.73000429054705,-1.37361844510649,
4.21316779226677));
#284067=CARTESIAN_POINT('Ctrl Pts',(-0.740927591673059,-1.36775737114848,
4.21229360323874));
#284068=CARTESIAN_POINT('Ctrl Pts',(-0.765957179094942,-1.3539394725189,
4.21029306445964));
#284069=CARTESIAN_POINT('Ctrl Pts',(-0.78001180952454,-1.34589157065514,
4.20917163470705));
#284070=CARTESIAN_POINT('Ctrl Pts',(-0.828063660513498,-1.31737070606209,
4.20533504707773));
#284071=CARTESIAN_POINT('Ctrl Pts',(-0.86140348088047,-1.29581615369214,
4.20266854238898));
#284072=CARTESIAN_POINT('Ctrl Pts',(-0.973731308771008,-1.21694149295012,
4.19353831862755));
#284073=CARTESIAN_POINT('Ctrl Pts',(-1.04812538270314,-1.1534872636348,
4.18721573433572));
#284074=CARTESIAN_POINT('Ctrl Pts',(-1.15473183470917,-1.04367278586619,
4.17698003211608));
#284075=CARTESIAN_POINT('Ctrl Pts',(-1.19121625059556,-1.00182896218303,
4.17321484360926));
#284076=CARTESIAN_POINT('Ctrl Pts',(-1.23559210044131,-0.945075131502092,
4.16820579803392));
#284077=CARTESIAN_POINT('Ctrl Pts',(-1.24558950565337,-0.931859211164798,
4.16704597325141));
#284078=CARTESIAN_POINT('Ctrl Pts',(-1.26150635746857,-0.910104298016887,
4.16514578395686));
#284079=CARTESIAN_POINT('Ctrl Pts',(-1.26755492288166,-0.901661040089997,
4.1644104608806));
#284080=CARTESIAN_POINT('Ctrl Pts',(-1.2790780776537,-0.885230633991515,
4.16298328801776));
#284081=CARTESIAN_POINT('Ctrl Pts',(-1.28456354424657,-0.877251672593394,
4.16229189751894));
#284082=CARTESIAN_POINT('Ctrl Pts',(-1.29721848882559,-0.858471031199396,
4.16066809946631));
#284083=CARTESIAN_POINT('Ctrl Pts',(-1.30432802803756,-0.847630046365558,
4.15973349516718));
#284084=CARTESIAN_POINT('Ctrl Pts',(-1.32739575439279,-0.811477698157759,
4.15662487147019));
#284085=CARTESIAN_POINT('Ctrl Pts',(-1.3427582095641,-0.785796223939521,
4.15442935754016));
#284086=CARTESIAN_POINT('Ctrl Pts',(-1.41963045210483,-0.648445274079435,
4.14274517768156));
#284087=CARTESIAN_POINT('Ctrl Pts',(-1.46797072736294,-0.52998375989957,
4.1328079311325));
#284088=CARTESIAN_POINT('Ctrl Pts',(-1.51438303316102,-0.358774672734246,
4.11909872449242));
#284089=CARTESIAN_POINT('Ctrl Pts',(-1.52512344569801,-0.309958979350414,
4.11526721089691));
#284090=CARTESIAN_POINT('Ctrl Pts',(-1.53660480328221,-0.242424902474009,
4.11013593563019));
#284091=CARTESIAN_POINT('Ctrl Pts',(-1.53938594642668,-0.224087354409639,
4.10875963379184));
#284092=CARTESIAN_POINT('Ctrl Pts',(-1.54276828708144,-0.198735207534343,
4.10688406701267));
#284093=CARTESIAN_POINT('Ctrl Pts',(-1.54365072219694,-0.191760588309655,
4.10637090949911));
#284094=CARTESIAN_POINT('Ctrl Pts',(-1.54508557325774,-0.179767371657291,
4.10549363458369));
#284095=CARTESIAN_POINT('Ctrl Pts',(-1.54566088781971,-0.174751705128819,
4.10512828784796));
#284096=CARTESIAN_POINT('Ctrl Pts',(-1.54676072045196,-0.164732605284701,
4.10440167023776));
#284097=CARTESIAN_POINT('Ctrl Pts',(-1.54728540311942,-0.159729272273086,
4.10404040022286));
#284098=CARTESIAN_POINT('Ctrl Pts',(-1.54834500636688,-0.149129461051616,
4.10327822400533));
#284099=CARTESIAN_POINT('Ctrl Pts',(-1.54887388244373,-0.143532413621816,
4.1028776514708));
#284100=CARTESIAN_POINT('Ctrl Pts',(-1.55007154318263,-0.130079294145007,
4.1019190803938));
#284101=CARTESIAN_POINT('Ctrl Pts',(-1.55071097441446,-0.122220669987757,
4.10136260885961));
#284102=CARTESIAN_POINT('Ctrl Pts',(-1.55407073087199,-0.0766445852303563,
4.09815370387891));
#284103=CARTESIAN_POINT('Ctrl Pts',(-1.55547489607258,-0.0388398935252902,
4.09556465134092));
#284104=CARTESIAN_POINT('Ctrl Pts',(-1.55549966639403,-0.00101874828225496,
4.09301352418007));
#284105=CARTESIAN_POINT('',(-1.55331871380611,-0.000780328647907862,3.39405694879054));
#284106=CARTESIAN_POINT('Ctrl Pts',(-1.55331871380611,-0.000780328647907862,
3.39405694879054));
#284107=CARTESIAN_POINT('Ctrl Pts',(-1.55425844430069,-0.210990804352394,
3.40906388991245));
#284108=CARTESIAN_POINT('Ctrl Pts',(-1.41654551139588,-0.939168704500731,
3.4611329709781));
#284109=CARTESIAN_POINT('Ctrl Pts',(-0.308692884081366,-1.81269447386996,
3.55026419198746));
#284110=CARTESIAN_POINT('Ctrl Pts',(1.35606994996762,-1.24186426112907,
3.66145061181863));
#284111=CARTESIAN_POINT('Ctrl Pts',(1.77861387826841,0.466567491694538,
3.77263703164979));
#284112=CARTESIAN_POINT('Ctrl Pts',(0.571870330903418,1.74760318061885,
3.88382345148095));
#284113=CARTESIAN_POINT('Ctrl Pts',(-1.09574000028678,1.43940039381927,
3.99096285577571));
#284114=CARTESIAN_POINT('Ctrl Pts',(-1.55401186045024,0.458497813133281,
4.06104012012673));
#284115=CARTESIAN_POINT('Ctrl Pts',(-1.55731595967384,-0.000935870630138446,
4.09405524453403));
#284116=CARTESIAN_POINT('',(-1.5555004206443,-7.0880047456861E-5,1.99259207059789));
#284117=CARTESIAN_POINT('Ctrl Pts',(-1.55549984885979,-0.000685709247415389,
3.39531142154411));
#284118=CARTESIAN_POINT('Ctrl Pts',(-1.5555077357725,0.0172053890135179,
3.39408737174109));
#284119=CARTESIAN_POINT('Ctrl Pts',(-1.55520695194502,0.0350947961981444,
3.39285526377583));
#284120=CARTESIAN_POINT('Ctrl Pts',(-1.55410834920964,0.0673345056559161,
3.39061728115537));
#284121=CARTESIAN_POINT('Ctrl Pts',(-1.55342009261955,0.0816865283590325,
3.3896147425859));
#284122=CARTESIAN_POINT('Ctrl Pts',(-1.55194765173723,0.105492581273357,
3.38794029322772));
#284123=CARTESIAN_POINT('Ctrl Pts',(-1.55127561405159,0.114952862421567,
3.38727186188798));
#284124=CARTESIAN_POINT('Ctrl Pts',(-1.54978728902936,0.133502364051424,
3.38595496162361));
#284125=CARTESIAN_POINT('Ctrl Pts',(-1.5489774419519,0.142591725889808,
3.38530671933281));
#284126=CARTESIAN_POINT('Ctrl Pts',(-1.54708650425045,0.161892012093361,
3.3839236964601));
#284127=CARTESIAN_POINT('Ctrl Pts',(-1.5459841945952,0.172100365817622,
3.38318827863173));
#284128=CARTESIAN_POINT('Ctrl Pts',(-1.54290446737667,0.198197932717347,
3.38129779779555));
#284129=CARTESIAN_POINT('Ctrl Pts',(-1.5407826724218,0.214068532688995,
3.38013825332279));
#284130=CARTESIAN_POINT('Ctrl Pts',(-1.5309765050801,0.279687368293068,
3.37530117728549));
#284131=CARTESIAN_POINT('Ctrl Pts',(-1.52112534256817,0.329075583013826,
3.37155682340179));
#284132=CARTESIAN_POINT('Ctrl Pts',(-1.4780791946597,0.500954882524119,
3.35815488130927));
#284133=CARTESIAN_POINT('Ctrl Pts',(-1.43232654386424,0.61976506444484,
3.34816705783662));
#284134=CARTESIAN_POINT('Ctrl Pts',(-1.35493077184496,0.764960077943228,
3.33560746827639));
#284135=CARTESIAN_POINT('Ctrl Pts',(-1.33599318579173,0.797573866895534,
3.33276516987259));
#284136=CARTESIAN_POINT('Ctrl Pts',(-1.31070573240019,0.837690369230111,
3.32926984236883));
#284137=CARTESIAN_POINT('Ctrl Pts',(-1.30544700914496,0.84586215831427,
3.32855790040048));
#284138=CARTESIAN_POINT('Ctrl Pts',(-1.29688058081125,0.858903749159421,
3.32742245103605));
#284139=CARTESIAN_POINT('Ctrl Pts',(-1.2936213197627,0.863804824812217,
3.32699591985836));
#284140=CARTESIAN_POINT('Ctrl Pts',(-1.28727696957423,0.873228620293653,
3.32617630295604));
#284141=CARTESIAN_POINT('Ctrl Pts',(-1.28419572108313,0.877753707409507,
3.32578299257696));
#284142=CARTESIAN_POINT('Ctrl Pts',(-1.27726305247355,0.887820299455287,
3.32490837618776));
#284143=CARTESIAN_POINT('Ctrl Pts',(-1.27339927968535,0.893353271823013,
3.32442788908106));
#284144=CARTESIAN_POINT('Ctrl Pts',(-1.25987182350577,0.912458670892332,
3.3227689086591));
#284145=CARTESIAN_POINT('Ctrl Pts',(-1.25002576769631,0.925901439743128,
3.32160188723255));
#284146=CARTESIAN_POINT('Ctrl Pts',(-1.16876716536299,1.0331837407003,3.31226688519429));
#284147=CARTESIAN_POINT('Ctrl Pts',(-1.08710138384595,1.11879571183531,
3.30466126401129));
#284148=CARTESIAN_POINT('Ctrl Pts',(-0.954699006467354,1.22926745527058,
3.29326694676563));
#284149=CARTESIAN_POINT('Ctrl Pts',(-0.911063097020174,1.26194769863122,
3.28963884513134));
#284150=CARTESIAN_POINT('Ctrl Pts',(-0.845813540617006,1.30566411336301,
3.2842997247697));
#284151=CARTESIAN_POINT('Ctrl Pts',(-0.825514625594606,1.3185919866123,
3.2826502510854));
#284152=CARTESIAN_POINT('Ctrl Pts',(-0.788293211595726,1.34110097706447,
3.27963898522203));
#284153=CARTESIAN_POINT('Ctrl Pts',(-0.771475211539229,1.35084564538847,
3.2782831394788));
#284154=CARTESIAN_POINT('Ctrl Pts',(-0.744864579569112,1.36560532348347,
3.27614258959337));
#284155=CARTESIAN_POINT('Ctrl Pts',(-0.735193438539752,1.37083614563701,
3.27536561744406));
#284156=CARTESIAN_POINT('Ctrl Pts',(-0.717019110824374,1.38041843997527,
3.27390685339807));
#284157=CARTESIAN_POINT('Ctrl Pts',(-0.708529673797578,1.38479499153461,
3.2732259897987));
#284158=CARTESIAN_POINT('Ctrl Pts',(-0.689426921675288,1.39442137276481,
3.27169483030861));
#284159=CARTESIAN_POINT('Ctrl Pts',(-0.678792987559742,1.39962870461525,
3.27084309613251));
#284160=CARTESIAN_POINT('Ctrl Pts',(-0.647451473830296,1.41453515094935,
3.26833396158715));
#284161=CARTESIAN_POINT('Ctrl Pts',(-0.626589068691735,1.42389927317071,
3.26666522174483));
#284162=CARTESIAN_POINT('Ctrl Pts',(-0.47704514450221,1.48709942448545,
3.25470739460431));
#284163=CARTESIAN_POINT('Ctrl Pts',(-0.341861119003655,1.52386084678205,
3.24383361008517));
#284164=CARTESIAN_POINT('Ctrl Pts',(-0.162917856204241,1.54748974369895,
3.22989149622495));
#284165=CARTESIAN_POINT('Ctrl Pts',(-0.122004647536606,1.55125177025516,
3.22674017747705));
#284166=CARTESIAN_POINT('Ctrl Pts',(-0.0644585428165128,1.55425201036867,
3.22239485025482));
#284167=CARTESIAN_POINT('Ctrl Pts',(-0.0479156046288272,1.55484994813515,
3.221155811736));
#284168=CARTESIAN_POINT('Ctrl Pts',(-0.0187626979887062,1.55543791491242,
3.21899352337906));
#284169=CARTESIAN_POINT('Ctrl Pts',(-0.00615669853451052,1.55553889957576,
3.21806551281425));
#284170=CARTESIAN_POINT('Ctrl Pts',(0.0129498160357867,1.55545967643265,
3.21667088918707));
#284171=CARTESIAN_POINT('Ctrl Pts',(0.0194498973300509,1.55539197900284,
3.21619852859483));
#284172=CARTESIAN_POINT('Ctrl Pts',(0.0313273775501246,1.55519380619296,
3.21533944719597));
#284173=CARTESIAN_POINT('Ctrl Pts',(0.0367046324515826,1.55507618824834,
3.21495206074781));
#284174=CARTESIAN_POINT('Ctrl Pts',(0.0489860842457927,1.55474381249586,
3.21407073633723));
#284175=CARTESIAN_POINT('Ctrl Pts',(0.055889576398885,1.55451095816053,
3.21357780092795));
#284176=CARTESIAN_POINT('Ctrl Pts',(0.0774708550021125,1.55363906776375,
3.21204387199123));
#284177=CARTESIAN_POINT('Ctrl Pts',(0.092141811009324,1.55283805147473,
3.21101131614066));
#284178=CARTESIAN_POINT('Ctrl Pts',(0.199493253137341,1.54544991648361,
3.20351604297488));
#284179=CARTESIAN_POINT('Ctrl Pts',(0.291442398205,1.53077733632387,3.19741820744105));
#284180=CARTESIAN_POINT('Ctrl Pts',(0.475133818724348,1.48430058569984,
3.18494937272082));
#284181=CARTESIAN_POINT('Ctrl Pts',(0.566307245292282,1.45196201879497,
3.17859810409414));
#284182=CARTESIAN_POINT('Ctrl Pts',(0.677369819467039,1.40050704327046,
3.17019387149855));
#284183=CARTESIAN_POINT('Ctrl Pts',(0.700572678976904,1.38904558568149,
3.168399869624));
#284184=CARTESIAN_POINT('Ctrl Pts',(0.734333446113561,1.37130777567308,
3.16572629846264));
#284185=CARTESIAN_POINT('Ctrl Pts',(0.745120997255188,1.36547622088822,
3.16486226758082));
#284186=CARTESIAN_POINT('Ctrl Pts',(0.764219184268598,1.35485838378746,
3.16331448402803));
#284187=CARTESIAN_POINT('Ctrl Pts',(0.772556723442959,1.35012158832192,
3.16263252609911));
#284188=CARTESIAN_POINT('Ctrl Pts',(0.790121664149505,1.33992646662185,
3.16118220624798));
#284189=CARTESIAN_POINT('Ctrl Pts',(0.799337457735834,1.33444924897875,
3.16041318603725));
#284190=CARTESIAN_POINT('Ctrl Pts',(0.823991568008839,1.31944956363078,
3.1583335729272));
#284191=CARTESIAN_POINT('Ctrl Pts',(0.839320718820421,1.30975185982128,
3.15701662268246));
#284192=CARTESIAN_POINT('Ctrl Pts',(0.933575167464377,1.2477893395441,3.14876533555377));
#284193=CARTESIAN_POINT('Ctrl Pts',(1.0077477123538,1.18868804963577,3.14157270549623));
#284194=CARTESIAN_POINT('Ctrl Pts',(1.13132734685638,1.0702955958185,3.12834476336232));
#284195=CARTESIAN_POINT('Ctrl Pts',(1.18259616088848,1.01336122102882,3.12237405607558));
#284196=CARTESIAN_POINT('Ctrl Pts',(1.25352969060025,0.921838588373931,
3.11352505338146));
#284197=CARTESIAN_POINT('Ctrl Pts',(1.27640936691958,0.889889209922782,
3.11056017698075));
#284198=CARTESIAN_POINT('Ctrl Pts',(1.30347669775379,0.84889663559047,3.10693843966159));
#284199=CARTESIAN_POINT('Ctrl Pts',(1.30881877140536,0.840636923102079,
3.10621761204142));
#284200=CARTESIAN_POINT('Ctrl Pts',(1.31724561325137,0.827332577136293,
3.10507142547053));
#284201=CARTESIAN_POINT('Ctrl Pts',(1.32038048605731,0.822320238110777,
3.10464294449875));
#284202=CARTESIAN_POINT('Ctrl Pts',(1.32635609051508,0.812643583401632,
3.10382231457011));
#284203=CARTESIAN_POINT('Ctrl Pts',(1.32920093092555,0.807982028799622,
3.10342991830714));
#284204=CARTESIAN_POINT('Ctrl Pts',(1.33547792592171,0.797573672101529,
3.10256006181482));
#284205=CARTESIAN_POINT('Ctrl Pts',(1.33889769904679,0.791819429466348,
3.10208338971987));
#284206=CARTESIAN_POINT('Ctrl Pts',(1.34893681546118,0.774676212593677,
3.1006752097505));
#284207=CARTESIAN_POINT('Ctrl Pts',(1.35544895306677,0.763224692712184,
3.09975007237662));
#284208=CARTESIAN_POINT('Ctrl Pts',(1.40725614898601,0.669367257532846,
3.09228123956157));
#284209=CARTESIAN_POINT('Ctrl Pts',(1.44514541329273,0.583079931158479,
3.08611387740205));
#284210=CARTESIAN_POINT('Ctrl Pts',(1.50927023125192,0.391569133807421,
3.07282379119534));
#284211=CARTESIAN_POINT('Ctrl Pts',(1.5327867362558,0.285978395670083,3.06571743832726));
#284212=CARTESIAN_POINT('Ctrl Pts',(1.54730815522713,0.160492373460545,
3.05695976396918));
#284213=CARTESIAN_POINT('Ctrl Pts',(1.54910203369279,0.142137849184999,
3.05567191206115));
#284214=CARTESIAN_POINT('Ctrl Pts',(1.55142717473284,0.113005690679382,
3.05361474084362));
#284215=CARTESIAN_POINT('Ctrl Pts',(1.55217337719482,0.102246570581569,
3.05285216620679));
#284216=CARTESIAN_POINT('Ctrl Pts',(1.55337090001753,0.0819196544109911,
3.051405708391));
#284217=CARTESIAN_POINT('Ctrl Pts',(1.55384584682706,0.0723537113672053,
3.05072260013752));
#284218=CARTESIAN_POINT('Ctrl Pts',(1.55472297659819,0.0506402257133242,
3.04916628665561));
#284219=CARTESIAN_POINT('Ctrl Pts',(1.55507117954116,0.0384912638372372,
3.04829143308399));
#284220=CARTESIAN_POINT('Ctrl Pts',(1.55560764351462,0.0068148427851182,
3.04599920135026));
#284221=CARTESIAN_POINT('Ctrl Pts',(1.55557059610145,-0.0127137285137947,
3.0445749298612));
#284222=CARTESIAN_POINT('Ctrl Pts',(1.55271382631048,-0.150534866323173,
3.03444082460383));
#284223=CARTESIAN_POINT('Ctrl Pts',(1.53677191627025,-0.268146328084544,
3.0253194534284));
#284224=CARTESIAN_POINT('Ctrl Pts',(1.48753633125281,-0.462067242021094,
3.00980268627363));
#284225=CARTESIAN_POINT('Ctrl Pts',(1.46118382423208,-0.539643681000942,
3.00347048282605));
#284226=CARTESIAN_POINT('Ctrl Pts',(1.42402474966382,-0.626005362658659,
2.99650394246048));
#284227=CARTESIAN_POINT('Ctrl Pts',(1.4190690451512,-0.63715953379422,2.99560597781891));
#284228=CARTESIAN_POINT('Ctrl Pts',(1.41130761331136,-0.654088879959099,
2.99424709185941));
#284229=CARTESIAN_POINT('Ctrl Pts',(1.40859671346612,-0.659906618434287,
2.99378084386519));
#284230=CARTESIAN_POINT('Ctrl Pts',(1.40354495235637,-0.67057499291413,
2.99292742251321));
#284231=CARTESIAN_POINT('Ctrl Pts',(1.40121487646781,-0.675430326566563,
2.99253964487023));
#284232=CARTESIAN_POINT('Ctrl Pts',(1.39584331010944,-0.686475978650507,
2.99165881074539));
#284233=CARTESIAN_POINT('Ctrl Pts',(1.39278581615823,-0.692658278493809,
2.99116674498264));
#284234=CARTESIAN_POINT('Ctrl Pts',(1.38317192115517,-0.71177665429668,
2.98964735041963));
#284235=CARTESIAN_POINT('Ctrl Pts',(1.37647543170785,-0.724641976812031,
2.98862817527424));
#284236=CARTESIAN_POINT('Ctrl Pts',(1.3254566038435,-0.81939950202934,2.98113180811487));
#284237=CARTESIAN_POINT('Ctrl Pts',(1.2740342114712,-0.897269485545784,
2.97502141484609));
#284238=CARTESIAN_POINT('Ctrl Pts',(1.15585714585161,-1.04539860130768,
2.96255166626708));
#284239=CARTESIAN_POINT('Ctrl Pts',(1.08890652164362,-1.11496358497814,
2.9562121773926));
#284240=CARTESIAN_POINT('Ctrl Pts',(0.996361347182489,-1.19478612902391,
2.94782092565125));
#284241=CARTESIAN_POINT('Ctrl Pts',(0.976349242542227,-1.21119439063923,
2.9460269529908));
#284242=CARTESIAN_POINT('Ctrl Pts',(0.946264435612997,-1.23463121686905,
2.94335341705531));
#284243=CARTESIAN_POINT('Ctrl Pts',(0.936502176574742,-1.24205244724363,
2.94248939157933));
#284244=CARTESIAN_POINT('Ctrl Pts',(0.918951569554182,-1.25506980458146,
2.94094161401569));
#284245=CARTESIAN_POINT('Ctrl Pts',(0.911197202413649,-1.26071085199513,
2.940259656617));
#284246=CARTESIAN_POINT('Ctrl Pts',(0.89466406161663,-1.27250595202141,
2.93880933399393));
#284247=CARTESIAN_POINT('Ctrl Pts',(0.885872866725031,-1.27864163642749,
2.93804031044704));
#284248=CARTESIAN_POINT('Ctrl Pts',(0.862038411275602,-1.29491275392559,
2.93596067851845));
#284249=CARTESIAN_POINT('Ctrl Pts',(0.846880549033466,-1.30487644882268,
2.93464371259216));
#284250=CARTESIAN_POINT('Ctrl Pts',(0.751916632796548,-1.36494729810438,
2.92642380692789));
#284251=CARTESIAN_POINT('Ctrl Pts',(0.66788293820132,-1.40797233920335,
2.91926510518129));
#284252=CARTESIAN_POINT('Ctrl Pts',(0.512984223212042,-1.47027944405818,
2.90636159479174));
#284253=CARTESIAN_POINT('Ctrl Pts',(0.443657067009222,-1.49266309939074,
2.90068624594157));
#284254=CARTESIAN_POINT('Ctrl Pts',(0.344920027935585,-1.51705241777078,
2.89289475474026));
#284255=CARTESIAN_POINT('Ctrl Pts',(0.3166329020955,-1.52320769413931,2.89069570854083));
#284256=CARTESIAN_POINT('Ctrl Pts',(0.269408842786897,-1.53211107610444,
2.88709520039433));
#284257=CARTESIAN_POINT('Ctrl Pts',(0.250564061370017,-1.53530557624678,
2.885676905425));
#284258=CARTESIAN_POINT('Ctrl Pts',(0.224088845984145,-1.53929306025271,
2.88371441088272));
#284259=CARTESIAN_POINT('Ctrl Pts',(0.216505050316037,-1.54037803995553,
2.88315569828781));
#284260=CARTESIAN_POINT('Ctrl Pts',(0.203497443583866,-1.54214101533942,
2.88220364259416));
#284261=CARTESIAN_POINT('Ctrl Pts',(0.198077583467954,-1.54284652370461,
2.88180880896478));
#284262=CARTESIAN_POINT('Ctrl Pts',(0.186653960671362,-1.5442723557932,
2.88098062801231));
#284263=CARTESIAN_POINT('Ctrl Pts',(0.180649584633809,-1.54498625910023,
2.88054763449921));
#284264=CARTESIAN_POINT('Ctrl Pts',(0.164253699734272,-1.54683879148834,
2.87937118997468));
#284265=CARTESIAN_POINT('Ctrl Pts',(0.153854396828151,-1.54790773789047,
2.87863148498996));
#284266=CARTESIAN_POINT('Ctrl Pts',(0.100578343193231,-1.55284176114131,
2.87487134683168));
#284267=CARTESIAN_POINT('Ctrl Pts',(0.057560981101624,-1.5550308845464,
2.87193239644717));
#284268=CARTESIAN_POINT('Ctrl Pts',(-0.0802648142245121,-1.55631607030563,
2.86266842176333));
#284269=CARTESIAN_POINT('Ctrl Pts',(-0.174919872631605,-1.54853705425943,
2.85652588245585));
#284270=CARTESIAN_POINT('Ctrl Pts',(-0.316172396099735,-1.52380414581933,
2.84701962467554));
#284271=CARTESIAN_POINT('Ctrl Pts',(-0.363640012103181,-1.51317858673255,
2.84376737223043));
#284272=CARTESIAN_POINT('Ctrl Pts',(-0.432120306244923,-1.49444081537108,
2.83892861385407));
#284273=CARTESIAN_POINT('Ctrl Pts',(-0.453580054199092,-1.48806799695418,
2.8373909016512));
#284274=CARTESIAN_POINT('Ctrl Pts',(-0.49238913721764,-1.4756255383185,
2.83456518407256));
#284275=CARTESIAN_POINT('Ctrl Pts',(-0.509782861052893,-1.46970717379218,
2.83328204508058));
#284276=CARTESIAN_POINT('Ctrl Pts',(-0.537200214639746,-1.45983292824975,
2.83123065555264));
#284277=CARTESIAN_POINT('Ctrl Pts',(-0.54729495559382,-1.45607845601704,
2.83046908341117));
#284278=CARTESIAN_POINT('Ctrl Pts',(-0.566293746814791,-1.44878687942852,
2.82902343861246));
#284279=CARTESIAN_POINT('Ctrl Pts',(-0.575205732336879,-1.44527173487081,
2.82834012994576));
#284280=CARTESIAN_POINT('Ctrl Pts',(-0.595371400568232,-1.43710175357742,
2.82678184912631));
#284281=CARTESIAN_POINT('Ctrl Pts',(-0.606603904317917,-1.43239667771578,
2.82590521241934));
#284282=CARTESIAN_POINT('Ctrl Pts',(-0.641104332128772,-1.41746654544249,
2.8231851082517));
#284283=CARTESIAN_POINT('Ctrl Pts',(-0.664176710399475,-1.40680323015921,
2.8213269021009));
#284284=CARTESIAN_POINT('Ctrl Pts',(-0.809354642963557,-1.33533918276053,
2.80937563272502));
#284285=CARTESIAN_POINT('Ctrl Pts',(-0.923259288802169,-1.2592710663737,
2.79873699650454));
#284286=CARTESIAN_POINT('Ctrl Pts',(-1.05639236039929,-1.14248664935626,
2.78505961495368));
#284287=CARTESIAN_POINT('Ctrl Pts',(-1.08595863090926,-1.11442131263817,
2.78193353458773));
#284288=CARTESIAN_POINT('Ctrl Pts',(-1.13128526157298,-1.06787655176599,
2.77703508152702));
#284289=CARTESIAN_POINT('Ctrl Pts',(-1.14777395513107,-1.05013417648145,
2.77522884340045));
#284290=CARTESIAN_POINT('Ctrl Pts',(-1.16940006563642,-1.02574553316021,
2.772834522134));
#284291=CARTESIAN_POINT('Ctrl Pts',(-1.1749068607934,-1.01943331769242,
2.77222253686207));
#284292=CARTESIAN_POINT('Ctrl Pts',(-1.18400778566412,-1.00882958889565,
2.77120768832872));
#284293=CARTESIAN_POINT('Ctrl Pts',(-1.18763016430407,-1.00456267720867,
2.7708028275426));
#284294=CARTESIAN_POINT('Ctrl Pts',(-1.19495567442057,-0.995838722501556,
2.76998233784379));
#284295=CARTESIAN_POINT('Ctrl Pts',(-1.19865706537833,-0.991380384941498,
2.76956682960448));
#284296=CARTESIAN_POINT('Ctrl Pts',(-1.20823410824967,-0.979712755133515,
2.76848896241829));
#284297=CARTESIAN_POINT('Ctrl Pts',(-1.21407028242947,-0.972471132479058,
2.76782935701626));
#284298=CARTESIAN_POINT('Ctrl Pts',(-1.23830678193464,-0.9418397841109,
2.76507628694547));
#284299=CARTESIAN_POINT('Ctrl Pts',(-1.2561002238835,-0.917975153863797,
2.76302090706399));
#284300=CARTESIAN_POINT('Ctrl Pts',(-1.32565405106469,-0.818876427995666,
2.75477523318911));
#284301=CARTESIAN_POINT('Ctrl Pts',(-1.37143103457888,-0.739660153392063,
2.74883143557132));
#284302=CARTESIAN_POINT('Ctrl Pts',(-1.44217690719349,-0.58780357603737,
2.73778741358157));
#284303=CARTESIAN_POINT('Ctrl Pts',(-1.46923468917447,-0.516463806544339,
2.73272630337374));
#284304=CARTESIAN_POINT('Ctrl Pts',(-1.49858463159502,-0.417780610220669,
2.72566456101477));
#284305=CARTESIAN_POINT('Ctrl Pts',(-1.50555047969143,-0.391936401843136,
2.72381048107124));
#284306=CARTESIAN_POINT('Ctrl Pts',(-1.51476830267501,-0.353852462789254,
2.72106456129103));
#284307=CARTESIAN_POINT('Ctrl Pts',(-1.5175459049029,-0.341744036951994,
2.72018953052219));
#284308=CARTESIAN_POINT('Ctrl Pts',(-1.52221393419901,-0.320214452702895,
2.71862948578663));
#284309=CARTESIAN_POINT('Ctrl Pts',(-1.52416267899098,-0.310806495407102,
2.71794637474028));
#284310=CARTESIAN_POINT('Ctrl Pts',(-1.52808424214077,-0.29094992063547,
2.71650132988515));
#284311=CARTESIAN_POINT('Ctrl Pts',(-1.53003731704036,-0.280497959797769,
2.71573880477576));
#284312=CARTESIAN_POINT('Ctrl Pts',(-1.53496036999895,-0.252569121602563,
2.71369577968821));
#284313=CARTESIAN_POINT('Ctrl Pts',(-1.53773891575525,-0.235060582158112,
2.71240930478595));
#284314=CARTESIAN_POINT('Ctrl Pts',(-1.55045903948366,-0.144987277893884,
2.70575909276499));
#284315=CARTESIAN_POINT('Ctrl Pts',(-1.55556419644944,-0.0718441416891806,
2.700246567499));
#284316=CARTESIAN_POINT('Ctrl Pts',(-1.55544729251868,0.0602401063572441,
2.69011614563084));
#284317=CARTESIAN_POINT('Ctrl Pts',(-1.5520539556199,0.119051021593196,
2.68554439663051));
#284318=CARTESIAN_POINT('Ctrl Pts',(-1.53663006928284,0.253314033008511,
2.67506863039724));
#284319=CARTESIAN_POINT('Ctrl Pts',(-1.52235890140084,0.328368855067391,
2.66918272575174));
#284320=CARTESIAN_POINT('Ctrl Pts',(-1.49972766186212,0.412945125829353,
2.66270585087675));
#284321=CARTESIAN_POINT('Ctrl Pts',(-1.49670266745485,0.423778104023444,
2.661879371346));
#284322=CARTESIAN_POINT('Ctrl Pts',(-1.49180463828114,0.440611691103604,
2.66060094330899));
#284323=CARTESIAN_POINT('Ctrl Pts',(-1.4900123593249,0.446635101540851,
2.66014467160318));
#284324=CARTESIAN_POINT('Ctrl Pts',(-1.48676890585172,0.457298703727562,
2.6593391976027));
#284325=CARTESIAN_POINT('Ctrl Pts',(-1.4853324634706,0.461943024553296,
2.65898918209753));
#284326=CARTESIAN_POINT('Ctrl Pts',(-1.48180726043102,0.473154284144634,
2.65814609308023));
#284327=CARTESIAN_POINT('Ctrl Pts',(-1.47969660477804,0.479714181876933,
2.6576542958845));
#284328=CARTESIAN_POINT('Ctrl Pts',(-1.47297701141184,0.500132237796858,
2.65612762176913));
#284329=CARTESIAN_POINT('Ctrl Pts',(-1.46821629617358,0.513940151752502,
2.65510106919811));
#284330=CARTESIAN_POINT('Ctrl Pts',(-1.4420601694539,0.58647138958084,2.64972954543161));
#284331=CARTESIAN_POINT('Ctrl Pts',(-1.41733209103663,0.64393931070276,
2.64554503686816));
#284332=CARTESIAN_POINT('Ctrl Pts',(-1.33926615848179,0.79891891723264,
2.63405552642741));
#284333=CARTESIAN_POINT('Ctrl Pts',(-1.27885508650744,0.8924314543115,2.62686123356053));
#284334=CARTESIAN_POINT('Ctrl Pts',(-1.18594555494629,1.00720237635497,
2.61684072213216));
#284335=CARTESIAN_POINT('Ctrl Pts',(-1.16188747570302,1.0348626129748,2.61432270622732));
#284336=CARTESIAN_POINT('Ctrl Pts',(-1.12707748545336,1.07213932308117,
2.61076285280136));
#284337=CARTESIAN_POINT('Ctrl Pts',(-1.117133854946,1.08249633355764,2.60975487567078));
#284338=CARTESIAN_POINT('Ctrl Pts',(-1.10077025343233,1.09907459922687,
2.60810937311888));
#284339=CARTESIAN_POINT('Ctrl Pts',(-1.09443735536906,1.10538092738372,
2.60747567038608));
#284340=CARTESIAN_POINT('Ctrl Pts',(-1.08103655137211,1.11849745316662,
2.60614095800911));
#284341=CARTESIAN_POINT('Ctrl Pts',(-1.07395785338585,1.12529600512105,
2.60543948094763));
#284342=CARTESIAN_POINT('Ctrl Pts',(-1.05681068718794,1.1414553918644,2.60374837890463));
#284343=CARTESIAN_POINT('Ctrl Pts',(-1.04668169252171,1.15075047344273,
2.60275600912948));
#284344=CARTESIAN_POINT('Ctrl Pts',(-1.01033311566897,1.18322954729875,
2.59921682805568));
#284345=CARTESIAN_POINT('Ctrl Pts',(-0.983457599414899,1.20565996630623,
2.5966394620104));
#284346=CARTESIAN_POINT('Ctrl Pts',(-0.913634231946479,1.26004611805021,
2.59003554245133));
#284347=CARTESIAN_POINT('Ctrl Pts',(-0.869753454586762,1.29072523469317,
2.58596712790093));
#284348=CARTESIAN_POINT('Ctrl Pts',(-0.803422174625369,1.33218018242369,
2.57995082056175));
#284349=CARTESIAN_POINT('Ctrl Pts',(-0.782152239793131,1.34477843965098,
2.57804081056432));
#284350=CARTESIAN_POINT('Ctrl Pts',(-0.674265484009122,1.40525446758967,
2.56846181834126));
#284351=CARTESIAN_POINT('Ctrl Pts',(-0.58351169985323,1.44529976761435,
2.56073222869852));
#284352=CARTESIAN_POINT('Ctrl Pts',(-0.476090414352199,1.48091849584164,
2.55231600459855));
#284353=CARTESIAN_POINT('Ctrl Pts',(-0.462558116849848,1.48520089561385,
2.55126883893735));
#284354=CARTESIAN_POINT('Ctrl Pts',(-0.442445494532603,1.49126411161708,
2.54973358684023));
#284355=CARTESIAN_POINT('Ctrl Pts',(-0.435909494093216,1.49318772560019,
2.54923795007389));
#284356=CARTESIAN_POINT('Ctrl Pts',(-0.424195283152444,1.49655186883216,
2.54835574290757));
#284357=CARTESIAN_POINT('Ctrl Pts',(-0.419022034265604,1.49800856869855,
2.54796827902632));
#284358=CARTESIAN_POINT('Ctrl Pts',(-0.407497936480815,1.5011891892828,
2.54710989502096));
#284359=CARTESIAN_POINT('Ctrl Pts',(-0.401143602755021,1.5028996521565,
2.54663974378318));
#284360=CARTESIAN_POINT('Ctrl Pts',(-0.382201824140878,1.50786971477544,
2.54524710669603));
#284361=CARTESIAN_POINT('Ctrl Pts',(-0.369583771644674,1.5110119708399,
2.54433098938682));
#284362=CARTESIAN_POINT('Ctrl Pts',(-0.280713189210971,1.53196337263462,
2.537950053831));
#284363=CARTESIAN_POINT('Ctrl Pts',(-0.203239994121519,1.54415303591295,
2.53275196510465));
#284364=CARTESIAN_POINT('Ctrl Pts',(-0.00458797329134095,1.56019027201008,
2.5196104806621));
#284365=CARTESIAN_POINT('Ctrl Pts',(0.116702262506103,1.555825071848,2.51172942870284));
#284366=CARTESIAN_POINT('Ctrl Pts',(0.255304162972019,1.5345264418901,2.50204770959194));
#284367=CARTESIAN_POINT('Ctrl Pts',(0.274294662811137,1.53124589740904,
2.50070721532751));
#284368=CARTESIAN_POINT('Ctrl Pts',(0.305081134146674,1.5253365711507,2.49850856577832));
#284369=CARTESIAN_POINT('Ctrl Pts',(0.316916412643089,1.52292157592523,
2.49765716165952));
#284370=CARTESIAN_POINT('Ctrl Pts',(0.338076413499842,1.51834652925434,
2.496123259775));
#284371=CARTESIAN_POINT('Ctrl Pts',(0.34741169198839,1.51623776270051,2.49544243290102));
#284372=CARTESIAN_POINT('Ctrl Pts',(0.367269598647034,1.51155900129803,
2.4939851115908));
#284373=CARTESIAN_POINT('Ctrl Pts',(0.377785980631142,1.50896498114537,
2.493207876223));
#284374=CARTESIAN_POINT('Ctrl Pts',(0.406344508247793,1.50160335146394,
2.4910818224862));
#284375=CARTESIAN_POINT('Ctrl Pts',(0.424328792285771,1.49662069483294,
2.48972614727725));
#284376=CARTESIAN_POINT('Ctrl Pts',(0.464112904334879,1.48482355276228,
2.48668827276499));
#284377=CARTESIAN_POINT('Ctrl Pts',(0.485860690893841,1.47785014809817,
2.48500127003085));
#284378=CARTESIAN_POINT('Ctrl Pts',(0.554863163920925,1.45403689020523,
2.47956263594423));
#284379=CARTESIAN_POINT('Ctrl Pts',(0.601456457976442,1.43539042299075,
2.4757582271719));
#284380=CARTESIAN_POINT('Ctrl Pts',(0.694898986650941,1.39264592092735,
2.46787209068947));
#284381=CARTESIAN_POINT('Ctrl Pts',(0.741591742530025,1.36835249869939,
2.46379071236233));
#284382=CARTESIAN_POINT('Ctrl Pts',(0.801748558382056,1.33306914501531,
2.45838254370962));
#284383=CARTESIAN_POINT('Ctrl Pts',(0.816390589839546,1.32415275192799,
2.45705400918685));
#284384=CARTESIAN_POINT('Ctrl Pts',(0.885058740395803,1.28076467279295,
2.45077228429649));
#284385=CARTESIAN_POINT('Ctrl Pts',(0.937074636785301,1.24321365575638,
2.44585893338128));
#284386=CARTESIAN_POINT('Ctrl Pts',(0.995232487775756,1.19549836943306,
2.44029521771209));
#284387=CARTESIAN_POINT('Ctrl Pts',(1.00375897998477,1.18834842747067,2.43947770530743));
#284388=CARTESIAN_POINT('Ctrl Pts',(1.01695968027796,1.17703543462833,2.43821012564714));
#284389=CARTESIAN_POINT('Ctrl Pts',(1.02168652594923,1.17293480299034,2.437755847137));
#284390=CARTESIAN_POINT('Ctrl Pts',(1.03004471355052,1.16559504685412,2.43695207678753));
#284391=CARTESIAN_POINT('Ctrl Pts',(1.03368565400222,1.16236736660693,2.43660179180238));
#284392=CARTESIAN_POINT('Ctrl Pts',(1.04247515713099,1.15450154304838,2.43575572143484));
#284393=CARTESIAN_POINT('Ctrl Pts',(1.04760795707743,1.14984600677477,2.43526123821138));
#284394=CARTESIAN_POINT('Ctrl Pts',(1.06361304437874,1.13513298420269,2.4337174082857));
#284395=CARTESIAN_POINT('Ctrl Pts',(1.07437330155477,1.12495406619094,2.43267665517642));
#284396=CARTESIAN_POINT('Ctrl Pts',(1.13118559941089,1.06965228880925,2.42715535032028));
#284397=CARTESIAN_POINT('Ctrl Pts',(1.17454943374723,1.02184760044184,2.42284529930123));
#284398=CARTESIAN_POINT('Ctrl Pts',(1.28776257538364,0.880276361759445,
2.41085367028134));
#284399=CARTESIAN_POINT('Ctrl Pts',(1.35019176636595,0.781152620464755,
2.40328474641407));
#284400=CARTESIAN_POINT('Ctrl Pts',(1.41428344615465,0.648325032257788,
2.39321923322024));
#284401=CARTESIAN_POINT('Ctrl Pts',(1.42680423993931,0.620284176525293,
2.39110057009331));
#284402=CARTESIAN_POINT('Ctrl Pts',(1.44310302604166,0.580672973156132,
2.38810574663187));
#284403=CARTESIAN_POINT('Ctrl Pts',(1.44758806243349,0.56939988788068,2.38725325082023));
#284404=CARTESIAN_POINT('Ctrl Pts',(1.45515380227828,0.549716171166069,
2.38576376958492));
#284405=CARTESIAN_POINT('Ctrl Pts',(1.45829462378703,0.541329143191026,
2.38512882029988));
#284406=CARTESIAN_POINT('Ctrl Pts',(1.46471952619258,0.523710756769226,
2.38379412137367));
#284407=CARTESIAN_POINT('Ctrl Pts',(1.4679891484409,0.514474585491307,2.38309392431404));
#284408=CARTESIAN_POINT('Ctrl Pts',(1.47560576324577,0.492294934418385,
2.3814109520692));
#284409=CARTESIAN_POINT('Ctrl Pts',(1.47986994425298,0.479324104288452,
2.38042549890981));
#284410=CARTESIAN_POINT('Ctrl Pts',(1.49426140604352,0.433524341763582,
2.37694053443858));
#284411=CARTESIAN_POINT('Ctrl Pts',(1.50347067842733,0.400419880560053,
2.37441170276013));
#284412=CARTESIAN_POINT('Ctrl Pts',(1.52386131966444,0.316445374706051,
2.36796780238964));
#284413=CARTESIAN_POINT('Ctrl Pts',(1.53359756216837,0.265270722382908,
2.36401348696345));
#284414=CARTESIAN_POINT('Ctrl Pts',(1.54840150330025,0.158540574057791,
2.35573327332648));
#284415=CARTESIAN_POINT('Ctrl Pts',(1.5530847935151,0.103002781284942,2.35140631493147));
#284416=CARTESIAN_POINT('Ctrl Pts',(1.55705900683752,-0.0275335522168997,
2.34128495902298));
#284417=CARTESIAN_POINT('Ctrl Pts',(1.5539277925416,-0.102478945719532,
2.33550989481253));
#284418=CARTESIAN_POINT('Ctrl Pts',(1.54413062484228,-0.18806042157606,
2.32913780045627));
#284419=CARTESIAN_POINT('Ctrl Pts',(1.54273407732375,-0.199192607245574,
2.32831341310625));
#284420=CARTESIAN_POINT('Ctrl Pts',(1.54036835215817,-0.216529449542107,
2.32703751539361));
#284421=CARTESIAN_POINT('Ctrl Pts',(1.53948187890611,-0.222744721809059,
2.32658170805749));
#284422=CARTESIAN_POINT('Ctrl Pts',(1.53784207805529,-0.233764060716008,
2.3257766334589));
#284423=CARTESIAN_POINT('Ctrl Pts',(1.53710384609906,-0.238570032796876,
2.32542655765306));
#284424=CARTESIAN_POINT('Ctrl Pts',(1.53526353409798,-0.250187403079162,
2.32458278504021));
#284425=CARTESIAN_POINT('Ctrl Pts',(1.53413865429954,-0.25699503887627,
2.32409037049015));
#284426=CARTESIAN_POINT('Ctrl Pts',(1.53048377052505,-0.278234329783161,
2.32255976414537));
#284427=CARTESIAN_POINT('Ctrl Pts',(1.527795054908,-0.292638386377204,2.321529958029));
#284428=CARTESIAN_POINT('Ctrl Pts',(1.51247974050745,-0.368710515476358,
2.31612441572394));
#284429=CARTESIAN_POINT('Ctrl Pts',(1.49632063215924,-0.429614799995563,
2.31191139501902));
#284430=CARTESIAN_POINT('Ctrl Pts',(1.44117882102562,-0.595984134309744,
2.30030913946422));
#284431=CARTESIAN_POINT('Ctrl Pts',(1.39440649916283,-0.698443136576814,
2.29303118518171));
#284432=CARTESIAN_POINT('Ctrl Pts',(1.3189907096299,-0.825279993650218,
2.28300485159366));
#284433=CARTESIAN_POINT('Ctrl Pts',(1.29994595318147,-0.854964187806847,
2.28057999181877));
#284434=CARTESIAN_POINT('Ctrl Pts',(1.27185405985485,-0.895638580607973,
2.27712856271953));
#284435=CARTESIAN_POINT('Ctrl Pts',(1.26363899684094,-0.907192195130692,
2.27613302945155));
#284436=CARTESIAN_POINT('Ctrl Pts',(1.25000789089061,-0.925818468415923,
2.27450222272955));
#284437=CARTESIAN_POINT('Ctrl Pts',(1.24468685447152,-0.932959909138211,
2.27387063408778));
#284438=CARTESIAN_POINT('Ctrl Pts',(1.23335462249982,-0.947899554690296,
2.27253571331624));
#284439=CARTESIAN_POINT('Ctrl Pts',(1.22733014337435,-0.955687135811766,
2.27183187833222));
#284440=CARTESIAN_POINT('Ctrl Pts',(1.21261249317965,-0.974343306852397,
2.27012601194322));
#284441=CARTESIAN_POINT('Ctrl Pts',(1.20384673886791,-0.985153259199103,
2.2691211138008));
#284442=CARTESIAN_POINT('Ctrl Pts',(1.17176637082182,-1.02364727816317,
2.26548168322839));
#284443=CARTESIAN_POINT('Ctrl Pts',(1.14763397031588,-1.05063126200674,
2.26281424143582));
#284444=CARTESIAN_POINT('Ctrl Pts',(1.08363814753125,-1.11735138489516,
2.25590806977828));
#284445=CARTESIAN_POINT('Ctrl Pts',(1.04252155941416,-1.15580854313394,
2.25162226449452));
#284446=CARTESIAN_POINT('Ctrl Pts',(0.958807850725194,-1.22600005716313,
2.24320608866604));
#284447=CARTESIAN_POINT('Ctrl Pts',(0.916486581412007,-1.25795101141336,
2.23908670700559));
#284448=CARTESIAN_POINT('Ctrl Pts',(0.813849181162596,-1.32750507491836,
2.22948365112596));
#284449=CARTESIAN_POINT('Ctrl Pts',(0.752414857500839,-1.36326611706069,
2.22402104690798));
#284450=CARTESIAN_POINT('Ctrl Pts',(0.678715557343776,-1.39966087814786,
2.21794115383653));
#284451=CARTESIAN_POINT('Ctrl Pts',(0.668632127924866,-1.40450577724835,
2.21711919550749));
#284452=CARTESIAN_POINT('Ctrl Pts',(0.652815819873923,-1.41189627001839,
2.21584623612641));
#284453=CARTESIAN_POINT('Ctrl Pts',(0.647118576021599,-1.41451656909695,
2.21539096846679));
#284454=CARTESIAN_POINT('Ctrl Pts',(0.636974679417972,-1.41910787537193,
2.21458635620258));
#284455=CARTESIAN_POINT('Ctrl Pts',(0.632534566482635,-1.42109251193333,
2.21423620848391));
#284456=CARTESIAN_POINT('Ctrl Pts',(0.621763302098159,-1.42584655391588,
2.21339163327394));
#284457=CARTESIAN_POINT('Ctrl Pts',(0.615422904301446,-1.42859464259952,
2.21289849500322));
#284458=CARTESIAN_POINT('Ctrl Pts',(0.595531579409114,-1.43705903921313,
2.21136327054586));
#284459=CARTESIAN_POINT('Ctrl Pts',(0.58191727851012,-1.44262568483293,
2.21032964235718));
#284460=CARTESIAN_POINT('Ctrl Pts',(0.509137048520994,-1.47118619296644,
2.20488391180023));
#284461=CARTESIAN_POINT('Ctrl Pts',(0.448677304091412,-1.49073806026603,
2.20063720684499));
#284462=CARTESIAN_POINT('Ctrl Pts',(0.276921853901774,-1.53487966169135,
2.18890085564967));
#284463=CARTESIAN_POINT('Ctrl Pts',(0.163888354734473,-1.55102564251602,
2.18152306847942));
#284464=CARTESIAN_POINT('Ctrl Pts',(0.0163931933713924,-1.55577932307457,
2.17148101105747));
#284465=CARTESIAN_POINT('Ctrl Pts',(-0.0173445752312792,-1.55576891756481,
2.1691586036353));
#284466=CARTESIAN_POINT('Ctrl Pts',(-0.0649586590946392,-1.55420532356505,
2.16583063974348));
#284467=CARTESIAN_POINT('Ctrl Pts',(-0.0788567690295112,-1.55356216580195,
2.16485320768083));
#284468=CARTESIAN_POINT('Ctrl Pts',(-0.102473699758015,-1.55215153763421,
2.16318107921345));
#284469=CARTESIAN_POINT('Ctrl Pts',(-0.112197521997491,-1.55147895993079,
2.16248938264003));
#284470=CARTESIAN_POINT('Ctrl Pts',(-0.131947422865425,-1.54992626137449,
2.16107760189209));
#284471=CARTESIAN_POINT('Ctrl Pts',(-0.141972547270079,-1.54904013024675,
2.16035736121882));
#284472=CARTESIAN_POINT('Ctrl Pts',(-0.166948353356754,-1.5465880066343,
2.15855362777078));
#284473=CARTESIAN_POINT('Ctrl Pts',(-0.181885968749375,-1.54490248229613,
2.15746643547949));
#284474=CARTESIAN_POINT('Ctrl Pts',(-0.241520691198428,-1.53729659197679,
2.15309096897472));
#284475=CARTESIAN_POINT('Ctrl Pts',(-0.285971297224774,-1.52965117479427,
2.14974954994905));
#284476=CARTESIAN_POINT('Ctrl Pts',(-0.408612427058461,-1.50302478682797,
2.14030119736805));
#284477=CARTESIAN_POINT('Ctrl Pts',(-0.485752132933097,-1.47989523383428,
2.13408739593804));
#284478=CARTESIAN_POINT('Ctrl Pts',(-0.637719242717976,-1.42116276919677,
2.12145124514738));
#284479=CARTESIAN_POINT('Ctrl Pts',(-0.712207207957305,-1.38533497941718,
2.11504806129051));
#284480=CARTESIAN_POINT('Ctrl Pts',(-0.796172754182559,-1.33637725621629,
2.10781015404));
#284481=CARTESIAN_POINT('Ctrl Pts',(-0.808734535092781,-1.32881289819332,
2.10672699109953));
#284482=CARTESIAN_POINT('Ctrl Pts',(-0.8270923000943,-1.31740157389273,
2.10514562134577));
#284483=CARTESIAN_POINT('Ctrl Pts',(-0.832972018173072,-1.31369182141907,
2.10463937343352));
#284484=CARTESIAN_POINT('Ctrl Pts',(-0.843234166005635,-1.30712041571836,
2.1037564864348));
#284485=CARTESIAN_POINT('Ctrl Pts',(-0.84762730303555,-1.30427589042998,
2.103378765626));
#284486=CARTESIAN_POINT('Ctrl Pts',(-0.856249026209486,-1.29863142276689,
2.10263799118104));
#284487=CARTESIAN_POINT('Ctrl Pts',(-0.860478318981203,-1.29583294896114,
2.10227483900512));
#284488=CARTESIAN_POINT('Ctrl Pts',(-0.872925706499312,-1.2875088455844,
2.10120646147114));
#284489=CARTESIAN_POINT('Ctrl Pts',(-0.881105008102596,-1.28192522976104,
2.10050497579205));
#284490=CARTESIAN_POINT('Ctrl Pts',(-0.922217986666207,-1.25327995586747,
2.09697871723892));
#284491=CARTESIAN_POINT('Ctrl Pts',(-0.954305219023846,-1.2290235429243,
2.09422560756095));
#284492=CARTESIAN_POINT('Ctrl Pts',(-1.0440451183946,-1.15554795148451,
2.08640678062015));
#284493=CARTESIAN_POINT('Ctrl Pts',(-1.09908878292764,-1.10332520752812,
2.08145604176351));
#284494=CARTESIAN_POINT('Ctrl Pts',(-1.2136248129733,-0.97754509315686,
2.07024919842545));
#284495=CARTESIAN_POINT('Ctrl Pts',(-1.27065470868303,-0.902171097299932,
2.06398616398876));
#284496=CARTESIAN_POINT('Ctrl Pts',(-1.33008984402866,-0.806703352588348,
2.05618629242116));
#284497=CARTESIAN_POINT('Ctrl Pts',(-1.33940635828878,-0.791138326572896,
2.05491907365427));
#284498=CARTESIAN_POINT('Ctrl Pts',(-1.35379251452682,-0.766120755842234,
2.05288721538097));
#284499=CARTESIAN_POINT('Ctrl Pts',(-1.35904045524121,-0.756772234931256,
2.05212903242805));
#284500=CARTESIAN_POINT('Ctrl Pts',(-1.36879850050741,-0.738960666047257,
2.05068608777694));
#284501=CARTESIAN_POINT('Ctrl Pts',(-1.37332781368055,-0.730508664937475,
2.05000205280315));
#284502=CARTESIAN_POINT('Ctrl Pts',(-1.38347042854234,-0.711154125130065,
2.0484368817918));
#284503=CARTESIAN_POINT('Ctrl Pts',(-1.38903346751614,-0.70022612522413,
2.04755402461027));
#284504=CARTESIAN_POINT('Ctrl Pts',(-1.40593148585003,-0.666037838958002,
2.04479400291232));
#284505=CARTESIAN_POINT('Ctrl Pts',(-1.41681515845416,-0.642560817213278,
2.04290146584884));
#284506=CARTESIAN_POINT('Ctrl Pts',(-1.46512328613503,-0.531154601066817,
2.03392809450377));
#284507=CARTESIAN_POINT('Ctrl Pts',(-1.49497334040125,-0.440182381467759,
2.02660365242428));
#284508=CARTESIAN_POINT('Ctrl Pts',(-1.53750718739498,-0.254355614388529,
2.01182994196964));
#284509=CARTESIAN_POINT('Ctrl Pts',(-1.55018181699109,-0.159889735983582,
2.00441474412428));
#284510=CARTESIAN_POINT('Ctrl Pts',(-1.55470317190636,-0.0515354464191655,
1.99635363519677));
#284511=CARTESIAN_POINT('Ctrl Pts',(-1.5550876673794,-0.0382129960173114,
1.9953703679584));
#284512=CARTESIAN_POINT('Ctrl Pts',(-1.55538747575055,-0.0194763737262476,
1.99400003548267));
#284513=CARTESIAN_POINT('Ctrl Pts',(-1.55544581760213,-0.0140655495503116,
1.99360577514135));
#284514=CARTESIAN_POINT('Ctrl Pts',(-1.55549184273964,-0.0057933654377718,
1.99300537652288));
#284515=CARTESIAN_POINT('Ctrl Pts',(-1.5554998676356,-0.00293223911665466,
1.99279814542823));
#284516=CARTESIAN_POINT('Ctrl Pts',(-1.55549999837604,-7.10784117823764E-5,
1.99259135320666));
#284517=CARTESIAN_POINT('',(-1.55549982855345,0.00073032197892629,0.594056225566802));
#284518=CARTESIAN_POINT('Ctrl Pts',(-1.55549999838269,-7.09326402445093E-5,
1.99259134267093));
#284519=CARTESIAN_POINT('Ctrl Pts',(-1.55550011902552,0.00257467473978788,
1.99240012971776));
#284520=CARTESIAN_POINT('Ctrl Pts',(-1.5554934901766,0.00522032312768005,
1.99220929232667));
#284521=CARTESIAN_POINT('Ctrl Pts',(-1.55545344292802,0.0131395633060705,
1.99163920398461));
#284522=CARTESIAN_POINT('Ctrl Pts',(-1.55539995576352,0.0184130683000571,
1.99126108665928));
#284523=CARTESIAN_POINT('Ctrl Pts',(-1.55518583217104,0.0324731182807974,
1.9902567440163));
#284524=CARTESIAN_POINT('Ctrl Pts',(-1.55497755216657,0.0412589119150026,
1.98963309219957));
#284525=CARTESIAN_POINT('Ctrl Pts',(-1.55383195840756,0.0768494635388745,
1.98712095748074));
#284526=CARTESIAN_POINT('Ctrl Pts',(-1.55227585696072,0.103631450805317,
1.9852632676013));
#284527=CARTESIAN_POINT('Ctrl Pts',(-1.54114975071259,0.2359231038927,1.97618943355107));
#284528=CARTESIAN_POINT('Ctrl Pts',(-1.52151073768281,0.340311387440798,
1.96933712843099));
#284529=CARTESIAN_POINT('Ctrl Pts',(-1.47620012588961,0.493234080229205,
1.95879324838937));
#284530=CARTESIAN_POINT('Ctrl Pts',(-1.45835128782466,0.543743970141623,
1.95522551716895));
#284531=CARTESIAN_POINT('Ctrl Pts',(-1.42458280387633,0.625595613504931,
1.9492040281258));
#284532=CARTESIAN_POINT('Ctrl Pts',(-1.41014239559989,0.657498402179297,
1.946794124451));
#284533=CARTESIAN_POINT('Ctrl Pts',(-1.38854981571307,0.701212307064922,
1.94338708375297));
#284534=CARTESIAN_POINT('Ctrl Pts',(-1.38229770795498,0.713457998393686,
1.94242089052324));
#284535=CARTESIAN_POINT('Ctrl Pts',(-1.37130569767732,0.734300529843034,
1.94075519802945));
#284536=CARTESIAN_POINT('Ctrl Pts',(-1.36664515939659,0.74293847986607,
1.94005852379389));
#284537=CARTESIAN_POINT('Ctrl Pts',(-1.35701005350414,0.760398933815207,
1.93863700571577));
#284538=CARTESIAN_POINT('Ctrl Pts',(-1.3520304477732,0.769218098575097,
1.93791200731901));
#284539=CARTESIAN_POINT('Ctrl Pts',(-1.33929165185802,0.791273346973648,
1.93608084505064));
#284540=CARTESIAN_POINT('Ctrl Pts',(-1.33142224798604,0.804444158751699,
1.93497073926801));
#284541=CARTESIAN_POINT('Ctrl Pts',(-1.30029264649927,0.854836645956708,
1.9306573571652));
#284542=CARTESIAN_POINT('Ctrl Pts',(-1.2756579420909,0.891180551142507,
1.927404426962));
#284543=CARTESIAN_POINT('Ctrl Pts',(-1.18737429775381,1.0102528921736,1.91624850390149));
#284544=CARTESIAN_POINT('Ctrl Pts',(-1.11695538469033,1.08760030364894,
1.90811976958717));
#284545=CARTESIAN_POINT('Ctrl Pts',(-1.00614055534385,1.18711931533115,
1.89659803953098));
#284546=CARTESIAN_POINT('Ctrl Pts',(-0.971674071230796,1.21549212942396,
1.89316614859026));
#284547=CARTESIAN_POINT('Ctrl Pts',(-0.922103941136729,1.25284026883781,
1.88847894450689));
#284548=CARTESIAN_POINT('Ctrl Pts',(-0.907998456237183,1.2631006608431,
1.88717165933163));
#284549=CARTESIAN_POINT('Ctrl Pts',(-0.882984045708801,1.28066060027152,
1.8849031171743));
#284550=CARTESIAN_POINT('Ctrl Pts',(-0.872149931336673,1.28806324597573,
1.88393646306876));
#284551=CARTESIAN_POINT('Ctrl Pts',(-0.856752480723873,1.29830052631937,
1.88258625746465));
#284552=CARTESIAN_POINT('Ctrl Pts',(-0.852266537285292,1.30124971530581,
1.88219566455542));
#284553=CARTESIAN_POINT('Ctrl Pts',(-0.843304653615774,1.30707529107742,
1.88142100669883));
#284554=CARTESIAN_POINT('Ctrl Pts',(-0.838829060163154,1.3099520475025,
1.8810369310333));
#284555=CARTESIAN_POINT('Ctrl Pts',(-0.829254704345398,1.31603691838133,
1.88022130734973));
#284556=CARTESIAN_POINT('Ctrl Pts',(-0.824151982743377,1.31923843479728,
1.87979018231144));
#284557=CARTESIAN_POINT('Ctrl Pts',(-0.8101637938208,1.32790197578502,1.87861766428272));
#284558=CARTESIAN_POINT('Ctrl Pts',(-0.801241585030922,1.3333045293833,
1.87787999281922));
#284559=CARTESIAN_POINT('Ctrl Pts',(-0.752195963517563,1.36233235816509,
1.87387651925841));
#284560=CARTESIAN_POINT('Ctrl Pts',(-0.711077348352883,1.38423920806529,
1.87070664351387));
#284561=CARTESIAN_POINT('Ctrl Pts',(-0.584851109755567,1.44437690464246,
1.86133514685087));
#284562=CARTESIAN_POINT('Ctrl Pts',(-0.497230389517025,1.47683406465405,
1.85528933328042));
#284563=CARTESIAN_POINT('Ctrl Pts',(-0.361663326583314,1.51360784052488,
1.84596910989143));
#284564=CARTESIAN_POINT('Ctrl Pts',(-0.315563745840759,1.52388583831371,
1.84280748966478));
#284565=CARTESIAN_POINT('Ctrl Pts',(-0.237444094746595,1.53760581690063,
1.83739824475472));
#284566=CARTESIAN_POINT('Ctrl Pts',(-0.205655107193223,1.54217932751838,
1.83518322890479));
#284567=CARTESIAN_POINT('Ctrl Pts',(-0.160518005571697,1.5472528866153,
1.83200640101201));
#284568=CARTESIAN_POINT('Ctrl Pts',(-0.147268679623912,1.54857012813722,
1.83107008111648));
#284569=CARTESIAN_POINT('Ctrl Pts',(-0.124301642582489,1.55055609370397,
1.82943961692518));
#284570=CARTESIAN_POINT('Ctrl Pts',(-0.114591392886377,1.55130393633264,
1.82874798904557));
#284571=CARTESIAN_POINT('Ctrl Pts',(-0.0946393150333385,1.55265221375609,
1.82732186996137));
#284572=CARTESIAN_POINT('Ctrl Pts',(-0.0843973119566849,1.55324260218084,
1.82658709892692));
#284573=CARTESIAN_POINT('Ctrl Pts',(-0.0581983907073313,1.55449292208767,
1.82470027823698));
#284574=CARTESIAN_POINT('Ctrl Pts',(-0.0422361381574831,1.55500847931637,
1.82354378103776));
#284575=CARTESIAN_POINT('Ctrl Pts',(0.0234933103115159,1.5561186779589,
1.8187514137237));
#284576=CARTESIAN_POINT('Ctrl Pts',(0.0732620038764054,1.55457034310108,
1.81505035108349));
#284577=CARTESIAN_POINT('Ctrl Pts',(0.270407781668295,1.53894934109003,
1.80009810148991));
#284578=CARTESIAN_POINT('Ctrl Pts',(0.415503406604053,1.5062652021141,1.78835395481735));
#284579=CARTESIAN_POINT('Ctrl Pts',(0.5734162539313,1.44610349257725,1.77566162403263));
#284580=CARTESIAN_POINT('Ctrl Pts',(0.592893914943601,1.43822753087092,
1.7740996106817));
#284581=CARTESIAN_POINT('Ctrl Pts',(0.619509805704261,1.42683248928841,
1.77197556856206));
#284582=CARTESIAN_POINT('Ctrl Pts',(0.626788512176499,1.42365006940703,
1.77139579521323));
#284583=CARTESIAN_POINT('Ctrl Pts',(0.639077635127231,1.41816445723189,
1.77041916671233));
#284584=CARTESIAN_POINT('Ctrl Pts',(0.644100701288704,1.41589015891949,
1.77002062206805));
#284585=CARTESIAN_POINT('Ctrl Pts',(0.654502993514511,1.411113487851,1.7691967475409));
#284586=CARTESIAN_POINT('Ctrl Pts',(0.65988014213341,1.40860698752215,1.7687716709764));
#284587=CARTESIAN_POINT('Ctrl Pts',(0.674219644867172,1.40182264905352,
1.76763989295659));
#284588=CARTESIAN_POINT('Ctrl Pts',(0.683155782202183,1.39748955622364,
1.76693647301081));
#284589=CARTESIAN_POINT('Ctrl Pts',(0.724560054180047,1.37692073344363,
1.76368322558629));
#284590=CARTESIAN_POINT('Ctrl Pts',(0.756497812027981,1.35963580973052,
1.76119085517492));
#284591=CARTESIAN_POINT('Ctrl Pts',(0.862428841797037,1.2974154377602,1.75288246817431));
#284592=CARTESIAN_POINT('Ctrl Pts',(0.933270141217674,1.2474290569299,1.74724799126482));
#284593=CARTESIAN_POINT('Ctrl Pts',(1.06692013292578,1.13533438299877,1.73574118046835));
#284594=CARTESIAN_POINT('Ctrl Pts',(1.12933538843239,1.07326660355181,1.72988464500874));
#284595=CARTESIAN_POINT('Ctrl Pts',(1.19774664278753,0.992624458682775,
1.72254716066191));
#284596=CARTESIAN_POINT('Ctrl Pts',(1.20908379401704,0.97878325963177,1.72129694597782));
#284597=CARTESIAN_POINT('Ctrl Pts',(1.22679568110929,0.956381936877579,
1.71928594827722));
#284598=CARTESIAN_POINT('Ctrl Pts',(1.23332564890251,0.947946140825158,
1.71853138833459));
#284599=CARTESIAN_POINT('Ctrl Pts',(1.24556602477969,0.931792726585121,
1.71709124157548));
#284600=CARTESIAN_POINT('Ctrl Pts',(1.25129278423249,0.924088073683303,
1.71640634108907));
#284601=CARTESIAN_POINT('Ctrl Pts',(1.26422733761367,0.906345514949345,
1.71483336758056));
#284602=CARTESIAN_POINT('Ctrl Pts',(1.2713874783141,0.896273851696018,1.71394350963868));
#284603=CARTESIAN_POINT('Ctrl Pts',(1.2899525016156,0.869489591299989,1.71158441954779));
#284604=CARTESIAN_POINT('Ctrl Pts',(1.30115226887173,0.852638438955944,
1.7101076171718));
#284605=CARTESIAN_POINT('Ctrl Pts',(1.36924433004655,0.745720214082705,
1.70077940995386));
#284606=CARTESIAN_POINT('Ctrl Pts',(1.41707688625113,0.650241378874098,
1.69260332749517));
#284607=CARTESIAN_POINT('Ctrl Pts',(1.48710430951796,0.46523276796336,1.67726423463463));
#284608=CARTESIAN_POINT('Ctrl Pts',(1.51185211980472,0.377130338140775,
1.67016002808387));
#284609=CARTESIAN_POINT('Ctrl Pts',(1.53108891465178,0.27479168608536,1.66243553926147));
#284610=CARTESIAN_POINT('Ctrl Pts',(1.53329605643026,0.262196427907781,
1.66149397353666));
#284611=CARTESIAN_POINT('Ctrl Pts',(1.53639653965271,0.243122712002632,
1.66008326283441));
#284612=CARTESIAN_POINT('Ctrl Pts',(1.53740469616542,0.236663864017908,
1.65960817600959));
#284613=CARTESIAN_POINT('Ctrl Pts',(1.53916778456204,0.224881494712323,
1.65874650661287));
#284614=CARTESIAN_POINT('Ctrl Pts',(1.53993585390863,0.219560295911548,
1.65835923127157));
#284615=CARTESIAN_POINT('Ctrl Pts',(1.54162158563639,0.207437311016124,
1.65748112547824));
#284616=CARTESIAN_POINT('Ctrl Pts',(1.54252183966121,0.200633322831078,
1.65699126644039));
#284617=CARTESIAN_POINT('Ctrl Pts',(1.54517839983285,0.179479667371458,
1.65547689251072));
#284618=CARTESIAN_POINT('Ctrl Pts',(1.54677978282656,0.165110814622839,
1.65446051162804));
#284619=CARTESIAN_POINT('Ctrl Pts',(1.55740149024055,0.0560064688572886,
1.6468215302343));
#284620=CARTESIAN_POINT('Ctrl Pts',(1.55791253660047,-0.0393687362579156,
1.64058392966498));
#284621=CARTESIAN_POINT('Ctrl Pts',(1.54046895486907,-0.240796233696122,
1.62727932236513));
#284622=CARTESIAN_POINT('Ctrl Pts',(1.52026721709253,-0.346137046444243,
1.62022915360096));
#284623=CARTESIAN_POINT('Ctrl Pts',(1.48410274825739,-0.466217960032814,
1.6115348493163));
#284624=CARTESIAN_POINT('Ctrl Pts',(1.47847293622781,-0.48377461726748,
1.61024732300868));
#284625=CARTESIAN_POINT('Ctrl Pts',(1.46905773703682,-0.511435145181902,
1.60819055237718));
#284626=CARTESIAN_POINT('Ctrl Pts',(1.46547687093669,-0.521607201512875,
1.60742804816584));
#284627=CARTESIAN_POINT('Ctrl Pts',(1.45851645669041,-0.54074183403431,
1.60598164971215));
#284628=CARTESIAN_POINT('Ctrl Pts',(1.45515931044908,-0.549712069336964,
1.60529852964687));
#284629=CARTESIAN_POINT('Ctrl Pts',(1.44735402371341,-0.569995031256815,
1.60374208655094));
#284630=CARTESIAN_POINT('Ctrl Pts',(1.4428557326985,-0.581287643631238,
1.60286711408027));
#284631=CARTESIAN_POINT('Ctrl Pts',(1.4307849704745,-0.610586742118264,
1.60057435155424));
#284632=CARTESIAN_POINT('Ctrl Pts',(1.42300506046359,-0.628504840817679,
1.59914966287416));
#284633=CARTESIAN_POINT('Ctrl Pts',(1.36575491028151,-0.753843402546534,
1.58901960665432));
#284634=CARTESIAN_POINT('Ctrl Pts',(1.30452108890336,-0.855441697763552,
1.57990319328091));
#284635=CARTESIAN_POINT('Ctrl Pts',(1.18245199558247,-1.0139456456087,1.56438738008204));
#284636=CARTESIAN_POINT('Ctrl Pts',(1.12746941164851,-1.07475309733351,
1.55805122582995));
#284637=CARTESIAN_POINT('Ctrl Pts',(1.0590760648374,-1.13933626586966,1.55108092240368));
#284638=CARTESIAN_POINT('Ctrl Pts',(1.05010271244677,-1.14761211035633,
1.55018284681016));
#284639=CARTESIAN_POINT('Ctrl Pts',(1.03626343600544,-1.16007738416169,
1.54882382951428));
#284640=CARTESIAN_POINT('Ctrl Pts',(1.03146771024912,-1.16434351147904,
1.54835755958695));
#284641=CARTESIAN_POINT('Ctrl Pts',(1.02259969182071,-1.17213443090819,
1.54750411991568));
#284642=CARTESIAN_POINT('Ctrl Pts',(1.01853544046042,-1.1756678153428,1.54711634564948));
#284643=CARTESIAN_POINT('Ctrl Pts',(1.00922479364915,-1.18367779627746,
1.54623554616341));
#284644=CARTESIAN_POINT('Ctrl Pts',(1.00396688956023,-1.18814068990092,
1.545743511371));
#284645=CARTESIAN_POINT('Ctrl Pts',(0.987155811791567,-1.20221860242269,
1.54418665134727));
#284646=CARTESIAN_POINT('Ctrl Pts',(0.975492452644591,-1.21170156537091,
1.54313076188003));
#284647=CARTESIAN_POINT('Ctrl Pts',(0.901765972264607,-1.2698906289622,
1.53659263589172));
#284648=CARTESIAN_POINT('Ctrl Pts',(0.836201816090604,-1.31399159004533,
1.53136919426979));
#284649=CARTESIAN_POINT('Ctrl Pts',(0.728765934765258,-1.37494381213463,
1.5232304284675));
#284650=CARTESIAN_POINT('Ctrl Pts',(0.689036824046572,-1.39527720676207,
1.52030343793704));
#284651=CARTESIAN_POINT('Ctrl Pts',(0.600494544366389,-1.43588809674943,
1.51386135826791));
#284652=CARTESIAN_POINT('Ctrl Pts',(0.551413544326983,-1.45544177468332,
1.5103407697118));
#284653=CARTESIAN_POINT('Ctrl Pts',(0.468602906810515,-1.48364234297905,
1.50438972313286));
#284654=CARTESIAN_POINT('Ctrl Pts',(0.435407203321454,-1.49372137612275,
1.50200172102691));
#284655=CARTESIAN_POINT('Ctrl Pts',(0.388667759609058,-1.50622221594098,
1.49862047343261));
#284656=CARTESIAN_POINT('Ctrl Pts',(0.375385336880381,-1.50958730082631,
1.49765753200508));
#284657=CARTESIAN_POINT('Ctrl Pts',(0.352523444031966,-1.51505895532117,
1.49599569570089));
#284658=CARTESIAN_POINT('Ctrl Pts',(0.342965160317022,-1.51725123413279,
1.49529959190405));
#284659=CARTESIAN_POINT('Ctrl Pts',(0.324648695049365,-1.52127036024526,
1.49396284993019));
#284660=CARTESIAN_POINT('Ctrl Pts',(0.315894201140588,-1.52311231748,1.49332272650682));
#284661=CARTESIAN_POINT('Ctrl Pts',(0.295270020285172,-1.52726621574631,
1.49181160125686));
#284662=CARTESIAN_POINT('Ctrl Pts',(0.283388451122589,-1.52951542948631,
1.49093863893509));
#284663=CARTESIAN_POINT('Ctrl Pts',(0.241492288320197,-1.53694156520723,
1.48785130352396));
#284664=CARTESIAN_POINT('Ctrl Pts',(0.211354839350661,-1.54137496793553,
1.48561384831914));
#284665=CARTESIAN_POINT('Ctrl Pts',(0.0528087382752864,-1.55996107100571,
1.47374876898916));
#284666=CARTESIAN_POINT('Ctrl Pts',(-0.0768491300443284,-1.55895811007058,
1.46366327116439));
#284667=CARTESIAN_POINT('Ctrl Pts',(-0.244469628369181,-1.53668848421321,
1.45060899316746));
#284668=CARTESIAN_POINT('Ctrl Pts',(-0.283864933524152,-1.52990131253699,
1.44754513010654));
#284669=CARTESIAN_POINT('Ctrl Pts',(-0.338868684202275,-1.51822687193035,
1.44330712236147));
#284670=CARTESIAN_POINT('Ctrl Pts',(-0.354726635850338,-1.51460023841246,
1.44209005175325));
#284671=CARTESIAN_POINT('Ctrl Pts',(-0.38260503991278,-1.50776268903657,
1.43996211760959));
#284672=CARTESIAN_POINT('Ctrl Pts',(-0.394649139467748,-1.50465511854824,
1.4390466903879));
#284673=CARTESIAN_POINT('Ctrl Pts',(-0.412896288484655,-1.49971287720815,
1.43766701973659));
#284674=CARTESIAN_POINT('Ctrl Pts',(-0.419126963398019,-1.4979835285174,
1.43719720670766));
#284675=CARTESIAN_POINT('Ctrl Pts',(-0.430522942544951,-1.49474385879403,
1.4363405050839));
#284676=CARTESIAN_POINT('Ctrl Pts',(-0.435691287271443,-1.49324556301258,
1.4359529763684));
#284677=CARTESIAN_POINT('Ctrl Pts',(-0.447517262238299,-1.48975060180827,
1.43506847751558));
#284678=CARTESIAN_POINT('Ctrl Pts',(-0.454169400266483,-1.4877361044164,
1.43457254019766));
#284679=CARTESIAN_POINT('Ctrl Pts',(-0.4750606902839,-1.48125631577529,
1.43301939573248));
#284680=CARTESIAN_POINT('Ctrl Pts',(-0.489249737735284,-1.47663051222814,
1.43197092991726));
#284681=CARTESIAN_POINT('Ctrl Pts',(-0.583033933464068,-1.44455537745482,
1.42506983814199));
#284682=CARTESIAN_POINT('Ctrl Pts',(-0.660364994078612,-1.41088296827782,
1.4195139224779));
#284683=CARTESIAN_POINT('Ctrl Pts',(-0.804495084826273,-1.33366256007784,
1.40874816494985));
#284684=CARTESIAN_POINT('Ctrl Pts',(-0.871421654623025,-1.29092658562996,
1.40355143959259));
#284685=CARTESIAN_POINT('Ctrl Pts',(-0.970550163391214,-1.21639370300923,
1.39518810442193));
#284686=CARTESIAN_POINT('Ctrl Pts',(-1.00512462099946,-1.18798364691941,
1.39212948084136));
#284687=CARTESIAN_POINT('Ctrl Pts',(-1.04958706184484,-1.14811672974715,
1.38796617300013));
#284688=CARTESIAN_POINT('Ctrl Pts',(-1.06060388538366,-1.13794744882559,
1.38691459258498));
#284689=CARTESIAN_POINT('Ctrl Pts',(-1.07876167149295,-1.12069381796013,
1.3851463628521));
#284690=CARTESIAN_POINT('Ctrl Pts',(-1.08598416941231,-1.11369643649439,
1.38443346623776));
#284691=CARTESIAN_POINT('Ctrl Pts',(-1.10007685701575,-1.09977556023671,
1.38302309476224));
#284692=CARTESIAN_POINT('Ctrl Pts',(-1.10695078617103,-1.09285649708828,
1.38232583376938));
#284693=CARTESIAN_POINT('Ctrl Pts',(-1.1234944072443,-1.07588802926341,
1.38062451185305));
#284694=CARTESIAN_POINT('Ctrl Pts',(-1.13309473160344,-1.06577250868071,
1.37961750499015));
#284695=CARTESIAN_POINT('Ctrl Pts',(-1.16556857436224,-1.03062121363665,
1.37614156031102));
#284696=CARTESIAN_POINT('Ctrl Pts',(-1.18775722482965,-1.00496897117351,
1.37364447290536));
#284697=CARTESIAN_POINT('Ctrl Pts',(-1.28060425666047,-0.890255428133158,
1.36263750146825));
#284698=CARTESIAN_POINT('Ctrl Pts',(-1.34220967966605,-0.7943346874261,
1.35380049791934));
#284699=CARTESIAN_POINT('Ctrl Pts',(-1.42104203417698,-0.63579949219518,
1.34009253128453));
#284700=CARTESIAN_POINT('Ctrl Pts',(-1.44578090698632,-0.577339335262993,
1.33521561712965));
#284701=CARTESIAN_POINT('Ctrl Pts',(-1.47177421462297,-0.503663589952632,
1.32940066046637));
#284702=CARTESIAN_POINT('Ctrl Pts',(-1.47646861112187,-0.489731388441157,
1.32831529212413));
#284703=CARTESIAN_POINT('Ctrl Pts',(-1.4830780131398,-0.469156252690684,
1.32673532298303));
#284704=CARTESIAN_POINT('Ctrl Pts',(-1.4851472291247,-0.462564260622396,
1.32623254887302));
#284705=CARTESIAN_POINT('Ctrl Pts',(-1.48859807323881,-0.451308850062166,
1.32538017497586));
#284706=CARTESIAN_POINT('Ctrl Pts',(-1.49000183658651,-0.44665247257127,
1.32502932202018));
#284707=CARTESIAN_POINT('Ctrl Pts',(-1.49316581611957,-0.435976406432577,
1.32422898535905));
#284708=CARTESIAN_POINT('Ctrl Pts',(-1.49491149247583,-0.429952572676887,
1.32378034360659));
#284709=CARTESIAN_POINT('Ctrl Pts',(-1.49967029050861,-0.413151888714799,
1.32253679958487));
#284710=CARTESIAN_POINT('Ctrl Pts',(-1.50260370409731,-0.402352570303646,
1.32174628796744));
#284711=CARTESIAN_POINT('Ctrl Pts',(-1.52349661870134,-0.322018361500382,
1.31592455248651));
#284712=CARTESIAN_POINT('Ctrl Pts',(-1.53674035490596,-0.251335933271153,
1.31112552824004));
#284713=CARTESIAN_POINT('Ctrl Pts',(-1.55196062677587,-0.120678045176283,
1.30242901063917));
#284714=CARTESIAN_POINT('Ctrl Pts',(-1.55544879049007,-0.0610252666929087,
1.29852343257111));
#284715=CARTESIAN_POINT('Ctrl Pts',(-1.55556451017232,0.0753844301872104,
1.28949615929373));
#284716=CARTESIAN_POINT('Ctrl Pts',(-1.54995612352385,0.151978427235645,
1.28435416547317));
#284717=CARTESIAN_POINT('Ctrl Pts',(-1.53610640855601,0.245512772204258,
1.27779331556791));
#284718=CARTESIAN_POINT('Ctrl Pts',(-1.53318543656123,0.263138349608341,
1.27654485595358));
#284719=CARTESIAN_POINT('Ctrl Pts',(-1.52803752297669,0.291196258961756,
1.27453602118211));
#284720=CARTESIAN_POINT('Ctrl Pts',(-1.52600566356196,0.30166311909529,
1.27378184543579));
#284721=CARTESIAN_POINT('Ctrl Pts',(-1.52194001851677,0.321513617165654,
1.27234200819764));
#284722=CARTESIAN_POINT('Ctrl Pts',(-1.51992663286587,0.330900965670557,
1.27165702888136));
#284723=CARTESIAN_POINT('Ctrl Pts',(-1.51512120871579,0.352336367341829,
1.27008326972483));
#284724=CARTESIAN_POINT('Ctrl Pts',(-1.51227215768968,0.364370824160014,
1.26919269832077));
#284725=CARTESIAN_POINT('Ctrl Pts',(-1.50287944293008,0.402036544633793,
1.26638256413903));
#284726=CARTESIAN_POINT('Ctrl Pts',(-1.49582559289182,0.427534372904009,
1.2644468131633));
#284727=CARTESIAN_POINT('Ctrl Pts',(-1.44396539905443,0.597958184317801,
1.25127379158226));
#284728=CARTESIAN_POINT('Ctrl Pts',(-1.37881774665419,0.735821562903013,
1.2393468258457));
#284729=CARTESIAN_POINT('Ctrl Pts',(-1.27040596013088,0.898657001686139,
1.22434587809634));
#284730=CARTESIAN_POINT('Ctrl Pts',(-1.24447989577291,0.934230327061191,
1.22101266279073));
#284731=CARTESIAN_POINT('Ctrl Pts',(-1.21054621632769,0.976866479589994,
1.21698911397459));
#284732=CARTESIAN_POINT('Ctrl Pts',(-1.20393154694693,0.985007160949235,
1.21621955657018));
#284733=CARTESIAN_POINT('Ctrl Pts',(-1.19336971412907,0.997740260143308,
1.21501457181498));
#284734=CARTESIAN_POINT('Ctrl Pts',(-1.18947736801325,1.00237742176221,
1.21457546279458));
#284735=CARTESIAN_POINT('Ctrl Pts',(-1.18202152118981,1.01115538613324,
1.21374391198384));
#284736=CARTESIAN_POINT('Ctrl Pts',(-1.17846326852695,1.01530016114741,
1.21335115067482));
#284737=CARTESIAN_POINT('Ctrl Pts',(-1.16987393422634,1.0251993209713,1.21241261847622));
#284738=CARTESIAN_POINT('Ctrl Pts',(-1.16482214663725,1.03093551828566,
1.21186836536251));
#284739=CARTESIAN_POINT('Ctrl Pts',(-1.14706630145771,1.05079975711348,
1.20998122343407));
#284740=CARTESIAN_POINT('Ctrl Pts',(-1.13414524325496,1.06473277467991,
1.20865325041874));
#284741=CARTESIAN_POINT('Ctrl Pts',(-1.10106927157342,1.09911362797249,
1.2053545529455));
#284742=CARTESIAN_POINT('Ctrl Pts',(-1.08059699787663,1.11924735710697,
1.20340259345937));
#284743=CARTESIAN_POINT('Ctrl Pts',(-1.00609126913938,1.18856974925828,
1.1965566831711));
#284744=CARTESIAN_POINT('Ctrl Pts',(-0.949162167166272,1.23450801561769,
1.19178128620634));
#284745=CARTESIAN_POINT('Ctrl Pts',(-0.811823094013529,1.33019541035699,
1.18075423134217));
#284746=CARTESIAN_POINT('Ctrl Pts',(-0.729701252242791,1.37695647376491,
1.17449221377283));
#284747=CARTESIAN_POINT('Ctrl Pts',(-0.627344598702263,1.42349852551739,
1.16669344762085));
#284748=CARTESIAN_POINT('Ctrl Pts',(-0.610702394312591,1.43071724508431,
1.16542621850667));
#284749=CARTESIAN_POINT('Ctrl Pts',(-0.58402985280599,1.44173656272076,
1.1633943484695));
#284750=CARTESIAN_POINT('Ctrl Pts',(-0.57407953304397,1.44572745170668,
1.16263616431264));
#284751=CARTESIAN_POINT('Ctrl Pts',(-0.555152645091275,1.45309247501296,
1.16119322077914));
#284752=CARTESIAN_POINT('Ctrl Pts',(-0.546184538974721,1.45648708957448,
1.16050918816043));
#284753=CARTESIAN_POINT('Ctrl Pts',(-0.525677952481883,1.46403323180203,
1.15894402753608));
#284754=CARTESIAN_POINT('Ctrl Pts',(-0.514120746931992,1.46813162049813,
1.15806117844692));
#284755=CARTESIAN_POINT('Ctrl Pts',(-0.478029880761631,1.48045167178435,
1.15530120179547));
#284756=CARTESIAN_POINT('Ctrl Pts',(-0.45333986770594,1.48819774726452,
1.15340870242827));
#284757=CARTESIAN_POINT('Ctrl Pts',(-0.33670986053917,1.52161685662852,
1.14444313599912));
#284758=CARTESIAN_POINT('Ctrl Pts',(-0.242739770323382,1.53940351201316,
1.13712706701058));
#284759=CARTESIAN_POINT('Ctrl Pts',(-0.0539903401947642,1.55741320465323,
1.12243307359287));
#284760=CARTESIAN_POINT('Ctrl Pts',(0.0403943634692655,1.55782613260909,
1.11508996816958));
#284761=CARTESIAN_POINT('Ctrl Pts',(0.147353240799339,1.54856076175381,
1.10710082913873));
#284762=CARTESIAN_POINT('Ctrl Pts',(0.160448820150422,1.54725874251856,
1.1061286491597));
#284763=CARTESIAN_POINT('Ctrl Pts',(0.180175331838236,1.5450442903511,1.10467474623197));
#284764=CARTESIAN_POINT('Ctrl Pts',(0.186819093495798,1.54425504371015,
1.10418688994393));
#284765=CARTESIAN_POINT('Ctrl Pts',(0.19887556176696,1.5427438462499,1.10330510814054));
#284766=CARTESIAN_POINT('Ctrl Pts',(0.204289946793778,1.54203621415017,
1.1029104128738));
#284767=CARTESIAN_POINT('Ctrl Pts',(0.215560818039924,1.54050276223701,
1.10209163850011));
#284768=CARTESIAN_POINT('Ctrl Pts',(0.221416478613796,1.5396720341906,1.10166783367192));
#284769=CARTESIAN_POINT('Ctrl Pts',(0.237006849981335,1.53736948363762,
1.10054334525802));
#284770=CARTESIAN_POINT('Ctrl Pts',(0.246732767878881,1.53583857571875,
1.09984586888428));
#284771=CARTESIAN_POINT('Ctrl Pts',(0.295297877051716,1.52772092642333,
1.09638027075595));
#284772=CARTESIAN_POINT('Ctrl Pts',(0.333895189023762,1.51975218066694,
1.093680875597));
#284773=CARTESIAN_POINT('Ctrl Pts',(0.446404473278318,1.4920293200046,1.08586344574943));
#284774=CARTESIAN_POINT('Ctrl Pts',(0.519211249974908,1.46828116653457,
1.08086686669834));
#284775=CARTESIAN_POINT('Ctrl Pts',(0.677453029612676,1.40341546865666,
1.06960056678341));
#284776=CARTESIAN_POINT('Ctrl Pts',(0.761463632359443,1.35966436708586,
1.0633248192028));
#284777=CARTESIAN_POINT('Ctrl Pts',(0.856237170966289,1.2987560169618,1.05551098162959));
#284778=CARTESIAN_POINT('Ctrl Pts',(0.871323554451145,1.28868324274627,
1.05424377363127));
#284779=CARTESIAN_POINT('Ctrl Pts',(0.895040775568518,1.2722410166312,1.05221189446662));
#284780=CARTESIAN_POINT('Ctrl Pts',(0.903788145309655,1.26604193151345,
1.05145367879232));
#284781=CARTESIAN_POINT('Ctrl Pts',(0.920237092274717,1.25412754919312,
1.05001064560518));
#284782=CARTESIAN_POINT('Ctrl Pts',(0.927951290303024,1.24843045897161,
1.04932655460965));
#284783=CARTESIAN_POINT('Ctrl Pts',(0.945409596321133,1.23528593810463,
1.04776121642826));
#284784=CARTESIAN_POINT('Ctrl Pts',(0.955119182492497,1.22779395051074,
1.04687824755671));
#284785=CARTESIAN_POINT('Ctrl Pts',(0.985040158112796,1.20413700063848,
1.04411771195132));
#284786=CARTESIAN_POINT('Ctrl Pts',(1.0049364571286,1.18758266982385,1.04222476646123));
#284787=CARTESIAN_POINT('Ctrl Pts',(1.09777369726286,1.10633529716653,1.03310799557386));
#284788=CARTESIAN_POINT('Ctrl Pts',(1.16492737130343,1.03538551027477,1.02562932804202));
#284789=CARTESIAN_POINT('Ctrl Pts',(1.28173779174257,0.886118993253203,
1.01093700402529));
#284790=CARTESIAN_POINT('Ctrl Pts',(1.33193853823549,0.808703548050602,
1.00376423871194));
#284791=CARTESIAN_POINT('Ctrl Pts',(1.38175212007759,0.714527782444577,
0.99583561286931));
#284792=CARTESIAN_POINT('Ctrl Pts',(1.38832767936271,0.701665994306596,
0.994769189952345));
#284793=CARTESIAN_POINT('Ctrl Pts',(1.39780460524719,0.682474148564347,
0.993204025876144));
#284794=CARTESIAN_POINT('Ctrl Pts',(1.40084395447192,0.676213648275335,
0.992697521384129));
#284795=CARTESIAN_POINT('Ctrl Pts',(1.40615896372874,0.665076069564426,
0.991803888519324));
#284796=CARTESIAN_POINT('Ctrl Pts',(1.40845145157185,0.660207332016687,
0.991415762194369));
#284797=CARTESIAN_POINT('Ctrl Pts',(1.4134395569626,0.649469458187675,0.990565314440879));
#284798=CARTESIAN_POINT('Ctrl Pts',(1.4161239343988,0.643595342384742,0.990103672237949));
#284799=CARTESIAN_POINT('Ctrl Pts',(1.42385621014514,0.626392494568939,
0.988761679621271));
#284800=CARTESIAN_POINT('Ctrl Pts',(1.42880544845994,0.615019577245407,
0.987887027531342));
#284801=CARTESIAN_POINT('Ctrl Pts',(1.43990681850609,0.5886520517134,0.985885216676517));
#284802=CARTESIAN_POINT('Ctrl Pts',(1.44596179006804,0.573617845990316,
0.984762988082385));
#284803=CARTESIAN_POINT('Ctrl Pts',(1.46604606495604,0.521409371128415,
0.98092242534933));
#284804=CARTESIAN_POINT('Ctrl Pts',(1.47888627647228,0.483791936155673,
0.978252864158474));
#284805=CARTESIAN_POINT('Ctrl Pts',(1.51824606616646,0.352192236121999,
0.969116115765335));
#284806=CARTESIAN_POINT('Ctrl Pts',(1.53735256498088,0.256238169444717,
0.962789957058778));
#284807=CARTESIAN_POINT('Ctrl Pts',(1.55300508476299,0.104032516626026,
0.952556490653376));
#284808=CARTESIAN_POINT('Ctrl Pts',(1.55572379976144,0.0486821573415437,
0.948797804397603));
#284809=CARTESIAN_POINT('Ctrl Pts',(1.55541437507945,-0.0232511031328495,
0.943796304505901));
#284810=CARTESIAN_POINT('Ctrl Pts',(1.55507869387626,-0.0398084298318202,
0.942637213105604));
#284811=CARTESIAN_POINT('Ctrl Pts',(1.55410256400944,-0.0667328787470038,
0.940737990149875));
#284812=CARTESIAN_POINT('Ctrl Pts',(1.55362250808619,-0.0771047954220716,
0.940002892249914));
#284813=CARTESIAN_POINT('Ctrl Pts',(1.55249421480392,-0.097137548993712,
0.938575994924655));
#284814=CARTESIAN_POINT('Ctrl Pts',(1.5518595368114,-0.10679869201468,0.937884653237171));
#284815=CARTESIAN_POINT('Ctrl Pts',(1.55016397141644,-0.129383327005083,
0.936260723444656));
#284816=CARTESIAN_POINT('Ctrl Pts',(1.54903160645721,-0.142300551066779,
0.935325935915946));
#284817=CARTESIAN_POINT('Ctrl Pts',(1.54475031973883,-0.18499536391627,
0.932215548937597));
#284818=CARTESIAN_POINT('Ctrl Pts',(1.54090327360402,-0.214694451259772,
0.930018415605765));
#284819=CARTESIAN_POINT('Ctrl Pts',(1.52948480331689,-0.286506930390575,
0.924620485594281));
#284820=CARTESIAN_POINT('Ctrl Pts',(1.52102861647656,-0.328452975793619,
0.921395149483289));
#284821=CARTESIAN_POINT('Ctrl Pts',(1.49539853146159,-0.433112353343308,
0.91317351482875));
#284822=CARTESIAN_POINT('Ctrl Pts',(1.47600221386355,-0.495196527239499,
0.908133147520748));
#284823=CARTESIAN_POINT('Ctrl Pts',(1.44667406404472,-0.571844844974288,
0.901768996687771));
#284824=CARTESIAN_POINT('Ctrl Pts',(1.44030336850702,-0.587706210834056,
0.900444349535024));
#284825=CARTESIAN_POINT('Ctrl Pts',(1.4088024861588,-0.662544623366514,
0.894164782443614));
#284826=CARTESIAN_POINT('Ctrl Pts',(1.38030054117883,-0.720043185061402,
0.889249712250288));
#284827=CARTESIAN_POINT('Ctrl Pts',(1.34277965306335,-0.785268646814441,
0.883684444331667));
#284828=CARTESIAN_POINT('Ctrl Pts',(1.33712818018458,-0.794853629945437,
0.882866966277334));
#284829=CARTESIAN_POINT('Ctrl Pts',(1.32813862447611,-0.80973279034294,
0.88159946622582));
#284830=CARTESIAN_POINT('Ctrl Pts',(1.32487075861659,-0.815068631609816,
0.881145232625444));
#284831=CARTESIAN_POINT('Ctrl Pts',(1.31900480806258,-0.824518183889099,
0.880341549281049));
#284832=CARTESIAN_POINT('Ctrl Pts',(1.31641958748473,-0.828639481330176,
0.879991306410469));
#284833=CARTESIAN_POINT('Ctrl Pts',(1.3101059226096,-0.838600453558989,
0.879145363411839));
#284834=CARTESIAN_POINT('Ctrl Pts',(1.30635774063827,-0.844427443614875,
0.878650964979895));
#284835=CARTESIAN_POINT('Ctrl Pts',(1.29447787244953,-0.862627671368899,
0.877107545084808));
#284836=CARTESIAN_POINT('Ctrl Pts',(1.2862080941584,-0.874910419584213,
0.876067112103536));
#284837=CARTESIAN_POINT('Ctrl Pts',(1.24102146719002,-0.939998393763268,
0.870549118694733));
#284838=CARTESIAN_POINT('Ctrl Pts',(1.20102177002697,-0.990595769730546,
0.866241856853231));
#284839=CARTESIAN_POINT('Ctrl Pts',(1.08011548284486,-1.12540479284887,
0.854262536242355));
#284840=CARTESIAN_POINT('Ctrl Pts',(0.992723629925456,-1.20319720618115,
0.846703145998765));
#284841=CARTESIAN_POINT('Ctrl Pts',(0.872244032368145,-1.28830265682975,
0.83663769092527));
#284842=CARTESIAN_POINT('Ctrl Pts',(0.84650472564177,-1.30535930645551,
0.834507680960866));
#284843=CARTESIAN_POINT('Ctrl Pts',(0.809945483264368,-1.32804985010774,
0.83149939687293));
#284844=CARTESIAN_POINT('Ctrl Pts',(0.799540009872801,-1.33434022949317,
0.83064507628571));
#284845=CARTESIAN_POINT('Ctrl Pts',(0.78133839875095,-1.34505423024224,
0.829153306560477));
#284846=CARTESIAN_POINT('Ctrl Pts',(0.773575680986267,-1.34953371033726,
0.828517909302391));
#284847=CARTESIAN_POINT('Ctrl Pts',(0.757251180852822,-1.35876664387708,
0.827183156970268));
#284848=CARTESIAN_POINT('Ctrl Pts',(0.748682380623921,-1.36350681269444,
0.826483361197453));
#284849=CARTESIAN_POINT('Ctrl Pts',(0.728087465584181,-1.37464703526844,
0.824803042643302));
#284850=CARTESIAN_POINT('Ctrl Pts',(0.71602109872874,-1.38097052586814,
0.823819864040173));
#284851=CARTESIAN_POINT('Ctrl Pts',(0.673425432805196,-1.40258484174555,
0.820352665509381));
#284852=CARTESIAN_POINT('Ctrl Pts',(0.642479214222601,-1.41702723137289,
0.817839726618729));
#284853=CARTESIAN_POINT('Ctrl Pts',(0.563635704947146,-1.45070926516517,
0.81144771297296));
#284854=CARTESIAN_POINT('Ctrl Pts',(0.515211722130124,-1.46860427794763,
0.807530222112154));
#284855=CARTESIAN_POINT('Ctrl Pts',(0.409479535773776,-1.5018040303023,
0.799016768452861));
#284856=CARTESIAN_POINT('Ctrl Pts',(0.352000771426533,-1.51630598873582,
0.794412440130713));
#284857=CARTESIAN_POINT('Ctrl Pts',(0.222994372100513,-1.54112239410058,
0.78423540809957));
#284858=CARTESIAN_POINT('Ctrl Pts',(0.151280085644583,-1.54980693845474,
0.778681197658446));
#284859=CARTESIAN_POINT('Ctrl Pts',(0.0680365170133073,-1.55405165719224,
0.772515785488483));
#284860=CARTESIAN_POINT('Ctrl Pts',(0.0568523321897233,-1.55450099788973,
0.771693367913762));
#284861=CARTESIAN_POINT('Ctrl Pts',(0.0393937461569052,-1.55501373976952,
0.770419802986291));
#284862=CARTESIAN_POINT('Ctrl Pts',(0.0331224372677322,-1.55515996153874,
0.769964384347709));
#284863=CARTESIAN_POINT('Ctrl Pts',(0.021984896215217,-1.55535224089054,
0.76915943880821));
#284864=CARTESIAN_POINT('Ctrl Pts',(0.0171192645325594,-1.55541340510226,
0.768809109064862));
#284865=CARTESIAN_POINT('Ctrl Pts',(0.00533892613749954,-1.55550620574388,
0.767964035816541));
#284866=CARTESIAN_POINT('Ctrl Pts',(-0.00157581618784463,-1.55551457142069,
0.767470582717171));
#284867=CARTESIAN_POINT('Ctrl Pts',(-0.0232057863965961,-1.55539650437889,
0.765934441211598));
#284868=CARTESIAN_POINT('Ctrl Pts',(-0.0379198374659211,-1.55510736659196,
0.764900213633982));
#284869=CARTESIAN_POINT('Ctrl Pts',(-0.116118566170711,-1.55246010154481,
0.759450272660226));
#284870=CARTESIAN_POINT('Ctrl Pts',(-0.179425560112246,-1.5464230653951,
0.755200066184727));
#284871=CARTESIAN_POINT('Ctrl Pts',(-0.354848892399446,-1.51877229410457,
0.743446326297378));
#284872=CARTESIAN_POINT('Ctrl Pts',(-0.465203075819883,-1.4886812068753,
0.736054560396688));
#284873=CARTESIAN_POINT('Ctrl Pts',(-0.602385267824321,-1.43451420336989,
0.726014921118387));
#284874=CARTESIAN_POINT('Ctrl Pts',(-0.633089345697491,-1.42123067018792,
0.723711455681568));
#284875=CARTESIAN_POINT('Ctrl Pts',(-0.675882810235645,-1.40105495214973,
0.720406084278627));
#284876=CARTESIAN_POINT('Ctrl Pts',(-0.688345942198975,-1.3949739761155,
0.719431758614794));
#284877=CARTESIAN_POINT('Ctrl Pts',(-0.70942330680691,-1.38433873349922,
0.717763084697398));
#284878=CARTESIAN_POINT('Ctrl Pts',(-0.718079248868177,-1.37986859584346,
0.717071699792114));
#284879=CARTESIAN_POINT('Ctrl Pts',(-0.735606519807462,-1.37060750871328,
0.715658930312276));
#284880=CARTESIAN_POINT('Ctrl Pts',(-0.744474383518997,-1.36581103318115,
0.714937375691222));
#284881=CARTESIAN_POINT('Ctrl Pts',(-0.766509028440103,-1.35361452179986,
0.713127116897841));
#284882=CARTESIAN_POINT('Ctrl Pts',(-0.779615571380525,-1.34610842625631,
0.712034661526545));
#284883=CARTESIAN_POINT('Ctrl Pts',(-0.807604575825206,-1.32953329199679,
0.709666881177451));
#284884=CARTESIAN_POINT('Ctrl Pts',(-0.822447971733887,-1.32040267113258,
0.708389447992213));
#284885=CARTESIAN_POINT('Ctrl Pts',(-0.865171431028327,-1.29312227989664,
0.70464787802131));
#284886=CARTESIAN_POINT('Ctrl Pts',(-0.892625077539465,-1.27432610304691,
0.702161374564172));
#284887=CARTESIAN_POINT('Ctrl Pts',(-0.988685215355922,-1.20393059419525,
0.693162316415759));
#284888=CARTESIAN_POINT('Ctrl Pts',(-1.05359295540303,-1.14755675013085,
0.686502611333705));
#284889=CARTESIAN_POINT('Ctrl Pts',(-1.16334215407464,-1.03504001332638,
0.674317888887702));
#284890=CARTESIAN_POINT('Ctrl Pts',(-1.20960140150812,-0.980581127914488,
0.668807902385738));
#284891=CARTESIAN_POINT('Ctrl Pts',(-1.26087083271932,-0.911049062565754,
0.662374611058342));
#284892=CARTESIAN_POINT('Ctrl Pts',(-1.26960575501918,-0.898836426917664,
0.661265693583988));
#284893=CARTESIAN_POINT('Ctrl Pts',(-1.28213375016899,-0.880773434201796,
0.659658211864933));
#284894=CARTESIAN_POINT('Ctrl Pts',(-1.28606619168883,-0.875021457631531,
0.659151080474249));
#284895=CARTESIAN_POINT('Ctrl Pts',(-1.29296643676138,-0.864781468675158,
0.658256916712449));
#284896=CARTESIAN_POINT('Ctrl Pts',(-1.29594976810098,-0.860304246706169,
0.65786887823863));
#284897=CARTESIAN_POINT('Ctrl Pts',(-1.30245604872051,-0.85042932259697,
0.657019440137136));
#284898=CARTESIAN_POINT('Ctrl Pts',(-1.30596873679009,-0.845025120396164,
0.65655871192874));
#284899=CARTESIAN_POINT('Ctrl Pts',(-1.31611794131899,-0.829196311699765,
0.655220783822836));
#284900=CARTESIAN_POINT('Ctrl Pts',(-1.32266414012252,-0.818713965021877,
0.654349241911004));
#284901=CARTESIAN_POINT('Ctrl Pts',(-1.3374671408684,-0.794369051698037,
0.652355504380398));
#284902=CARTESIAN_POINT('Ctrl Pts',(-1.34563470015674,-0.780453614269328,
0.651238192052071));
#284903=CARTESIAN_POINT('Ctrl Pts',(-1.37303007173308,-0.732069839464504,
0.647420405751045));
#284904=CARTESIAN_POINT('Ctrl Pts',(-1.39116288887486,-0.69699648300642,
0.644768161173048));
#284905=CARTESIAN_POINT('Ctrl Pts',(-1.45339524223424,-0.564494253885719,
0.635029697397613));
#284906=CARTESIAN_POINT('Ctrl Pts',(-1.48874816292867,-0.463293363835836,
0.628118192579953));
#284907=CARTESIAN_POINT('Ctrl Pts',(-1.5245725570003,-0.312379502804916,
0.617692962149108));
#284908=CARTESIAN_POINT('Ctrl Pts',(-1.53351674771813,-0.265005807328792,
0.614407765930124));
#284909=CARTESIAN_POINT('Ctrl Pts',(-1.54245194867326,-0.201671165547637,
0.609955003993573));
#284910=CARTESIAN_POINT('Ctrl Pts',(-1.5444184294341,-0.186013321596209,
0.608849415306203));
#284911=CARTESIAN_POINT('Ctrl Pts',(-1.54726452085034,-0.160178144410728,
0.607016021853066));
#284912=CARTESIAN_POINT('Ctrl Pts',(-1.54828273566704,-0.150016988513915,
0.606292605833772));
#284913=CARTESIAN_POINT('Ctrl Pts',(-1.55001853938621,-0.130788022989853,
0.604918861160473));
#284914=CARTESIAN_POINT('Ctrl Pts',(-1.55075678723504,-0.121722470209087,
0.604269213089911));
#284915=CARTESIAN_POINT('Ctrl Pts',(-1.55210380397938,-0.103171547151945,
0.602935533875908));
#284916=CARTESIAN_POINT('Ctrl Pts',(-1.55270522115207,-0.0936860459676571,
0.602251299817703));
#284917=CARTESIAN_POINT('Ctrl Pts',(-1.55391914855842,-0.0712918716144281,
0.600630245641894));
#284918=CARTESIAN_POINT('Ctrl Pts',(-1.55445778287666,-0.058380079888536,
0.599691163043238));
#284919=CARTESIAN_POINT('Ctrl Pts',(-1.55528652596405,-0.030037318954975,
0.597619631210879));
#284920=CARTESIAN_POINT('Ctrl Pts',(-1.55550797093957,-0.0146059614368184,
0.596485179220674));
#284921=CARTESIAN_POINT('Ctrl Pts',(-1.5554997809254,0.000825554981074353,
0.595343941296876));
#284922=CARTESIAN_POINT('',(-0.903577283124934,-1.26614704652365,4.13766671841787E-5));
#284923=CARTESIAN_POINT('Ctrl Pts',(-0.903577283124934,-1.26614704652365,
4.13766671842897E-5));
#284924=CARTESIAN_POINT('Ctrl Pts',(-0.854864239968711,-1.30091078056915,
0.00435153502361089));
#284925=CARTESIAN_POINT('Ctrl Pts',(-0.804029053149215,-1.33293958991072,
0.00866169338003741));
#284926=CARTESIAN_POINT('Ctrl Pts',(-0.75141824501022,-1.36196581126905,
0.0129718517364641));
#284927=CARTESIAN_POINT('Ctrl Pts',(-0.701345114626583,-1.38959195536439,
0.0170741099793956));
#284928=CARTESIAN_POINT('Ctrl Pts',(-0.64966423731578,-1.41449818738748,
0.0211763682223272));
#284929=CARTESIAN_POINT('Ctrl Pts',(-0.596706059304791,-1.43649647712375,
0.0252786264652587));
#284930=CARTESIAN_POINT('Ctrl Pts',(-0.543795605076904,-1.45847494288481,
0.0293771879178177));
#284931=CARTESIAN_POINT('Ctrl Pts',(-0.48961061798377,-1.47755045266205,
0.0334757493703768));
#284932=CARTESIAN_POINT('Ctrl Pts',(-0.434504797180995,-1.49358154488689,
0.0375743108229358));
#284933=CARTESIAN_POINT('Ctrl Pts',(-0.379426492987175,-1.50960463212624,
0.0416708256947322));
#284934=CARTESIAN_POINT('Ctrl Pts',(-0.323428775682673,-1.52258616624964,
0.0457673405665284));
#284935=CARTESIAN_POINT('Ctrl Pts',(-0.266881681598629,-1.53243414802304,
0.0498638554383248));
#284936=CARTESIAN_POINT('Ctrl Pts',(-0.21034010396998,-1.54228116907594,
0.0539599706743499));
#284937=CARTESIAN_POINT('Ctrl Pts',(-0.153249779571496,-1.54899515564964,
0.0580560859103751));
#284938=CARTESIAN_POINT('Ctrl Pts',(-0.0959898131972683,-1.55253541207998,
0.0621522011464002));
#284939=CARTESIAN_POINT('Ctrl Pts',(-0.0386749267085929,-1.55607906409891,
0.0662522451153917));
#284940=CARTESIAN_POINT('Ctrl Pts',(0.0188093951990522,-1.55644287993823,
0.0703522890843831));
#284941=CARTESIAN_POINT('Ctrl Pts',(0.0760816915993679,-1.55363825461508,
0.0744523330533746));
#284942=CARTESIAN_POINT('Ctrl Pts',(0.133386106680123,-1.5508320564396,
0.0785546763539856));
#284943=CARTESIAN_POINT('Ctrl Pts',(0.190477731422078,-1.54485393887542,
0.0826570196545963));
#284944=CARTESIAN_POINT('Ctrl Pts',(0.246981163227441,-1.53576709009238,
0.0867593629552073));
#284945=CARTESIAN_POINT('Ctrl Pts',(0.303581603655238,-1.52666464043955,
0.0908687494151384));
#284946=CARTESIAN_POINT('Ctrl Pts',(0.359591319092611,-1.51444292904211,
0.0949781358750698));
#284947=CARTESIAN_POINT('Ctrl Pts',(0.414647503255705,-1.49921569430279,
0.099087522335001));
#284948=CARTESIAN_POINT('Ctrl Pts',(0.434286939269945,-1.49378389210142,
0.100553407297143));
#284949=CARTESIAN_POINT('Ctrl Pts',(0.453805212795988,-1.48797009989777,
0.102019292259285));
#284950=CARTESIAN_POINT('Ctrl Pts',(0.473186488074858,-1.48178095462973,
0.103485177221427));
#284951=CARTESIAN_POINT('Ctrl Pts',(0.528121056988836,-1.46423835114498,
0.107640102906867));
#284952=CARTESIAN_POINT('Ctrl Pts',(0.582189715412371,-1.44360129555919,
0.111795028592307));
#284953=CARTESIAN_POINT('Ctrl Pts',(0.635020698669741,-1.41997498649131,
0.115949954277747));
#284954=CARTESIAN_POINT('Ctrl Pts',(0.687760721448913,-1.39638935545436,
0.12009772631955));
#284955=CARTESIAN_POINT('Ctrl Pts',(0.739266829154363,-1.36982489740558,
0.124245498361353));
#284956=CARTESIAN_POINT('Ctrl Pts',(0.789184128374671,-1.3404359968016,
0.128393270403156));
#284957=CARTESIAN_POINT('Ctrl Pts',(0.839053413900563,-1.31107536434744,
0.132537052848918));
#284958=CARTESIAN_POINT('Ctrl Pts',(0.887336474303002,-1.27889593474542,
0.13668083529468));
#284959=CARTESIAN_POINT('Ctrl Pts',(0.933701655331761,-1.24409865719352,
0.140824617740442));
#284960=CARTESIAN_POINT('Ctrl Pts',(0.980039891137898,-1.20932160215277,
0.144965992018307));
#284961=CARTESIAN_POINT('Ctrl Pts',(1.02446204317353,-1.17193002621499,
0.149107366296172));
#284962=CARTESIAN_POINT('Ctrl Pts',(1.0666660281567,-1.13216775893699,0.153248740574037));
#284963=CARTESIAN_POINT('Ctrl Pts',(1.10886155281276,-1.09241346251265,
0.157389284660604));
#284964=CARTESIAN_POINT('Ctrl Pts',(1.14883941601361,-1.05028977407605,
0.161529828747171));
#284965=CARTESIAN_POINT('Ctrl Pts',(1.18633284133866,-1.00607884361085,
0.165670372833738));
#284966=CARTESIAN_POINT('Ctrl Pts',(1.22386110008989,-0.961826838792772,
0.169814763710389));
#284967=CARTESIAN_POINT('Ctrl Pts',(1.25889997157673,-0.915484113028016,
0.17395915458704));
#284968=CARTESIAN_POINT('Ctrl Pts',(1.29122251180059,-0.867366517119135,
0.178103545463692));
#284969=CARTESIAN_POINT('Ctrl Pts',(1.32355891279799,-0.819228287092538,
0.182249713566483));
#284970=CARTESIAN_POINT('Ctrl Pts',(1.35317639412173,-0.769314116146701,
0.186395881669274));
#284971=CARTESIAN_POINT('Ctrl Pts',(1.37989273735347,-0.717966770400374,
0.190542049772064));
#284972=CARTESIAN_POINT('Ctrl Pts',(1.40666131973601,-0.66651902387262,
0.194696324983634));
#284973=CARTESIAN_POINT('Ctrl Pts',(1.43051721271553,-0.613632976563166,
0.198850600195203));
#284974=CARTESIAN_POINT('Ctrl Pts',(1.45132573982812,-0.559672982117566,
0.203004875406773));
#284975=CARTESIAN_POINT('Ctrl Pts',(1.47080505381337,-0.509159859840303,
0.206893782622042));
#284976=CARTESIAN_POINT('Ctrl Pts',(1.48761426769546,-0.457706128643404,
0.210782689837312));
#284977=CARTESIAN_POINT('Ctrl Pts',(1.50168317545456,-0.405620377393322,
0.214671597052581));
#284978=CARTESIAN_POINT('Ctrl Pts',(1.51666767026187,-0.350144950124534,
0.218813589520731));
#284979=CARTESIAN_POINT('Ctrl Pts',(1.5286062889074,-0.293718260314706,
0.222955581988881));
#284980=CARTESIAN_POINT('Ctrl Pts',(1.53738418093832,-0.236706844431258,
0.227097574457031));
#284981=CARTESIAN_POINT('Ctrl Pts',(1.54614616940765,-0.179798720381579,
0.231232062568538));
#284982=CARTESIAN_POINT('Ctrl Pts',(1.55175871768408,-0.122308484821582,
0.235366550680045));
#284983=CARTESIAN_POINT('Ctrl Pts',(1.55415735577001,-0.0646155051513709,
0.239501038791552));
#284984=CARTESIAN_POINT('Ctrl Pts',(1.55655356090739,-0.00698104370958413,
0.24363133327463));
#284985=CARTESIAN_POINT('Ctrl Pts',(1.555742292153,0.050855235112751,0.247761627757708));
#284986=CARTESIAN_POINT('Ctrl Pts',(1.55171076002969,0.108507913112747,
0.251891922240785));
#284987=CARTESIAN_POINT('Ctrl Pts',(1.5476817547115,0.166124456691066,0.2560196280184));
#284988=CARTESIAN_POINT('Ctrl Pts',(1.54043652274323,0.223557107356094,
0.260147333796014));
#284989=CARTESIAN_POINT('Ctrl Pts',(1.53001434149962,0.28042176236072,0.264275039573629));
#284990=CARTESIAN_POINT('Ctrl Pts',(1.51959465360752,0.337272813344219,
0.268401757859161));
#284991=CARTESIAN_POINT('Ctrl Pts',(1.50599961916479,0.393555624638792,
0.272528476144693));
#284992=CARTESIAN_POINT('Ctrl Pts',(1.48931989462697,0.448894755447546,
0.276655194430224));
#284993=CARTESIAN_POINT('Ctrl Pts',(1.4726251746609,0.504283637315656,0.280785622723546));
#284994=CARTESIAN_POINT('Ctrl Pts',(1.45284037227224,0.558726641250366,
0.284916051016867));
#284995=CARTESIAN_POINT('Ctrl Pts',(1.43010610996875,0.611863354214026,
0.289046479310188));
#284996=CARTESIAN_POINT('Ctrl Pts',(1.4073626044815,0.66502167123926,0.293178586932587));
#284997=CARTESIAN_POINT('Ctrl Pts',(1.38166747992618,0.716872168703091,
0.297310694554986));
#284998=CARTESIAN_POINT('Ctrl Pts',(1.35320828435611,0.767077303242633,
0.301442802177385));
#284999=CARTESIAN_POINT('Ctrl Pts',(1.3246931272864,0.817381159989961,0.305583035080018));
#285000=CARTESIAN_POINT('Ctrl Pts',(1.29340332031575,0.866032746432876,
0.30972326798265));
#285001=CARTESIAN_POINT('Ctrl Pts',(1.25957038880755,0.912722677289872,
0.313863500885282));
#285002=CARTESIAN_POINT('Ctrl Pts',(1.22689834291113,0.957810569348262,
0.317861672884771));
#285003=CARTESIAN_POINT('Ctrl Pts',(1.19185523221823,1.00106898154561,0.321859844884259));
#285004=CARTESIAN_POINT('Ctrl Pts',(1.15468296304764,1.04225117167002,0.325858016883747));
#285005=CARTESIAN_POINT('Ctrl Pts',(1.11610928740658,1.08498594357101,0.330006921250001));
#285006=CARTESIAN_POINT('Ctrl Pts',(1.07507917194319,1.1256659486238,0.334155825616254));
#285007=CARTESIAN_POINT('Ctrl Pts',(1.03184004939355,1.1639958601591,0.338304729982508));
#285008=CARTESIAN_POINT('Ctrl Pts',(0.988677842284126,1.2022575889505,0.342446254115608));
#285009=CARTESIAN_POINT('Ctrl Pts',(0.94331481395107,1.23817717943636,0.346587778248709));
#285010=CARTESIAN_POINT('Ctrl Pts',(0.896036373130515,1.27149481635873,
0.350729302381809));
#285011=CARTESIAN_POINT('Ctrl Pts',(0.848804996947713,1.30477928631355,
0.354866703719621));
#285012=CARTESIAN_POINT('Ctrl Pts',(0.799662409525528,1.33546663634278,
0.359004105057433));
#285013=CARTESIAN_POINT('Ctrl Pts',(0.748926998363193,1.36333730276946,
0.363141506395245));
#285014=CARTESIAN_POINT('Ctrl Pts',(0.698222611097356,1.39119092672716,
0.367276377777983));
#285015=CARTESIAN_POINT('Ctrl Pts',(0.645927786148217,1.41623103119483,
0.371411249160722));
#285016=CARTESIAN_POINT('Ctrl Pts',(0.592387918214518,1.43828258848999,
0.37554612054346));
#285017=CARTESIAN_POINT('Ctrl Pts',(0.538860231172223,1.46032912882051,
0.379680051198826));
#285018=CARTESIAN_POINT('Ctrl Pts',(0.484088544589072,1.47938827365183,
0.383813981854192));
#285019=CARTESIAN_POINT('Ctrl Pts',(0.428438729962962,1.49533290763887,
0.387947912509558));
#285020=CARTESIAN_POINT('Ctrl Pts',(0.37273875664476,1.51129191295837,0.392085569189103));
#285021=CARTESIAN_POINT('Ctrl Pts',(0.316159574878584,1.52413065256782,
0.396223225868648));
#285022=CARTESIAN_POINT('Ctrl Pts',(0.259081434718245,1.53377216697407,
0.400360882548193));
#285023=CARTESIAN_POINT('Ctrl Pts',(0.201979838666644,1.5434176434981,0.404500239570897));
#285024=CARTESIAN_POINT('Ctrl Pts',(0.144379393759639,1.54986321606351,
0.408639596593601));
#285025=CARTESIAN_POINT('Ctrl Pts',(0.0866665186968121,1.55308375966558,
0.412778953616306));
#285026=CARTESIAN_POINT('Ctrl Pts',(0.0288411893126411,1.55631057854063,
0.41692637623242));
#285027=CARTESIAN_POINT('Ctrl Pts',(-0.0290964855246801,1.5562998092828,
0.421073798848535));
#285028=CARTESIAN_POINT('Ctrl Pts',(-0.086759951318526,1.5530785430387,
0.425221221464649));
#285029=CARTESIAN_POINT('Ctrl Pts',(-0.141554429018789,1.55001754767623,
0.429162293214736));
#285030=CARTESIAN_POINT('Ctrl Pts',(-0.196100950596859,1.54405805300416,
0.433103364964823));
#285031=CARTESIAN_POINT('Ctrl Pts',(-0.250076008008153,1.53526617894706,
0.43704443671491));
#285032=CARTESIAN_POINT('Ctrl Pts',(-0.30689233740269,1.52601149657374,
0.441192968304496));
#285033=CARTESIAN_POINT('Ctrl Pts',(-0.363313166993611,1.51357924117281,
0.445341499894082));
#285034=CARTESIAN_POINT('Ctrl Pts',(-0.418956256220377,1.49801732479094,
0.449490031483667));
#285035=CARTESIAN_POINT('Ctrl Pts',(-0.474500677109199,1.48248300336194,
0.453631206747022));
#285036=CARTESIAN_POINT('Ctrl Pts',(-0.52926959769328,1.46383017528532,
0.457772382010377));
#285037=CARTESIAN_POINT('Ctrl Pts',(-0.582890043296543,1.44215791348443,
0.461913557273732));
#285038=CARTESIAN_POINT('Ctrl Pts',(-0.63645729780394,1.42050715041116,
0.46605062452105));
#285039=CARTESIAN_POINT('Ctrl Pts',(-0.688877854292931,1.39584308225942,
0.470187691768368));
#285040=CARTESIAN_POINT('Ctrl Pts',(-0.739794699741476,1.36831431046906,
0.474324759015686));
#285041=CARTESIAN_POINT('Ctrl Pts',(-0.790680597008529,1.34080227116513,
0.47845931167855));
#285042=CARTESIAN_POINT('Ctrl Pts',(-0.840064137935306,1.31042922695258,
0.482593864341414));
#285043=CARTESIAN_POINT('Ctrl Pts',(-0.887611108960229,1.27739060950455,
0.486728417004278));
#285044=CARTESIAN_POINT('Ctrl Pts',(-0.93514744547065,1.24435938158415,
0.49086204491927));
#285045=CARTESIAN_POINT('Ctrl Pts',(-0.98084760021021,1.20866406100027,
0.494995672834262));
#285046=CARTESIAN_POINT('Ctrl Pts',(-1.02440653623954,1.17054324931192,
0.499129300749254));
#285047=CARTESIAN_POINT('Ctrl Pts',(-1.06800502952157,1.13238781890423,
0.50326668254299));
#285048=CARTESIAN_POINT('Ctrl Pts',(-1.10945802465527,1.09180283844611,
0.507404064336726));
#285049=CARTESIAN_POINT('Ctrl Pts',(-1.14849484981261,1.04906617043631,
0.511541446130461));
#285050=CARTESIAN_POINT('Ctrl Pts',(-1.18754785708328,1.00631178660045,
0.515680543011958));
#285051=CARTESIAN_POINT('Ctrl Pts',(-1.22418236682099,0.961404340584704,
0.519819639893454));
#285052=CARTESIAN_POINT('Ctrl Pts',(-1.25816793488278,0.914654960973155,
0.52395873677495));
#285053=CARTESIAN_POINT('Ctrl Pts',(-1.29221996491882,0.867814158553604,
0.528105928049627));
#285054=CARTESIAN_POINT('Ctrl Pts',(-1.32361241689602,0.819124662742743,
0.532253119324303));
#285055=CARTESIAN_POINT('Ctrl Pts',(-1.35215866213414,0.768926005813061,
0.536400310598979));
#285056=CARTESIAN_POINT('Ctrl Pts',(-1.37930295036351,0.72119269444196,
0.540343825914677));
#285057=CARTESIAN_POINT('Ctrl Pts',(-1.40387393461122,0.672095371638328,
0.544287341230373));
#285058=CARTESIAN_POINT('Ctrl Pts',(-1.42575171809473,0.621942351307516,
0.548230856546071));
#285059=CARTESIAN_POINT('Ctrl Pts',(-1.45109454208923,0.563846010423896,
0.552798952516151));
#285060=CARTESIAN_POINT('Ctrl Pts',(-1.47291535250019,0.504123591953479,
0.557367048486231));
#285061=CARTESIAN_POINT('Ctrl Pts',(-1.49102528336013,0.443197308634467,
0.561935144456311));
#285062=CARTESIAN_POINT('Ctrl Pts',(-1.50907657817563,0.382468291461024,
0.566488449918329));
#285063=CARTESIAN_POINT('Ctrl Pts',(-1.52344080755184,0.320543489155571,
0.571041755380347));
#285064=CARTESIAN_POINT('Ctrl Pts',(-1.53397736366261,0.257863719376566,
0.575595060842365));
#285065=CARTESIAN_POINT('Ctrl Pts',(-1.54446015602563,0.195503778894309,
0.580125132644003));
#285066=CARTESIAN_POINT('Ctrl Pts',(-1.55115409873917,0.132396873497183,
0.584655204445641));
#285067=CARTESIAN_POINT('Ctrl Pts',(-1.55396909178788,0.0689950126310516,
0.589185276247278));
#285068=CARTESIAN_POINT('Ctrl Pts',(-1.55497803006196,0.0462707774485264,
0.590808926020452));
#285069=CARTESIAN_POINT('Ctrl Pts',(-1.55548913384293,0.0235087962157958,
0.592432575793627));
#285070=CARTESIAN_POINT('Ctrl Pts',(-1.55549982855345,0.00073032197892629,
0.594056225566802));
#285071=CARTESIAN_POINT('',(0.903606778650206,-1.26612599672284,0.));
#285072=CARTESIAN_POINT('Origin',(0.,0.,0.));
#285073=CARTESIAN_POINT('',(-1.55549967063145,0.00101225759537372,0.455943774396301));
#285074=CARTESIAN_POINT('Ctrl Pts',(0.903606778650206,-1.26612599672284,
-2.66453525910038E-15));
#285075=CARTESIAN_POINT('Ctrl Pts',(0.951852882766262,-1.23169379421253,
0.00424525219639006));
#285076=CARTESIAN_POINT('Ctrl Pts',(0.998166564555117,-1.19447316528589,
0.0084905043927825));
#285077=CARTESIAN_POINT('Ctrl Pts',(1.04222410325038,-1.1547073952322,0.0127357565891753));
#285078=CARTESIAN_POINT('Ctrl Pts',(1.08626041427952,-1.11496078499804,
0.0169789633513723));
#285079=CARTESIAN_POINT('Ctrl Pts',(1.12804237788175,-1.07267179026597,
0.0212221701135694));
#285080=CARTESIAN_POINT('Ctrl Pts',(1.1672798477831,-1.02812353681815,0.0254653768757664));
#285081=CARTESIAN_POINT('Ctrl Pts',(1.20650768566346,-0.9835862190834,0.0297075420148228));
#285082=CARTESIAN_POINT('Ctrl Pts',(1.24319194927828,-0.93679110831928,
0.0339497071538796));
#285083=CARTESIAN_POINT('Ctrl Pts',(1.27708111921595,-0.888056341085483,
0.038191872292936));
#285084=CARTESIAN_POINT('Ctrl Pts',(1.3109722297727,-0.83931878311885,0.0424342803540421));
#285085=CARTESIAN_POINT('Ctrl Pts',(1.34206765177606,-0.78864174716061,
0.0466766884151483));
#285086=CARTESIAN_POINT('Ctrl Pts',(1.37015878773367,-0.736372966910253,
0.0509190964762545));
#285087=CARTESIAN_POINT('Ctrl Pts',(1.39826003751312,-0.684085368014315,
0.055163031957234));
#285088=CARTESIAN_POINT('Ctrl Pts',(1.4233546235329,-0.630205314661143,
0.0594069674382136));
#285089=CARTESIAN_POINT('Ctrl Pts',(1.44528039378935,-0.57510419345377,
0.0636509029191932));
#285090=CARTESIAN_POINT('Ctrl Pts',(1.46723931600862,-0.519919758853032,
0.0679012552689841));
#285091=CARTESIAN_POINT('Ctrl Pts',(1.48601967649052,-0.463511022720185,
0.072151607618775));
#285092=CARTESIAN_POINT('Ctrl Pts',(1.50150818912007,-0.406267655622951,
0.0764019599685659));
#285093=CARTESIAN_POINT('Ctrl Pts',(1.51700870532063,-0.348979925013326,
0.0806556063342175));
#285094=CARTESIAN_POINT('Ctrl Pts',(1.52921219044332,-0.290856750535091,
0.084909252699869));
#285095=CARTESIAN_POINT('Ctrl Pts',(1.53805649602739,-0.232298224332338,
0.0891628990655207));
#285096=CARTESIAN_POINT('Ctrl Pts',(1.54691960323129,-0.17361521179909,
0.0934255880226038));
#285097=CARTESIAN_POINT('Ctrl Pts',(1.55240921601056,-0.11449548309292,
0.0976882769796872));
#285098=CARTESIAN_POINT('Ctrl Pts',(1.55451513276463,-0.0553439428100182,
0.10195096593677));
#285099=CARTESIAN_POINT('Ctrl Pts',(1.55602369846608,-0.0129709550429866,
0.105004527452993));
#285100=CARTESIAN_POINT('Ctrl Pts',(1.55579701690475,0.0294182924525364,
0.108058088969215));
#285101=CARTESIAN_POINT('Ctrl Pts',(1.55384772416179,0.0716763567519665,
0.111111650485437));
#285102=CARTESIAN_POINT('Ctrl Pts',(1.55122696287,0.128490962758032,0.115217065566218));
#285103=CARTESIAN_POINT('Ctrl Pts',(1.54547918115449,0.185306670723197,
0.119322480646998));
#285104=CARTESIAN_POINT('Ctrl Pts',(1.53659989632352,0.241745752017594,
0.123427895727778));
#285105=CARTESIAN_POINT('Ctrl Pts',(1.52769669037597,0.298336882251616,
0.12754437094624));
#285106=CARTESIAN_POINT('Ctrl Pts',(1.51564503470383,0.354548813343556,
0.131660846164702));
#285107=CARTESIAN_POINT('Ctrl Pts',(1.50049316548028,0.410000622373876,
0.135777321383164));
#285108=CARTESIAN_POINT('Ctrl Pts',(1.48542979547808,0.465128547806137,
0.139869753043293));
#285109=CARTESIAN_POINT('Ctrl Pts',(1.46730243414887,0.519504679849655,
0.143962184703423));
#285110=CARTESIAN_POINT('Ctrl Pts',(1.44620997094002,0.572762577298553,
0.148054616363552));
#285111=CARTESIAN_POINT('Ctrl Pts',(1.42513293513202,0.625981520978749,
0.152144054746741));
#285112=CARTESIAN_POINT('Ctrl Pts',(1.40109528796121,0.678083355662404,
0.15623349312993));
#285113=CARTESIAN_POINT('Ctrl Pts',(1.37424533484884,0.728718059091574,
0.160322931513119));
#285114=CARTESIAN_POINT('Ctrl Pts',(1.34740416125953,0.779336205748967,
0.164411032712649));
#285115=CARTESIAN_POINT('Ctrl Pts',(1.31775275451934,0.828487701729929,
0.16849913391218));
#285116=CARTESIAN_POINT('Ctrl Pts',(1.28548597986787,0.875845902863714,
0.17258723511171));
#285117=CARTESIAN_POINT('Ctrl Pts',(1.25283847284091,0.92376290792542,0.176723573933306));
#285118=CARTESIAN_POINT('Ctrl Pts',(1.21751374817111,0.969843534822608,
0.180859912754903));
#285119=CARTESIAN_POINT('Ctrl Pts',(1.17975806830724,1.01378062235572,0.1849962515765));
#285120=CARTESIAN_POINT('Ctrl Pts',(1.14239776976453,1.05725759623762,0.189089274237086));
#285121=CARTESIAN_POINT('Ctrl Pts',(1.10265761423722,1.09863536954959,0.193182296897672));
#285122=CARTESIAN_POINT('Ctrl Pts',(1.06081405722401,1.13765275281869,0.197275319558258));
#285123=CARTESIAN_POINT('Ctrl Pts',(1.01830625923178,1.17728951328015,0.20143331646036));
#285124=CARTESIAN_POINT('Ctrl Pts',(0.973628121102911,1.21448990844618,
0.205591313362462));
#285125=CARTESIAN_POINT('Ctrl Pts',(0.927102762918045,1.24902390569185,
0.209749310264563));
#285126=CARTESIAN_POINT('Ctrl Pts',(0.880577404733179,1.28355790293752,
0.213907307166665));
#285127=CARTESIAN_POINT('Ctrl Pts',(0.832205342047452,1.31542525247013,
0.218065304068767));
#285128=CARTESIAN_POINT('Ctrl Pts',(0.782335877333532,1.34444442988053,
0.222223300970868));
#285129=CARTESIAN_POINT('Ctrl Pts',(0.732509368814128,1.37343861096428,
0.226377716288031));
#285130=CARTESIAN_POINT('Ctrl Pts',(0.680966157084891,1.39971889273661,
0.230532131605194));
#285131=CARTESIAN_POINT('Ctrl Pts',(0.628032950359753,1.42307935943939,
0.234686546922357));
#285132=CARTESIAN_POINT('Ctrl Pts',(0.575193788895018,1.44639832211643,
0.238833581181494));
#285133=CARTESIAN_POINT('Ctrl Pts',(0.520970005675055,1.46680755965869,
0.242980615440632));
#285134=CARTESIAN_POINT('Ctrl Pts',(0.465713586530266,1.48414659158761,
0.247127649699769));
#285135=CARTESIAN_POINT('Ctrl Pts',(0.410512158653983,1.5014683676868,0.251270556824395));
#285136=CARTESIAN_POINT('Ctrl Pts',(0.354280623928115,1.51572583817242,
0.255413463949021));
#285137=CARTESIAN_POINT('Ctrl Pts',(0.297390058907445,1.52680693044767,
0.259556371073646));
#285138=CARTESIAN_POINT('Ctrl Pts',(0.240534433202252,1.53788121727497,
0.263696733833684));
#285139=CARTESIAN_POINT('Ctrl Pts',(0.183021087950222,1.54578289435644,
0.267837096593722));
#285140=CARTESIAN_POINT('Ctrl Pts',(0.125233215870697,1.55045054472649,
0.27197745935376));
#285141=CARTESIAN_POINT('Ctrl Pts',(0.0674588154273806,1.5551171069636,
0.276116856903298));
#285142=CARTESIAN_POINT('Ctrl Pts',(0.00941053221514308,1.55655109758077,
0.280256254452836));
#285143=CARTESIAN_POINT('Ctrl Pts',(-0.0485235526154023,1.55474297388397,
0.284395652002374));
#285144=CARTESIAN_POINT('Ctrl Pts',(-0.106508490692881,1.55293326305655,
0.288538683022716));
#285145=CARTESIAN_POINT('Ctrl Pts',(-0.16437851010345,1.54787576549528,
0.292681714043058));
#285146=CARTESIAN_POINT('Ctrl Pts',(-0.22174712659336,1.53961308835941,
0.296824745063399));
#285147=CARTESIAN_POINT('Ctrl Pts',(-0.279138774167105,1.53134709410659,
0.30096943933624));
#285148=CARTESIAN_POINT('Ctrl Pts',(-0.336028107311789,1.519873455748,0.305114133609081));
#285149=CARTESIAN_POINT('Ctrl Pts',(-0.392038530311958,1.50528603286912,
0.309258827881922));
#285150=CARTESIAN_POINT('Ctrl Pts',(-0.448155821396572,1.49067077713598,
0.31341143024604));
#285151=CARTESIAN_POINT('Ctrl Pts',(-0.503390354672071,1.47293002177716,
0.317564032610157));
#285152=CARTESIAN_POINT('Ctrl Pts',(-0.557381292354335,1.45220740424135,
0.321716634974275));
#285153=CARTESIAN_POINT('Ctrl Pts',(-0.607733958478008,1.43288121568486,
0.325589407134954));
#285154=CARTESIAN_POINT('Ctrl Pts',(-0.657004868931625,1.41096214318115,
0.329462179295632));
#285155=CARTESIAN_POINT('Ctrl Pts',(-0.704920767250419,1.38660266907975,
0.333334951456311));
#285156=CARTESIAN_POINT('Ctrl Pts',(-0.756331651611818,1.36046641472427,
0.337490203652274));
#285157=CARTESIAN_POINT('Ctrl Pts',(-0.806390623719567,1.33141440363412,
0.341645455848236));
#285158=CARTESIAN_POINT('Ctrl Pts',(-0.854747604328637,1.29961024268604,
0.345800708044198));
#285159=CARTESIAN_POINT('Ctrl Pts',(-0.903021453830198,1.26786075668022,
0.349948816892651));
#285160=CARTESIAN_POINT('Ctrl Pts',(-0.949598689923335,1.2333687953876,
0.354096925741104));
#285161=CARTESIAN_POINT('Ctrl Pts',(-0.994153791582626,1.19634380036923,
0.358245034589556));
#285162=CARTESIAN_POINT('Ctrl Pts',(-1.03866610911375,1.1593543586786,0.362389160207941));
#285163=CARTESIAN_POINT('Ctrl Pts',(-1.08115974297499,1.11983703316806,
0.366533285826326));
#285164=CARTESIAN_POINT('Ctrl Pts',(-1.1213395937073,1.07804348965353,0.37067741144471));
#285165=CARTESIAN_POINT('Ctrl Pts',(-1.16149615113547,1.0362741749428,0.374819134605727));
#285166=CARTESIAN_POINT('Ctrl Pts',(-1.19934122602266,0.992231631646827,
0.378960857766743));
#285167=CARTESIAN_POINT('Ctrl Pts',(-1.23461579669431,0.946205096452601,
0.38310258092776));
#285168=CARTESIAN_POINT('Ctrl Pts',(-1.26988333983836,0.900187730831256,
0.387243478959701));
#285169=CARTESIAN_POINT('Ctrl Pts',(-1.30258108037958,0.85218756974644,
0.391384376991643));
#285170=CARTESIAN_POINT('Ctrl Pts',(-1.33249100202178,0.802525999286622,
0.395525275023585));
#285171=CARTESIAN_POINT('Ctrl Pts',(-1.36242868649098,0.752818332230301,
0.399670016697683));
#285172=CARTESIAN_POINT('Ctrl Pts',(-1.38957311222174,0.701446619159402,
0.40381475837178));
#285173=CARTESIAN_POINT('Ctrl Pts',(-1.41375099283611,0.648759108032348,
0.407959500045878));
#285174=CARTESIAN_POINT('Ctrl Pts',(-1.43793926211777,0.596048958319524,
0.412106022618103));
#285175=CARTESIAN_POINT('Ctrl Pts',(-1.45915825416503,0.542022366868642,
0.416252545190328));
#285176=CARTESIAN_POINT('Ctrl Pts',(-1.47728315018204,0.487046963021249,
0.420399067762553));
#285177=CARTESIAN_POINT('Ctrl Pts',(-1.49544339049082,0.4319643548781,0.424553676224122));
#285178=CARTESIAN_POINT('Ctrl Pts',(-1.5104973412724,0.375929739341496,
0.428708284685691));
#285179=CARTESIAN_POINT('Ctrl Pts',(-1.52237057598149,0.319324410883043,
0.43286289314726));
#285180=CARTESIAN_POINT('Ctrl Pts',(-1.53340539788194,0.266716193033383,
0.436724129412089));
#285181=CARTESIAN_POINT('Ctrl Pts',(-1.54169334567415,0.21361545867419,
0.440585365676917));
#285182=CARTESIAN_POINT('Ctrl Pts',(-1.54721495399917,0.160331332313241,
0.444446601941745));
#285183=CARTESIAN_POINT('Ctrl Pts',(-1.55269531303319,0.107445266137791,
0.44827899275993));
#285184=CARTESIAN_POINT('Ctrl Pts',(-1.55546501227888,0.0542704956696049,
0.452111383578116));
#285185=CARTESIAN_POINT('Ctrl Pts',(-1.55549967063145,0.00101225759537372,
0.455943774396301));
#285186=CARTESIAN_POINT('',(-1.55549938660524,-0.00138140172760619,1.85539343273712));
#285187=CARTESIAN_POINT('Ctrl Pts',(-1.55549962201023,0.00108440122680404,
0.457011256470473));
#285188=CARTESIAN_POINT('Ctrl Pts',(-1.5555667906038,-0.0952643664786917,
0.463522872456782));
#285189=CARTESIAN_POINT('Ctrl Pts',(-1.54668208355373,-0.191420635597107,
0.469766099184208));
#285190=CARTESIAN_POINT('Ctrl Pts',(-1.51736458895052,-0.34807208354269,
0.480306286301398));
#285191=CARTESIAN_POINT('Ctrl Pts',(-1.5020245696063,-0.409231530846319,
0.484515805592852));
#285192=CARTESIAN_POINT('Ctrl Pts',(-1.47503044214394,-0.494536919273511,
0.490652697112903));
#285193=CARTESIAN_POINT('Ctrl Pts',(-1.46639774811665,-0.519575857388309,
0.492487163666517));
#285194=CARTESIAN_POINT('Ctrl Pts',(-1.45276447622374,-0.556067682209315,
0.495216689650924));
#285195=CARTESIAN_POINT('Ctrl Pts',(-1.44825804897068,-0.567701063900379,
0.496095351772404));
#285196=CARTESIAN_POINT('Ctrl Pts',(-1.43998888066032,-0.588308542359477,
0.49766770145831));
#285197=CARTESIAN_POINT('Ctrl Pts',(-1.43628090183011,-0.597304010173798,
0.498359507023726));
#285198=CARTESIAN_POINT('Ctrl Pts',(-1.42825833213423,-0.616259849989553,
0.499829221071941));
#285199=CARTESIAN_POINT('Ctrl Pts',(-1.4239234020208,-0.626210986858212,
0.500607795169071));
#285200=CARTESIAN_POINT('Ctrl Pts',(-1.41199445171519,-0.652830300236169,
0.502709913162139));
#285201=CARTESIAN_POINT('Ctrl Pts',(-1.4042097937536,-0.669410587084619,
0.504039955699443));
#285202=CARTESIAN_POINT('Ctrl Pts',(-1.35580405346299,-0.767946755324809,
0.512072867808739));
#285203=CARTESIAN_POINT('Ctrl Pts',(-1.30831836597364,-0.846312187792799,
0.519016683963832));
#285204=CARTESIAN_POINT('Ctrl Pts',(-1.2149772121204,-0.973558347105258,
0.531210936975088));
#285205=CARTESIAN_POINT('Ctrl Pts',(-1.17233508295044,-1.02450765349571,
0.536387174881569));
#285206=CARTESIAN_POINT('Ctrl Pts',(-1.10256064712219,-1.09779441213796,
0.544179981801476));
#285207=CARTESIAN_POINT('Ctrl Pts',(-1.07771061982276,-1.1221999355986,
0.546840678859995));
#285208=CARTESIAN_POINT('Ctrl Pts',(-1.04106387193628,-1.15584997325019,
0.550582626796932));
#285209=CARTESIAN_POINT('Ctrl Pts',(-1.0299216335618,-1.16578926645013,
0.551697646722261));
#285210=CARTESIAN_POINT('Ctrl Pts',(-1.01015004584692,-1.18292149395355,
0.553634444765031));
#285211=CARTESIAN_POINT('Ctrl Pts',(-1.00158281784291,-1.19018412628193,
0.554460358583519));
#285212=CARTESIAN_POINT('Ctrl Pts',(-0.988005322102365,-1.20144362610956,
0.555747556718756));
#285213=CARTESIAN_POINT('Ctrl Pts',(-0.983047944712801,-1.20550323333759,
0.556213073350035));
#285214=CARTESIAN_POINT('Ctrl Pts',(-0.974052946841916,-1.21277686955253,
0.557049506370322));
#285215=CARTESIAN_POINT('Ctrl Pts',(-0.970024368040723,-1.21600148238476,
0.557421154172974));
#285216=CARTESIAN_POINT('Ctrl Pts',(-0.960516268764562,-1.22353476974095,
0.558291472733171));
#285217=CARTESIAN_POINT('Ctrl Pts',(-0.955023736897941,-1.22782673951306,
0.558788968528576));
#285218=CARTESIAN_POINT('Ctrl Pts',(-0.937971839341733,-1.24096776494697,
0.560317971301154));
#285219=CARTESIAN_POINT('Ctrl Pts',(-0.926316560127726,-1.2496918962324,
0.561341294350341));
#285220=CARTESIAN_POINT('Ctrl Pts',(-0.838174312089929,-1.31375667834253,
0.568933312501299));
#285221=CARTESIAN_POINT('Ctrl Pts',(-0.756902700560442,-1.36220270384782,
0.575124928745838));
#285222=CARTESIAN_POINT('Ctrl Pts',(-0.575125304043796,-1.44923517816546,
0.588389690283717));
#285223=CARTESIAN_POINT('Ctrl Pts',(-0.474017020858618,-1.48538058091112,
0.595446141950153));
#285224=CARTESIAN_POINT('Ctrl Pts',(-0.351753700339952,-1.51532262894242,
0.604169862864003));
#285225=CARTESIAN_POINT('Ctrl Pts',(-0.333423697013755,-1.51946106264904,
0.605481795312001));
#285226=CARTESIAN_POINT('Ctrl Pts',(-0.304227608808861,-1.52549905177316,
0.607580183211123));
#285227=CARTESIAN_POINT('Ctrl Pts',(-0.293408151255459,-1.52761691548243,
0.608359683975519));
#285228=CARTESIAN_POINT('Ctrl Pts',(-0.272911744290726,-1.53140322642213,
0.609840380750816));
#285229=CARTESIAN_POINT('Ctrl Pts',(-0.263239683424221,-1.53309540571897,
0.610540785661379));
#285230=CARTESIAN_POINT('Ctrl Pts',(-0.241213080022269,-1.53673449759373,
0.612139982973226));
#285231=CARTESIAN_POINT('Ctrl Pts',(-0.228849916592012,-1.53862417920436,
0.613040533770189));
#285232=CARTESIAN_POINT('Ctrl Pts',(-0.196443564155182,-1.54317820628427,
0.615409372237364));
#285233=CARTESIAN_POINT('Ctrl Pts',(-0.176369447261966,-1.54560111200429,
0.616885063252536));
#285234=CARTESIAN_POINT('Ctrl Pts',(-0.0476575329217699,-1.55859634331593,
0.626403878854123));
#285235=CARTESIAN_POINT('Ctrl Pts',(0.0617727447775499,-1.5580980607613,
0.634787487670447));
#285236=CARTESIAN_POINT('Ctrl Pts',(0.256258299720361,-1.53668565651187,
0.649949991889133));
#285237=CARTESIAN_POINT('Ctrl Pts',(0.341356401174011,-1.52004932154656,
0.656667032904326));
#285238=CARTESIAN_POINT('Ctrl Pts',(0.437570273885015,-1.49274689260988,
0.664092969128434));
#285239=CARTESIAN_POINT('Ctrl Pts',(0.450457470168279,-1.48890870431262,
0.665083810553853));
#285240=CARTESIAN_POINT('Ctrl Pts',(0.469757372351605,-1.48288708445105,
0.666560329559166));
#285241=CARTESIAN_POINT('Ctrl Pts',(0.476207833531309,-1.48082821353068,
0.667052567352394));
#285242=CARTESIAN_POINT('Ctrl Pts',(0.48788234539948,-1.47701774574191,
0.667940931733326));
#285243=CARTESIAN_POINT('Ctrl Pts',(0.493110705210416,-1.47528046116991,
0.66833783413931));
#285244=CARTESIAN_POINT('Ctrl Pts',(0.504941530025822,-1.47127937968552,
0.669233842330833));
#285245=CARTESIAN_POINT('Ctrl Pts',(0.511538104108221,-1.46899888865372,
0.669731973769434));
#285246=CARTESIAN_POINT('Ctrl Pts',(0.531868360863221,-1.46181699428555,
0.671263323820655));
#285247=CARTESIAN_POINT('Ctrl Pts',(0.545549123394672,-1.45676664988181,
0.6722883407645));
#285248=CARTESIAN_POINT('Ctrl Pts',(0.647528959665822,-1.41748189028475,
0.679902469179764));
#285249=CARTESIAN_POINT('Ctrl Pts',(0.732620110252397,-1.3754350492819,
0.686112818056511));
#285250=CARTESIAN_POINT('Ctrl Pts',(0.903823441089378,-1.27041137090509,
0.699334689682724));
#285251=CARTESIAN_POINT('Ctrl Pts',(0.988352246591539,-1.20581825710198,
0.706329223151749));
#285252=CARTESIAN_POINT('Ctrl Pts',(1.07940745208067,-1.1201860486624,0.714990427013295));
#285253=CARTESIAN_POINT('Ctrl Pts',(1.09293354099202,-1.10699297760284,
0.716309400724588));
#285254=CARTESIAN_POINT('Ctrl Pts',(1.11397054148655,-1.08571246882721,
0.71841533495862));
#285255=CARTESIAN_POINT('Ctrl Pts',(1.12164174907549,-1.07778555739638,
0.719195220407781));
#285256=CARTESIAN_POINT('Ctrl Pts',(1.13596162029258,-1.0626698993592,0.720674298863155));
#285257=CARTESIAN_POINT('Ctrl Pts',(1.14262800828263,-1.05549862359959,
0.721372679105271));
#285258=CARTESIAN_POINT('Ctrl Pts',(1.15759924031393,-1.03908547410529,
0.722963914867381));
#285259=CARTESIAN_POINT('Ctrl Pts',(1.16586185040426,-1.02980617245094,
0.723858488477346));
#285260=CARTESIAN_POINT('Ctrl Pts',(1.18712089011909,-1.00534747056702,
0.726204034046302));
#285261=CARTESIAN_POINT('Ctrl Pts',(1.19993715984496,-0.990015296872858,
0.727662213679683));
#285262=CARTESIAN_POINT('Ctrl Pts',(1.29901309735352,-0.866739491199842,
0.739296697016701));
#285263=CARTESIAN_POINT('Ctrl Pts',(1.37082093130347,-0.748001743211682,
0.750050803731656));
#285264=CARTESIAN_POINT('Ctrl Pts',(1.44915592951412,-0.568232994353586,
0.765209965825307));
#285265=CARTESIAN_POINT('Ctrl Pts',(1.46932932540556,-0.513823296881486,
0.769655047176511));
#285266=CARTESIAN_POINT('Ctrl Pts',(1.49061345318299,-0.444808226909711,
0.775026277013295));
#285267=CARTESIAN_POINT('Ctrl Pts',(1.49462124918349,-0.431149840675565,
0.77607648628857));
#285268=CARTESIAN_POINT('Ctrl Pts',(1.50029442656547,-0.41078531242999,
0.777621543818321));
#285269=CARTESIAN_POINT('Ctrl Pts',(1.50210339490843,-0.404120446376975,
0.778123923972071));
#285270=CARTESIAN_POINT('Ctrl Pts',(1.50527014882244,-0.392137916189078,
0.779020985674077));
#285271=CARTESIAN_POINT('Ctrl Pts',(1.50664423998674,-0.38682489987429,
0.779416558839735));
#285272=CARTESIAN_POINT('Ctrl Pts',(1.50965406194167,-0.374927837351514,
0.780297482009525));
#285273=CARTESIAN_POINT('Ctrl Pts',(1.51127486933405,-0.3683402555975,0.780781984877572));
#285274=CARTESIAN_POINT('Ctrl Pts',(1.51602044387741,-0.348493645790211,
0.782232409933254));
#285275=CARTESIAN_POINT('Ctrl Pts',(1.51901429496548,-0.335203538695478,
0.783191294002216));
#285276=CARTESIAN_POINT('Ctrl Pts',(1.54379068837973,-0.218060194606904,
0.791548698154986));
#285277=CARTESIAN_POINT('Ctrl Pts',(1.55507099733175,-0.112254400347374,
0.798459455698855));
#285278=CARTESIAN_POINT('Ctrl Pts',(1.55587052273721,0.0912578720928381,
0.811861676785551));
#285279=CARTESIAN_POINT('Ctrl Pts',(1.54711022833714,0.188433933236837,
0.818314123034896));
#285280=CARTESIAN_POINT('Ctrl Pts',(1.52597396101626,0.302193047239724,
0.826337218270069));
#285281=CARTESIAN_POINT('Ctrl Pts',(1.52230191923734,0.320178051528094,
0.827619264765608));
#285282=CARTESIAN_POINT('Ctrl Pts',(1.51594212305779,0.348738691168585,
0.829679151322305));
#285283=CARTESIAN_POINT('Ctrl Pts',(1.51345978607519,0.35935867903532,0.830450421998017));
#285284=CARTESIAN_POINT('Ctrl Pts',(1.50853616955192,0.379466520340075,
0.831921315337869));
#285285=CARTESIAN_POINT('Ctrl Pts',(1.50611652046251,0.388959167032835,
0.832620209723373));
#285286=CARTESIAN_POINT('Ctrl Pts',(1.500382335635,0.410599112165217,0.834224092354007));
#285287=CARTESIAN_POINT('Ctrl Pts',(1.49700968322077,0.42273014443356,0.835130922750599));
#285288=CARTESIAN_POINT('Ctrl Pts',(1.48773344529977,0.454591641501024,
0.837533702436166));
#285289=CARTESIAN_POINT('Ctrl Pts',(1.48158482280585,0.47424751174372,0.83903747482399));
#285290=CARTESIAN_POINT('Ctrl Pts',(1.43503539622272,0.613304138525477,
0.84983423902332));
#285291=CARTESIAN_POINT('Ctrl Pts',(1.38064881879389,0.727506111240285,
0.859596094983298));
#285292=CARTESIAN_POINT('Ctrl Pts',(1.27703955255074,0.890660294626937,
0.874570790014807));
#285293=CARTESIAN_POINT('Ctrl Pts',(1.23732649886358,0.945055963326695,
0.879755852415531));
#285294=CARTESIAN_POINT('Ctrl Pts',(1.1844633732475,1.008393885516,0.885901408536068));
#285295=CARTESIAN_POINT('Ctrl Pts',(1.1745435130652,1.01993102355494,0.887025422848414));
#285296=CARTESIAN_POINT('Ctrl Pts',(1.15975660654385,1.03662678487482,0.888656557062117));
#285297=CARTESIAN_POINT('Ctrl Pts',(1.1550213922533,1.04190021894522,0.889172437665247));
#285298=CARTESIAN_POINT('Ctrl Pts',(1.14690453652376,1.05081631772866,0.890045555180362));
#285299=CARTESIAN_POINT('Ctrl Pts',(1.14354127878659,1.05447536521609,0.890404117735157));
#285300=CARTESIAN_POINT('Ctrl Pts',(1.13580786444651,1.06280839550965,0.891221232468432));
#285301=CARTESIAN_POINT('Ctrl Pts',(1.13142634310609,1.06747160362377,0.891678914329007));
#285302=CARTESIAN_POINT('Ctrl Pts',(1.11915997915638,1.08036619301065,0.892946119010653));
#285303=CARTESIAN_POINT('Ctrl Pts',(1.11121305249337,1.0885383511476,0.893751105976));
#285304=CARTESIAN_POINT('Ctrl Pts',(1.04939098454774,1.15072989959583,0.89989894688164));
#285305=CARTESIAN_POINT('Ctrl Pts',(0.991689325822598,1.20081487450592,
0.904980637209143));
#285306=CARTESIAN_POINT('Ctrl Pts',(0.882984838000079,1.28196700428943,
0.913937370298206));
#285307=CARTESIAN_POINT('Ctrl Pts',(0.833441039812106,1.31471578876308,
0.917821697021506));
#285308=CARTESIAN_POINT('Ctrl Pts',(0.740216072170568,1.3689461857553,0.924972121924322));
#285309=CARTESIAN_POINT('Ctrl Pts',(0.697169266407,1.39136190415368,0.928217222696012));
#285310=CARTESIAN_POINT('Ctrl Pts',(0.623337585155679,1.42552074065277,
0.933761166256555));
#285311=CARTESIAN_POINT('Ctrl Pts',(0.593099823651336,1.43836416321218,
0.936025565390904));
#285312=CARTESIAN_POINT('Ctrl Pts',(0.549798943921752,1.455158537499,0.939272883801638));
#285313=CARTESIAN_POINT('Ctrl Pts',(0.537054350148807,1.45991022061633,
0.940229177484577));
#285314=CARTESIAN_POINT('Ctrl Pts',(0.514878171840621,1.46784869534701,
0.941894943933038));
#285315=CARTESIAN_POINT('Ctrl Pts',(0.505475130639414,1.471113254714,0.942601797908856));
#285316=CARTESIAN_POINT('Ctrl Pts',(0.487286977595107,1.47723287651671,
0.943970416310896));
#285317=CARTESIAN_POINT('Ctrl Pts',(0.478506468261634,1.48010037599804,
0.944631736441497));
#285318=CARTESIAN_POINT('Ctrl Pts',(0.45516699280603,1.4874930900141,0.946391486587428));
#285319=CARTESIAN_POINT('Ctrl Pts',(0.44056647568861,1.49188264751281,0.947494286903442));
#285320=CARTESIAN_POINT('Ctrl Pts',(0.385939202546553,1.50743418912896,
0.951628997277283));
#285321=CARTESIAN_POINT('Ctrl Pts',(0.345538066029537,1.51720458540493,
0.954704682306651));
#285322=CARTESIAN_POINT('Ctrl Pts',(0.200801540429353,1.54612612969485,
0.965791826674418));
#285323=CARTESIAN_POINT('Ctrl Pts',(0.0949630653714379,1.55621462636507,
0.974047963165034));
#285324=CARTESIAN_POINT('Ctrl Pts',(-0.0559913897572137,1.55514116567435,
0.985724820824158));
#285325=CARTESIAN_POINT('Ctrl Pts',(-0.100889800028146,1.55287503087043,
0.989181178242875));
#285326=CARTESIAN_POINT('Ctrl Pts',(-0.163155952180584,1.54701980245475,
0.993905219898409));
#285327=CARTESIAN_POINT('Ctrl Pts',(-0.180653775625082,1.54507423994506,
0.99522499395512));
#285328=CARTESIAN_POINT('Ctrl Pts',(-0.211274280481429,1.54114224977883,
0.99751688192636));
#285329=CARTESIAN_POINT('Ctrl Pts',(-0.224411383193359,1.53928419010894,
0.998494433833281));
#285330=CARTESIAN_POINT('Ctrl Pts',(-0.244164707031287,1.53623207949619,
0.999954095289645));
#285331=CARTESIAN_POINT('Ctrl Pts',(-0.250799188246721,1.53516291575941,
1.00044260375327));
#285332=CARTESIAN_POINT('Ctrl Pts',(-0.262846802068166,1.53314122423497,
1.00132626850513));
#285333=CARTESIAN_POINT('Ctrl Pts',(-0.268261963517385,1.53220298132465,
1.00172217333455));
#285334=CARTESIAN_POINT('Ctrl Pts',(-0.280556865955555,1.53000555746569,
1.00261819566548));
#285335=CARTESIAN_POINT('Ctrl Pts',(-0.287433207140765,1.52872866047809,
1.00311731744504));
#285336=CARTESIAN_POINT('Ctrl Pts',(-0.308720488495415,1.52462702144165,
1.00465689438221));
#285337=CARTESIAN_POINT('Ctrl Pts',(-0.323100720097368,1.52164445920999,
1.00568899843103));
#285338=CARTESIAN_POINT('Ctrl Pts',(-0.429084344549661,1.49809240321099,
1.01325162524607));
#285339=CARTESIAN_POINT('Ctrl Pts',(-0.518713084477981,1.46946792720439,
1.01941027179441));
#285340=CARTESIAN_POINT('Ctrl Pts',(-0.704128088134424,1.39115465056524,
1.0326582204513));
#285341=CARTESIAN_POINT('Ctrl Pts',(-0.798429144647447,1.33925889842552,
1.03973112062725));
#285342=CARTESIAN_POINT('Ctrl Pts',(-0.901952185799104,1.267442408511,1.04846429388587));
#285343=CARTESIAN_POINT('Ctrl Pts',(-0.917081415561585,1.25653874982622,
1.04976642006812));
#285344=CARTESIAN_POINT('Ctrl Pts',(-0.940797808409407,1.23878981262018,
1.05185145801397));
#285345=CARTESIAN_POINT('Ctrl Pts',(-0.949515132629066,1.23212082116985,
1.05262752910011));
#285346=CARTESIAN_POINT('Ctrl Pts',(-0.965877333017481,1.21932652572685,
1.05410312057771));
#285347=CARTESIAN_POINT('Ctrl Pts',(-0.973536378812643,1.21322014071722,
1.05480186695245));
#285348=CARTESIAN_POINT('Ctrl Pts',(-0.990839102785638,1.19915572142229,
1.05639916425593));
#285349=CARTESIAN_POINT('Ctrl Pts',(-1.00044541603695,1.1911530230881,1.05729948977088));
#285350=CARTESIAN_POINT('Ctrl Pts',(-1.02536546171615,1.16987885457939,
1.05967145602723));
#285351=CARTESIAN_POINT('Ctrl Pts',(-1.04051769312572,1.15642281330667,
1.06115058098789));
#285352=CARTESIAN_POINT('Ctrl Pts',(-1.13576896981674,1.068446458573,1.07069279486908));
#285353=CARTESIAN_POINT('Ctrl Pts',(-1.20806624565432,0.985959662678294,
1.07909938235777));
#285354=CARTESIAN_POINT('Ctrl Pts',(-1.30722649945376,0.84537962799422,
1.09243929040788));
#285355=CARTESIAN_POINT('Ctrl Pts',(-1.34022367375399,0.792028501665256,
1.09730380989563));
#285356=CARTESIAN_POINT('Ctrl Pts',(-1.38007405115606,0.71793869536358,
1.10369493054856));
#285357=CARTESIAN_POINT('Ctrl Pts',(-1.38984354128897,0.69883859904247,
1.10531151582231));
#285358=CARTESIAN_POINT('Ctrl Pts',(-1.40594456819935,0.665685653655146,
1.1080577591964));
#285359=CARTESIAN_POINT('Ctrl Pts',(-1.41246796315006,0.651729866562969,
1.10919604179432));
#285360=CARTESIAN_POINT('Ctrl Pts',(-1.42170473411073,0.631178804893287,
1.11084411979572));
#285361=CARTESIAN_POINT('Ctrl Pts',(-1.42458155922438,0.624658643736115,
1.11136290949679));
#285362=CARTESIAN_POINT('Ctrl Pts',(-1.42939106584519,0.613552113380901,
1.11223941913728));
#285363=CARTESIAN_POINT('Ctrl Pts',(-1.43134667873592,0.608975946136397,
1.11259849044811));
#285364=CARTESIAN_POINT('Ctrl Pts',(-1.43575770227557,0.598515430978733,
1.11341451693047));
#285365=CARTESIAN_POINT('Ctrl Pts',(-1.43819893581681,0.592625282665485,
1.11387062074019));
#285366=CARTESIAN_POINT('Ctrl Pts',(-1.44486673250526,0.576253501019198,
1.11512945363952));
#285367=CARTESIAN_POINT('Ctrl Pts',(-1.4490154930026,0.565740305007305,
1.11592773952806));
#285368=CARTESIAN_POINT('Ctrl Pts',(-1.47657752076345,0.493603674622777,
1.12134284332101));
#285369=CARTESIAN_POINT('Ctrl Pts',(-1.49617058988019,0.430582922156333,
1.12576578668999));
#285370=CARTESIAN_POINT('Ctrl Pts',(-1.51533686452467,0.351527832558421,
1.13115628620731));
#285371=CARTESIAN_POINT('Ctrl Pts',(-1.51874441249173,0.336501188304759,
1.1321739530784));
#285372=CARTESIAN_POINT('Ctrl Pts',(-1.53558372126133,0.256768376439463,
1.13754786909517));
#285373=CARTESIAN_POINT('Ctrl Pts',(-1.54510468653155,0.191307616159485,
1.14187314482944));
#285374=CARTESIAN_POINT('Ctrl Pts',(-1.55379146551128,0.0839399700524597,
1.14905062467077));
#285375=CARTESIAN_POINT('Ctrl Pts',(-1.55548131816251,0.0423238287938353,
1.15185205604702));
#285376=CARTESIAN_POINT('Ctrl Pts',(-1.55551296434398,-0.0287841686642868,
1.15671477152007));
#285377=CARTESIAN_POINT('Ctrl Pts',(-1.55468822481587,-0.0582532439779469,
1.15875216244121));
#285378=CARTESIAN_POINT('Ctrl Pts',(-1.55229908074582,-0.100571042043388,
1.16171912500648));
#285379=CARTESIAN_POINT('Ctrl Pts',(-1.55141079476226,-0.113452627472457,
1.16262775926683));
#285380=CARTESIAN_POINT('Ctrl Pts',(-1.54956025863199,-0.136164559849562,
1.16424024185819));
#285381=CARTESIAN_POINT('Ctrl Pts',(-1.54866453946752,-0.145999720843197,
1.16494197334169));
#285382=CARTESIAN_POINT('Ctrl Pts',(-1.54660747269596,-0.166430726568488,
1.16640724792754));
#285383=CARTESIAN_POINT('Ctrl Pts',(-1.54543074575371,-0.177024464298145,
1.16717123888365));
#285384=CARTESIAN_POINT('Ctrl Pts',(-1.54207507834714,-0.204644394702371,
1.16917458920361));
#285385=CARTESIAN_POINT('Ctrl Pts',(-1.53972307445613,-0.221647661151528,
1.17041931347244));
#285386=CARTESIAN_POINT('Ctrl Pts',(-1.52672751156655,-0.305363885208652,
1.17660671100398));
#285387=CARTESIAN_POINT('Ctrl Pts',(-1.51202855627964,-0.371364042153737,
1.18167485282669));
#285388=CARTESIAN_POINT('Ctrl Pts',(-1.46750389802551,-0.523772371611034,
1.19381273799877));
#285389=CARTESIAN_POINT('Ctrl Pts',(-1.43426224024523,-0.608929817575973,
1.20094413117703));
#285390=CARTESIAN_POINT('Ctrl Pts',(-1.3710025359645,-0.736585035208035,
1.21191077349881));
#285391=CARTESIAN_POINT('Ctrl Pts',(-1.34599517033465,-0.781347317049105,
1.21581086931402));
#285392=CARTESIAN_POINT('Ctrl Pts',(-1.31303049034542,-0.834056615237349,
1.220406305716));
#285393=CARTESIAN_POINT('Ctrl Pts',(-1.30714240766572,-0.843254558249755,
1.22120829486619));
#285394=CARTESIAN_POINT('Ctrl Pts',(-1.29771081646496,-0.857651708381463,
1.22246281191104));
#285395=CARTESIAN_POINT('Ctrl Pts',(-1.29423194176983,-0.862892519792311,
1.22291930738669));
#285396=CARTESIAN_POINT('Ctrl Pts',(-1.28762220543469,-0.872719967603617,
1.22377478192885));
#285397=CARTESIAN_POINT('Ctrl Pts',(-1.28449855785755,-0.877310972128718,
1.22417417738702));
#285398=CARTESIAN_POINT('Ctrl Pts',(-1.27702994394212,-0.88816262092167,
1.22511780225973));
#285399=CARTESIAN_POINT('Ctrl Pts',(-1.27266345419126,-0.894408216474298,
1.22566058594377));
#285400=CARTESIAN_POINT('Ctrl Pts',(-1.25768147751872,-0.915505764924107,
1.22749397917557));
#285401=CARTESIAN_POINT('Ctrl Pts',(-1.24685003006503,-0.93020351679451,
1.22877101727788));
#285402=CARTESIAN_POINT('Ctrl Pts',(-1.21935652090631,-0.96616746207214,
1.23190475083995));
#285403=CARTESIAN_POINT('Ctrl Pts',(-1.20239408396714,-0.987197313793401,
1.23374522635645));
#285404=CARTESIAN_POINT('Ctrl Pts',(-1.13586368164649,-1.06542036572257,
1.24066832882985));
#285405=CARTESIAN_POINT('Ctrl Pts',(-1.08269177466586,-1.11941357724221,
1.24561390154537));
#285406=CARTESIAN_POINT('Ctrl Pts',(-0.955255417888559,-1.23120801735341,
1.25678414448857));
#285407=CARTESIAN_POINT('Ctrl Pts',(-0.879267805452882,-1.28657326453854,
1.26301529545086));
#285408=CARTESIAN_POINT('Ctrl Pts',(-0.783005216485522,-1.34418013835143,
1.27079444114156));
#285409=CARTESIAN_POINT('Ctrl Pts',(-0.767083937934294,-1.3533290789868,
1.27207700421522));
#285410=CARTESIAN_POINT('Ctrl Pts',(-0.741446228486962,-1.36746366784155,
1.27413806744307));
#285411=CARTESIAN_POINT('Ctrl Pts',(-0.731832470041748,-1.37263273218507,
1.27491000285651));
#285412=CARTESIAN_POINT('Ctrl Pts',(-0.713478623286334,-1.38225348486681,
1.27638240945695));
#285413=CARTESIAN_POINT('Ctrl Pts',(-0.704749239279571,-1.38672453787717,
1.27708215383941));
#285414=CARTESIAN_POINT('Ctrl Pts',(-0.684699884456577,-1.39675529755161,
1.27868836683183));
#285415=CARTESIAN_POINT('Ctrl Pts',(-0.673353544311358,-1.40226041803387,
1.27959668393535));
#285416=CARTESIAN_POINT('Ctrl Pts',(-0.637572473563439,-1.41908660158885,
1.28245975648336));
#285417=CARTESIAN_POINT('Ctrl Pts',(-0.612911139429624,-1.42991090978217,
1.28443123317565));
#285418=CARTESIAN_POINT('Ctrl Pts',(-0.51846649577302,-1.46847228254375,
1.2919791936791));
#285419=CARTESIAN_POINT('Ctrl Pts',(-0.446996181757044,-1.49178077546112,
1.2976932427901));
#285420=CARTESIAN_POINT('Ctrl Pts',(-0.286929015755493,-1.53144482291081,
1.31041992715441));
#285421=CARTESIAN_POINT('Ctrl Pts',(-0.198017415474529,-1.54545827418027,
1.31744646766776));
#285422=CARTESIAN_POINT('Ctrl Pts',(-0.0771367020315843,-1.55390213161356,
1.32665242690842));
#285423=CARTESIAN_POINT('Ctrl Pts',(-0.0458199122565539,-1.5551407568817,
1.32900501243914));
#285424=CARTESIAN_POINT('Ctrl Pts',(-0.00489881964357937,-1.55552182446076,
1.33201992615547));
#285425=CARTESIAN_POINT('Ctrl Pts',(0.00468788955820674,-1.5555224784307,
1.33272199149779));
#285426=CARTESIAN_POINT('Ctrl Pts',(0.020211613933411,-1.55538001633029,
1.33385132533914));
#285427=CARTESIAN_POINT('Ctrl Pts',(0.0261486915189897,-1.5552915333344,
1.3342814600661));
#285428=CARTESIAN_POINT('Ctrl Pts',(0.0377972704043039,-1.55505120732822,
1.33512170412584));
#285429=CARTESIAN_POINT('Ctrl Pts',(0.0435086664827107,-1.5549018904,1.33553193138178));
#285430=CARTESIAN_POINT('Ctrl Pts',(0.0577510003757015,-1.55445100810447,
1.33655081701692));
#285431=CARTESIAN_POINT('Ctrl Pts',(0.0662806956698605,-1.55411067587106,
1.33715737041014));
#285432=CARTESIAN_POINT('Ctrl Pts',(0.0994073218862273,-1.5525156980521,
1.33950034896991));
#285433=CARTESIAN_POINT('Ctrl Pts',(0.123977409930485,-1.55074710506303,
1.34121097164783));
#285434=CARTESIAN_POINT('Ctrl Pts',(0.189861032241237,-1.54442862306083,
1.34574992320626));
#285435=CARTESIAN_POINT('Ctrl Pts',(0.231052783091895,-1.53880541340218,
1.34853702695684));
#285436=CARTESIAN_POINT('Ctrl Pts',(0.410932677112957,-1.50686210852141,
1.36067295138658));
#285437=CARTESIAN_POINT('Ctrl Pts',(0.545875724765493,-1.46339231768407,
1.36975238936702));
#285438=CARTESIAN_POINT('Ctrl Pts',(0.690512897958219,-1.39396735512701,
1.38082935574176));
#285439=CARTESIAN_POINT('Ctrl Pts',(0.707761793780437,-1.38528922479972,
1.38217244160508));
#285440=CARTESIAN_POINT('Ctrl Pts',(0.735660538247319,-1.37059595447917,
1.38438393971862));
#285441=CARTESIAN_POINT('Ctrl Pts',(0.746409197767083,-1.36477213931963,
1.38524567247444));
#285442=CARTESIAN_POINT('Ctrl Pts',(0.765621502787687,-1.35406772166482,
1.38680413561767));
#285443=CARTESIAN_POINT('Ctrl Pts',(0.774110013920347,-1.34923287788809,
1.38749920420814));
#285444=CARTESIAN_POINT('Ctrl Pts',(0.792189151700143,-1.33870868298107,
1.38899389547905));
#285445=CARTESIAN_POINT('Ctrl Pts',(0.801765215616671,-1.33299554274951,
1.3897943510423));
#285446=CARTESIAN_POINT('Ctrl Pts',(0.827897292041068,-1.31702152383822,
1.39200341003502));
#285447=CARTESIAN_POINT('Ctrl Pts',(0.84432277875606,-1.30655218104267,
1.39341956971928));
#285448=CARTESIAN_POINT('Ctrl Pts',(0.880546408791246,-1.28249548759209,
1.39660654759216));
#285449=CARTESIAN_POINT('Ctrl Pts',(0.90023488562465,-1.26875280870725,
1.39838279544393));
#285450=CARTESIAN_POINT('Ctrl Pts',(0.963043442986792,-1.22271395950808,
1.40419548675255));
#285451=CARTESIAN_POINT('Ctrl Pts',(1.0048024940037,-1.18863493566952,1.40829255975161));
#285452=CARTESIAN_POINT('Ctrl Pts',(1.12018947394772,-1.08403666708012,
1.42027398422075));
#285453=CARTESIAN_POINT('Ctrl Pts',(1.1887665406834,-1.00836219614682,1.42826516503495));
#285454=CARTESIAN_POINT('Ctrl Pts',(1.26681465376374,-0.903111598444006,
1.43819998393924));
#285455=CARTESIAN_POINT('Ctrl Pts',(1.28351709523609,-0.879212185338064,
1.44038488009582));
#285456=CARTESIAN_POINT('Ctrl Pts',(1.30467656212726,-0.847045868174035,
1.44321977400832));
#285457=CARTESIAN_POINT('Ctrl Pts',(1.30974358964377,-0.839189713646754,
1.443904068003));
#285458=CARTESIAN_POINT('Ctrl Pts',(1.31788474974255,-0.82631390564759,
1.44501188820905));
#285459=CARTESIAN_POINT('Ctrl Pts',(1.32100166720112,-0.821321789944566,
1.44543809144491));
#285460=CARTESIAN_POINT('Ctrl Pts',(1.32710885166144,-0.811415695895693,
1.44627711518188));
#285461=CARTESIAN_POINT('Ctrl Pts',(1.33010032338837,-0.806502614758559,
1.44669000237211));
#285462=CARTESIAN_POINT('Ctrl Pts',(1.33756176764775,-0.794093779853041,
1.44772499070053));
#285463=CARTESIAN_POINT('Ctrl Pts',(1.34199612736557,-0.786576644082907,
1.44834484051555));
#285464=CARTESIAN_POINT('Ctrl Pts',(1.35948221668216,-0.756355822300801,
1.45081006741578));
#285465=CARTESIAN_POINT('Ctrl Pts',(1.3720238183528,-0.73335998998503,1.45262608250589));
#285466=CARTESIAN_POINT('Ctrl Pts',(1.40481737908016,-0.669441689255441,
1.45754273695903));
#285467=CARTESIAN_POINT('Ctrl Pts',(1.42385875274836,-0.627925887114373,
1.46059326815475));
#285468=CARTESIAN_POINT('Ctrl Pts',(1.48191550369624,-0.48506678902023,
1.47080897015905));
#285469=CARTESIAN_POINT('Ctrl Pts',(1.51214302299441,-0.380507574229137,
1.47784531193719));
#285470=CARTESIAN_POINT('Ctrl Pts',(1.5380915965182,-0.235311709009577,
1.4878331823631));
#285471=CARTESIAN_POINT('Ctrl Pts',(1.54350087863081,-0.196728193498538,
1.49050458654459));
#285472=CARTESIAN_POINT('Ctrl Pts',(1.54896732048858,-0.143184568467055,
1.4942583592442));
#285473=CARTESIAN_POINT('Ctrl Pts',(1.55026587102076,-0.128363868896053,
1.49530222521613));
#285474=CARTESIAN_POINT('Ctrl Pts',(1.55202069131992,-0.104384225476753,
1.49700008483808));
#285475=CARTESIAN_POINT('Ctrl Pts',(1.55260892065239,-0.0952356330571008,
1.49764993042762));
#285476=CARTESIAN_POINT('Ctrl Pts',(1.55366955793473,-0.0760994320696083,
1.49901385790617));
#285477=CARTESIAN_POINT('Ctrl Pts',(1.55412660000661,-0.0661114314141855,
1.4997283886078));
#285478=CARTESIAN_POINT('Ctrl Pts',(1.55498820463812,-0.0422455166606131,
1.50144237900248));
#285479=CARTESIAN_POINT('Ctrl Pts',(1.5553033074422,-0.0283654522450213,
1.50244458035445));
#285480=CARTESIAN_POINT('Ctrl Pts',(1.55575604579002,0.020255873733048,
1.50597510563191));
#285481=CARTESIAN_POINT('Ctrl Pts',(1.55491560377014,0.0549935096948878,
1.50853328257311));
#285482=CARTESIAN_POINT('Ctrl Pts',(1.54987777706318,0.142237614018786,
1.51505273970803));
#285483=CARTESIAN_POINT('Ctrl Pts',(1.54417562876676,0.194610662774658,
1.5190539239068));
#285484=CARTESIAN_POINT('Ctrl Pts',(1.51995382481115,0.34547108914028,1.53079979181471));
#285485=CARTESIAN_POINT('Ctrl Pts',(1.49456589202119,0.442586280914189,
1.53865232079548));
#285486=CARTESIAN_POINT('Ctrl Pts',(1.44892060415021,0.566784260805124,
1.54871249385081));
#285487=CARTESIAN_POINT('Ctrl Pts',(1.43688718364285,0.596632964086019,
1.55112983874934));
#285488=CARTESIAN_POINT('Ctrl Pts',(1.4200424895114,0.634943405783003,1.55421372410286));
#285489=CARTESIAN_POINT('Ctrl Pts',(1.4160668124303,0.643761288074544,1.55492220859574));
#285490=CARTESIAN_POINT('Ctrl Pts',(1.40951048026205,0.657948271929512,
1.5560592665619));
#285491=CARTESIAN_POINT('Ctrl Pts',(1.40698086437202,0.663340465383115,
1.55649077658034));
#285492=CARTESIAN_POINT('Ctrl Pts',(1.40196982481974,0.673864489478773,
1.55733147094709));
#285493=CARTESIAN_POINT('Ctrl Pts',(1.39949107190796,0.678997408824249,
1.55774079136288));
#285494=CARTESIAN_POINT('Ctrl Pts',(1.39325890216053,0.691723662517195,
1.55875413331943));
#285495=CARTESIAN_POINT('Ctrl Pts',(1.38947149657993,0.699300337887208,
1.55935609952396));
#285496=CARTESIAN_POINT('Ctrl Pts',(1.3746650186864,0.728325313324788,1.56165844701148));
#285497=CARTESIAN_POINT('Ctrl Pts',(1.36320901522437,0.749548544321978,
1.56333415315856));
#285498=CARTESIAN_POINT('Ctrl Pts',(1.33132508145061,0.805465077072625,
1.56775149698088));
#285499=CARTESIAN_POINT('Ctrl Pts',(1.3100355540923,0.839647414166252,1.57045457043898));
#285500=CARTESIAN_POINT('Ctrl Pts',(1.21323744756987,0.982404134451389,
1.58192323263047));
#285501=CARTESIAN_POINT('Ctrl Pts',(1.12538782026016,1.0819262973633,1.59043357673954));
#285502=CARTESIAN_POINT('Ctrl Pts',(1.00470901529274,1.18783129182071,1.60142706512667));
#285503=CARTESIAN_POINT('Ctrl Pts',(0.98290288403607,1.20593744946568,1.60338770829089));
#285504=CARTESIAN_POINT('Ctrl Pts',(0.950609760612354,1.23129329133685,
1.60626303635411));
#285505=CARTESIAN_POINT('Ctrl Pts',(0.94050828501287,1.23902632540372,1.60715859058409));
#285506=CARTESIAN_POINT('Ctrl Pts',(0.922420091037247,1.25252482069572,
1.60875613879582));
#285507=CARTESIAN_POINT('Ctrl Pts',(0.914471228237063,1.25834002376041,
1.60945614683852));
#285508=CARTESIAN_POINT('Ctrl Pts',(0.89773323729511,1.27034279239836,1.61092626326136));
#285509=CARTESIAN_POINT('Ctrl Pts',(0.888934154772039,1.27651550452427,
1.61169689287338));
#285510=CARTESIAN_POINT('Ctrl Pts',(0.865576464393049,1.29254272059753,
1.61373725446418));
#285511=CARTESIAN_POINT('Ctrl Pts',(0.850913922238565,1.30224220103209,
1.61501272148755));
#285512=CARTESIAN_POINT('Ctrl Pts',(0.773023566605363,1.35189064248421,
1.62176320386917));
#285513=CARTESIAN_POINT('Ctrl Pts',(0.707149446321878,1.3874834157055,1.6273939314499));
#285514=CARTESIAN_POINT('Ctrl Pts',(0.594068773299685,1.43843286369268,
1.6369102049889));
#285515=CARTESIAN_POINT('Ctrl Pts',(0.54822245540609,1.45652278051361,1.64072867946952));
#285516=CARTESIAN_POINT('Ctrl Pts',(0.42737081080698,1.49769268073475,1.65062893832811));
#285517=CARTESIAN_POINT('Ctrl Pts',(0.351331225187655,1.51733252410523,
1.65670267151562));
#285518=CARTESIAN_POINT('Ctrl Pts',(0.259188183155168,1.53382922490932,
1.66367506506825));
#285519=CARTESIAN_POINT('Ctrl Pts',(0.244209164679686,1.53628530389922,
1.66479631358244));
#285520=CARTESIAN_POINT('Ctrl Pts',(0.22218809743989,1.53956581480797,1.66642457852482));
#285521=CARTESIAN_POINT('Ctrl Pts',(0.215173086553863,1.54056190944774,
1.66694029530586));
#285522=CARTESIAN_POINT('Ctrl Pts',(0.202702832726107,1.54224577776568,
1.66785148397202));
#285523=CARTESIAN_POINT('Ctrl Pts',(0.197250467302218,1.54295260257322,
1.66824797533813));
#285524=CARTESIAN_POINT('Ctrl Pts',(0.185207857687381,1.54444888190396,
1.66911948068802));
#285525=CARTESIAN_POINT('Ctrl Pts',(0.178616200459464,1.54522508283851,
1.66959375997708));
#285526=CARTESIAN_POINT('Ctrl Pts',(0.159229282447211,1.54738227458015,
1.67098114426803));
#285527=CARTESIAN_POINT('Ctrl Pts',(0.146421232818584,1.54864673794288,
1.67188809751811));
#285528=CARTESIAN_POINT('Ctrl Pts',(0.116741337360638,1.55120533239833,
1.67397060996629));
#285529=CARTESIAN_POINT('Ctrl Pts',(0.0998608721853694,1.55238345217501,
1.6751407564622));
#285530=CARTESIAN_POINT('Ctrl Pts',(0.0408382982810627,1.55553595321183,
1.67919289210649));
#285531=CARTESIAN_POINT('Ctrl Pts',(-0.00136447965634196,1.55607150533019,
1.68202070158236));
#285532=CARTESIAN_POINT('Ctrl Pts',(-0.183054574874739,1.55098386289037,
1.69408914816562));
#285533=CARTESIAN_POINT('Ctrl Pts',(-0.32139648054752,1.52832012647518,
1.70307427924817));
#285534=CARTESIAN_POINT('Ctrl Pts',(-0.473638613469977,1.48176663257494,
1.71406063104891));
#285535=CARTESIAN_POINT('Ctrl Pts',(-0.492306769605151,1.47566929732042,
1.71542613496786));
#285536=CARTESIAN_POINT('Ctrl Pts',(-0.522491641841563,1.46517389679756,
1.71766697821376));
#285537=CARTESIAN_POINT('Ctrl Pts',(-0.534080683110418,1.4609893469953,
1.71853532928839));
#285538=CARTESIAN_POINT('Ctrl Pts',(-0.554774433803354,1.4532381670657,
1.72010095796282));
#285539=CARTESIAN_POINT('Ctrl Pts',(-0.563897633739579,1.44972248837634,
1.72079650753148));
#285540=CARTESIAN_POINT('Ctrl Pts',(-0.583294025785787,1.44203718565611,
1.72228698529944));
#285541=CARTESIAN_POINT('Ctrl Pts',(-0.593556943234001,1.43784328376957,
1.72308269878754));
#285542=CARTESIAN_POINT('Ctrl Pts',(-0.621444048696768,1.42609788065748,
1.72526476231324));
#285543=CARTESIAN_POINT('Ctrl Pts',(-0.638974304079398,1.41832988004247,
1.72665836313679));
#285544=CARTESIAN_POINT('Ctrl Pts',(-0.751669339079574,1.3658792112092,
1.7357645804769));
#285545=CARTESIAN_POINT('Ctrl Pts',(-0.842221872722308,1.31197832860232,
1.74379837533384));
#285546=CARTESIAN_POINT('Ctrl Pts',(-1.00332520279295,1.19249153917397,
1.75933724312972));
#285547=CARTESIAN_POINT('Ctrl Pts',(-1.07462400233896,1.12866466672871,
1.76678432371324));
#285548=CARTESIAN_POINT('Ctrl Pts',(-1.14948835431144,1.04807769543371,
1.77496802123196));
#285549=CARTESIAN_POINT('Ctrl Pts',(-1.15920491005059,1.03732075509186,
1.77603784584846));
#285550=CARTESIAN_POINT('Ctrl Pts',(-1.17336065019996,1.02120195362672,
1.77760598315025));
#285551=CARTESIAN_POINT('Ctrl Pts',(-1.17791616794025,1.01594397080627,
1.77811213995246));
#285552=CARTESIAN_POINT('Ctrl Pts',(-1.18600484813376,1.00648045928285,
1.77901330801262));
#285553=CARTESIAN_POINT('Ctrl Pts',(-1.18955116860387,1.00228660315738,
1.77940924517836));
#285554=CARTESIAN_POINT('Ctrl Pts',(-1.19740383972254,0.992899693714939,
1.78028786328329));
#285555=CARTESIAN_POINT('Ctrl Pts',(-1.20169869421266,0.9876973271344,1.78076972789808));
#285556=CARTESIAN_POINT('Ctrl Pts',(-1.21443044850802,0.972069340231864,
1.78220273877384));
#285557=CARTESIAN_POINT('Ctrl Pts',(-1.22276677085871,0.961562048103047,
1.78314710764514));
#285558=CARTESIAN_POINT('Ctrl Pts',(-1.2834213639873,0.8830469352148,1.79007523044091));
#285559=CARTESIAN_POINT('Ctrl Pts',(-1.33017595046773,0.810912105934072,
1.79574073476288));
#285560=CARTESIAN_POINT('Ctrl Pts',(-1.41010766359066,0.661899236267086,
1.80687727471846));
#285561=CARTESIAN_POINT('Ctrl Pts',(-1.44351100257382,0.585481861399606,
1.81233333670593));
#285562=CARTESIAN_POINT('Ctrl Pts',(-1.48402225490741,0.467916910113274,
1.82073812119626));
#285563=CARTESIAN_POINT('Ctrl Pts',(-1.49586213260795,0.428560716483626,
1.82355180738951));
#285564=CARTESIAN_POINT('Ctrl Pts',(-1.50992349584839,0.374087793830485,
1.82747336029534));
#285565=CARTESIAN_POINT('Ctrl Pts',(-1.51350182778367,0.35933665216795,
1.82853790909864));
#285566=CARTESIAN_POINT('Ctrl Pts',(-1.51890618730803,0.335543267928228,
1.83026034838203));
#285567=CARTESIAN_POINT('Ctrl Pts',(-1.5208687090463,0.326532775853882,
1.83091385024171));
#285568=CARTESIAN_POINT('Ctrl Pts',(-1.52478328782911,0.307758525152647,
1.83227829957696));
#285569=CARTESIAN_POINT('Ctrl Pts',(-1.5267219405675,0.297992436725351,
1.83298964064143));
#285570=CARTESIAN_POINT('Ctrl Pts',(-1.53038802978201,0.278548667689275,
1.83440929547135));
#285571=CARTESIAN_POINT('Ctrl Pts',(-1.53211774498378,0.268871882569186,
1.83511750068595));
#285572=CARTESIAN_POINT('Ctrl Pts',(-1.53595638774626,0.246155816974868,
1.83678417298149));
#285573=CARTESIAN_POINT('Ctrl Pts',(-1.53799114730412,0.233104959547902,
1.83774492517261));
#285574=CARTESIAN_POINT('Ctrl Pts',(-1.55034034614246,0.146680298957285,
1.84412968162698));
#285575=CARTESIAN_POINT('Ctrl Pts',(-1.55556516654839,0.072688768575606,
1.84970986030065));
#285576=CARTESIAN_POINT('Ctrl Pts',(-1.55549938660524,-0.00138140172760619,
1.85539343273712));
#285577=CARTESIAN_POINT('',(-1.5554992988366,0.00127668674633576,3.25533865702281));
#285578=CARTESIAN_POINT('Ctrl Pts',(-1.55549938782948,-0.00138002250719613,
1.85539332690641));
#285579=CARTESIAN_POINT('Ctrl Pts',(-1.55539766380321,-0.116038776085956,
1.86419135181066));
#285580=CARTESIAN_POINT('Ctrl Pts',(-1.54261929930628,-0.230336009965302,
1.87321326259203));
#285581=CARTESIAN_POINT('Ctrl Pts',(-1.51371361985,-0.358512387846686,1.88312415629134));
#285582=CARTESIAN_POINT('Ctrl Pts',(-1.50977061259033,-0.374770335955011,
1.88437665157453));
#285583=CARTESIAN_POINT('Ctrl Pts',(-1.502359557691,-0.403309745667421,
1.88656365234119));
#285584=CARTESIAN_POINT('Ctrl Pts',(-1.49900126965122,-0.415617869024133,
1.88750297429455));
#285585=CARTESIAN_POINT('Ctrl Pts',(-1.49367239580812,-0.434242755299764,
1.88891709446616));
#285586=CARTESIAN_POINT('Ctrl Pts',(-1.49181241324735,-0.440590200221338,
1.88939773949122));
#285587=CARTESIAN_POINT('Ctrl Pts',(-1.48833177301127,-0.452193576340129,
1.89027376325001));
#285588=CARTESIAN_POINT('Ctrl Pts',(-1.48672369933094,-0.457452883697398,
1.89066981244072));
#285589=CARTESIAN_POINT('Ctrl Pts',(-1.48297157566527,-0.469495646941254,
1.89157444234581));
#285590=CARTESIAN_POINT('Ctrl Pts',(-1.48080884848271,-0.476273048004625,
1.89208193889876));
#285591=CARTESIAN_POINT('Ctrl Pts',(-1.47400589228505,-0.497097288868325,
1.89363700425126));
#285592=CARTESIAN_POINT('Ctrl Pts',(-1.46921155942735,-0.511093455747034,
1.89467617237059));
#285593=CARTESIAN_POINT('Ctrl Pts',(-1.43496540015201,-0.606601947318413,
1.90173991902198));
#285594=CARTESIAN_POINT('Ctrl Pts',(-1.398941372988,-0.685608333104245,
1.90745038881136));
#285595=CARTESIAN_POINT('Ctrl Pts',(-1.3188162463593,-0.828395524329324,
1.91822998347317));
#285596=CARTESIAN_POINT('Ctrl Pts',(-1.27617860128657,-0.892682812343315,
1.92328542963743));
#285597=CARTESIAN_POINT('Ctrl Pts',(-1.2019558003225,-0.988343279150782,
1.93145374223992));
#285598=CARTESIAN_POINT('Ctrl Pts',(-1.17349225906434,-1.02197628038131,
1.93446608983305));
#285599=CARTESIAN_POINT('Ctrl Pts',(-1.13361391707814,-1.0652317240849,
1.9385672398285));
#285600=CARTESIAN_POINT('Ctrl Pts',(-1.12343122537579,-1.0759653314339,
1.93960475333125));
#285601=CARTESIAN_POINT('Ctrl Pts',(-1.1127785721042,-1.0868782395644,1.94068101230253));
#285602=CARTESIAN_POINT('Ctrl Pts',(-1.11245972113799,-1.0872045929896,
1.94071321813696));
#285603=CARTESIAN_POINT('Ctrl Pts',(-1.11182075533274,-1.08785801806167,
1.94077774084313));
#285604=CARTESIAN_POINT('Ctrl Pts',(-1.11150063964671,-1.08818508881249,
1.9408100577495));
#285605=CARTESIAN_POINT('Ctrl Pts',(-1.11085785637062,-1.08884125810893,
1.94087493248099));
#285606=CARTESIAN_POINT('Ctrl Pts',(-1.11053518677012,-1.0891703546118,
1.94090749039098));
#285607=CARTESIAN_POINT('Ctrl Pts',(-1.10988593429973,-1.08983195037405,
1.94097298414055));
#285608=CARTESIAN_POINT('Ctrl Pts',(-1.10955934817187,-1.09016444635479,
1.94100592011898));
#285609=CARTESIAN_POINT('Ctrl Pts',(-1.10913530607355,-1.09059577391743,
1.94104867332845));
#285610=CARTESIAN_POINT('Ctrl Pts',(-1.10903798594903,-1.09069473959835,
1.94105848467777));
#285611=CARTESIAN_POINT('Ctrl Pts',(-1.10883031820993,-1.09090586219629,
1.94107941912415));
#285612=CARTESIAN_POINT('Ctrl Pts',(-1.10871996682877,-1.09101801539249,
1.94109054238435));
#285613=CARTESIAN_POINT('Ctrl Pts',(-1.10848378181274,-1.09125798399325,
1.94111434740593));
#285614=CARTESIAN_POINT('Ctrl Pts',(-1.10835794309461,-1.09138579436876,
1.94112702938747));
#285615=CARTESIAN_POINT('Ctrl Pts',(-1.1080876687569,-1.09166020844547,
1.94115426482042));
#285616=CARTESIAN_POINT('Ctrl Pts',(-1.10794322615939,-1.09180680523697,
1.94116881857421));
#285617=CARTESIAN_POINT('Ctrl Pts',(-1.10763172607929,-1.09212282550781,
1.94120020112357));
#285618=CARTESIAN_POINT('Ctrl Pts',(-1.10746465882821,-1.09229223931097,
1.9412170303429));
#285619=CARTESIAN_POINT('Ctrl Pts',(-1.10710262592472,-1.09265918872381,
1.94125349426287));
#285620=CARTESIAN_POINT('Ctrl Pts',(-1.10690764629187,-1.09285671046684,
1.94127312957035));
#285621=CARTESIAN_POINT('Ctrl Pts',(-1.10648268386012,-1.09328698308489,
1.94131591858198));
#285622=CARTESIAN_POINT('Ctrl Pts',(-1.10625268050981,-1.09351971355331,
1.94133907317904));
#285623=CARTESIAN_POINT('Ctrl Pts',(-1.10574786039744,-1.09403019697703,
1.94138988458568));
#285624=CARTESIAN_POINT('Ctrl Pts',(-1.10547301244669,-1.09430791892531,
1.94141754275191));
#285625=CARTESIAN_POINT('Ctrl Pts',(-1.10486451802979,-1.09492231298259,
1.94147876284793));
#285626=CARTESIAN_POINT('Ctrl Pts',(-1.10453082236997,-1.09525893609783,
1.94151232692011));
#285627=CARTESIAN_POINT('Ctrl Pts',(-1.10378389823267,-1.09601172436885,
1.94158743515946));
#285628=CARTESIAN_POINT('Ctrl Pts',(-1.10337058832985,-1.09642780827496,
1.94162898287835));
#285629=CARTESIAN_POINT('Ctrl Pts',(-1.10084977933089,-1.09896266729653,
1.94188230439833));
#285630=CARTESIAN_POINT('Ctrl Pts',(-1.09873642619557,-1.10107558609246,
1.94209433402723));
#285631=CARTESIAN_POINT('Ctrl Pts',(-1.08967135732866,-1.11008670594664,
1.94300236399372));
#285632=CARTESIAN_POINT('Ctrl Pts',(-1.08266080413106,-1.11692512588829,
1.9437009558404));
#285633=CARTESIAN_POINT('Ctrl Pts',(-1.06656567676514,-1.1323311492053,
1.94529693241653));
#285634=CARTESIAN_POINT('Ctrl Pts',(-1.05744167308058,-1.14085637372283,
1.94619608098515));
#285635=CARTESIAN_POINT('Ctrl Pts',(-1.03328489056309,-1.16288907189579,
1.94856285216569));
#285636=CARTESIAN_POINT('Ctrl Pts',(-1.01809022296345,-1.17621464259349,
1.95003790586758));
#285637=CARTESIAN_POINT('Ctrl Pts',(-0.918484476451701,-1.26019164313763,
1.95962484838615));
#285638=CARTESIAN_POINT('Ctrl Pts',(-0.827049608415514,-1.32199736519118,
1.96808505058503));
#285639=CARTESIAN_POINT('Ctrl Pts',(-0.674941817056807,-1.40282004166848,
1.98144150415998));
#285640=CARTESIAN_POINT('Ctrl Pts',(-0.618299532874221,-1.42869066529152,
1.98626941227193));
#285641=CARTESIAN_POINT('Ctrl Pts',(-0.540329777371615,-1.45879412091462,
1.99261808916061));
#285642=CARTESIAN_POINT('Ctrl Pts',(-0.520244685389792,-1.466077119928,
1.99422778722588));
#285643=CARTESIAN_POINT('Ctrl Pts',(-0.485474015382528,-1.47788058831197,
1.99696362938833));
#285644=CARTESIAN_POINT('Ctrl Pts',(-0.47086009117039,-1.48260138763152,
1.99809831525367));
#285645=CARTESIAN_POINT('Ctrl Pts',(-0.449372939634831,-1.48919269293787,
1.99974223400038));
#285646=CARTESIAN_POINT('Ctrl Pts',(-0.44255351093921,-1.49123348636273,
2.00026039763147));
#285647=CARTESIAN_POINT('Ctrl Pts',(-0.430943404808324,-1.49462128708306,
2.00113624115592));
#285648=CARTESIAN_POINT('Ctrl Pts',(-0.426159967493677,-1.49599221080461,
2.00149526616931));
#285649=CARTESIAN_POINT('Ctrl Pts',(-0.415225589968901,-1.49906927811483,
2.00231174440553));
#285650=CARTESIAN_POINT('Ctrl Pts',(-0.409070633807719,-1.50076054438941,
2.00276834132166));
#285651=CARTESIAN_POINT('Ctrl Pts',(-0.391961307568011,-1.50534878606043,
2.0040297201373));
#285652=CARTESIAN_POINT('Ctrl Pts',(-0.380985159378353,-1.50816410324995,
2.00483003137214));
#285653=CARTESIAN_POINT('Ctrl Pts',(-0.30115048221717,-1.52771399659727,
2.0105933208075));
#285654=CARTESIAN_POINT('Ctrl Pts',(-0.231240828331398,-1.53984808799809,
2.01533146352502));
#285655=CARTESIAN_POINT('Ctrl Pts',(-0.0684365885804611,-1.55676212503987,
2.02615742909475));
#285656=CARTESIAN_POINT('Ctrl Pts',(0.0245348630282996,-1.55807232634197,
2.03219540300838));
#285657=CARTESIAN_POINT('Ctrl Pts',(0.16571045946522,-1.54741717025975,
2.0417127036691));
#285658=CARTESIAN_POINT('Ctrl Pts',(0.214149168785505,-1.54146009386573,
2.04503912423425));
#285659=CARTESIAN_POINT('Ctrl Pts',(0.277625416038463,-1.53060396759468,
2.04952448294937));
#285660=CARTESIAN_POINT('Ctrl Pts',(0.292985301201792,-1.52773818421614,
2.05061961676102));
#285661=CARTESIAN_POINT('Ctrl Pts',(0.318430182148028,-1.52259295551962,
2.05245140719212));
#285662=CARTESIAN_POINT('Ctrl Pts',(0.328540529136187,-1.52044342232063,
2.05318390680175));
#285663=CARTESIAN_POINT('Ctrl Pts',(0.348315016184895,-1.51603278208599,
2.05462608885738));
#285664=CARTESIAN_POINT('Ctrl Pts',(0.357980435145784,-1.51377962283028,
2.05533548510163));
#285665=CARTESIAN_POINT('Ctrl Pts',(0.381252728963373,-1.50811914447127,
2.05705474797271));
#285666=CARTESIAN_POINT('Ctrl Pts',(0.394836136360542,-1.50462001805791,
2.05806752047571));
#285667=CARTESIAN_POINT('Ctrl Pts',(0.440521215259556,-1.49219017973418,
2.06150626528908));
#285668=CARTESIAN_POINT('Ctrl Pts',(0.472380651540062,-1.48241245322546,
2.06395909942711));
#285669=CARTESIAN_POINT('Ctrl Pts',(0.622569341500666,-1.43098613555469,
2.07579301286842));
#285670=CARTESIAN_POINT('Ctrl Pts',(0.735874886143945,-1.37615129242733,
2.0855876369283));
#285671=CARTESIAN_POINT('Ctrl Pts',(0.88774336493013,-1.27848938378069,
2.09952265803288));
#285672=CARTESIAN_POINT('Ctrl Pts',(0.932527325422741,-1.24620122134243,
2.1037394158671));
#285673=CARTESIAN_POINT('Ctrl Pts',(0.985459974905064,-1.20358308071593,
2.10878008222338));
#285674=CARTESIAN_POINT('Ctrl Pts',(0.995316232333132,-1.19544519743005,
2.10972117495512));
#285675=CARTESIAN_POINT('Ctrl Pts',(1.01012316929054,-1.18290965128527,
2.11113739920062));
#285676=CARTESIAN_POINT('Ctrl Pts',(1.01514763618166,-1.17860058600255,
2.11161840291368));
#285677=CARTESIAN_POINT('Ctrl Pts',(1.02429606178485,-1.17065283945922,
2.11249475999196));
#285678=CARTESIAN_POINT('Ctrl Pts',(1.02842831697937,-1.1670242891593,2.11289078748289));
#285679=CARTESIAN_POINT('Ctrl Pts',(1.03785736953752,-1.15865562173357,
2.11379496283577));
#285680=CARTESIAN_POINT('Ctrl Pts',(1.04314101940135,-1.15390103049611,
2.11430203094919));
#285681=CARTESIAN_POINT('Ctrl Pts',(1.05929735111034,-1.13916078328038,
2.11585449457541));
#285682=CARTESIAN_POINT('Ctrl Pts',(1.07006100707179,-1.12905608846639,
2.11689152946694));
#285683=CARTESIAN_POINT('Ctrl Pts',(1.14361667709788,-1.05800659433596,
2.12401166516163));
#285684=CARTESIAN_POINT('Ctrl Pts',(1.20132075686359,-0.992002885792999,
2.12977420013549));
#285685=CARTESIAN_POINT('Ctrl Pts',(1.29848195831708,-0.859868962894762,
2.14057151719666));
#285686=CARTESIAN_POINT('Ctrl Pts',(1.33918239325432,-0.794996562404126,
2.14559206674625));
#285687=CARTESIAN_POINT('Ctrl Pts',(1.39550125711051,-0.688541049955402,
2.15371817552177));
#285688=CARTESIAN_POINT('Ctrl Pts',(1.41439915191265,-0.648835105475695,
2.15672503191962));
#285689=CARTESIAN_POINT('Ctrl Pts',(1.43749296474405,-0.59449311724066,
2.16084148555709));
#285690=CARTESIAN_POINT('Ctrl Pts',(1.44319394585411,-0.580516405219747,
2.1619002543274));
#285691=CARTESIAN_POINT('Ctrl Pts',(1.452415349523,-0.556933143339107,2.16368797581798));
#285692=CARTESIAN_POINT('Ctrl Pts',(1.45604610560108,-0.547370626708334,
2.16441319219326));
#285693=CARTESIAN_POINT('Ctrl Pts',(1.46304097097454,-0.528385706957744,
2.16585402044033));
#285694=CARTESIAN_POINT('Ctrl Pts',(1.46640900760776,-0.518965270367493,
2.16656946070947));
#285695=CARTESIAN_POINT('Ctrl Pts',(1.4744235644756,-0.49584735907924,2.16832671618908));
#285696=CARTESIAN_POINT('Ctrl Pts',(1.47897026979995,-0.482116547920775,
2.16937176081428));
#285697=CARTESIAN_POINT('Ctrl Pts',(1.49417213802951,-0.433967679865874,
2.17304211728533));
#285698=CARTESIAN_POINT('Ctrl Pts',(1.50382173816676,-0.39924693208229,
2.17569940947452));
#285699=CARTESIAN_POINT('Ctrl Pts',(1.54088387259139,-0.24536551774025,
2.18753002070522));
#285700=CARTESIAN_POINT('Ctrl Pts',(1.55539458831865,-0.123557648279827,
2.1970798225649));
#285701=CARTESIAN_POINT('Ctrl Pts',(1.55553296007454,0.0377582192192761,
2.20952720089324));
#285702=CARTESIAN_POINT('Ctrl Pts',(1.55409278180253,0.0768407869833449,
2.21252285128286));
#285703=CARTESIAN_POINT('Ctrl Pts',(1.54942064576688,0.139409496562854,
2.217250422461));
#285704=CARTESIAN_POINT('Ctrl Pts',(1.54712236280516,0.162947526642347,
2.21901321562704));
#285705=CARTESIAN_POINT('Ctrl Pts',(1.54328025722834,0.194774264110559,
2.22136773155015));
#285706=CARTESIAN_POINT('Ctrl Pts',(1.54220469289375,0.203114893769966,
2.22198204573692));
#285707=CARTESIAN_POINT('Ctrl Pts',(1.54028832278048,0.217081747189404,
2.22300573810681));
#285708=CARTESIAN_POINT('Ctrl Pts',(1.53948421314118,0.22271273844153,2.22341708741911));
#285709=CARTESIAN_POINT('Ctrl Pts',(1.53777220045454,0.234249017978596,
2.22425684989843));
#285710=CARTESIAN_POINT('Ctrl Pts',(1.53686113685671,0.24015368447963,2.2246850861318));
#285711=CARTESIAN_POINT('Ctrl Pts',(1.53437277576003,0.255686567157601,
2.22580778999951));
#285712=CARTESIAN_POINT('Ctrl Pts',(1.53273884468729,0.265305639805893,
2.22649917723953));
#285713=CARTESIAN_POINT('Ctrl Pts',(1.52517979735085,0.307403241879653,
2.22951057803652));
#285714=CARTESIAN_POINT('Ctrl Pts',(1.51831160417563,0.339706377809358,
2.23178362614877));
#285715=CARTESIAN_POINT('Ctrl Pts',(1.48924287049191,0.457806530981507,
2.24003649951594));
#285716=CARTESIAN_POINT('Ctrl Pts',(1.46075174486595,0.54188369691448,2.24580624208016));
#285717=CARTESIAN_POINT('Ctrl Pts',(1.39547094697615,0.691208551927479,
2.25655529653191));
#285718=CARTESIAN_POINT('Ctrl Pts',(1.36084505007439,0.757104642076446,
2.26149757570754));
#285719=CARTESIAN_POINT('Ctrl Pts',(1.30745616033011,0.843126567547134,
2.26844084409891));
#285720=CARTESIAN_POINT('Ctrl Pts',(1.29267945993515,0.865611740769411,
2.27030433832295));
#285721=CARTESIAN_POINT('Ctrl Pts',(1.27013384601024,0.898052990519306,
2.2730726045484));
#285722=CARTESIAN_POINT('Ctrl Pts',(1.26281442332016,0.908316506621834,
2.27396051022109));
#285723=CARTESIAN_POINT('Ctrl Pts',(1.24958069110846,0.926404077567346,
2.27554767344445));
#285724=CARTESIAN_POINT('Ctrl Pts',(1.24371553872132,0.934263383220231,
2.27624500702461));
#285725=CARTESIAN_POINT('Ctrl Pts',(1.23116497526757,0.950753506638161,
2.27772481333258));
#285726=CARTESIAN_POINT('Ctrl Pts',(1.22446225836271,0.959370415066531,
2.27850794189771));
#285727=CARTESIAN_POINT('Ctrl Pts',(1.20623766986802,0.982297538656482,
2.2806187450607));
#285728=CARTESIAN_POINT('Ctrl Pts',(1.19455237199734,0.99647496081217,2.28195289011951));
#285729=CARTESIAN_POINT('Ctrl Pts',(1.12378142793482,1.07930516013351,2.28992465464507));
#285730=CARTESIAN_POINT('Ctrl Pts',(1.05905206007119,1.14288568392219,2.29679616853486));
#285731=CARTESIAN_POINT('Ctrl Pts',(0.938808884967153,1.24196486926266,
2.30882495251858));
#285732=CARTESIAN_POINT('Ctrl Pts',(0.885884504091287,1.28025289650019,
2.31390917683055));
#285733=CARTESIAN_POINT('Ctrl Pts',(0.800764486532074,1.33402068692155,
2.32166102547224));
#285734=CARTESIAN_POINT('Ctrl Pts',(0.770177471462459,1.35191048144166,
2.32436784422616));
#285735=CARTESIAN_POINT('Ctrl Pts',(0.719547973294031,1.37924612293637,
2.32869535335961));
#285736=CARTESIAN_POINT('Ctrl Pts',(0.699868450528997,1.38933560946832,
2.33034137323948));
#285737=CARTESIAN_POINT('Ctrl Pts',(0.672602661587294,1.40258802859208,
2.3325666139198));
#285738=CARTESIAN_POINT('Ctrl Pts',(0.66519764102275,1.40611508229561,2.33316546535463));
#285739=CARTESIAN_POINT('Ctrl Pts',(0.652646288225694,1.41197201713396,
2.33417084305072));
#285740=CARTESIAN_POINT('Ctrl Pts',(0.64751460216541,1.41433270448369,2.33457918998582));
#285741=CARTESIAN_POINT('Ctrl Pts',(0.637552528365851,1.41884988742301,
2.33536654013391));
#285742=CARTESIAN_POINT('Ctrl Pts',(0.632723873011264,1.42100975796641,
2.33574576479558));
#285743=CARTESIAN_POINT('Ctrl Pts',(0.619389434832095,1.42689284297884,
2.33678664153988));
#285744=CARTESIAN_POINT('Ctrl Pts',(0.610861010176141,1.43056467689743,
2.33744526832366));
#285745=CARTESIAN_POINT('Ctrl Pts',(0.575934502633639,1.44523265874609,
2.34011576202334));
#285746=CARTESIAN_POINT('Ctrl Pts',(0.549266616642322,1.45557701021844,
2.34209279048607));
#285747=CARTESIAN_POINT('Ctrl Pts',(0.426108367136655,1.49948205331072,
2.35100945428563));
#285748=CARTESIAN_POINT('Ctrl Pts',(0.326736865578115,1.52422494240192,
2.35762719296997));
#285749=CARTESIAN_POINT('Ctrl Pts',(0.172105757888236,1.54689636808768,
2.36795670534419));
#285750=CARTESIAN_POINT('Ctrl Pts',(0.118193038426011,1.55194667340341,
2.37156112276727));
#285751=CARTESIAN_POINT('Ctrl Pts',(0.040072717003073,1.55517013570473,
2.37687622538465));
#285752=CARTESIAN_POINT('Ctrl Pts',(0.0159970198222962,1.55560405338306,
2.37852660299121));
#285753=CARTESIAN_POINT('Ctrl Pts',(-0.0275986947589804,1.55537764775832,
2.38154457177184));
#285754=CARTESIAN_POINT('Ctrl Pts',(-0.0471148847599626,1.55490882164833,
2.38290630049015));
#285755=CARTESIAN_POINT('Ctrl Pts',(-0.0777660575102398,1.55359493905898,
2.38506441648142));
#285756=CARTESIAN_POINT('Ctrl Pts',(-0.0889100284350443,1.55299703462569,
2.38585309266295));
#285757=CARTESIAN_POINT('Ctrl Pts',(-0.109793925943065,1.55165104126194,
2.3873391381327));
#285758=CARTESIAN_POINT('Ctrl Pts',(-0.119535163569938,1.55093100965304,
2.38803559434104));
#285759=CARTESIAN_POINT('Ctrl Pts',(-0.141438166121551,1.54910445715876,
2.38960930408768));
#285760=CARTESIAN_POINT('Ctrl Pts',(-0.153594853992635,1.54794637473847,
2.39048813320202));
#285761=CARTESIAN_POINT('Ctrl Pts',(-0.184889446118301,1.5445928903599,
2.39276494020047));
#285762=CARTESIAN_POINT('Ctrl Pts',(-0.20400194867309,1.54218495892787,
2.39416945296401));
#285763=CARTESIAN_POINT('Ctrl Pts',(-0.343858009883367,1.52191966394549,
2.40455402296631));
#285764=CARTESIAN_POINT('Ctrl Pts',(-0.462149943665086,1.49026296231562,
2.41397497573814));
#285765=CARTESIAN_POINT('Ctrl Pts',(-0.646620728020674,1.416799962059,2.42936872344793));
#285766=CARTESIAN_POINT('Ctrl Pts',(-0.71556105113216,1.3832626028976,2.43528505050216));
#285767=CARTESIAN_POINT('Ctrl Pts',(-0.793277116467618,1.33808415915099,
2.44195952771564));
#285768=CARTESIAN_POINT('Ctrl Pts',(-0.80471084533521,1.33123938023058,
2.44294146355601));
#285769=CARTESIAN_POINT('Ctrl Pts',(-0.821784025259197,1.32071819122326,
2.44440610512512));
#285770=CARTESIAN_POINT('Ctrl Pts',(-0.82748952939745,1.31715094354143,
2.44489528191534));
#285771=CARTESIAN_POINT('Ctrl Pts',(-0.837810349862731,1.31060453215268,
2.44577941074295));
#285772=CARTESIAN_POINT('Ctrl Pts',(-0.842433162973482,1.30763786661403,
2.44617511979236));
#285773=CARTESIAN_POINT('Ctrl Pts',(-0.852891450730796,1.30084783457559,
2.44706971098408));
#285774=CARTESIAN_POINT('Ctrl Pts',(-0.858717021864208,1.29700963635568,
2.44756760826211));
#285775=CARTESIAN_POINT('Ctrl Pts',(-0.876650846225012,1.28502007324017,
2.44909973684198));
#285776=CARTESIAN_POINT('Ctrl Pts',(-0.888670764131352,1.27673709437543,
2.45012572940544));
#285777=CARTESIAN_POINT('Ctrl Pts',(-0.977694610603518,1.21352384745478,
2.45773244897799));
#285778=CARTESIAN_POINT('Ctrl Pts',(-1.04967218386716,1.15183346022872,
2.4639348035101));
#285779=CARTESIAN_POINT('Ctrl Pts',(-1.19008112911974,1.00732757317931,
2.47719636364454));
#285780=CARTESIAN_POINT('Ctrl Pts',(-1.25644942980204,0.923218634373557,
2.48423891499443));
#285781=CARTESIAN_POINT('Ctrl Pts',(-1.32364145012773,0.81725167992026,
2.49293631527651));
#285782=CARTESIAN_POINT('Ctrl Pts',(-1.33332957760313,0.8013483529362,2.49423658732745));
#285783=CARTESIAN_POINT('Ctrl Pts',(-1.3482675063486,0.77580623721678,2.49631933710385));
#285784=CARTESIAN_POINT('Ctrl Pts',(-1.35370501926065,0.766278863154737,
2.49709499990096));
#285785=CARTESIAN_POINT('Ctrl Pts',(-1.36380664970438,0.748136108161155,
2.49857024215581));
#285786=CARTESIAN_POINT('Ctrl Pts',(-1.36849105313386,0.739532584500603,
2.49926905194541));
#285787=CARTESIAN_POINT('Ctrl Pts',(-1.37897292911854,0.719840584258869,
2.5008670937725));
#285788=CARTESIAN_POINT('Ctrl Pts',(-1.38471842951952,0.70872537696288,
2.50176810696074));
#285789=CARTESIAN_POINT('Ctrl Pts',(-1.39943089255954,0.679400756655263,
2.50414319899922));
#285790=CARTESIAN_POINT('Ctrl Pts',(-1.40817635435763,0.661083575841854,
2.50562479456309));
#285791=CARTESIAN_POINT('Ctrl Pts',(-1.46139610257825,0.543765114623971,
2.51510572608007));
#285792=CARTESIAN_POINT('Ctrl Pts',(-1.49575663871181,0.440525656554097,
2.52344245407549));
#285793=CARTESIAN_POINT('Ctrl Pts',(-1.53269384923529,0.272816253003401,
2.53675796073022));
#285794=CARTESIAN_POINT('Ctrl Pts',(-1.54251754667993,0.210284498665895,
2.54166745801651));
#285795=CARTESIAN_POINT('Ctrl Pts',(-1.55054931629728,0.125864307528075,
2.54811066000505));
#285796=CARTESIAN_POINT('Ctrl Pts',(-1.55214488539939,0.104361688238147,
2.54973559341003));
#285797=CARTESIAN_POINT('Ctrl Pts',(-1.55411634820297,0.0673920468857548,
2.5524944570358));
#285798=CARTESIAN_POINT('Ctrl Pts',(-1.55470948410108,0.0519401563658736,
2.55363710890477));
#285799=CARTESIAN_POINT('Ctrl Pts',(-1.55523953592187,0.0293458324678964,
2.55529029927697));
#285800=CARTESIAN_POINT('Ctrl Pts',(-1.5553578205403,0.0222091742669988,
2.55580990630177));
#285801=CARTESIAN_POINT('Ctrl Pts',(-1.55547521635391,0.010093767225684,
2.55668736398283));
#285802=CARTESIAN_POINT('Ctrl Pts',(-1.55549955549121,0.00511551151385498,
2.557046573119));
#285803=CARTESIAN_POINT('Ctrl Pts',(-1.55550055500129,-0.00623305962615394,
2.55786233385983));
#285804=CARTESIAN_POINT('Ctrl Pts',(-1.55546198620683,-0.012603212781979,
2.55831803909298));
#285805=CARTESIAN_POINT('Ctrl Pts',(-1.55524298703307,-0.0305564130730573,
2.55959663681348));
#285806=CARTESIAN_POINT('Ctrl Pts',(-1.55497229327071,-0.0421382398781189,
2.56041475226322));
#285807=CARTESIAN_POINT('Ctrl Pts',(-1.55151865201902,-0.14208785809607,
2.56742536402354));
#285808=CARTESIAN_POINT('Ctrl Pts',(-1.54093473269642,-0.230052205931801,
2.57326556273727));
#285809=CARTESIAN_POINT('Ctrl Pts',(-1.50025345598643,-0.425708079098914,
2.58642749510838));
#285810=CARTESIAN_POINT('Ctrl Pts',(-1.46593299070998,-0.532000676093453,
2.59371962145271));
#285811=CARTESIAN_POINT('Ctrl Pts',(-1.41234607174449,-0.652123656267256,
2.60278982029931));
#285812=CARTESIAN_POINT('Ctrl Pts',(-1.40377590850392,-0.670372899502131,
2.60419084196302));
#285813=CARTESIAN_POINT('Ctrl Pts',(-1.38933344545103,-0.699634476207907,
2.60647811831808));
#285814=CARTESIAN_POINT('Ctrl Pts',(-1.38367888090329,-0.71075210965624,
2.60735688284124));
#285815=CARTESIAN_POINT('Ctrl Pts',(-1.37334759914768,-0.730474164112806,
2.60893391649939));
#285816=CARTESIAN_POINT('Ctrl Pts',(-1.36872211959065,-0.739104785436426,
2.609630353344));
#285817=CARTESIAN_POINT('Ctrl Pts',(-1.35873155424431,-0.757330612515072,
2.61111483964458));
#285818=CARTESIAN_POINT('Ctrl Pts',(-1.35334564165858,-0.766913721265497,
2.61190360352719));
#285819=CARTESIAN_POINT('Ctrl Pts',(-1.33850956452036,-0.792668408354602,
2.61404625489145));
#285820=CARTESIAN_POINT('Ctrl Pts',(-1.32886841967543,-0.808727226098879,
2.61540695696289));
#285821=CARTESIAN_POINT('Ctrl Pts',(-1.26290386521413,-0.914235969747585,
2.62451671066246));
#285822=CARTESIAN_POINT('Ctrl Pts',(-1.19788859299908,-0.997901965547171,
2.63259193483123));
#285823=CARTESIAN_POINT('Ctrl Pts',(-1.05876675300837,-1.14357546689536,
2.64819660719498));
#285824=CARTESIAN_POINT('Ctrl Pts',(-0.98636330789025,-1.20658296999755,
2.65566661867988));
#285825=CARTESIAN_POINT('Ctrl Pts',(-0.896877519961867,-1.27098395511725,
2.66386892084485));
#285826=CARTESIAN_POINT('Ctrl Pts',(-0.88501863454347,-1.2792699309887,
2.66493658310487));
#285827=CARTESIAN_POINT('Ctrl Pts',(-0.86729223401037,-1.29129111760527,
2.66650218660591));
#285828=CARTESIAN_POINT('Ctrl Pts',(-0.861512901900403,-1.29515408134049,
2.6670079367547));
#285829=CARTESIAN_POINT('Ctrl Pts',(-0.851121331254836,-1.3019995747806,
2.6679086862076));
#285830=CARTESIAN_POINT('Ctrl Pts',(-0.846518999023105,-1.30499655187472,
2.668304607402));
#285831=CARTESIAN_POINT('Ctrl Pts',(-0.836224045776677,-1.31162310505729,
2.66918356046608));
#285832=CARTESIAN_POINT('Ctrl Pts',(-0.830523578087623,-1.31524005992995,
2.66966577232733));
#285833=CARTESIAN_POINT('Ctrl Pts',(-0.813407597652296,-1.32594451933331,
2.67110088586049));
#285834=CARTESIAN_POINT('Ctrl Pts',(-0.801923252731891,-1.33292157194271,
2.67204698064825));
#285835=CARTESIAN_POINT('Ctrl Pts',(-0.715163636109373,-1.3841031007335,
2.67908063328668));
#285836=CARTESIAN_POINT('Ctrl Pts',(-0.636366223611446,-1.42205584958139,
2.6848387232741));
#285837=CARTESIAN_POINT('Ctrl Pts',(-0.452738611381837,-1.49215965588439,
2.69778134061773));
#285838=CARTESIAN_POINT('Ctrl Pts',(-0.346879587030923,-1.5202577847029,
2.70494050612235));
#285839=CARTESIAN_POINT('Ctrl Pts',(-0.218929636560006,-1.54014961246158,
2.71386820928867));
#285840=CARTESIAN_POINT('Ctrl Pts',(-0.198844780007939,-1.54287125297838,
2.71527649834339));
#285841=CARTESIAN_POINT('Ctrl Pts',(-0.166292301277465,-1.54663617706073,
2.71757326615754));
#285842=CARTESIAN_POINT('Ctrl Pts',(-0.153854817415822,-1.54792288974287,
2.71845415010745));
#285843=CARTESIAN_POINT('Ctrl Pts',(-0.131648827777653,-1.54994992901314,
2.72003352291209));
#285844=CARTESIAN_POINT('Ctrl Pts',(-0.121886182132722,-1.55074818938852,
2.72073015823583));
#285845=CARTESIAN_POINT('Ctrl Pts',(-0.101170665819472,-1.55224520970062,
2.72221351316046));
#285846=CARTESIAN_POINT('Ctrl Pts',(-0.090216684847592,-1.55292035629755,
2.72300093331751));
#285847=CARTESIAN_POINT('Ctrl Pts',(-0.0606365381526791,-1.55442950124089,
2.7251359829264));
#285848=CARTESIAN_POINT('Ctrl Pts',(-0.0420015573161472,-1.55504459009035,
2.7264903441582));
#285849=CARTESIAN_POINT('Ctrl Pts',(0.0832035800980689,-1.55692515335418,
2.73565654078751));
#285850=CARTESIAN_POINT('Ctrl Pts',(0.189629552180823,-1.54756939757743,
2.74380067338946));
#285851=CARTESIAN_POINT('Ctrl Pts',(0.387439694919848,-1.5094630316795,
2.75940790943861));
#285852=CARTESIAN_POINT('Ctrl Pts',(0.478805181620457,-1.4830161427106,
2.76680866590746));
#285853=CARTESIAN_POINT('Ctrl Pts',(0.58075284263949,-1.44309333117666,
2.7749553681401));
#285854=CARTESIAN_POINT('Ctrl Pts',(0.594235285658215,-1.43759406390524,
2.77603009763281));
#285855=CARTESIAN_POINT('Ctrl Pts',(0.614054524904569,-1.42918363373173,
2.7776039844008));
#285856=CARTESIAN_POINT('Ctrl Pts',(0.620451694047221,-1.4264180729525,
2.77811106574666));
#285857=CARTESIAN_POINT('Ctrl Pts',(0.631857142329225,-1.42139613435803,
2.77901319204208));
#285858=CARTESIAN_POINT('Ctrl Pts',(0.636872279363323,-1.4191561301606,
2.77940917197704));
#285859=CARTESIAN_POINT('Ctrl Pts',(0.648010399062634,-1.41411036719839,
2.78028705356704));
#285860=CARTESIAN_POINT('Ctrl Pts',(0.654127126092434,-1.41129136443887,
2.78076814714088));
#285861=CARTESIAN_POINT('Ctrl Pts',(0.672318521165484,-1.40276385484631,
2.78219648133684));
#285862=CARTESIAN_POINT('Ctrl Pts',(0.68433856242492,-1.39693929351222,
2.78313701008648));
#285863=CARTESIAN_POINT('Ctrl Pts',(0.767404857507903,-1.35535822626818,
2.78962435781514));
#285864=CARTESIAN_POINT('Ctrl Pts',(0.835702109495037,-1.31434836909438,
2.79489841887045));
#285865=CARTESIAN_POINT('Ctrl Pts',(0.99702095342509,-1.19980111192904,
2.80794189397891));
#285866=CARTESIAN_POINT('Ctrl Pts',(1.08533392765734,-1.12054457248056,
2.81565897009086));
#285867=CARTESIAN_POINT('Ctrl Pts',(1.17684048033486,-1.01735563020484,
2.82517657911611));
#285868=CARTESIAN_POINT('Ctrl Pts',(1.18959156249913,-1.00241600632822,
2.82654226451089));
#285869=CARTESIAN_POINT('Ctrl Pts',(1.20987641695494,-0.977717310240944,
2.82878334579099));
#285870=CARTESIAN_POINT('Ctrl Pts',(1.21758330809194,-0.968102760741714,
2.82965175090586));
#285871=CARTESIAN_POINT('Ctrl Pts',(1.23119906186796,-0.950696962391031,
2.83121743917183));
#285872=CARTESIAN_POINT('Ctrl Pts',(1.23715028524705,-0.942939556906977,
2.83191299375885));
#285873=CARTESIAN_POINT('Ctrl Pts',(1.24969262166492,-0.926267513191243,
2.83340344113505));
#285874=CARTESIAN_POINT('Ctrl Pts',(1.25626231689482,-0.917337524578084,
2.83419911884223));
#285875=CARTESIAN_POINT('Ctrl Pts',(1.2739308659039,-0.892775408800065,
2.83638097617753));
#285876=CARTESIAN_POINT('Ctrl Pts',(1.28483673297722,-0.877007577101856,
2.83777440425378));
#285877=CARTESIAN_POINT('Ctrl Pts',(1.35324907908477,-0.774080487737208,
2.84682827946445));
#285878=CARTESIAN_POINT('Ctrl Pts',(1.40213587293735,-0.681535629227672,
2.8548051814281));
#285879=CARTESIAN_POINT('Ctrl Pts',(1.47759110572958,-0.495561895356006,
2.87035177757698));
#285880=CARTESIAN_POINT('Ctrl Pts',(1.50543778992949,-0.40313434349261,
2.87786602469441));
#285881=CARTESIAN_POINT('Ctrl Pts',(1.52741839930122,-0.294586442780442,
2.88610490051894));
#285882=CARTESIAN_POINT('Ctrl Pts',(1.53008350546317,-0.280415129016086,
2.88716901798968));
#285883=CARTESIAN_POINT('Ctrl Pts',(1.53373938815161,-0.259368336220924,
2.88873046445844));
#285884=CARTESIAN_POINT('Ctrl Pts',(1.5348817094358,-0.252520469656944,
2.88923554488033));
#285885=CARTESIAN_POINT('Ctrl Pts',(1.53684552288602,-0.240242064227605,
2.89013560374212));
#285886=CARTESIAN_POINT('Ctrl Pts',(1.53768414161506,-0.234814595174138,
2.89053149747706));
#285887=CARTESIAN_POINT('Ctrl Pts',(1.53949076964472,-0.222697339799118,
2.89141099888998));
#285888=CARTESIAN_POINT('Ctrl Pts',(1.54044393938668,-0.216005576654915,
2.89189378049337));
#285889=CARTESIAN_POINT('Ctrl Pts',(1.54316703302176,-0.195952559333154,
2.89333235461984));
#285890=CARTESIAN_POINT('Ctrl Pts',(1.54480701410226,-0.182573871970163,
2.89428129150704));
#285891=CARTESIAN_POINT('Ctrl Pts',(1.55619948955721,-0.078445722021177,
2.90159492216196));
#285892=CARTESIAN_POINT('Ctrl Pts',(1.55812277664384,0.0129950524360213,
2.9075991633634));
#285893=CARTESIAN_POINT('Ctrl Pts',(1.54499353158286,0.208760255190567,
2.92051469334018));
#285894=CARTESIAN_POINT('Ctrl Pts',(1.52740396972473,0.312441301828331,
2.92740588520839));
#285895=CARTESIAN_POINT('Ctrl Pts',(1.49408736732152,0.43324382785128,2.93604388757908));
#285896=CARTESIAN_POINT('Ctrl Pts',(1.48827110621277,0.452820410129335,
2.93746262765813));
#285897=CARTESIAN_POINT('Ctrl Pts',(1.47826158420891,0.484231753921325,
2.93977303930185));
#285898=CARTESIAN_POINT('Ctrl Pts',(1.47430736753666,0.496140577344502,
2.940656964417));
#285899=CARTESIAN_POINT('Ctrl Pts',(1.46700908661723,0.517262631852202,
2.94223970377167));
#285900=CARTESIAN_POINT('Ctrl Pts',(1.46372116829506,0.526494657129671,
2.9429366339863));
#285901=CARTESIAN_POINT('Ctrl Pts',(1.45657552064951,0.545974256252145,
2.94441841501438));
#285902=CARTESIAN_POINT('Ctrl Pts',(1.45269639984995,0.556213353270231,
2.94520394678798));
#285903=CARTESIAN_POINT('Ctrl Pts',(1.44196425145482,0.583663001433325,
2.94732832183653));
#285904=CARTESIAN_POINT('Ctrl Pts',(1.43491153687599,0.600792999314781,
2.94867378131963));
#285905=CARTESIAN_POINT('Ctrl Pts',(1.41861542388964,0.638449013400624,
2.95167675658858));
#285906=CARTESIAN_POINT('Ctrl Pts',(1.40922911693774,0.658908236596135,
2.9533387911244));
#285907=CARTESIAN_POINT('Ctrl Pts',(1.37815767813013,0.722931045069323,
2.95863818788996));
#285908=CARTESIAN_POINT('Ctrl Pts',(1.35487234529474,0.765681400764424,
2.96232482689632));
#285909=CARTESIAN_POINT('Ctrl Pts',(1.29890812074448,0.857858324668858,
2.97059220564359));
#285910=CARTESIAN_POINT('Ctrl Pts',(1.2653307724911,0.906653576759187,2.97518796305924));
#285911=CARTESIAN_POINT('Ctrl Pts',(1.18235978619529,1.01361231563654,2.98567925259935));
#285912=CARTESIAN_POINT('Ctrl Pts',(1.13129763027273,1.07030509337,2.99155700391633));
#285913=CARTESIAN_POINT('Ctrl Pts',(1.06805415707966,1.13091572828657,2.99803860412343));
#285914=CARTESIAN_POINT('Ctrl Pts',(1.05974147901181,1.13870895527512,2.99887601786343));
#285915=CARTESIAN_POINT('Ctrl Pts',(1.04662901232294,1.15073406208911,3.00017348630406));
#285916=CARTESIAN_POINT('Ctrl Pts',(1.04188768452709,1.15502866970968,3.00063794667816));
#285917=CARTESIAN_POINT('Ctrl Pts',(1.03341311851624,1.16261012951901,3.00145961257004));
#285918=CARTESIAN_POINT('Ctrl Pts',(1.02969055468353,1.16590837955585,3.00181764508412));
#285919=CARTESIAN_POINT('Ctrl Pts',(1.02061760574342,1.17386980558304,3.00268336971854));
#285920=CARTESIAN_POINT('Ctrl Pts',(1.01525103571093,1.17851430086269,3.0031896939099));
#285921=CARTESIAN_POINT('Ctrl Pts',(0.998259434841465,1.19301746632251,
3.00477554750283));
#285922=CARTESIAN_POINT('Ctrl Pts',(0.986520752139677,1.20274246012717,
3.00584598639344));
#285923=CARTESIAN_POINT('Ctrl Pts',(0.922036760475447,1.25458526120429,
3.01160343496773));
#285924=CARTESIAN_POINT('Ctrl Pts',(0.866729441571061,1.29341341674157,
3.01610499621465));
#285925=CARTESIAN_POINT('Ctrl Pts',(0.700724577967221,1.39450961375287,
3.0289487991788));
#285926=CARTESIAN_POINT('Ctrl Pts',(0.58472926498728,1.44698325229681,3.03717895612942));
#285927=CARTESIAN_POINT('Ctrl Pts',(0.444616677790696,1.49073607025549,
3.0473039978929));
#285928=CARTESIAN_POINT('Ctrl Pts',(0.42546728813207,1.49631398651695,3.04869033409328));
#285929=CARTESIAN_POINT('Ctrl Pts',(0.394236965006558,1.50476293232934,
3.05095842104059));
#285930=CARTESIAN_POINT('Ctrl Pts',(0.382219221502569,1.50786031114583,
3.05183289105533));
#285931=CARTESIAN_POINT('Ctrl Pts',(0.360661518525709,1.51314218671221,
3.05340520323229));
#285932=CARTESIAN_POINT('Ctrl Pts',(0.351135471216502,1.51538110091543,
3.05410125611887));
#285933=CARTESIAN_POINT('Ctrl Pts',(0.33082778656826,1.5199522689229,3.05558812439613));
#285934=CARTESIAN_POINT('Ctrl Pts',(0.320041246530315,1.52226000179959,
3.0563796828771));
#285935=CARTESIAN_POINT('Ctrl Pts',(0.290700729305727,1.52821165035157,
3.05853816200943));
#285936=CARTESIAN_POINT('Ctrl Pts',(0.27210392994007,1.53163218662357,3.05991207103515));
#285937=CARTESIAN_POINT('Ctrl Pts',(0.152424391623346,1.55139666412117,
3.06879487980418));
#285938=CARTESIAN_POINT('Ctrl Pts',(0.0500174042206302,1.5580614854054,
3.07660765917065));
#285939=CARTESIAN_POINT('Ctrl Pts',(-0.151265261186869,1.55129228761786,
3.09220214510162));
#285940=CARTESIAN_POINT('Ctrl Pts',(-0.249711572484758,1.5385175650785,
3.09993692614429));
#285941=CARTESIAN_POINT('Ctrl Pts',(-0.36020133242299,1.51328752380114,
3.10836592528096));
#285942=CARTESIAN_POINT('Ctrl Pts',(-0.374077901651606,1.50991718033658,
3.10941953550798));
#285943=CARTESIAN_POINT('Ctrl Pts',(-0.39460370976266,1.50463151166356,
3.11096865103442));
#285944=CARTESIAN_POINT('Ctrl Pts',(-0.401289287039485,1.50286226469941,
3.11147173846072));
#285945=CARTESIAN_POINT('Ctrl Pts',(-0.413262071626968,1.49960823696858,
3.11236975085337));
#285946=CARTESIAN_POINT('Ctrl Pts',(-0.41855342979647,1.49813999125748,
3.11276557145872));
#285947=CARTESIAN_POINT('Ctrl Pts',(-0.43036432674885,1.49479524236072,
3.113646742671));
#285948=CARTESIAN_POINT('Ctrl Pts',(-0.436879472812004,1.49290408304393,
3.11413124888338));
#285949=CARTESIAN_POINT('Ctrl Pts',(-0.456420685281606,1.48709295071666,
3.11558032605132));
#285950=CARTESIAN_POINT('Ctrl Pts',(-0.469408332446109,1.48304454974816,
3.11653789236266));
#285951=CARTESIAN_POINT('Ctrl Pts',(-0.499638140100143,1.47318463524574,
3.11875742298126));
#285952=CARTESIAN_POINT('Ctrl Pts',(-0.516835054623095,1.46723986842436,
3.12001292420044));
#285953=CARTESIAN_POINT('Ctrl Pts',(-0.578441692784673,1.44472554956781,
3.12449832805364));
#285954=CARTESIAN_POINT('Ctrl Pts',(-0.622195490663908,1.42642916181906,
3.127660990113));
#285955=CARTESIAN_POINT('Ctrl Pts',(-0.768868037623708,1.35705995177762,
3.13839893840018));
#285956=CARTESIAN_POINT('Ctrl Pts',(-0.866923512173226,1.29661556168341,
3.14584365517639));
#285957=CARTESIAN_POINT('Ctrl Pts',(-0.982950057962604,1.20600076044267,
3.15587400533882));
#285958=CARTESIAN_POINT('Ctrl Pts',(-1.00783865995165,1.1852804045838,3.15810525264408));
#285959=CARTESIAN_POINT('Ctrl Pts',(-1.04143270502985,1.15548910081853,
3.16124265130202));
#285960=CARTESIAN_POINT('Ctrl Pts',(-1.05070319900776,1.14706578394168,
3.16212234648344));
#285961=CARTESIAN_POINT('Ctrl Pts',(-1.0665910842775,1.13227558941044,3.16365503861152));
#285962=CARTESIAN_POINT('Ctrl Pts',(-1.07325578841065,1.12596028239409,
3.16430583382692));
#285963=CARTESIAN_POINT('Ctrl Pts',(-1.08705242355571,1.11265314534313,
3.16566986609521));
#285964=CARTESIAN_POINT('Ctrl Pts',(-1.09417368295046,1.1056509107157,3.16638353736243));
#285965=CARTESIAN_POINT('Ctrl Pts',(-1.10133637441836,1.09847096658192,
3.1671113628377));
#285966=CARTESIAN_POINT('Ctrl Pts',(-1.1014458626608,1.09836118179211,3.16712249070733));
#285967=CARTESIAN_POINT('Ctrl Pts',(-1.10165197161736,1.09815445278218,
3.16714344316502));
#285968=CARTESIAN_POINT('Ctrl Pts',(-1.10174859596465,1.09805751216576,
3.16715326759318));
#285969=CARTESIAN_POINT('Ctrl Pts',(-1.10217388008621,1.09763072336411,
3.16719651723325));
#285970=CARTESIAN_POINT('Ctrl Pts',(-1.10250240423269,1.09730074067112,
3.16722994841665));
#285971=CARTESIAN_POINT('Ctrl Pts',(-1.10315555665418,1.09664409901889,
3.16729645740822));
#285972=CARTESIAN_POINT('Ctrl Pts',(-1.10348018813518,1.09631744329928,
3.16732953507058));
#285973=CARTESIAN_POINT('Ctrl Pts',(-1.10412692923241,1.09566609116397,
3.16739547572099));
#285974=CARTESIAN_POINT('Ctrl Pts',(-1.1044490408081,1.09534139675261,3.16742833861797));
#285975=CARTESIAN_POINT('Ctrl Pts',(-1.10509204237063,1.0946926673083,3.16749398163268));
#285976=CARTESIAN_POINT('Ctrl Pts',(-1.10541293315803,1.09436863312852,
3.16752676171061));
#285977=CARTESIAN_POINT('Ctrl Pts',(-1.11613713336564,1.0835298511363,3.16862297261422));
#285978=CARTESIAN_POINT('Ctrl Pts',(-1.12638973211028,1.07286773746764,
3.16969294893012));
#285979=CARTESIAN_POINT('Ctrl Pts',(-1.16653057742277,1.02991390597024,
3.17397206823615));
#285980=CARTESIAN_POINT('Ctrl Pts',(-1.19519221515717,0.996509461924799,
3.17723161271355));
#285981=CARTESIAN_POINT('Ctrl Pts',(-1.26996313341132,0.901493203385047,
3.18632775768287));
#285982=CARTESIAN_POINT('Ctrl Pts',(-1.31297533672047,0.837609561656838,
3.19226036085286));
#285983=CARTESIAN_POINT('Ctrl Pts',(-1.39412737780445,0.695366349155964,
3.20495741208171));
#285984=CARTESIAN_POINT('Ctrl Pts',(-1.43078035342767,0.616438087350189,
3.21170935005537));
#285985=CARTESIAN_POINT('Ctrl Pts',(-1.46573798987217,0.520971233778383,
3.21927935009162));
#285986=CARTESIAN_POINT('Ctrl Pts',(-1.47062420942662,0.507014159832948,
3.22037151192684));
#285987=CARTESIAN_POINT('Ctrl Pts',(-1.47756506522608,0.48624306196291,
3.22197331956063));
#285988=CARTESIAN_POINT('Ctrl Pts',(-1.47977300648383,0.479481690862227,
3.22249107366785));
#285989=CARTESIAN_POINT('Ctrl Pts',(-1.48360582688244,0.467465769476506,
3.22340442581184));
#285990=CARTESIAN_POINT('Ctrl Pts',(-1.48524930984756,0.462217466200462,
3.22380106321185));
#285991=CARTESIAN_POINT('Ctrl Pts',(-1.48880835674623,0.450636979885078,
3.22467118189785));
#285992=CARTESIAN_POINT('Ctrl Pts',(-1.49071139651586,0.444301189905672,
3.22514394494026));
#285993=CARTESIAN_POINT('Ctrl Pts',(-1.49616723767508,0.425707319864655,
3.22652230342076));
#285994=CARTESIAN_POINT('Ctrl Pts',(-1.49960977716647,0.413417064395333,
3.22742186735222));
#285995=CARTESIAN_POINT('Ctrl Pts',(-1.50721625996785,0.384914926079717,
3.22948454254925));
#285996=CARTESIAN_POINT('Ctrl Pts',(-1.51127066093205,0.368675190079421,
3.230642384677));
#285997=CARTESIAN_POINT('Ctrl Pts',(-1.54183408149476,0.237264552494566,
3.23989532945207));
#285998=CARTESIAN_POINT('Ctrl Pts',(-1.55540235308476,0.119474178713039,
3.24749806769915));
#285999=CARTESIAN_POINT('Ctrl Pts',(-1.55549947486934,0.00127815539530785,
3.25533825218605));
#286000=CARTESIAN_POINT('',(-1.55745492001379,-0.000856371120316864,4.65594377439631));
#286001=CARTESIAN_POINT('Ctrl Pts',(-1.55549947609198,0.00127666658565867,
3.25533835094186));
#286002=CARTESIAN_POINT('Ctrl Pts',(-1.55555636301431,-0.068034756513225,
3.25993592059349));
#286003=CARTESIAN_POINT('Ctrl Pts',(-1.5509806632431,-0.137266448596484,
3.26459545993076));
#286004=CARTESIAN_POINT('Ctrl Pts',(-1.54000197289467,-0.219452747316245,
3.27034228132855));
#286005=CARTESIAN_POINT('Ctrl Pts',(-1.53802239591289,-0.232922035318707,
3.27129093017571));
#286006=CARTESIAN_POINT('Ctrl Pts',(-1.5342860329217,-0.256215095950785,
3.27294431259784));
#286007=CARTESIAN_POINT('Ctrl Pts',(-1.53261100875688,-0.266051299250875,
3.2736464905484));
#286008=CARTESIAN_POINT('Ctrl Pts',(-1.52906086660576,-0.285751502078462,
3.27506123479516));
#286009=CARTESIAN_POINT('Ctrl Pts',(-1.527184642059,-0.295614808819637,
3.27577380436043));
#286010=CARTESIAN_POINT('Ctrl Pts',(-1.52342183017665,-0.314403218942805,
3.27713961400922));
#286011=CARTESIAN_POINT('Ctrl Pts',(-1.52155195041569,-0.323331273436458,
3.27779229414113));
#286012=CARTESIAN_POINT('Ctrl Pts',(-1.51648168317265,-0.346521575533898,
3.27949743458108));
#286013=CARTESIAN_POINT('Ctrl Pts',(-1.51315866393737,-0.360755773846104,
3.28055377093904));
#286014=CARTESIAN_POINT('Ctrl Pts',(-1.50067230704378,-0.411030004087195,
3.28432044354167));
#286015=CARTESIAN_POINT('Ctrl Pts',(-1.49041848385317,-0.446783336945632,
3.2870651047785));
#286016=CARTESIAN_POINT('Ctrl Pts',(-1.45422352076932,-0.557807889208187,
3.29580263104219));
#286017=CARTESIAN_POINT('Ctrl Pts',(-1.42378348872899,-0.631469236309211,
3.30192359216912));
#286018=CARTESIAN_POINT('Ctrl Pts',(-1.35044173655222,-0.776368094074657,
3.31450909850219));
#286019=CARTESIAN_POINT('Ctrl Pts',(-1.3071924930239,-0.847165847015035,
3.32095745088693));
#286020=CARTESIAN_POINT('Ctrl Pts',(-1.24595308124008,-0.93147063269499,
3.32878976067696));
#286021=CARTESIAN_POINT('Ctrl Pts',(-1.23304232537736,-0.948495314694816,
3.33037949802974));
#286022=CARTESIAN_POINT('Ctrl Pts',(-1.21466800451578,-0.971714908216085,
3.33255321819721));
#286023=CARTESIAN_POINT('Ctrl Pts',(-1.20950040489606,-0.978139561962613,
3.33315526586101));
#286024=CARTESIAN_POINT('Ctrl Pts',(-1.200701706323,-0.988902248617583,
3.33416441677587));
#286025=CARTESIAN_POINT('Ctrl Pts',(-1.19709763246799,-0.993262053784068,
3.33457337170336));
#286026=CARTESIAN_POINT('Ctrl Pts',(-1.19008433822079,-1.0016523257877,
3.33536056396761));
#286027=CARTESIAN_POINT('Ctrl Pts',(-1.18667829302194,-1.0056852116544,
3.33573903357952));
#286028=CARTESIAN_POINT('Ctrl Pts',(-1.17726103923134,-1.01672113648853,
3.33677522908943));
#286029=CARTESIAN_POINT('Ctrl Pts',(-1.1712078082803,-1.02368828493918,
3.33742997574959));
#286030=CARTESIAN_POINT('Ctrl Pts',(-1.14646344119339,-1.05166174111665,
3.3400631875505));
#286031=CARTESIAN_POINT('Ctrl Pts',(-1.12726506000858,-1.07221479757286,
3.34200802260382));
#286032=CARTESIAN_POINT('Ctrl Pts',(-1.03558854550464,-1.16517391154232,
3.35091688400592));
#286033=CARTESIAN_POINT('Ctrl Pts',(-0.956623215333674,-1.23083300241658,
3.35755332282966));
#286034=CARTESIAN_POINT('Ctrl Pts',(-0.826791936735691,-1.31869046926926,
3.36791364693219));
#286035=CARTESIAN_POINT('Ctrl Pts',(-0.780255727280477,-1.34674784641127,
3.37153026591221));
#286036=CARTESIAN_POINT('Ctrl Pts',(-0.701055197233776,-1.38901409910495,
3.37763249794857));
#286037=CARTESIAN_POINT('Ctrl Pts',(-0.669200171694033,-1.40463851742739,
3.38007317469693));
#286038=CARTESIAN_POINT('Ctrl Pts',(-0.624076741214118,-1.42488743515708,
3.38352849780757));
#286039=CARTESIAN_POINT('Ctrl Pts',(-0.611236276924471,-1.43044264934545,
3.38451149394211));
#286040=CARTESIAN_POINT('Ctrl Pts',(-0.58907611692635,-1.43967702308222,
3.38620846075533));
#286041=CARTESIAN_POINT('Ctrl Pts',(-0.579792439598855,-1.44344079226404,
3.38691952834639));
#286042=CARTESIAN_POINT('Ctrl Pts',(-0.560827180617548,-1.45091716856823,
3.38837278597361));
#286043=CARTESIAN_POINT('Ctrl Pts',(-0.551143553121849,-1.45462315765944,
3.38911515553482));
#286044=CARTESIAN_POINT('Ctrl Pts',(-0.526629839128992,-1.46372480176176,
3.39099567970757));
#286045=CARTESIAN_POINT('Ctrl Pts',(-0.511753661466734,-1.46899198045441,
3.39213802629635));
#286046=CARTESIAN_POINT('Ctrl Pts',(-0.453035621932517,-1.48878202011007,
3.39665307910348));
#286047=CARTESIAN_POINT('Ctrl Pts',(-0.408640205822372,-1.50157435847985,
3.40008095443692));
#286048=CARTESIAN_POINT('Ctrl Pts',(-0.255513450740731,-1.53840337355354,
3.41195667891545));
#286049=CARTESIAN_POINT('Ctrl Pts',(-0.144807330525522,-1.55273876693325,
3.42065880800892));
#286050=CARTESIAN_POINT('Ctrl Pts',(0.004132861190327,-1.55595081339322,
3.43214501955476));
#286051=CARTESIAN_POINT('Ctrl Pts',(0.0418235546820907,-1.55539422096193,
3.43502941324711));
#286052=CARTESIAN_POINT('Ctrl Pts',(0.10249371456765,-1.55229097424402,
3.4396036949247));
#286053=CARTESIAN_POINT('Ctrl Pts',(0.125500868627657,-1.55060049933973,
3.44132227232295));
#286054=CARTESIAN_POINT('Ctrl Pts',(0.156757604052148,-1.54760354399071,
3.44362797298079));
#286055=CARTESIAN_POINT('Ctrl Pts',(0.165045507128445,-1.54674162829495,
3.44423654443791));
#286056=CARTESIAN_POINT('Ctrl Pts',(0.178963991088941,-1.54518099998449,
3.44525341771928));
#286057=CARTESIAN_POINT('Ctrl Pts',(0.184598319631074,-1.54451801459293,
3.44566363465049));
#286058=CARTESIAN_POINT('Ctrl Pts',(0.196182702561097,-1.54309059385179,
3.44650397005745));
#286059=CARTESIAN_POINT('Ctrl Pts',(0.202132152454718,-1.54232254403329,
3.44693388769497));
#286060=CARTESIAN_POINT('Ctrl Pts',(0.217855738457863,-1.54020014619171,
3.44806607293528));
#286061=CARTESIAN_POINT('Ctrl Pts',(0.227621885920454,-1.53878715340594,
3.44876516564103));
#286062=CARTESIAN_POINT('Ctrl Pts',(0.271145959533851,-1.53206652598437,
3.45186502830363));
#286063=CARTESIAN_POINT('Ctrl Pts',(0.3047397487805,-1.52573984587856,3.45421536161804));
#286064=CARTESIAN_POINT('Ctrl Pts',(0.423769812313167,-1.4992339788108,
3.46247986473848));
#286065=CARTESIAN_POINT('Ctrl Pts',(0.50767681155227,-1.47293921695385,
3.46819518351669));
#286066=CARTESIAN_POINT('Ctrl Pts',(0.657267589050469,-1.41174791254404,
3.47885653038172));
#286067=CARTESIAN_POINT('Ctrl Pts',(0.723528001101439,-1.37896278804597,
3.48376618340053));
#286068=CARTESIAN_POINT('Ctrl Pts',(0.810393459367767,-1.32799303095066,
3.49067338773692));
#286069=CARTESIAN_POINT('Ctrl Pts',(0.83322345134701,-1.31378901710073,
3.49253566037138));
#286070=CARTESIAN_POINT('Ctrl Pts',(0.866197374562894,-1.29206856901142,
3.49530245564349));
#286071=CARTESIAN_POINT('Ctrl Pts',(0.876637011429837,-1.2850084094341,
3.49619013832473));
#286072=CARTESIAN_POINT('Ctrl Pts',(0.895045087005136,-1.27223060150572,
3.49777705307115));
#286073=CARTESIAN_POINT('Ctrl Pts',(0.903047502523863,-1.26656291250153,
3.4984743634031));
#286074=CARTESIAN_POINT('Ctrl Pts',(0.919845763184944,-1.25442546117433,
3.4999542773811));
#286075=CARTESIAN_POINT('Ctrl Pts',(0.928628107287691,-1.24793801640575,
3.50073753825502));
#286076=CARTESIAN_POINT('Ctrl Pts',(0.952009400812185,-1.23028296758673,
3.50284908880825));
#286077=CARTESIAN_POINT('Ctrl Pts',(0.96647950255674,-1.21894848002039,
3.50418385694387));
#286078=CARTESIAN_POINT('Ctrl Pts',(1.04910836862365,-1.15182866070994,
3.51197338114825));
#286079=CARTESIAN_POINT('Ctrl Pts',(1.11261984906035,-1.09060062878491,
3.51864824440964));
#286080=CARTESIAN_POINT('Ctrl Pts',(1.21422681537294,-0.974485543846351,
3.53055160158723));
#286081=CARTESIAN_POINT('Ctrl Pts',(1.25462195207191,-0.92189613788677,
3.53571338341064));
#286082=CARTESIAN_POINT('Ctrl Pts',(1.31181505121666,-0.836686860943733,
3.54361973557424));
#286083=CARTESIAN_POINT('Ctrl Pts',(1.33102451339317,-0.805777715987354,
3.54640173933781));
#286084=CARTESIAN_POINT('Ctrl Pts',(1.36034198325775,-0.754690032562884,
3.5508340548911));
#286085=CARTESIAN_POINT('Ctrl Pts',(1.37112573231021,-0.734916131178003,
3.5525110996419));
#286086=CARTESIAN_POINT('Ctrl Pts',(1.38527243511559,-0.707579484864783,
3.55477079903634));
#286087=CARTESIAN_POINT('Ctrl Pts',(1.38900955555442,-0.700214902430107,
3.55537385257168));
#286088=CARTESIAN_POINT('Ctrl Pts',(1.3952084484232,-0.687754068677631,
3.55638419238375));
#286089=CARTESIAN_POINT('Ctrl Pts',(1.39770134830342,-0.682673581395842,
3.55679334010321));
#286090=CARTESIAN_POINT('Ctrl Pts',(1.40279022515602,-0.672157802693309,
3.55763432365127));
#286091=CARTESIAN_POINT('Ctrl Pts',(1.40538244155005,-0.666720873983832,
3.55806593501159));
#286092=CARTESIAN_POINT('Ctrl Pts',(1.412185309762,-0.6522365225579,3.55920766714626));
#286093=CARTESIAN_POINT('Ctrl Pts',(1.41634067935657,-0.643163217408742,
3.55991451678114));
#286094=CARTESIAN_POINT('Ctrl Pts',(1.43485049291289,-0.601697263365362,
3.56310988445278));
#286095=CARTESIAN_POINT('Ctrl Pts',(1.44818417662808,-0.568857264653831,
3.56554405044368));
#286096=CARTESIAN_POINT('Ctrl Pts',(1.49425029679426,-0.443248864300203,
3.57459958442957));
#286097=CARTESIAN_POINT('Ctrl Pts',(1.5192831974232,-0.347900607583221,
3.58097242439141));
#286098=CARTESIAN_POINT('Ctrl Pts',(1.54342790764834,-0.20012347509704,
3.59088301926671));
#286099=CARTESIAN_POINT('Ctrl Pts',(1.54919415116144,-0.149050211108787,
3.59431165320413));
#286100=CARTESIAN_POINT('Ctrl Pts',(1.55388797615725,-0.0745339383343615,
3.59939324396655));
#286101=CARTESIAN_POINT('Ctrl Pts',(1.5548300263918,-0.0512508509370472,
3.60099195633002));
#286102=CARTESIAN_POINT('Ctrl Pts',(1.55559076982541,-0.008929635308371,
3.60392421222815));
#286103=CARTESIAN_POINT('Ctrl Pts',(1.55558358735467,0.0101009605514342,
3.60525240250771));
#286104=CARTESIAN_POINT('Ctrl Pts',(1.55502026716753,0.0401803687480065,
3.60736939480889));
#286105=CARTESIAN_POINT('Ctrl Pts',(1.55469539221525,0.0512320155038053,
3.60815098067865));
#286106=CARTESIAN_POINT('Ctrl Pts',(1.55386110397078,0.072052751544113,
3.60963101894076));
#286107=CARTESIAN_POINT('Ctrl Pts',(1.55337729501805,0.0818223730589093,
3.61032863566028));
#286108=CARTESIAN_POINT('Ctrl Pts',(1.55207311622877,0.10393402554231,3.61191500533818));
#286109=CARTESIAN_POINT('Ctrl Pts',(1.55119761624159,0.116272003274297,
3.61280544138234));
#286110=CARTESIAN_POINT('Ctrl Pts',(1.54853805511277,0.148331510439461,
3.6151334898225));
#286111=CARTESIAN_POINT('Ctrl Pts',(1.54652442686002,0.168031173773354,
3.61657814104813));
#286112=CARTESIAN_POINT('Ctrl Pts',(1.53007923902965,0.303329315987584,
3.62660155423526));
#286113=CARTESIAN_POINT('Ctrl Pts',(1.50307908287751,0.417006390805818,
3.6355763257446));
#286114=CARTESIAN_POINT('Ctrl Pts',(1.43600468167521,0.603442703668241,
3.65094057835458));
#286115=CARTESIAN_POINT('Ctrl Pts',(1.40233782785666,0.678014777586669,
3.65726679036765));
#286116=CARTESIAN_POINT('Ctrl Pts',(1.35671870508305,0.760961646743699,
3.66429079966784));
#286117=CARTESIAN_POINT('Ctrl Pts',(1.3503300756,0.772241535201837,3.66524552776955));
#286118=CARTESIAN_POINT('Ctrl Pts',(1.34044864771552,0.789190707527497,
3.66667793867374));
#286119=CARTESIAN_POINT('Ctrl Pts',(1.33705943048695,0.794919262412172,
3.66716169082696));
#286120=CARTESIAN_POINT('Ctrl Pts',(1.33080429584923,0.805338679960141,
3.66804062519395));
#286121=CARTESIAN_POINT('Ctrl Pts',(1.32795022312521,0.81003621538047,3.66843650954346));
#286122=CARTESIAN_POINT('Ctrl Pts',(1.32137249300323,0.820734336989193,
3.66933730214877));
#286123=CARTESIAN_POINT('Ctrl Pts',(1.31763280997389,0.826724803318949,
3.66984116374378));
#286124=CARTESIAN_POINT('Ctrl Pts',(1.30579495149924,0.845403066585856,
3.67141119406506));
#286125=CARTESIAN_POINT('Ctrl Pts',(1.2975530429848,0.857999385199282,3.6724685275511));
#286126=CARTESIAN_POINT('Ctrl Pts',(1.24269319555203,0.939244057838746,
3.67929249444921));
#286127=CARTESIAN_POINT('Ctrl Pts',(1.19082224234533,1.00419713148771,3.68477259516927));
#286128=CARTESIAN_POINT('Ctrl Pts',(1.07953499067042,1.12272804470259,3.69548070074411));
#286129=CARTESIAN_POINT('Ctrl Pts',(1.02069138965888,1.17647871004343,3.70069560540467));
#286130=CARTESIAN_POINT('Ctrl Pts',(0.922573193418669,1.25318014357146,
3.70909199998385));
#286131=CARTESIAN_POINT('Ctrl Pts',(0.885969910606948,1.2793195337588,3.71216547836994));
#286132=CARTESIAN_POINT('Ctrl Pts',(0.835539459915452,1.3121301025144,3.71635906223002));
#286133=CARTESIAN_POINT('Ctrl Pts',(0.822669699609553,1.32023714978015,
3.71742576513364));
#286134=CARTESIAN_POINT('Ctrl Pts',(0.800930067702131,1.33349029856865,
3.71922308037209));
#286135=CARTESIAN_POINT('Ctrl Pts',(0.792124272593447,1.33873988413531,
3.71994986578926));
#286136=CARTESIAN_POINT('Ctrl Pts',(0.774640299040049,1.34893008217025,
3.72139085839308));
#286137=CARTESIAN_POINT('Ctrl Pts',(0.765965153526019,1.35387493310429,
3.7221048682509));
#286138=CARTESIAN_POINT('Ctrl Pts',(0.744697785910184,1.36572754566991,
3.72385326496467));
#286139=CARTESIAN_POINT('Ctrl Pts',(0.732056561704041,1.37254496687758,
3.72489080527215));
#286140=CARTESIAN_POINT('Ctrl Pts',(0.68799732726288,1.39552433507698,3.72850230566189));
#286141=CARTESIAN_POINT('Ctrl Pts',(0.656126503702749,1.41078918793012,
3.73110687668809));
#286142=CARTESIAN_POINT('Ctrl Pts',(0.51104245775799,1.4742989105341,3.7429366879226));
#286143=CARTESIAN_POINT('Ctrl Pts',(0.392873733313165,1.51008711481171,
3.75254761875624));
#286144=CARTESIAN_POINT('Ctrl Pts',(0.233165331413972,1.53842448422345,
3.76506406446787));
#286145=CARTESIAN_POINT('Ctrl Pts',(0.194332170346677,1.54381066942751,
3.76806725649022));
#286146=CARTESIAN_POINT('Ctrl Pts',(0.131768949098832,1.5500897167826,3.77280518281364));
#286147=CARTESIAN_POINT('Ctrl Pts',(0.108150609741525,1.55191648905868,
3.77457093955468));
#286148=CARTESIAN_POINT('Ctrl Pts',(0.0760961965679511,1.55366033000777,
3.77692872170522));
#286149=CARTESIAN_POINT('Ctrl Pts',(0.067690391582637,1.55404925006199,
3.77754341612601));
#286150=CARTESIAN_POINT('Ctrl Pts',(0.0535968243735233,1.55458675989007,
3.7785675607031));
#286151=CARTESIAN_POINT('Ctrl Pts',(0.0479107405784851,1.55477238805508,
3.77897898570384));
#286152=CARTESIAN_POINT('Ctrl Pts',(0.0362529875301706,1.55508895085637,
3.7798187137457));
#286153=CARTESIAN_POINT('Ctrl Pts',(0.0302813823038815,1.5552166940008,
3.78024684141266));
#286154=CARTESIAN_POINT('Ctrl Pts',(0.0145610975131198,1.55546239759026,
3.78136893310438));
#286155=CARTESIAN_POINT('Ctrl Pts',(0.00481159307827026,1.55552311372443,
3.7820598227982));
#286156=CARTESIAN_POINT('Ctrl Pts',(-0.0378791804796244,1.5553875848365,
3.78506565517926));
#286157=CARTESIAN_POINT('Ctrl Pts',(-0.0708115042965037,1.5542366239092,
3.78733384626596));
#286158=CARTESIAN_POINT('Ctrl Pts',(-0.192146242715132,1.54613076872397,
3.79558602115116));
#286159=CARTESIAN_POINT('Ctrl Pts',(-0.279946816427306,1.53266851477264,
3.80135920426103));
#286160=CARTESIAN_POINT('Ctrl Pts',(-0.438421594734923,1.49428903064163,
3.81211379406688));
#286161=CARTESIAN_POINT('Ctrl Pts',(-0.509359238614342,1.47161972996556,
3.81705812668869));
#286162=CARTESIAN_POINT('Ctrl Pts',(-0.603373620719994,1.433961071814,3.82400366610278));
#286163=CARTESIAN_POINT('Ctrl Pts',(-0.628083494394794,1.4233113002842,
3.82586723775084));
#286164=CARTESIAN_POINT('Ctrl Pts',(-0.663947013090571,1.40673861449331,
3.82863559706412));
#286165=CARTESIAN_POINT('Ctrl Pts',(-0.675325429118334,1.40131178324793,
3.82952351672298));
#286166=CARTESIAN_POINT('Ctrl Pts',(-0.695435761739544,1.39141852806241,
3.83111069536805));
#286167=CARTESIAN_POINT('Ctrl Pts',(-0.70419386320616,1.38700663802407,
3.8318080302416));
#286168=CARTESIAN_POINT('Ctrl Pts',(-0.722612125356986,1.37750903461496,
3.83328782927408));
#286169=CARTESIAN_POINT('Ctrl Pts',(-0.732261593166479,1.37240386624409,
3.83407094918143));
#286170=CARTESIAN_POINT('Ctrl Pts',(-0.758003556853467,1.35843599722655,
3.83618170406055));
#286171=CARTESIAN_POINT('Ctrl Pts',(-0.773993651662779,1.349389315307,3.83751580898132));
#286172=CARTESIAN_POINT('Ctrl Pts',(-0.867912742242529,1.29403433782016,
3.84549280420195));
#286173=CARTESIAN_POINT('Ctrl Pts',(-0.941819358241475,1.24127688537395,
3.85236999399862));
#286174=CARTESIAN_POINT('Ctrl Pts',(-1.06046185601247,1.13986230438382,
3.86442027611628));
#286175=CARTESIAN_POINT('Ctrl Pts',(-1.10748649053048,1.09422989997088,
3.86952048497875));
#286176=CARTESIAN_POINT('Ctrl Pts',(-1.17519305250935,1.01967832718774,
3.87727363263458));
#286177=CARTESIAN_POINT('Ctrl Pts',(-1.19799771081896,0.992786187595589,
3.8799667157724));
#286178=CARTESIAN_POINT('Ctrl Pts',(-1.22922439433509,0.953317847773736,
3.88375158797986));
#286179=CARTESIAN_POINT('Ctrl Pts',(-1.23840652782861,0.941359039846569,
3.88487746700926));
#286180=CARTESIAN_POINT('Ctrl Pts',(-1.25444861533644,0.919824759463701,
3.88686537699504));
#286181=CARTESIAN_POINT('Ctrl Pts',(-1.2613763252139,0.910301436390494,
3.88773113941705));
#286182=CARTESIAN_POINT('Ctrl Pts',(-1.27190747065873,0.895473467697975,
3.88905754314952));
#286183=CARTESIAN_POINT('Ctrl Pts',(-1.2755871992015,0.89022393051287,3.88952301757761));
#286184=CARTESIAN_POINT('Ctrl Pts',(-1.28237846404818,0.880406874625131,
3.8903856460625));
#286185=CARTESIAN_POINT('Ctrl Pts',(-1.28549814657052,0.875845480949425,
3.89078331274325));
#286186=CARTESIAN_POINT('Ctrl Pts',(-1.29267178610846,0.865235756789333,
3.89170115675782));
#286187=CARTESIAN_POINT('Ctrl Pts',(-1.296707673361,0.859175463389674,3.89222013882502));
#286188=CARTESIAN_POINT('Ctrl Pts',(-1.30986283085658,0.839117804373722,
3.89392125255312));
#286189=CARTESIAN_POINT('Ctrl Pts',(-1.31879955375557,0.825001285624095,
3.89509216559827));
#286190=CARTESIAN_POINT('Ctrl Pts',(-1.3889888555903,0.710073554214989,
3.90443856161685));
#286191=CARTESIAN_POINT('Ctrl Pts',(-1.43882834576127,0.602723390326337,
3.9120491754229));
#286192=CARTESIAN_POINT('Ctrl Pts',(-1.49322458637397,0.439115322474908,
3.92344314042068));
#286193=CARTESIAN_POINT('Ctrl Pts',(-1.50767126371583,0.386611679851463,
3.92706709070472));
#286194=CARTESIAN_POINT('Ctrl Pts',(-1.52695175419809,0.298764894657836,
3.93318024184384));
#286195=CARTESIAN_POINT('Ctrl Pts',(-1.53337567603653,0.263819700083939,
3.93562428435745));
#286196=CARTESIAN_POINT('Ctrl Pts',(-1.54065543975724,0.214841804074365,
3.93908357142496));
#286197=CARTESIAN_POINT('Ctrl Pts',(-1.54252631174179,0.200969499884393,
3.94006706569299));
#286198=CARTESIAN_POINT('Ctrl Pts',(-1.54541459944443,0.177128044713284,
3.94176462251039));
#286199=CARTESIAN_POINT('Ctrl Pts',(-1.54652338701966,0.167170671057837,
3.94247577667004));
#286200=CARTESIAN_POINT('Ctrl Pts',(-1.54846004680897,0.148105887376254,
3.94384185183636));
#286201=CARTESIAN_POINT('Ctrl Pts',(-1.5493039488103,0.139000496565293,
3.9444962381434));
#286202=CARTESIAN_POINT('Ctrl Pts',(-1.55110068309366,0.117558550688944,
3.94604205657141));
#286203=CARTESIAN_POINT('Ctrl Pts',(-1.55198668479284,0.10521718357475,
3.94693554192459));
#286204=CARTESIAN_POINT('Ctrl Pts',(-1.55459300703015,0.0616397275709051,
3.95010443167856));
#286205=CARTESIAN_POINT('Ctrl Pts',(-1.55551809585118,0.0303655654496407,
3.95240415978236));
#286206=CARTESIAN_POINT('Ctrl Pts',(-1.55547231161344,-0.0476181484890411,
3.95820590104762));
#286207=CARTESIAN_POINT('Ctrl Pts',(-1.55334140971594,-0.0942939081123456,
3.96173918062137));
#286208=CARTESIAN_POINT('Ctrl Pts',(-1.54073147060111,-0.233032009695838,
3.97240384497363));
#286209=CARTESIAN_POINT('Ctrl Pts',(-1.52412881540005,-0.32432620919854,
3.97964783186824));
#286210=CARTESIAN_POINT('Ctrl Pts',(-1.4869309447167,-0.459187395178376,
3.99039505726241));
#286211=CARTESIAN_POINT('Ctrl Pts',(-1.47228260805344,-0.504184070953742,
3.99398587024141));
#286212=CARTESIAN_POINT('Ctrl Pts',(-1.45179123062934,-0.558569120201987,
3.99827969010788));
#286213=CARTESIAN_POINT('Ctrl Pts',(-1.44787199215751,-0.568650992428621,
3.99907364317118));
#286214=CARTESIAN_POINT('Ctrl Pts',(-1.44153915635084,-0.584451553349586,
4.00031384539995));
#286215=CARTESIAN_POINT('Ctrl Pts',(-1.43919604853425,-0.590197843946866,
4.00076401621179));
#286216=CARTESIAN_POINT('Ctrl Pts',(-1.43468118832606,-0.601083407594687,
4.00161495703086));
#286217=CARTESIAN_POINT('Ctrl Pts',(-1.43251616607369,-0.606225049022795,
4.00201607337361));
#286218=CARTESIAN_POINT('Ctrl Pts',(-1.42725963287987,-0.618523207418431,
4.00297374024622));
#286219=CARTESIAN_POINT('Ctrl Pts',(-1.42414190776367,-0.625668323590043,
4.00352871988585));
#286220=CARTESIAN_POINT('Ctrl Pts',(-1.41309686450117,-0.650470680257412,
4.00545127401956));
#286221=CARTESIAN_POINT('Ctrl Pts',(-1.40489343614958,-0.668004024275859,
4.00680343264835));
#286222=CARTESIAN_POINT('Ctrl Pts',(-1.38345455373738,-0.71168265731973,
4.01016573946192));
#286223=CARTESIAN_POINT('Ctrl Pts',(-1.36980329919845,-0.737616328855921,
4.01215644565738));
#286224=CARTESIAN_POINT('Ctrl Pts',(-1.29513009721513,-0.870242934748685,
4.02238746669098));
#286225=CARTESIAN_POINT('Ctrl Pts',(-1.22235378308397,-0.969813704185752,
4.03027642134697));
#286226=CARTESIAN_POINT('Ctrl Pts',(-1.10615650274413,-1.09465400701222,
4.04174466215157));
#286227=CARTESIAN_POINT('Ctrl Pts',(-1.07211847421113,-1.12801190828714,
4.04499321356094));
#286228=CARTESIAN_POINT('Ctrl Pts',(-1.02472604408822,-1.17037202627195,
4.04941813880094));
#286229=CARTESIAN_POINT('Ctrl Pts',(-1.01268380604388,-1.18080719063618,
4.05053449303518));
#286230=CARTESIAN_POINT('Ctrl Pts',(-0.992520155394636,-1.19774461326445,
4.05239209867542));
#286231=CARTESIAN_POINT('Ctrl Pts',(-0.984489831481499,-1.20435384321748,
4.05312894092772));
#286232=CARTESIAN_POINT('Ctrl Pts',(-0.968611105441615,-1.21715764586873,
4.05458055688707));
#286233=CARTESIAN_POINT('Ctrl Pts',(-0.960768049935251,-1.22335806455184,
4.05529504774315));
#286234=CARTESIAN_POINT('Ctrl Pts',(-0.941895262668087,-1.23798473778365,
4.05700872623285));
#286235=CARTESIAN_POINT('Ctrl Pts',(-0.930811624898668,-1.24633967784649,
4.05801065270189));
#286236=CARTESIAN_POINT('Ctrl Pts',(-0.891619971065352,-1.27506830212165,
4.06153897143121));
#286237=CARTESIAN_POINT('Ctrl Pts',(-0.862944986432265,-1.29464703513419,
4.06409516576382));
#286238=CARTESIAN_POINT('Ctrl Pts',(-0.789237489385882,-1.34143603405404,
4.07060808817145));
#286239=CARTESIAN_POINT('Ctrl Pts',(-0.743437111667417,-1.3673502593512,
4.07460461377696));
#286240=CARTESIAN_POINT('Ctrl Pts',(-0.606938331285853,-1.43569481976947,
4.086339297418));
#286241=CARTESIAN_POINT('Ctrl Pts',(-0.513348007765128,-1.471756596708,
4.09418535212595));
#286242=CARTESIAN_POINT('Ctrl Pts',(-0.385807390659938,-1.50724164016124,
4.10425171739215));
#286243=CARTESIAN_POINT('Ctrl Pts',(-0.354406796487647,-1.51493263491683,
4.10668027535148));
#286244=CARTESIAN_POINT('Ctrl Pts',(-0.313310687500327,-1.5236503866108,
4.1097760943613));
#286245=CARTESIAN_POINT('Ctrl Pts',(-0.303815677927547,-1.52557206783121,
4.11048568510528));
#286246=CARTESIAN_POINT('Ctrl Pts',(-0.288451463368745,-1.52853247109323,
4.11162408486959));
#286247=CARTESIAN_POINT('Ctrl Pts',(-0.282593345493416,-1.52962634856159,
4.11205584242167));
#286248=CARTESIAN_POINT('Ctrl Pts',(-0.271122003646222,-1.53170022346064,
4.11289663437999));
#286249=CARTESIAN_POINT('Ctrl Pts',(-0.265509466965103,-1.53268308531037,
4.11330580794468));
#286250=CARTESIAN_POINT('Ctrl Pts',(-0.251551126431596,-1.53504848181344,
4.11431824254814));
#286251=CARTESIAN_POINT('Ctrl Pts',(-0.24319903622933,-1.5363938453776,
4.11491945637877));
#286252=CARTESIAN_POINT('Ctrl Pts',(-0.21108226003102,-1.54129878239369,
4.1172152163504));
#286253=CARTESIAN_POINT('Ctrl Pts',(-0.18724582537996,-1.54437586755347,
4.11888526746431));
#286254=CARTESIAN_POINT('Ctrl Pts',(-0.123523976250556,-1.55110462430929,
4.12328307603711));
#286255=CARTESIAN_POINT('Ctrl Pts',(-0.0835514152619075,-1.55377068897858,
4.12597268762222));
#286256=CARTESIAN_POINT('Ctrl Pts',(0.0867945690688311,-1.55853828223923,
4.13730572784092));
#286257=CARTESIAN_POINT('Ctrl Pts',(0.217040533817466,-1.54579031712021,
4.1456981263094));
#286258=CARTESIAN_POINT('Ctrl Pts',(0.372688360659897,-1.51047633387656,
4.15660861019962));
#286259=CARTESIAN_POINT('Ctrl Pts',(0.401016193033821,-1.50320364404451,
4.1586288487825));
#286260=CARTESIAN_POINT('Ctrl Pts',(0.44066172065978,-1.49182494396618,
4.16151431790095));
#286261=CARTESIAN_POINT('Ctrl Pts',(0.452163641438075,-1.48837913268049,
4.16235842387365));
#286262=CARTESIAN_POINT('Ctrl Pts',(0.473135331305632,-1.4818307895587,
4.16391094319124));
#286263=CARTESIAN_POINT('Ctrl Pts',(0.482617461309397,-1.47876972793605,
4.16461797554794));
#286264=CARTESIAN_POINT('Ctrl Pts',(0.501821237273909,-1.47236590919811,
4.16606058684343));
#286265=CARTESIAN_POINT('Ctrl Pts',(0.511540444756746,-1.46901745692718,
4.16679632310891));
#286266=CARTESIAN_POINT('Ctrl Pts',(0.535686612504368,-1.46042996291988,
4.16863860241251));
#286267=CARTESIAN_POINT('Ctrl Pts',(0.550070273671818,-1.45507336105971,
4.16974899183166));
#286268=CARTESIAN_POINT('Ctrl Pts',(0.607420527841876,-1.43274375911232,
4.17423007916018));
#286269=CARTESIAN_POINT('Ctrl Pts',(0.649696643971826,-1.4140749054633,
4.17765648196432));
#286270=CARTESIAN_POINT('Ctrl Pts',(0.765968103723009,-1.35641488122914,
4.18743699152699));
#286271=CARTESIAN_POINT('Ctrl Pts',(0.837737361423566,-1.31330187714632,
4.19390679510054));
#286272=CARTESIAN_POINT('Ctrl Pts',(0.968460980688698,-1.21968235243341,
4.20637475262519));
#286273=CARTESIAN_POINT('Ctrl Pts',(1.02780604910925,-1.17011060104426,
4.21235210903685));
#286274=CARTESIAN_POINT('Ctrl Pts',(1.09307680214227,-1.10677534448577,
4.21912667166947));
#286275=CARTESIAN_POINT('Ctrl Pts',(1.10279858796273,-1.09708881425005,
4.22014128701344));
#286276=CARTESIAN_POINT('Ctrl Pts',(1.1172146170892,-1.08233976404249,4.22165260112901));
#286277=CARTESIAN_POINT('Ctrl Pts',(1.12200513677592,-1.07737288961849,
4.2221559742804));
#286278=CARTESIAN_POINT('Ctrl Pts',(1.13061904688261,-1.06832210152479,
4.22306293666984));
#286279=CARTESIAN_POINT('Ctrl Pts',(1.13445375662044,-1.06424913435824,
4.22346736411819));
#286280=CARTESIAN_POINT('Ctrl Pts',(1.14237104355563,-1.05574851009407,
4.22430361062023));
#286281=CARTESIAN_POINT('Ctrl Pts',(1.14645000402595,-1.05131770140907,
4.22473516563412));
#286282=CARTESIAN_POINT('Ctrl Pts',(1.1572166626495,-1.03948513793583,4.22587658019079));
#286283=CARTESIAN_POINT('Ctrl Pts',(1.16385920863137,-1.03204239861211,
4.22658317181343));
#286284=CARTESIAN_POINT('Ctrl Pts',(1.19636563296458,-0.994907060185455,
4.23005604184625));
#286285=CARTESIAN_POINT('Ctrl Pts',(1.22116957323579,-0.964300927551207,
4.23275401298611));
#286286=CARTESIAN_POINT('Ctrl Pts',(1.30195294417028,-0.856496563878149,
4.24184214171614));
#286287=CARTESIAN_POINT('Ctrl Pts',(1.35198784658911,-0.775112208608297,
4.24802346935023));
#286288=CARTESIAN_POINT('Ctrl Pts',(1.42777754541445,-0.621889939401246,
4.25934114650452));
#286289=CARTESIAN_POINT('Ctrl Pts',(1.45630764139306,-0.551780416484015,
4.26441171813131));
#286290=CARTESIAN_POINT('Ctrl Pts',(1.48519418118801,-0.462713944126869,
4.27090767291552));
#286291=CARTESIAN_POINT('Ctrl Pts',(1.49046244341471,-0.445452138387839,
4.27216870564984));
#286292=CARTESIAN_POINT('Ctrl Pts',(1.4984145121989,-0.417674362722119,
4.27420332569781));
#286293=CARTESIAN_POINT('Ctrl Pts',(1.50129077436602,-0.407214837291524,
4.27497064562625));
#286294=CARTESIAN_POINT('Ctrl Pts',(1.50656243274258,-0.38722907859397,
4.27643953320159));
#286295=CARTESIAN_POINT('Ctrl Pts',(1.50897746215083,-0.377708530013534,
4.27714042670784));
#286296=CARTESIAN_POINT('Ctrl Pts',(1.5143165043891,-0.355792038500418,
4.27875689460406));
#286297=CARTESIAN_POINT('Ctrl Pts',(1.51717872458511,-0.343381930037367,
4.27967440354252));
#286298=CARTESIAN_POINT('Ctrl Pts',(1.52576696915168,-0.303939028265735,
4.28259821991962));
#286299=CARTESIAN_POINT('Ctrl Pts',(1.53092493928949,-0.276789499428705,
4.28462228312947));
#286300=CARTESIAN_POINT('Ctrl Pts',(1.54846620686007,-0.168853212719599,
4.29271972697537));
#286301=CARTESIAN_POINT('Ctrl Pts',(1.55519629308363,-0.0872919911474576,
4.29895896746634));
#286302=CARTESIAN_POINT('Ctrl Pts',(1.55586346478858,0.098326730918669,
4.31331337322562));
#286303=CARTESIAN_POINT('Ctrl Pts',(1.54582262077034,0.202026372092642,
4.32144838887056));
#286304=CARTESIAN_POINT('Ctrl Pts',(1.52252841199517,0.318937057322911,
4.330329074781));
#286305=CARTESIAN_POINT('Ctrl Pts',(1.51932265387485,0.333874724630308,
4.33145775846546));
#286306=CARTESIAN_POINT('Ctrl Pts',(1.51430454115261,0.355685905525536,
4.3330946850782));
#286307=CARTESIAN_POINT('Ctrl Pts',(1.51266444930041,0.362597539780806,
4.33361175561433));
#286308=CARTESIAN_POINT('Ctrl Pts',(1.50967078006561,0.374839465202833,
4.33452437947045));
#286309=CARTESIAN_POINT('Ctrl Pts',(1.50833621821043,0.380174098199845,
4.33492096549748));
#286310=CARTESIAN_POINT('Ctrl Pts',(1.50533208384289,0.391917623420193,
4.33579154021094));
#286311=CARTESIAN_POINT('Ctrl Pts',(1.50364984899622,0.398323037392287,
4.3362648051862));
#286312=CARTESIAN_POINT('Ctrl Pts',(1.49859695868434,0.417074556115698,
4.3376461494757));
#286313=CARTESIAN_POINT('Ctrl Pts',(1.49511469013908,0.42939040640479,4.33854815762039));
#286314=CARTESIAN_POINT('Ctrl Pts',(1.46968026487253,0.515281698378234,
4.34481117080252));
#286315=CARTESIAN_POINT('Ctrl Pts',(1.44245579916602,0.587196603964978,
4.3499152653411));
#286316=CARTESIAN_POINT('Ctrl Pts',(1.35815914445827,0.768161681067344,
4.36308715390869));
#286317=CARTESIAN_POINT('Ctrl Pts',(1.29329237660476,0.872960396127775,
4.37108256010794));
#286318=CARTESIAN_POINT('Ctrl Pts',(1.20483247410068,0.984035915579096,
4.38088829476144));
#286319=CARTESIAN_POINT('Ctrl Pts',(1.19261036136383,0.998813518399144,
4.38222240886461));
#286320=CARTESIAN_POINT('Ctrl Pts',(1.17217969383585,1.02260623851326,4.38442215672389));
#286321=CARTESIAN_POINT('Ctrl Pts',(1.16413258591279,1.03175775308362,4.38528123277082));
#286322=CARTESIAN_POINT('Ctrl Pts',(1.14944449943468,1.04807106811368,4.38683684102738));
#286323=CARTESIAN_POINT('Ctrl Pts',(1.14284195322776,1.05526673551619,4.3875317380446));
#286324=CARTESIAN_POINT('Ctrl Pts',(1.12853796545918,1.07056398665135,4.3890282227934));
#286325=CARTESIAN_POINT('Ctrl Pts',(1.12081611614997,1.0786456372188,4.38983066314579));
#286326=CARTESIAN_POINT('Ctrl Pts',(1.09931235063688,1.10067114118755,4.3920510435793));
#286327=CARTESIAN_POINT('Ctrl Pts',(1.08535330708724,1.11443830647471,4.39347666956744));
#286328=CARTESIAN_POINT('Ctrl Pts',(1.05358204312197,1.14460967918957,4.39668845242944));
#286329=CARTESIAN_POINT('Ctrl Pts',(1.03563977848757,1.16086888616069,4.39848016864262));
#286330=CARTESIAN_POINT('Ctrl Pts',(0.976023545371014,1.21241053459215,
4.40436428628152));
#286331=CARTESIAN_POINT('Ctrl Pts',(0.93287347035545,1.2459162415818,4.40851899233695));
#286332=CARTESIAN_POINT('Ctrl Pts',(0.788461193608527,1.34633746460596,
4.42205685030198));
#286333=CARTESIAN_POINT('Ctrl Pts',(0.68110640947927,1.40370646831769,4.43161176280327));
#286334=CARTESIAN_POINT('Ctrl Pts',(0.554857044827869,1.45324413927628,
4.44169873445635));
#286335=CARTESIAN_POINT('Ctrl Pts',(0.541468875106046,1.45828541939911,
4.44275428887964));
#286336=CARTESIAN_POINT('Ctrl Pts',(0.521502921761343,1.46549064989815,
4.44430568706108));
#286337=CARTESIAN_POINT('Ctrl Pts',(0.514977623360456,1.46779637371578,
4.44480914414829));
#286338=CARTESIAN_POINT('Ctrl Pts',(0.503247241294266,1.47185346396776,
4.4457075351346));
#286339=CARTESIAN_POINT('Ctrl Pts',(0.498048062421503,1.47362089275558,
4.44610336832191));
#286340=CARTESIAN_POINT('Ctrl Pts',(0.486409431881543,1.47750873836931,
4.44698422546984));
#286341=CARTESIAN_POINT('Ctrl Pts',(0.479965373711866,1.47961462956449,
4.44746840846465));
#286342=CARTESIAN_POINT('Ctrl Pts',(0.460572748866469,1.48581203060468,
4.44891551400076));
#286343=CARTESIAN_POINT('Ctrl Pts',(0.447583751237351,1.48977631402793,
4.44987145998965));
#286344=CARTESIAN_POINT('Ctrl Pts',(0.417114737421031,1.49864106330821,
4.45208657303177));
#286345=CARTESIAN_POINT('Ctrl Pts',(0.399597260356206,1.50340674288423,
4.45333931247084));
#286346=CARTESIAN_POINT('Ctrl Pts',(0.336223622955492,1.51946169591212,
4.45781029859209));
#286347=CARTESIAN_POINT('Ctrl Pts',(0.289939783824997,1.52896885616167,
4.4609617607184));
#286348=CARTESIAN_POINT('Ctrl Pts',(0.130450489089249,1.5542250205593,4.47164957218641));
#286349=CARTESIAN_POINT('Ctrl Pts',(0.015991750870176,1.55960751440904,
4.47905534009747));
#286350=CARTESIAN_POINT('Ctrl Pts',(-0.130992605140568,1.55032659356239,
4.48908360602945));
#286351=CARTESIAN_POINT('Ctrl Pts',(-0.163885808665665,1.5471951356909,
4.4913590915998));
#286352=CARTESIAN_POINT('Ctrl Pts',(-0.210532257092109,1.54125020519325,
4.49464430575546));
#286353=CARTESIAN_POINT('Ctrl Pts',(-0.224387083733287,1.53929413707484,
4.49562741106794));
#286354=CARTESIAN_POINT('Ctrl Pts',(-0.248014680780174,1.53563255479586,
4.49731747701489));
#286355=CARTESIAN_POINT('Ctrl Pts',(-0.257801149013188,1.53401994267171,
4.49802147490781));
#286356=CARTESIAN_POINT('Ctrl Pts',(-0.277762879412105,1.53053424259463,
4.49946591602658));
#286357=CARTESIAN_POINT('Ctrl Pts',(-0.287936193238695,1.52865300967978,
4.50020658472581));
#286358=CARTESIAN_POINT('Ctrl Pts',(-0.313469873230396,1.52366743572125,
4.50207734904723));
#286359=CARTESIAN_POINT('Ctrl Pts',(-0.328803182672927,1.52043225754525,
4.5032115476481));
#286360=CARTESIAN_POINT('Ctrl Pts',(-0.392093831705592,1.50607641205929,
4.5079395589005));
#286361=CARTESIAN_POINT('Ctrl Pts',(-0.439553805427336,1.49291500489612,
4.51159724810286));
#286362=CARTESIAN_POINT('Ctrl Pts',(-0.565851344477908,1.45134609599004,
4.52164103805286));
#286363=CARTESIAN_POINT('Ctrl Pts',(-0.643145931642067,1.41878608896666,
4.52813243896421));
#286364=CARTESIAN_POINT('Ctrl Pts',(-0.782514091629438,1.34634000438426,
4.54030951863989));
#286365=CARTESIAN_POINT('Ctrl Pts',(-0.845124405740421,1.30794748917469,
4.54597778303221));
#286366=CARTESIAN_POINT('Ctrl Pts',(-0.91595310478424,1.25729800457961,
4.55246374315616));
#286367=CARTESIAN_POINT('Ctrl Pts',(-0.927004001535046,1.24917251690668,
4.55347781972311));
#286368=CARTESIAN_POINT('Ctrl Pts',(-0.943449858177091,1.23674177033131,
4.55498847274661));
#286369=CARTESIAN_POINT('Ctrl Pts',(-0.948925667629875,1.23254530280128,
4.55549171582995));
#286370=CARTESIAN_POINT('Ctrl Pts',(-0.958790440415365,1.2248805771586,
4.55639851608721));
#286371=CARTESIAN_POINT('Ctrl Pts',(-0.963188954090369,1.22142481543671,
4.55680291048711));
#286372=CARTESIAN_POINT('Ctrl Pts',(-0.972177367732558,1.21428417488792,
4.55762929282815));
#286373=CARTESIAN_POINT('Ctrl Pts',(-0.976765131178521,1.21059686655703,
4.55805110505833));
#286374=CARTESIAN_POINT('Ctrl Pts',(-0.988254807495022,1.20125446829591,
4.55910787151927));
#286375=CARTESIAN_POINT('Ctrl Pts',(-0.995129312439812,1.19556577551092,
4.5597404979481));
#286376=CARTESIAN_POINT('Ctrl Pts',(-1.01055285188049,1.18257749752043,
4.56116163803271));
#286377=CARTESIAN_POINT('Ctrl Pts',(-1.01907256729912,1.17524368717213,
4.5619479184038));
#286378=CARTESIAN_POINT('Ctrl Pts',(-1.04456400227764,1.15281487924561,
4.56430706176713));
#286379=CARTESIAN_POINT('Ctrl Pts',(-1.06128600675228,1.1374393293851,4.56586357498902));
#286380=CARTESIAN_POINT('Ctrl Pts',(-1.12781625365688,1.07352094294783,
4.57212286691856));
#286381=CARTESIAN_POINT('Ctrl Pts',(-1.17468248355205,1.02202701168424,
4.57669151303501));
#286382=CARTESIAN_POINT('Ctrl Pts',(-1.27994257098291,0.889528242054865,
4.58782939772139));
#286383=CARTESIAN_POINT('Ctrl Pts',(-1.33428664738122,0.805722903756993,
4.59439430221794));
#286384=CARTESIAN_POINT('Ctrl Pts',(-1.38971605353195,0.699065029421539,
4.60267843433187));
#286385=CARTESIAN_POINT('Ctrl Pts',(-1.39883052236613,0.680643612435232,
4.60410603977543));
#286386=CARTESIAN_POINT('Ctrl Pts',(-1.41293361117383,0.650659092704301,
4.60642801993813));
#286387=CARTESIAN_POINT('Ctrl Pts',(-1.41815165344996,0.639206160628075,
4.60731451849287));
#286388=CARTESIAN_POINT('Ctrl Pts',(-1.4271863137001,0.618720937621211,
4.60890011559736));
#286389=CARTESIAN_POINT('Ctrl Pts',(-1.43105762849586,0.609713398697462,
4.60959730430087));
#286390=CARTESIAN_POINT('Ctrl Pts',(-1.43906345737749,0.590589569964072,
4.6110777975717));
#286391=CARTESIAN_POINT('Ctrl Pts',(-1.44317700958168,0.580465143000246,
4.61186176678974));
#286392=CARTESIAN_POINT('Ctrl Pts',(-1.45393870893787,0.553156365958523,
4.61397731623647));
#286393=CARTESIAN_POINT('Ctrl Pts',(-1.4603885804072,0.53589632822872,4.6153154177468));
#286394=CARTESIAN_POINT('Ctrl Pts',(-1.50010621636561,0.423564340365713,
4.62403424400703));
#286395=CARTESIAN_POINT('Ctrl Pts',(-1.52437313714131,0.325583720036536,
4.63170932982582));
#286396=CARTESIAN_POINT('Ctrl Pts',(-1.55002255233211,0.150890432230857,
4.64537475581589));
#286397=CARTESIAN_POINT('Ctrl Pts',(-1.55553734988942,0.0751104264812811,
4.65128965469626));
#286398=CARTESIAN_POINT('Ctrl Pts',(-1.55549980963818,-0.00076955545019349,
4.65706464148559));
#286399=CARTESIAN_POINT('',(-1.55596383579478,0.00138071545366179,5.3559437743963));
#286400=CARTESIAN_POINT('Ctrl Pts',(-1.55745492001379,-0.000856371120316864,
4.65594377439631));
#286401=CARTESIAN_POINT('Ctrl Pts',(-1.5577850741697,-0.0506891626144068,
4.65952562306032));
#286402=CARTESIAN_POINT('Ctrl Pts',(-1.53301192978291,-0.615473136307116,
4.70014468855281));
#286403=CARTESIAN_POINT('Ctrl Pts',(-0.844041411881997,-1.63316067010957,
4.77780097087378));
#286404=CARTESIAN_POINT('Ctrl Pts',(0.913973507436636,-1.59507746114991,
4.88891262135923));
#286405=CARTESIAN_POINT('Ctrl Pts',(1.83577980123458,-0.0976329900371924,
5.00002427184466));
#286406=CARTESIAN_POINT('Ctrl Pts',(1.0780025055099,1.48913742733129,5.1111359223301));
#286407=CARTESIAN_POINT('Ctrl Pts',(-0.666056105926533,1.7134727727987,
5.22224757281553));
#286408=CARTESIAN_POINT('Ctrl Pts',(-1.49938299705611,0.726891414718789,
5.30385019017093));
#286409=CARTESIAN_POINT('Ctrl Pts',(-1.55693038683329,0.106378444150779,
5.34841559069786));
#286410=CARTESIAN_POINT('Ctrl Pts',(-1.55596383579478,0.00138071545366179,
5.3559437743963));
#286411=CARTESIAN_POINT('',(-1.5554995157997,-0.00134118142063625,6.75626796741665));
#286412=CARTESIAN_POINT('Ctrl Pts',(-1.55549937213162,0.0013976044270106,
5.35621070370163));
#286413=CARTESIAN_POINT('Ctrl Pts',(-1.55558531673232,-0.0942566235089736,
5.3625138632035));
#286414=CARTESIAN_POINT('Ctrl Pts',(-1.54684820960077,-0.189710805692918,
5.36876803926013));
#286415=CARTESIAN_POINT('Ctrl Pts',(-1.52501392228005,-0.307393315677365,
5.37690504084912));
#286416=CARTESIAN_POINT('Ctrl Pts',(-1.5200816041754,-0.330922850003075,
5.37855285049613));
#286417=CARTESIAN_POINT('Ctrl Pts',(-1.5113927892051,-0.368063987588195,
5.38119346912254));
#286418=CARTESIAN_POINT('Ctrl Pts',(-1.50799268936484,-0.381755535595127,
5.38217551296266));
#286419=CARTESIAN_POINT('Ctrl Pts',(-1.50113613180991,-0.407843269366331,
5.38406447062459));
#286420=CARTESIAN_POINT('Ctrl Pts',(-1.49771113072265,-0.420246558421885,
5.3849703301972));
#286421=CARTESIAN_POINT('Ctrl Pts',(-1.491396389121,-0.442056405599685,
5.3865776675289));
#286422=CARTESIAN_POINT('Ctrl Pts',(-1.48857049217765,-0.45148082674486,
5.38727704048428));
#286423=CARTESIAN_POINT('Ctrl Pts',(-1.48246071469624,-0.471175912638168,
5.38874902987812));
#286424=CARTESIAN_POINT('Ctrl Pts',(-1.47915907633452,-0.481440471221005,
5.38952219552156));
#286425=CARTESIAN_POINT('Ctrl Pts',(-1.47014353531056,-0.508500702703793,
5.39157685581394));
#286426=CARTESIAN_POINT('Ctrl Pts',(-1.46424869983214,-0.525233924775626,
5.39286423208727));
#286427=CARTESIAN_POINT('Ctrl Pts',(-1.43385982406354,-0.607005814791225,
5.39924124640113));
#286428=CARTESIAN_POINT('Ctrl Pts',(-1.40531565354724,-0.670444175584406,
5.40446337431976));
#286429=CARTESIAN_POINT('Ctrl Pts',(-1.32600998858741,-0.819206405149396,
5.41736928707314));
#286430=CARTESIAN_POINT('Ctrl Pts',(-1.27114121913679,-0.901997980377709,
5.42513387974268));
#286431=CARTESIAN_POINT('Ctrl Pts',(-1.18266814132577,-1.01123511881884,
5.43589568734301));
#286432=CARTESIAN_POINT('Ctrl Pts',(-1.15528336216924,-1.04241135930595,
5.43903275673746));
#286433=CARTESIAN_POINT('Ctrl Pts',(-1.11981458544122,-1.0796734544794,
5.44283018234965));
#286434=CARTESIAN_POINT('Ctrl Pts',(-1.11287737747529,-1.08682263064699,
5.44356105654601));
#286435=CARTESIAN_POINT('Ctrl Pts',(-1.10218029217275,-1.09763673717239,
5.44466946420265));
#286436=CARTESIAN_POINT('Ctrl Pts',(-1.09846991186274,-1.10134992538673,
5.44505057771528));
#286437=CARTESIAN_POINT('Ctrl Pts',(-1.09083577014417,-1.1089128852218,
5.44582776885242));
#286438=CARTESIAN_POINT('Ctrl Pts',(-1.08691040384544,-1.11276063934723,
5.44622365859345));
#286439=CARTESIAN_POINT('Ctrl Pts',(-1.07789402754417,-1.12150551048198,
5.44712459352676));
#286440=CARTESIAN_POINT('Ctrl Pts',(-1.07278996803996,-1.12638884684528,
5.44762859065801));
#286441=CARTESIAN_POINT('Ctrl Pts',(-1.05669881880009,-1.14157554345909,
5.44919948917127));
#286442=CARTESIAN_POINT('Ctrl Pts',(-1.04559483499751,-1.15175457463726,
5.45025754140244));
#286443=CARTESIAN_POINT('Ctrl Pts',(-0.972198027713824,-1.21710097263523,
5.45709802230677));
#286444=CARTESIAN_POINT('Ctrl Pts',(-0.905703620700305,-1.26736280163341,
5.4625923547523));
#286445=CARTESIAN_POINT('Ctrl Pts',(-0.768516086060986,-1.35472109603187,
5.47330367461397));
#286446=CARTESIAN_POINT('Ctrl Pts',(-0.698369563857121,-1.39218001083551,
5.47850761995188));
#286447=CARTESIAN_POINT('Ctrl Pts',(-0.584559364932492,-1.44218137832236,
5.4868888329545));
#286448=CARTESIAN_POINT('Ctrl Pts',(-0.542687119889451,-1.45845358293211,
5.48995862669651));
#286449=CARTESIAN_POINT('Ctrl Pts',(-0.485776403117846,-1.47777964827052,
5.49414794795821));
#286450=CARTESIAN_POINT('Ctrl Pts',(-0.471309695152091,-1.4824569286404,
5.49521421705987));
#286451=CARTESIAN_POINT('Ctrl Pts',(-0.446978573678549,-1.4899313669626,
5.49701100742747));
#286452=CARTESIAN_POINT('Ctrl Pts',(-0.437150661268289,-1.49284447074134,
5.49773770674514));
#286453=CARTESIAN_POINT('Ctrl Pts',(-0.417692586986589,-1.49840344449549,
5.49917868836068));
#286454=CARTESIAN_POINT('Ctrl Pts',(-0.408064305743027,-1.50105412743808,
5.49989277472525));
#286455=CARTESIAN_POINT('Ctrl Pts',(-0.384523034735545,-1.50729184764809,
5.50164164707594));
#286456=CARTESIAN_POINT('Ctrl Pts',(-0.370584826813751,-1.51077911642587,
5.50267959058349));
#286457=CARTESIAN_POINT('Ctrl Pts',(-0.322180536323446,-1.52217949740251,
5.50629381664485));
#286458=CARTESIAN_POINT('Ctrl Pts',(-0.287496681634273,-1.52910954706044,
5.50890077050358));
#286459=CARTESIAN_POINT('Ctrl Pts',(-0.13122929556239,-1.5548283845244,
5.52073050285651));
#286460=CARTESIAN_POINT('Ctrl Pts',(-0.00792084691592195,-1.56033358620807,
5.53033853746785));
#286461=CARTESIAN_POINT('Ctrl Pts',(0.153798402359041,-1.54837387686308,
5.54285171111443));
#286462=CARTESIAN_POINT('Ctrl Pts',(0.1927549427831,-1.54400827494375,5.54585454690231));
#286463=CARTESIAN_POINT('Ctrl Pts',(0.254925886865817,-1.53465106498951,
5.55059198419846));
#286464=CARTESIAN_POINT('Ctrl Pts',(0.278262517331183,-1.53059179008015,
5.5523576010522));
#286465=CARTESIAN_POINT('Ctrl Pts',(0.309753500900875,-1.5243699737273,
5.55471522904924));
#286466=CARTESIAN_POINT('Ctrl Pts',(0.317994975877967,-1.52267207631725,
5.55532990553891));
#286467=CARTESIAN_POINT('Ctrl Pts',(0.331784854154872,-1.51971425722947,
5.55635402879094));
#286468=CARTESIAN_POINT('Ctrl Pts',(0.337340772573969,-1.51849063887314,
5.5567654502225));
#286469=CARTESIAN_POINT('Ctrl Pts',(0.348715976276974,-1.51591988342108,
5.55760517987894));
#286470=CARTESIAN_POINT('Ctrl Pts',(0.354534411427445,-1.51456966806042,
5.55803331265621));
#286471=CARTESIAN_POINT('Ctrl Pts',(0.369829327204941,-1.51092738779717,
5.55915543317448));
#286472=CARTESIAN_POINT('Ctrl Pts',(0.379292476112181,-1.50857964088849,
5.55984634629906));
#286473=CARTESIAN_POINT('Ctrl Pts',(0.420632491226343,-1.49790984510663,
5.56285244064451));
#286474=CARTESIAN_POINT('Ctrl Pts',(0.452264978096047,-1.4886646255289,
5.56512086021581));
#286475=CARTESIAN_POINT('Ctrl Pts',(0.567845195753168,-1.45085902982517,
5.5733730678543));
#286476=CARTESIAN_POINT('Ctrl Pts',(0.64960364070555,-1.41614182337517,
5.57914608903986));
#286477=CARTESIAN_POINT('Ctrl Pts',(0.793697844034987,-1.33983458289773,
5.58990041838939));
#286478=CARTESIAN_POINT('Ctrl Pts',(0.856843679048442,-1.30035770027303,
5.59484465442616));
#286479=CARTESIAN_POINT('Ctrl Pts',(0.938652431895123,-1.24065937744863,
5.60179008700938));
#286480=CARTESIAN_POINT('Ctrl Pts',(0.959968982974912,-1.22423996106562,
5.60365365500379));
#286481=CARTESIAN_POINT('Ctrl Pts',(0.990632091123183,-1.19932782236166,
5.60642200991812));
#286482=CARTESIAN_POINT('Ctrl Pts',(1.00031891218933,-1.19126035053432,
5.6073099289106));
#286483=CARTESIAN_POINT('Ctrl Pts',(1.0173650090175,-1.17670933426509,5.6088971068135));
#286484=CARTESIAN_POINT('Ctrl Pts',(1.02476312004483,-1.17027217290432,
5.60959444161794));
#286485=CARTESIAN_POINT('Ctrl Pts',(1.04026717331089,-1.15652221440282,
5.61107424097318));
#286486=CARTESIAN_POINT('Ctrl Pts',(1.04835795131679,-1.14919320348493,
5.61185736127656));
#286487=CARTESIAN_POINT('Ctrl Pts',(1.06985570951289,-1.12930355197775,
5.61396811839095));
#286488=CARTESIAN_POINT('Ctrl Pts',(1.08311804401966,-1.11658989818164,
5.61530222517486));
#286489=CARTESIAN_POINT('Ctrl Pts',(1.16046536077529,-1.03976773436914,
5.62327898012649));
#286490=CARTESIAN_POINT('Ctrl Pts',(1.21906098424805,-0.970402868061441,
5.6301559091766));
#286491=CARTESIAN_POINT('Ctrl Pts',(1.30899372531837,-0.842852099371245,
5.64220522456008));
#286492=CARTESIAN_POINT('Ctrl Pts',(1.34329585058496,-0.787032700459085,
5.64730472036477));
#286493=CARTESIAN_POINT('Ctrl Pts',(1.39050724397153,-0.698077903848779,
5.65505781487955));
#286494=CARTESIAN_POINT('Ctrl Pts',(1.40597239169172,-0.666382110462548,
5.65775151512342));
#286495=CARTESIAN_POINT('Ctrl Pts',(1.42933346770172,-0.614061740775941,
5.66206068763612));
#286496=CARTESIAN_POINT('Ctrl Pts',(1.43789093100254,-0.593747238334971,
5.66370124748263));
#286497=CARTESIAN_POINT('Ctrl Pts',(1.44903321819478,-0.565641305514525,
5.66592041504713));
#286498=CARTESIAN_POINT('Ctrl Pts',(1.45199203502418,-0.558002233052944,
5.66651851958697));
#286499=CARTESIAN_POINT('Ctrl Pts',(1.45688822315515,-0.545058564772707,
5.667523016475));
#286500=CARTESIAN_POINT('Ctrl Pts',(1.4588572819491,-0.539766216982017,
5.66793122226028));
#286501=CARTESIAN_POINT('Ctrl Pts',(1.46287492950057,-0.528785159327553,
5.66877287389834));
#286502=CARTESIAN_POINT('Ctrl Pts',(1.46491923413133,-0.523095062967969,
5.66920607350375));
#286503=CARTESIAN_POINT('Ctrl Pts',(1.47028443648326,-0.507883459298711,
5.67035675746368));
#286504=CARTESIAN_POINT('Ctrl Pts',(1.47354608337174,-0.498341134917042,
5.67107087943219));
#286505=CARTESIAN_POINT('Ctrl Pts',(1.48822300225059,-0.453997707047249,
5.67435682347362));
#286506=CARTESIAN_POINT('Ctrl Pts',(1.49850070941619,-0.418829025386111,
5.67687044951284));
#286507=CARTESIAN_POINT('Ctrl Pts',(1.52872485273135,-0.299965156299139,
5.685161907478));
#286508=CARTESIAN_POINT('Ctrl Pts',(1.54297212330114,-0.214983277069093,
5.69076351474443));
#286509=CARTESIAN_POINT('Ctrl Pts',(1.55616805129081,-0.056727371821594,
5.70124165488428));
#286510=CARTESIAN_POINT('Ctrl Pts',(1.55711760750708,0.016127356831905,
5.70608323596208));
#286511=CARTESIAN_POINT('Ctrl Pts',(1.55143230707139,0.115580607876705,
5.71291532420794));
#286512=CARTESIAN_POINT('Ctrl Pts',(1.54920637812199,0.142339492025496,
5.71477511687613));
#286513=CARTESIAN_POINT('Ctrl Pts',(1.54492050773076,0.181547617547816,
5.717538925979));
#286514=CARTESIAN_POINT('Ctrl Pts',(1.54339975958793,0.194051740965268,
5.7184261559439));
#286515=CARTESIAN_POINT('Ctrl Pts',(1.54042541914366,0.21625430506051,5.7200125667303));
#286516=CARTESIAN_POINT('Ctrl Pts',(1.53903163929107,0.225960177073611,
5.72070983036372));
#286517=CARTESIAN_POINT('Ctrl Pts',(1.53589154316561,0.246448195176311,
5.72218996484407));
#286518=CARTESIAN_POINT('Ctrl Pts',(1.53412324306125,0.257226377156094,
5.72297349575075));
#286519=CARTESIAN_POINT('Ctrl Pts',(1.5290721040272,0.286106991555049,5.72508657061025));
#286520=CARTESIAN_POINT('Ctrl Pts',(1.52558146109087,0.304170777022648,
5.72642260932998));
#286521=CARTESIAN_POINT('Ctrl Pts',(1.5034801599464,0.408567112708702,5.73423103027641));
#286522=CARTESIAN_POINT('Ctrl Pts',(1.47786753119561,0.493236482940582,
5.74092477707952));
#286523=CARTESIAN_POINT('Ctrl Pts',(1.42078531439761,0.636642508259966,
5.75283336754041));
#286524=CARTESIAN_POINT('Ctrl Pts',(1.39246843390347,0.696402296672161,
5.7579807637065));
#286525=CARTESIAN_POINT('Ctrl Pts',(1.3428273672816,0.785947982165514,5.76586842651184));
#286526=CARTESIAN_POINT('Ctrl Pts',(1.32410800354323,0.817091129403761,
5.76864603584951));
#286527=CARTESIAN_POINT('Ctrl Pts',(1.29593763783856,0.860443043205675,
5.77253633624833));
#286528=CARTESIAN_POINT('Ctrl Pts',(1.28737003745574,0.873209608348753,
5.77368500032928));
#286529=CARTESIAN_POINT('Ctrl Pts',(1.27180601621621,0.895674396455829,
5.77570892759108));
#286530=CARTESIAN_POINT('Ctrl Pts',(1.26488448940693,0.905422784695,5.7765881080773));
#286531=CARTESIAN_POINT('Ctrl Pts',(1.25405753382366,0.920305129523615,
5.77793055892267));
#286532=CARTESIAN_POINT('Ctrl Pts',(1.25023160654899,0.925495955461203,
5.77839884126318));
#286533=CARTESIAN_POINT('Ctrl Pts',(1.24307092910497,0.935085762268642,
5.77926383393281));
#286534=CARTESIAN_POINT('Ctrl Pts',(1.23974500886189,0.939490836605487,
5.7796610865468));
#286535=CARTESIAN_POINT('Ctrl Pts',(1.23201267474367,0.949619497351625,
5.78057443674902));
#286536=CARTESIAN_POINT('Ctrl Pts',(1.22758975599729,0.955330213560184,
5.78108937954889));
#286537=CARTESIAN_POINT('Ctrl Pts',(1.21301351235378,0.973882151080955,
5.78276294149331));
#286538=CARTESIAN_POINT('Ctrl Pts',(1.20269682720201,0.986594457165662,
5.78391083554846));
#286539=CARTESIAN_POINT('Ctrl Pts',(1.11614808355367,1.08986479951813,5.7932679704173));
#286540=CARTESIAN_POINT('Ctrl Pts',(1.02999733747858,1.17162513625742,5.80090448671055));
#286541=CARTESIAN_POINT('Ctrl Pts',(0.891871292510244,1.27558337587649,
5.81232872904528));
#286542=CARTESIAN_POINT('Ctrl Pts',(0.846662041159824,1.30602834453988,
5.81595586007929));
#286543=CARTESIAN_POINT('Ctrl Pts',(0.77921752453907,1.34647123623106,5.82130104505155));
#286544=CARTESIAN_POINT('Ctrl Pts',(0.758197237054425,1.35841878339606,
5.82295798458011));
#286545=CARTESIAN_POINT('Ctrl Pts',(0.719661920385412,1.37914845594972,
5.82598682054461));
#286546=CARTESIAN_POINT('Ctrl Pts',(0.702242964093857,1.38809888082407,
5.82735278810835));
#286547=CARTESIAN_POINT('Ctrl Pts',(0.674627860022165,1.40163559327147,
5.82951610025713));
#286548=CARTESIAN_POINT('Ctrl Pts',(0.664542927173833,1.40644508321132,
5.83030567018541));
#286549=CARTESIAN_POINT('Ctrl Pts',(0.64554730742276,1.41525414854056,5.8317924916393));
#286550=CARTESIAN_POINT('Ctrl Pts',(0.636649015966238,1.41927927257646,
5.83248882043665));
#286551=CARTESIAN_POINT('Ctrl Pts',(0.616557656453333,1.42814059917551,
5.83406102660246));
#286552=CARTESIAN_POINT('Ctrl Pts',(0.605344556061724,1.43292947051775,
5.83493846667957));
#286553=CARTESIAN_POINT('Ctrl Pts',(0.576333307597518,1.44491825256296,
5.8372091670389));
#286554=CARTESIAN_POINT('Ctrl Pts',(0.558456550749057,1.45192116106146,
5.838608903285));
#286555=CARTESIAN_POINT('Ctrl Pts',(0.407609661955568,1.50781484236892,
5.85042914943818));
#286556=CARTESIAN_POINT('Ctrl Pts',(0.26868330361232,1.53864988422778,5.86146444892349));
#286557=CARTESIAN_POINT('Ctrl Pts',(0.0863364101492555,1.55365253157216,
5.87559775140957));
#286558=CARTESIAN_POINT('Ctrl Pts',(0.0450028621525554,1.5553987795473,
5.87877149858463));
#286559=CARTESIAN_POINT('Ctrl Pts',(-0.0209021069935472,1.55555327188271,
5.88374242399738));
#286560=CARTESIAN_POINT('Ctrl Pts',(-0.045450296293988,1.55502968586492,
5.88557408704744));
#286561=CARTESIAN_POINT('Ctrl Pts',(-0.0784947149493644,1.55354160546452,
5.88800432310237));
#286562=CARTESIAN_POINT('Ctrl Pts',(-0.0870089019708607,1.55308802070189,
5.88862732159931));
#286563=CARTESIAN_POINT('Ctrl Pts',(-0.101219370355704,1.55221374306362,
5.88966136026361));
#286564=CARTESIAN_POINT('Ctrl Pts',(-0.106917745895264,1.55183164830491,
5.89007445664075));
#286565=CARTESIAN_POINT('Ctrl Pts',(-0.118538214655707,1.55098814375979,
5.89091353501011));
#286566=CARTESIAN_POINT('Ctrl Pts',(-0.124459981987208,1.55052418442428,
5.89133937497956));
#286567=CARTESIAN_POINT('Ctrl Pts',(-0.139943306781881,1.54922181837421,
5.89244855361125));
#286568=CARTESIAN_POINT('Ctrl Pts',(-0.14950020318254,1.54832880009703,
5.89312894484608));
#286569=CARTESIAN_POINT('Ctrl Pts',(-0.190333666649957,1.54413161534271,
5.89602028030618));
#286570=CARTESIAN_POINT('Ctrl Pts',(-0.22151677520207,1.5399675336043,5.89818875342736));
#286571=CARTESIAN_POINT('Ctrl Pts',(-0.341118895516244,1.52028751652238,
5.90642758635648));
#286572=CARTESIAN_POINT('Ctrl Pts',(-0.428262739292278,1.4980754079734,
5.91227207783509));
#286573=CARTESIAN_POINT('Ctrl Pts',(-0.583852471675827,1.44372008845948,
5.92314084936476));
#286574=CARTESIAN_POINT('Ctrl Pts',(-0.652803918329675,1.41388000833656,
5.92812719440873));
#286575=CARTESIAN_POINT('Ctrl Pts',(-0.743204149788014,1.36673075384221,
5.93511923856452));
#286576=CARTESIAN_POINT('Ctrl Pts',(-0.766751060834749,1.35366097080675,
5.93698441954035));
#286577=CARTESIAN_POINT('Ctrl Pts',(-0.800809040487302,1.33358320104073,
5.93975471640259));
#286578=CARTESIAN_POINT('Ctrl Pts',(-0.811593754188938,1.32704741247412,
5.94064292950013));
#286579=CARTESIAN_POINT('Ctrl Pts',(-0.83062223454267,1.3151969936329,5.94223043501111));
#286580=CARTESIAN_POINT('Ctrl Pts',(-0.838897539471974,1.30993409712202,
5.94292780036533));
#286581=CARTESIAN_POINT('Ctrl Pts',(-0.856276182275182,1.29864948023584,
5.94440745751945));
#286582=CARTESIAN_POINT('Ctrl Pts',(-0.865366974146432,1.29260951631273,
5.94519040323862));
#286583=CARTESIAN_POINT('Ctrl Pts',(-0.889577974643689,1.27615374142328,
5.94730017499007));
#286584=CARTESIAN_POINT('Ctrl Pts',(-0.904578155033677,1.26556534899134,
5.94863346046612));
#286585=CARTESIAN_POINT('Ctrl Pts',(-0.995295577312708,1.19909252703306,
5.95686249562552));
#286586=CARTESIAN_POINT('Ctrl Pts',(-1.06598621673972,1.1367073447424,5.96401237613621));
#286587=CARTESIAN_POINT('Ctrl Pts',(-1.18009144516023,1.01595161050615,
5.97685118783924));
#286588=CARTESIAN_POINT('Ctrl Pts',(-1.2258862259353,0.960196185592179,
5.98247047858549));
#286589=CARTESIAN_POINT('Ctrl Pts',(-1.28446663821339,0.877819813031491,
5.99021451888064));
#286590=CARTESIAN_POINT('Ctrl Pts',(-1.30061847700068,0.853706012913974,
5.99241941237853));
#286591=CARTESIAN_POINT('Ctrl Pts',(-1.32633260302091,0.812890831728273,
5.99603418944769));
#286592=CARTESIAN_POINT('Ctrl Pts',(-1.33627635010345,0.796439126779588,
5.99746081153981));
#286593=CARTESIAN_POINT('Ctrl Pts',(-1.34981064983257,0.773079492025513,
5.99943988121767));
#286594=CARTESIAN_POINT('Ctrl Pts',(-1.3536577553296,0.766323286649535,
6.00000691104201));
#286595=CARTESIAN_POINT('Ctrl Pts',(-1.3601766443748,0.754672665979396,
6.00097517289035));
#286596=CARTESIAN_POINT('Ctrl Pts',(-1.36287302262578,0.749792281335528,
6.00137791891593));
#286597=CARTESIAN_POINT('Ctrl Pts',(-1.36851951928948,0.739441142460499,
6.00222599980405));
#286598=CARTESIAN_POINT('Ctrl Pts',(-1.37146316051516,0.733967084274369,
6.00267093668019));
#286599=CARTESIAN_POINT('Ctrl Pts',(-1.37946041295764,0.71887911336415,
6.00388796944352));
#286600=CARTESIAN_POINT('Ctrl Pts',(-1.38444638839404,0.709229459137353,
6.00465599552949));
#286601=CARTESIAN_POINT('Ctrl Pts',(-1.41102523810121,0.65644126384849,
6.00880589471036));
#286602=CARTESIAN_POINT('Ctrl Pts',(-1.43070583210502,0.612363637095453,
6.01208537771746));
#286603=CARTESIAN_POINT('Ctrl Pts',(-1.48216328983869,0.481025496373257,
6.0215280720004));
#286604=CARTESIAN_POINT('Ctrl Pts',(-1.5082185515259,0.391754536142064,
6.02754730405343));
#286605=CARTESIAN_POINT('Ctrl Pts',(-1.53504658811036,0.255588328982511,
6.03676405215725));
#286606=CARTESIAN_POINT('Ctrl Pts',(-1.54192852476428,0.210117463223652,
6.03984552260478));
#286607=CARTESIAN_POINT('Ctrl Pts',(-1.5501299691439,0.132957920080517,
6.04513988470019));
#286608=CARTESIAN_POINT('Ctrl Pts',(-1.55251282870585,0.10141209130756,
6.04732246046617));
#286609=CARTESIAN_POINT('Ctrl Pts',(-1.55453412009693,0.056423960080094,
6.05047241574247));
#286610=CARTESIAN_POINT('Ctrl Pts',(-1.55496267751271,0.0430237781187197,
6.05141533463132));
#286611=CARTESIAN_POINT('Ctrl Pts',(-1.55540682487816,0.0197035962003662,
6.05306524379105));
#286612=CARTESIAN_POINT('Ctrl Pts',(-1.55550083692798,0.00978573443703066,
6.05376975090866));
#286613=CARTESIAN_POINT('Ctrl Pts',(-1.55549909763968,-0.0106881064554486,
6.05523024010196));
#286614=CARTESIAN_POINT('Ctrl Pts',(-1.55539074839895,-0.0212435405207699,
6.05598657912256));
#286615=CARTESIAN_POINT('Ctrl Pts',(-1.55483411414781,-0.0484683925111042,
6.05794646875803));
#286616=CARTESIAN_POINT('Ctrl Pts',(-1.55422520519461,-0.0651327792238609,
6.05915495677717));
#286617=CARTESIAN_POINT('Ctrl Pts',(-1.55016624014936,-0.142226349352791,
6.06478876843065));
#286618=CARTESIAN_POINT('Ctrl Pts',(-1.54345929040669,-0.202423744467183,
6.06931341446638));
#286619=CARTESIAN_POINT('Ctrl Pts',(-1.52176676867994,-0.329337445247056,
6.07911553554798));
#286620=CARTESIAN_POINT('Ctrl Pts',(-1.50585582606494,-0.395770526459621,
6.08440585842539));
#286621=CARTESIAN_POINT('Ctrl Pts',(-1.48108355806372,-0.475613061167336,
6.09088764160246));
#286622=CARTESIAN_POINT('Ctrl Pts',(-1.47631370872973,-0.490218450630519,
6.09207832059499));
#286623=CARTESIAN_POINT('Ctrl Pts',(-1.44986360236758,-0.567319435010784,
6.09838467393077));
#286624=CARTESIAN_POINT('Ctrl Pts',(-1.42442700875866,-0.628462864214943,
6.1034618624759));
#286625=CARTESIAN_POINT('Ctrl Pts',(-1.39017211730538,-0.697946658725506,
6.10919291824926));
#286626=CARTESIAN_POINT('Ctrl Pts',(-1.3850626921306,-0.708032070463512,
6.11002369241933));
#286627=CARTESIAN_POINT('Ctrl Pts',(-1.37689970307731,-0.723718264022471,
6.11131312762399));
#286628=CARTESIAN_POINT('Ctrl Pts',(-1.37392100609101,-0.729357245068671,
6.11177611064862));
#286629=CARTESIAN_POINT('Ctrl Pts',(-1.36855596925432,-0.739364308122387,
6.11259653487212));
#286630=CARTESIAN_POINT('Ctrl Pts',(-1.36618331313805,-0.743739320669714,
6.11295478783968));
#286631=CARTESIAN_POINT('Ctrl Pts',(-1.36036212388585,-0.754351330746923,
6.11382281394205));
#286632=CARTESIAN_POINT('Ctrl Pts',(-1.35689166803833,-0.760576126899796,
6.11433119889839));
#286633=CARTESIAN_POINT('Ctrl Pts',(-1.34578569962224,-0.780178407881677,
6.11593037418026));
#286634=CARTESIAN_POINT('Ctrl Pts',(-1.33799392398079,-0.793466951915784,
6.11701185621647));
#286635=CARTESIAN_POINT('Ctrl Pts',(-1.31888299194205,-0.824977544242013,
6.11957552335834));
#286636=CARTESIAN_POINT('Ctrl Pts',(-1.30738158604779,-0.843085869274714,
6.12104814451345));
#286637=CARTESIAN_POINT('Ctrl Pts',(-1.26082544157125,-0.913140795127486,
6.12676661893265));
#286638=CARTESIAN_POINT('Ctrl Pts',(-1.22301747645506,-0.963190711970936,
6.13090094481871));
#286639=CARTESIAN_POINT('Ctrl Pts',(-1.11122641123908,-1.0939446321787,
6.14222872492545));
#286640=CARTESIAN_POINT('Ctrl Pts',(-1.03160466908351,-1.16932770880662,
6.14939532639174));
#286641=CARTESIAN_POINT('Ctrl Pts',(-0.928644949325772,-1.24804220952798,
6.15833102810828));
#286642=CARTESIAN_POINT('Ctrl Pts',(-0.912309961394032,-1.2600322489267,
6.15973895539476));
#286643=CARTESIAN_POINT('Ctrl Pts',(-0.885524878100282,-1.27889884101396,
6.16203525080687));
#286644=CARTESIAN_POINT('Ctrl Pts',(-0.87521754050084,-1.28597464821886,
6.16291602934773));
#286645=CARTESIAN_POINT('Ctrl Pts',(-0.856684683270905,-1.2983711127966,
6.16449528568368));
#286646=CARTESIAN_POINT('Ctrl Pts',(-0.848491990772424,-1.30373982322956,
6.16519191100446));
#286647=CARTESIAN_POINT('Ctrl Pts',(-0.831012775589663,-1.31495949789832,
6.1666753215411));
#286648=CARTESIAN_POINT('Ctrl Pts',(-0.821713975969679,-1.32079023488473,
6.16746280799881));
#286649=CARTESIAN_POINT('Ctrl Pts',(-0.796451019078721,-1.3362611255164,
6.16959823254077));
#286650=CARTESIAN_POINT('Ctrl Pts',(-0.780374387270222,-1.34571311240985,
6.17095290647922));
#286651=CARTESIAN_POINT('Ctrl Pts',(-0.670629947093092,-1.40760765918242,
6.18017595688249));
#286652=CARTESIAN_POINT('Ctrl Pts',(-0.571938099225301,-1.4505109901271,
6.18838189143427));
#286653=CARTESIAN_POINT('Ctrl Pts',(-0.380077221206418,-1.51127334080108,
6.20397566409862));
#286654=CARTESIAN_POINT('Ctrl Pts',(-0.288123983018666,-1.5314677451081,
6.21129864726842));
#286655=CARTESIAN_POINT('Ctrl Pts',(-0.180338789975893,-1.54508048030575,
6.21938415874202));
#286656=CARTESIAN_POINT('Ctrl Pts',(-0.165747872438668,-1.54671375959143,
6.22046800520865));
#286657=CARTESIAN_POINT('Ctrl Pts',(-0.144176343286324,-1.54881965415474,
6.22205256878175));
#286658=CARTESIAN_POINT('Ctrl Pts',(-0.137212671830504,-1.54945210536004,
6.22256135961418));
#286659=CARTESIAN_POINT('Ctrl Pts',(-0.124770650079497,-1.5504975693983,
6.22346526205088));
#286660=CARTESIAN_POINT('Ctrl Pts',(-0.119294127819881,-1.55092854183307,
6.22386132542982));
#286661=CARTESIAN_POINT('Ctrl Pts',(-0.107118547973533,-1.55182181725444,
6.22473786655048));
#286662=CARTESIAN_POINT('Ctrl Pts',(-0.100418670971426,-1.552269767414,
6.22521755127845));
#286663=CARTESIAN_POINT('Ctrl Pts',(-0.0804855581062721,-1.55347288536532,
6.22663736911018));
#286664=CARTESIAN_POINT('Ctrl Pts',(-0.0672449320482256,-1.55410233912994,
6.22757090877339));
#286665=CARTESIAN_POINT('Ctrl Pts',(-0.0364232754980438,-1.55517292097122,
6.2297251461664));
#286666=CARTESIAN_POINT('Ctrl Pts',(-0.0188393123344847,-1.55548532891337,
6.23093989416172));
#286667=CARTESIAN_POINT('Ctrl Pts',(0.0436076222808084,-1.55553563222086,
6.2352153177454));
#286668=CARTESIAN_POINT('Ctrl Pts',(0.0884522904674536,-1.55363107599078,
6.23821524926752));
#286669=CARTESIAN_POINT('Ctrl Pts',(0.238513135872617,-1.54073814325777,
6.24819780976266));
#286670=CARTESIAN_POINT('Ctrl Pts',(0.342669068901392,-1.52096676111891,
6.2550530850836));
#286671=CARTESIAN_POINT('Ctrl Pts',(0.484235677872064,-1.47880269779657,
6.26502955175859));
#286672=CARTESIAN_POINT('Ctrl Pts',(0.523953538708725,-1.46520093882124,
6.26790195922347));
#286673=CARTESIAN_POINT('Ctrl Pts',(0.577331201005106,-1.44447325192899,
6.27189252533987));
#286674=CARTESIAN_POINT('Ctrl Pts',(0.591509182244664,-1.43872552953729,
6.27296529032807));
#286675=CARTESIAN_POINT('Ctrl Pts',(0.614113879890847,-1.42917103096822,
6.27469751492509));
#286676=CARTESIAN_POINT('Ctrl Pts',(0.622595689112525,-1.42549650804733,
6.27535248902964));
#286677=CARTESIAN_POINT('Ctrl Pts',(0.640130815558017,-1.41771351974834,
6.27671727888139));
#286678=CARTESIAN_POINT('Ctrl Pts',(0.64917847608371,-1.41359342911686,
6.27742746704519));
#286679=CARTESIAN_POINT('Ctrl Pts',(0.670463164444214,-1.40365344777023,
6.27911275370506));
#286680=CARTESIAN_POINT('Ctrl Pts',(0.682664681716703,-1.39775991037981,
6.28009035503571));
#286681=CARTESIAN_POINT('Ctrl Pts',(0.723900558677622,-1.37717357638062,
6.28343456857516));
#286682=CARTESIAN_POINT('Ctrl Pts',(0.752548418749775,-1.36173039328814,
6.2858269663938));
#286683=CARTESIAN_POINT('Ctrl Pts',(0.822092391067357,-1.32137647037919,
6.29181216249458));
#286684=CARTESIAN_POINT('Ctrl Pts',(0.8623608136677,-1.2954554156237,6.29543678593333));
#286685=CARTESIAN_POINT('Ctrl Pts',(0.978225544185035,-1.21307403237337,
6.30632981229798));
#286686=CARTESIAN_POINT('Ctrl Pts',(1.0499512268174,-1.15155337491335,6.31371105405096));
#286687=CARTESIAN_POINT('Ctrl Pts',(1.14630439332128,-1.05237833928184,
6.32431404357605));
#286688=CARTESIAN_POINT('Ctrl Pts',(1.17559860995362,-1.01955021373039,
6.32764598769831));
#286689=CARTESIAN_POINT('Ctrl Pts',(1.21020919732241,-0.977285661478002,
6.33168047380303));
#286690=CARTESIAN_POINT('Ctrl Pts',(1.21686908622495,-0.968980499864533,
6.33246162700637));
#286691=CARTESIAN_POINT('Ctrl Pts',(1.22725272037933,-0.955755752651247,
6.33368641295464));
#286692=CARTESIAN_POINT('Ctrl Pts',(1.2310332082275,-0.950881455385524,
6.33413381294903));
#286693=CARTESIAN_POINT('Ctrl Pts',(1.23818564166113,-0.941545452995228,
6.33498290087094));
#286694=CARTESIAN_POINT('Ctrl Pts',(1.24156254484114,-0.937088027678857,
6.33538490402003));
#286695=CARTESIAN_POINT('Ctrl Pts',(1.24963916014926,-0.926306802196228,
6.33634931514273));
#286696=CARTESIAN_POINT('Ctrl Pts',(1.25431499805997,-0.919965333614888,
6.33691009243683));
#286697=CARTESIAN_POINT('Ctrl Pts',(1.27062739148011,-0.897486539030024,
6.3388762481788));
#286698=CARTESIAN_POINT('Ctrl Pts',(1.28200292409924,-0.881160969669723,
6.34026526410836));
#286699=CARTESIAN_POINT('Ctrl Pts',(1.30999075605402,-0.839304436537132,
6.34374179873587));
#286700=CARTESIAN_POINT('Ctrl Pts',(1.3261727321144,-0.813494833954837,
6.34580814461137));
#286701=CARTESIAN_POINT('Ctrl Pts',(1.41207755286116,-0.667096016959532,
6.35720222918962));
#286702=CARTESIAN_POINT('Ctrl Pts',(1.46611358120125,-0.53804619447234,
6.36610160924919));
#286703=CARTESIAN_POINT('Ctrl Pts',(1.51096540254233,-0.371069968189813,
6.3778680522512));
#286704=CARTESIAN_POINT('Ctrl Pts',(1.51862798041751,-0.33834619855023,
6.38018166426069));
#286705=CARTESIAN_POINT('Ctrl Pts',(1.52798580398463,-0.291611770038952,
6.383510999614));
#286706=CARTESIAN_POINT('Ctrl Pts',(1.53055982170805,-0.27778526046897,
6.38449903724833));
#286707=CARTESIAN_POINT('Ctrl Pts',(1.53463098715914,-0.254138961044634,
6.38619493638745));
#286708=CARTESIAN_POINT('Ctrl Pts',(1.53622223312982,-0.244336080824954,
6.38689978236669));
#286709=CARTESIAN_POINT('Ctrl Pts',(1.53927634060736,-0.22431056581014,
6.38834363687092));
#286710=CARTESIAN_POINT('Ctrl Pts',(1.54073148577742,-0.214087276413975,
6.38908285116062));
#286711=CARTESIAN_POINT('Ctrl Pts',(1.54412595618445,-0.18840884348777,
6.3909452461585));
#286712=CARTESIAN_POINT('Ctrl Pts',(1.54593508591862,-0.172937960586361,
6.3920724539712));
#286713=CARTESIAN_POINT('Ctrl Pts',(1.55240177881252,-0.109376671855721,
6.39672618905824));
#286714=CARTESIAN_POINT('Ctrl Pts',(1.55504942575179,-0.0611138412537209,
6.40031406956253));
#286715=CARTESIAN_POINT('Ctrl Pts',(1.55619706319746,0.078231641107936,
6.41083300909571));
#286716=CARTESIAN_POINT('Ctrl Pts',(1.54895208455727,0.169155897202332,
6.4179044551809));
#286717=CARTESIAN_POINT('Ctrl Pts',(1.5216212421582,0.331063378447491,6.43062504940875));
#286718=CARTESIAN_POINT('Ctrl Pts',(1.50436476533654,0.402272736222639,
6.43626143208353));
#286719=CARTESIAN_POINT('Ctrl Pts',(1.47871397640773,0.482818715153832,
6.44251551563358));
#286720=CARTESIAN_POINT('Ctrl Pts',(1.47515342250538,0.493590250884616,
6.44334920409742));
#286721=CARTESIAN_POINT('Ctrl Pts',(1.46940479591095,0.510363179346324,
6.44464216588145));
#286722=CARTESIAN_POINT('Ctrl Pts',(1.46729715338321,0.516391418078666,
6.44510579784246));
#286723=CARTESIAN_POINT('Ctrl Pts',(1.46348139463083,0.527093173282791,
6.44592676553356));
#286724=CARTESIAN_POINT('Ctrl Pts',(1.46178795700808,0.531771544571668,
6.44628491972709));
#286725=CARTESIAN_POINT('Ctrl Pts',(1.45761880402742,0.54311902387671,6.44715192629896));
#286726=CARTESIAN_POINT('Ctrl Pts',(1.45511974709323,0.549779391066904,
6.44765939945809));
#286727=CARTESIAN_POINT('Ctrl Pts',(1.44709070011319,0.57073970807169,6.44925267136657));
#286728=CARTESIAN_POINT('Ctrl Pts',(1.44139473368578,0.584975706143436,
6.45032925865656));
#286729=CARTESIAN_POINT('Ctrl Pts',(1.42727863467998,0.618797488116978,
6.45287909081194));
#286730=CARTESIAN_POINT('Ctrl Pts',(1.41866439451288,0.638299354561281,
6.45434290943217));
#286731=CARTESIAN_POINT('Ctrl Pts',(1.38344938703752,0.713785144098534,
6.46000702449176));
#286732=CARTESIAN_POINT('Ctrl Pts',(1.35391175207459,0.768339489650345,
6.46409796101389));
#286733=CARTESIAN_POINT('Ctrl Pts',(1.26294173033783,0.914735046839377,
6.47544856891413));
#286734=CARTESIAN_POINT('Ctrl Pts',(1.19488373283583,1.00200366986148,6.48267785933118));
#286735=CARTESIAN_POINT('Ctrl Pts',(1.10411636862351,1.09586308642367,6.49168086023593));
#286736=CARTESIAN_POINT('Ctrl Pts',(1.08978286835239,1.11011805464705,6.49308553341458));
#286737=CARTESIAN_POINT('Ctrl Pts',(1.06615141036347,1.13272122797636,6.49537757916382));
#286738=CARTESIAN_POINT('Ctrl Pts',(1.05702322604058,1.14124409903041,6.49625740907143));
#286739=CARTESIAN_POINT('Ctrl Pts',(1.04055528899516,1.15625293726304,6.49783561782297));
#286740=CARTESIAN_POINT('Ctrl Pts',(1.03325494969245,1.1627813058819,6.49853215370037));
#286741=CARTESIAN_POINT('Ctrl Pts',(1.01763735108328,1.17648421730729,6.50001606767491));
#286742=CARTESIAN_POINT('Ctrl Pts',(1.00930480794283,1.18364043741981,6.50080415320396));
#286743=CARTESIAN_POINT('Ctrl Pts',(0.986593000568982,1.20273176379965,
6.50294296633643));
#286744=CARTESIAN_POINT('Ctrl Pts',(0.972073723275396,1.21449663007365,
6.5043004666651));
#286745=CARTESIAN_POINT('Ctrl Pts',(0.939406467759112,1.24000557966923,
6.50733462873188));
#286746=CARTESIAN_POINT('Ctrl Pts',(0.921161902605812,1.25361836297864,
6.50901595731434));
#286747=CARTESIAN_POINT('Ctrl Pts',(0.862297848461558,1.29555960697576,
6.51440042743986));
#286748=CARTESIAN_POINT('Ctrl Pts',(0.820624309325186,1.32234911374503,
6.51815464351103));
#286749=CARTESIAN_POINT('Ctrl Pts',(0.741133028161882,1.36824325540462,
6.52519607614092));
#286750=CARTESIAN_POINT('Ctrl Pts',(0.703672843656824,1.38788041956314,
6.52846828671478));
#286751=CARTESIAN_POINT('Ctrl Pts',(0.587665381173473,1.4427881279482,6.5384196612024));
#286752=CARTESIAN_POINT('Ctrl Pts',(0.506940802201569,1.47309266588005,
6.54510772098529));
#286753=CARTESIAN_POINT('Ctrl Pts',(0.409686326087777,1.50065396704992,
6.55263478671519));
#286754=CARTESIAN_POINT('Ctrl Pts',(0.395196675119465,1.50453476088218,
6.55374258475157));
#286755=CARTESIAN_POINT('Ctrl Pts',(0.373815036447922,1.50993122257484,
6.55535515005548));
#286756=CARTESIAN_POINT('Ctrl Pts',(0.366965774705469,1.51161043386029,
6.55586839007227));
#286757=CARTESIAN_POINT('Ctrl Pts',(0.354758378299096,1.51451541753442,
6.5567769554744));
#286758=CARTESIAN_POINT('Ctrl Pts',(0.349404902511015,1.5157594380868,6.55717327619879));
#286759=CARTESIAN_POINT('Ctrl Pts',(0.33754580152315,1.51844904080439,6.55804650678551));
#286760=CARTESIAN_POINT('Ctrl Pts',(0.331037374574748,1.51988121860436,
6.55852266160173));
#286761=CARTESIAN_POINT('Ctrl Pts',(0.311803573228189,1.52398420010299,
6.55992125836218));
#286762=CARTESIAN_POINT('Ctrl Pts',(0.299053300794659,1.52653740958012,
6.56083739751321));
#286763=CARTESIAN_POINT('Ctrl Pts',(0.209158548276875,1.5433690098154,6.56722907994443));
#286764=CARTESIAN_POINT('Ctrl Pts',(0.131051990876703,1.55195489855696,
6.57243730879988));
#286765=CARTESIAN_POINT('Ctrl Pts',(-0.06762881234151,1.55867999008879,
6.58554757648713));
#286766=CARTESIAN_POINT('Ctrl Pts',(-0.187931072268608,1.54878509231677,
6.59338895931649));
#286767=CARTESIAN_POINT('Ctrl Pts',(-0.324949528546164,1.52130407281854,
6.6030355771444));
#286768=CARTESIAN_POINT('Ctrl Pts',(-0.343938707067638,1.51712372151877,
6.60438783855577));
#286769=CARTESIAN_POINT('Ctrl Pts',(-0.374769925576929,1.50972784593649,
6.60661135180177));
#286770=CARTESIAN_POINT('Ctrl Pts',(-0.386661439848873,1.50672611363478,
6.60747579851123));
#286771=CARTESIAN_POINT('Ctrl Pts',(-0.407961925842405,1.50108054819163,
6.60903719294024));
#286772=CARTESIAN_POINT('Ctrl Pts',(-0.417383928199067,1.49848803585847,
6.60973245171103));
#286773=CARTESIAN_POINT('Ctrl Pts',(-0.43747790596324,1.49275486189797,
6.61122537882337));
#286774=CARTESIAN_POINT('Ctrl Pts',(-0.448141814171445,1.48958816402604,
6.61202386028917));
#286775=CARTESIAN_POINT('Ctrl Pts',(-0.47726051154654,1.48060025102701,
6.61422166631972));
#286776=CARTESIAN_POINT('Ctrl Pts',(-0.495641514521877,1.47454878713076,
6.61562841909124));
#286777=CARTESIAN_POINT('Ctrl Pts',(-0.609296137251965,1.43476584402496,
6.62445215960411));
#286778=CARTESIAN_POINT('Ctrl Pts',(-0.701188979346341,1.39216437900338,
6.63216340705928));
#286779=CARTESIAN_POINT('Ctrl Pts',(-0.874252612711406,1.2904288646669,
6.6477065476552));
#286780=CARTESIAN_POINT('Ctrl Pts',(-0.95516678188034,1.23174021493512,
6.65549629929759));
#286781=CARTESIAN_POINT('Ctrl Pts',(-1.04053293827773,1.15631846625218,
6.66396676215639));
#286782=CARTESIAN_POINT('Ctrl Pts',(-1.0510277820373,1.14678761331466,6.66501260687379));
#286783=CARTESIAN_POINT('Ctrl Pts',(-1.0664322061526,1.13240900239201,6.66655260043478));
#286784=CARTESIAN_POINT('Ctrl Pts',(-1.07144185506442,1.12767023331067,
6.66705420733686));
#286785=CARTESIAN_POINT('Ctrl Pts',(-1.08038382572163,1.119098382594,6.6679507080363));
#286786=CARTESIAN_POINT('Ctrl Pts',(-1.08432752013084,1.11527764821498,
6.66834648284114));
#286787=CARTESIAN_POINT('Ctrl Pts',(-1.08832564946389,1.11136292074297,
6.66874812933775));
#286788=CARTESIAN_POINT('Ctrl Pts',(-1.0884001832469,1.11128992706291,6.66875561705156));
#286789=CARTESIAN_POINT('Ctrl Pts',(-1.08854596694684,1.11114712697881,
6.66877026288232));
#286790=CARTESIAN_POINT('Ctrl Pts',(-1.08861721749292,1.11107732121913,
6.66877742104919));
#286791=CARTESIAN_POINT('Ctrl Pts',(-1.08875667137687,1.11094066882643,
6.66879143152402));
#286792=CARTESIAN_POINT('Ctrl Pts',(-1.0888248752721,1.11087382276696,6.66879828387612));
#286793=CARTESIAN_POINT('Ctrl Pts',(-1.08895845027991,1.11074288291457,
6.66881170423066));
#286794=CARTESIAN_POINT('Ctrl Pts',(-1.08902382188681,1.11067878963472,
6.66881827227216));
#286795=CARTESIAN_POINT('Ctrl Pts',(-1.08915192705843,1.11055316734779,
6.66883114354127));
#286796=CARTESIAN_POINT('Ctrl Pts',(-1.08921466106545,1.11049163879851,
6.66883744680381));
#286797=CARTESIAN_POINT('Ctrl Pts',(-1.08933766832161,1.11037097472219,
6.66884980630065));
#286798=CARTESIAN_POINT('Ctrl Pts',(-1.08939794196289,1.11031183960944,
6.6688558625658));
#286799=CARTESIAN_POINT('Ctrl Pts',(-1.08951619020484,1.11019580609909,
6.66886774429265));
#286800=CARTESIAN_POINT('Ctrl Pts',(-1.08957416516664,1.11013890806507,
6.66887356978293));
#286801=CARTESIAN_POINT('Ctrl Pts',(-1.08968796390896,1.11002720571694,
6.6688850047953));
#286802=CARTESIAN_POINT('Ctrl Pts',(-1.08974378801396,1.10997240173115,
6.66889061434301));
#286803=CARTESIAN_POINT('Ctrl Pts',(-1.0898534204975,1.10986475640839,6.6689016310616));
#286804=CARTESIAN_POINT('Ctrl Pts',(-1.08990722916613,1.10981191537079,
6.6689070382553));
#286805=CARTESIAN_POINT('Ctrl Pts',(-1.0900129551008,1.10970807558055,6.66891766274094));
#286806=CARTESIAN_POINT('Ctrl Pts',(-1.09006487262972,1.10965707709861,
6.66892288005357));
#286807=CARTESIAN_POINT('Ctrl Pts',(-1.09016693060908,1.10955681168099,
6.66893313624929));
#286808=CARTESIAN_POINT('Ctrl Pts',(-1.09021707129827,1.10950754499062,
6.66893817515116));
#286809=CARTESIAN_POINT('Ctrl Pts',(-1.09031568091837,1.10941064108924,
6.66894808509454));
#286810=CARTESIAN_POINT('Ctrl Pts',(-1.09036415006567,1.10936300410195,
6.66895295615304));
#286811=CARTESIAN_POINT('Ctrl Pts',(-1.0904595137815,1.10926926538505,6.66896254016237));
#286812=CARTESIAN_POINT('Ctrl Pts',(-1.09050640855141,1.10922316385513,
6.66896725312908));
#286813=CARTESIAN_POINT('Ctrl Pts',(-1.09059871335894,1.10913240890158,
6.66897652997197));
#286814=CARTESIAN_POINT('Ctrl Pts',(-1.09064412357299,1.10908775566756,
6.66898109386188));
#286815=CARTESIAN_POINT('Ctrl Pts',(-1.09073354242938,1.10899981660498,
6.66899008089764));
#286816=CARTESIAN_POINT('Ctrl Pts',(-1.09077755123862,1.10895653094443,
6.66899450405661));
#286817=CARTESIAN_POINT('Ctrl Pts',(-1.0908642444119,1.10887125215194,6.66900321737164));
#286818=CARTESIAN_POINT('Ctrl Pts',(-1.0909069289252,1.10882925917761,6.66900750753934));
#286819=CARTESIAN_POINT('Ctrl Pts',(-1.09099104510587,1.10874649621885,
6.66901596205854));
#286820=CARTESIAN_POINT('Ctrl Pts',(-1.09103247691917,1.10870572637034,
6.6690201264216));
#286821=CARTESIAN_POINT('Ctrl Pts',(-1.09111415430529,1.10862534494907,
6.66902833601719));
#286822=CARTESIAN_POINT('Ctrl Pts',(-1.09115440000655,1.10858573350695,
6.66903238125977));
#286823=CARTESIAN_POINT('Ctrl Pts',(-1.09123376718447,1.10850760862078,
6.66904035883964));
#286824=CARTESIAN_POINT('Ctrl Pts',(-1.09127288877918,1.10846909529735,
6.66904429118615));
#286825=CARTESIAN_POINT('Ctrl Pts',(-1.09135006558836,1.1083931104047,6.66905204878057));
#286826=CARTESIAN_POINT('Ctrl Pts',(-1.09138812090421,1.10835563895416,
6.66905587403622));
#286827=CARTESIAN_POINT('Ctrl Pts',(-1.09146321913879,1.10828168529951,
6.66906342286819));
#286828=CARTESIAN_POINT('Ctrl Pts',(-1.09150026216013,1.10824520319625,
6.66906714645256));
#286829=CARTESIAN_POINT('Ctrl Pts',(-1.09157338629161,1.10817317911278,
6.66907449701031));
#286830=CARTESIAN_POINT('Ctrl Pts',(-1.09160946749354,1.10813763722904,
6.66907812399084));
#286831=CARTESIAN_POINT('Ctrl Pts',(-1.09168071522846,1.10806744760209,
6.6690852860838));
#286832=CARTESIAN_POINT('Ctrl Pts',(-1.09171588185033,1.10803279994453,
6.66908882120322));
#286833=CARTESIAN_POINT('Ctrl Pts',(-1.09178534471715,1.10796435564476,
6.66909580402081));
#286834=CARTESIAN_POINT('Ctrl Pts',(-1.0918196410374,1.10793055908906,6.66909925172475));
#286835=CARTESIAN_POINT('Ctrl Pts',(-1.09188740482526,1.10786377655022,
6.66910606388045));
#286836=CARTESIAN_POINT('Ctrl Pts',(-1.0919208723733,1.10783079063713,6.66910942833863));
#286837=CARTESIAN_POINT('Ctrl Pts',(-1.09198701764736,1.10776559135729,
6.66911607792168));
#286838=CARTESIAN_POINT('Ctrl Pts',(-1.09201969543987,1.10773337806394,
6.66911936305166));
#286839=CARTESIAN_POINT('Ctrl Pts',(-1.09208429787825,1.10766968828154,
6.6691258576608));
#286840=CARTESIAN_POINT('Ctrl Pts',(-1.09211622259116,1.10763821185582,
6.66912906714524));
#286841=CARTESIAN_POINT('Ctrl Pts',(-1.09217935341624,1.10757596213176,
6.66913541393205));
#286842=CARTESIAN_POINT('Ctrl Pts',(-1.09221055958131,1.10754518890197,
6.66913855123838));
#286843=CARTESIAN_POINT('Ctrl Pts',(-1.09227228583246,1.10748431385728,
6.6691447569346));
#286844=CARTESIAN_POINT('Ctrl Pts',(-1.09230280597647,1.10745421209797,
6.66914782532903));
#286845=CARTESIAN_POINT('Ctrl Pts',(-1.09746371224851,1.10236363310358,
6.66966669057766));
#286846=CARTESIAN_POINT('Ctrl Pts',(-1.1025590053112,1.09726743526625,6.67017975877982));
#286847=CARTESIAN_POINT('Ctrl Pts',(-1.11983656254871,1.07974493821374,
6.6719230686367));
#286848=CARTESIAN_POINT('Ctrl Pts',(-1.131846175951,1.06714917334659,6.67314095470289));
#286849=CARTESIAN_POINT('Ctrl Pts',(-1.16121950359434,1.03528834536938,
6.6761434115943));
#286850=CARTESIAN_POINT('Ctrl Pts',(-1.17831805758621,1.01578512041306,
6.67791273848272));
#286851=CARTESIAN_POINT('Ctrl Pts',(-1.2529751205085,0.92620510722277,6.68578611546857));
#286852=CARTESIAN_POINT('Ctrl Pts',(-1.30482965855053,0.851600981969717,
6.69167789013816));
#286853=CARTESIAN_POINT('Ctrl Pts',(-1.39013041861455,0.702620807524076,
6.70302339135113));
#286854=CARTESIAN_POINT('Ctrl Pts',(-1.42481485192995,0.629315990117589,
6.70843894290526));
#286855=CARTESIAN_POINT('Ctrl Pts',(-1.46010886109509,0.536650090761397,
6.71531674934382));
#286856=CARTESIAN_POINT('Ctrl Pts',(-1.4662850396723,0.519537621729463,
6.71658770015387));
#286857=CARTESIAN_POINT('Ctrl Pts',(-1.4756725230675,0.492025608169173,
6.71863448457448));
#286858=CARTESIAN_POINT('Ctrl Pts',(-1.47907739622488,0.481693512081849,
6.71940391419971));
#286859=CARTESIAN_POINT('Ctrl Pts',(-1.48534750426522,0.461973346459717,
6.72087436026123));
#286860=CARTESIAN_POINT('Ctrl Pts',(-1.48823281057048,0.452592172591282,
6.72157467808227));
#286861=CARTESIAN_POINT('Ctrl Pts',(-1.49464083950695,0.431033302250648,
6.72318624572058));
#286862=CARTESIAN_POINT('Ctrl Pts',(-1.49810381557494,0.418838736108049,
6.72409938942112));
#286863=CARTESIAN_POINT('Ctrl Pts',(-1.50503386946227,0.393248937519981,
6.72601937915204));
#286864=CARTESIAN_POINT('Ctrl Pts',(-1.50847202054401,0.379847094819705,
6.72702706863294));
#286865=CARTESIAN_POINT('Ctrl Pts',(-1.51722895557466,0.343716984974257,
6.72975006165938));
#286866=CARTESIAN_POINT('Ctrl Pts',(-1.5222154932883,0.320912691410175,
6.73147549490136));
#286867=CARTESIAN_POINT('Ctrl Pts',(-1.54593999569257,0.199371862087244,
6.74070921023653));
#286868=CARTESIAN_POINT('Ctrl Pts',(-1.55558598292837,0.0991205215353596,
6.74847856869965));
#286869=CARTESIAN_POINT('Ctrl Pts',(-1.55549942258976,-0.00134026972157471,
6.75626805975221));
#286870=CARTESIAN_POINT('',(-1.55549984414273,0.000696327469871839,8.15470034727716));
#286871=CARTESIAN_POINT('Ctrl Pts',(-1.55549942181485,-0.00134116877393629,
6.75626812946259));
#286872=CARTESIAN_POINT('Ctrl Pts',(-1.5554461534246,-0.063122319539924,
6.76105849302685));
#286873=CARTESIAN_POINT('Ctrl Pts',(-1.55171219940939,-0.124851075365541,
6.7658402330438));
#286874=CARTESIAN_POINT('Ctrl Pts',(-1.54162423982075,-0.208519539276235,
6.77220341735004));
#286875=CARTESIAN_POINT('Ctrl Pts',(-1.53844928112679,-0.230780488588829,
6.77388458400084));
#286876=CARTESIAN_POINT('Ctrl Pts',(-1.53357353590428,-0.260362541119816,
6.77609637094553));
#286877=CARTESIAN_POINT('Ctrl Pts',(-1.53230097168609,-0.267750220934243,
6.77664686579246));
#286878=CARTESIAN_POINT('Ctrl Pts',(-1.52999610729815,-0.280575822450825,
6.7775989942437));
#286879=CARTESIAN_POINT('Ctrl Pts',(-1.52898811242992,-0.286017892866135,
6.77800187249552));
#286880=CARTESIAN_POINT('Ctrl Pts',(-1.52691077494489,-0.296908337838535,
6.77880569152405));
#286881=CARTESIAN_POINT('Ctrl Pts',(-1.52584126543406,-0.302356598336974,
6.77920660629134));
#286882=CARTESIAN_POINT('Ctrl Pts',(-1.52349706924055,-0.313969022474034,
6.78005841743401));
#286883=CARTESIAN_POINT('Ctrl Pts',(-1.52221411771467,-0.32013130216559,
6.78050884911209));
#286884=CARTESIAN_POINT('Ctrl Pts',(-1.51859979672911,-0.336978491869008,
6.78173635807546));
#286885=CARTESIAN_POINT('Ctrl Pts',(-1.51619304242764,-0.347647123527009,
6.78250934340579));
#286886=CARTESIAN_POINT('Ctrl Pts',(-1.50178050697461,-0.408536028846398,
6.78690077674055));
#286887=CARTESIAN_POINT('Ctrl Pts',(-1.48739118857214,-0.458164901468319,
6.79040158755986));
#286888=CARTESIAN_POINT('Ctrl Pts',(-1.44623515003946,-0.577540401726483,
6.79883400490558));
#286889=CARTESIAN_POINT('Ctrl Pts',(-1.41686658450207,-0.646249833735386,
6.80370107320709));
#286890=CARTESIAN_POINT('Ctrl Pts',(-1.34588956625881,-0.783971014842977,
6.8139381989304));
#286891=CARTESIAN_POINT('Ctrl Pts',(-1.30363297067819,-0.852389494143139,
6.81930503997048));
#286892=CARTESIAN_POINT('Ctrl Pts',(-1.24530166720978,-0.932282754148224,
6.82615841330256));
#286893=CARTESIAN_POINT('Ctrl Pts',(-1.23404625924128,-0.947131012362532,
6.82745871579829));
#286894=CARTESIAN_POINT('Ctrl Pts',(-1.21564554086568,-0.970520502722886,
6.82955235875172));
#286895=CARTESIAN_POINT('Ctrl Pts',(-1.20867027774878,-0.979193686331489,
6.83033898558679));
#286896=CARTESIAN_POINT('Ctrl Pts',(-1.19539754825953,-0.995339355260532,
6.83182326719274));
#286897=CARTESIAN_POINT('Ctrl Pts',(-1.18912154120859,-1.00282884020603,
6.83252003109609));
#286898=CARTESIAN_POINT('Ctrl Pts',(-1.17481580233906,-1.01957750102682,
6.83409726426136));
#286899=CARTESIAN_POINT('Ctrl Pts',(-1.1667464491589,-1.02880180668721,
6.83497933916206));
#286900=CARTESIAN_POINT('Ctrl Pts',(-1.14561563383917,-1.05238867783107,
6.83727043639612));
#286901=CARTESIAN_POINT('Ctrl Pts',(-1.13239314314989,-1.06660340145885,
6.83868613242321));
#286902=CARTESIAN_POINT('Ctrl Pts',(-1.02081250534313,-1.18214330882122,
6.85049203245228));
#286903=CARTESIAN_POINT('Ctrl Pts',(-0.909356587658479,-1.26987193777603,
6.86149158030753));
#286904=CARTESIAN_POINT('Ctrl Pts',(-0.739278683446118,-1.36974166954489,
6.87672737289926));
#286905=CARTESIAN_POINT('Ctrl Pts',(-0.689414015507849,-1.39550522593221,
6.88102175348416));
#286906=CARTESIAN_POINT('Ctrl Pts',(-0.625480108252798,-1.42427221183914,
6.88623352718092));
#286907=CARTESIAN_POINT('Ctrl Pts',(-0.612620589762229,-1.42985060362415,
6.88726739355208));
#286908=CARTESIAN_POINT('Ctrl Pts',(-0.593352770495425,-1.43790120118648,
6.88879330201121));
#286909=CARTESIAN_POINT('Ctrl Pts',(-0.587001087161837,-1.44050584972729,
6.88929261253773));
#286910=CARTESIAN_POINT('Ctrl Pts',(-0.575538372071205,-1.44511798138018,
6.8901867834907));
#286911=CARTESIAN_POINT('Ctrl Pts',(-0.570433768911676,-1.44714053075377,
6.89058250217757));
#286912=CARTESIAN_POINT('Ctrl Pts',(-0.558952956790455,-1.4516192771095,
6.89146700014445));
#286913=CARTESIAN_POINT('Ctrl Pts',(-0.552571169897768,-1.4540605353574,
6.89195489916148));
#286914=CARTESIAN_POINT('Ctrl Pts',(-0.533204469464826,-1.46132306061495,
6.89342476323711));
#286915=CARTESIAN_POINT('Ctrl Pts',(-0.520170625972542,-1.46601318153408,
6.89439942409662));
#286916=CARTESIAN_POINT('Ctrl Pts',(-0.409268263025892,-1.50425510388419,
6.90258403153818));
#286917=CARTESIAN_POINT('Ctrl Pts',(-0.308325178944143,-1.52814462107105,
6.90933314052739));
#286918=CARTESIAN_POINT('Ctrl Pts',(-0.110563328351952,-1.55453426958151,
6.92247001865898));
#286919=CARTESIAN_POINT('Ctrl Pts',(-0.0144229815356042,-1.55839329633926,
6.92882376640449));
#286920=CARTESIAN_POINT('Ctrl Pts',(0.101786994824133,-1.55229967286303,
6.93686995498935));
#286921=CARTESIAN_POINT('Ctrl Pts',(0.122097436235896,-1.55083429676156,
6.93828908533171));
#286922=CARTESIAN_POINT('Ctrl Pts',(0.153660673008433,-1.54793318575309,
6.94051752941965));
#286923=CARTESIAN_POINT('Ctrl Pts',(0.164936918928933,-1.54677230081224,
6.94131825185264));
#286924=CARTESIAN_POINT('Ctrl Pts',(0.185888506627563,-1.54438363625017,
6.94281506713614));
#286925=CARTESIAN_POINT('Ctrl Pts',(0.195566996028052,-1.54318790007325,
6.94351011855532));
#286926=CARTESIAN_POINT('Ctrl Pts',(0.217103300699262,-1.54032132929337,
6.94506508747444));
#286927=CARTESIAN_POINT('Ctrl Pts',(0.228954240663342,-1.53860442656739,
6.94592641826281));
#286928=CARTESIAN_POINT('Ctrl Pts',(0.259021359296099,-1.53389339806876,
6.94812667599386));
#286929=CARTESIAN_POINT('Ctrl Pts',(0.27720576871111,-1.5307115759328,6.94947141671542));
#286930=CARTESIAN_POINT('Ctrl Pts',(0.42186162728375,-1.50273828642227,
6.96028519078677));
#286931=CARTESIAN_POINT('Ctrl Pts',(0.544839975684998,-1.4626433210855,
6.97025463646216));
#286932=CARTESIAN_POINT('Ctrl Pts',(0.723153844803379,-1.37886851131739,
6.98551999840515));
#286933=CARTESIAN_POINT('Ctrl Pts',(0.78290315444691,-1.34584338039981,
6.99077787995999));
#286934=CARTESIAN_POINT('Ctrl Pts',(0.85318161246795,-1.30072895182504,
6.99699966905268));
#286935=CARTESIAN_POINT('Ctrl Pts',(0.865943926294487,-1.29226770958556,
6.99813095822854));
#286936=CARTESIAN_POINT('Ctrl Pts',(0.88444683298687,-1.27960329672584,
6.99977092028087));
#286937=CARTESIAN_POINT('Ctrl Pts',(0.890286378098173,-1.275547320818,7.00028846548509));
#286938=CARTESIAN_POINT('Ctrl Pts',(0.900164546658569,-1.26858534958289,
7.00116361802363));
#286939=CARTESIAN_POINT('Ctrl Pts',(0.904217298551562,-1.26569983801713,
7.00152256475879));
#286940=CARTESIAN_POINT('Ctrl Pts',(0.913442605078443,-1.2590646008625,
7.00233935437786));
#286941=CARTESIAN_POINT('Ctrl Pts',(0.91860598346655,-1.25530239900733,
7.00279633666392));
#286942=CARTESIAN_POINT('Ctrl Pts',(0.932882436973186,-1.24476485961514,
7.00405984158212));
#286943=CARTESIAN_POINT('Ctrl Pts',(0.941944947884429,-1.23792121392969,
7.00486186928048));
#286944=CARTESIAN_POINT('Ctrl Pts',(1.00960641433873,-1.18565267516654,
7.01085659277416));
#286945=CARTESIAN_POINT('Ctrl Pts',(1.06497373604432,-1.1361828360166,7.01580269717447));
#286946=CARTESIAN_POINT('Ctrl Pts',(1.15701988429581,-1.04127556060515,
7.02453770223003));
#286947=CARTESIAN_POINT('Ctrl Pts',(1.19506866054603,-0.997376911891578,
7.02833733818701));
#286948=CARTESIAN_POINT('Ctrl Pts',(1.2615472873886,-0.911395998857486,
7.03553371262308));
#286949=CARTESIAN_POINT('Ctrl Pts',(1.29054306154434,-0.86985183864208,
7.03891526839405));
#286950=CARTESIAN_POINT('Ctrl Pts',(1.33544449265191,-0.798318612393778,
7.0446653053254));
#286951=CARTESIAN_POINT('Ctrl Pts',(1.35248838172107,-0.769090043153864,
7.04699565563088));
#286952=CARTESIAN_POINT('Ctrl Pts',(1.37509926747398,-0.727235348715366,
7.05032079150911));
#286953=CARTESIAN_POINT('Ctrl Pts',(1.38147270935295,-0.715054109673106,
7.05128711639731));
#286954=CARTESIAN_POINT('Ctrl Pts',(1.39219044984248,-0.693891562426556,
7.05296440412041));
#286955=CARTESIAN_POINT('Ctrl Pts',(1.39661141823699,-0.684949842730259,
7.05367264010257));
#286956=CARTESIAN_POINT('Ctrl Pts',(1.40494274349596,-0.667683102002845,
7.05503970456329));
#286957=CARTESIAN_POINT('Ctrl Pts',(1.40886587335198,-0.659364680123545,
7.05569805382979));
#286958=CARTESIAN_POINT('Ctrl Pts',(1.41901046871758,-0.637350617893801,
7.0574399643089));
#286959=CARTESIAN_POINT('Ctrl Pts',(1.42510729624343,-0.623598977807107,
7.05852773630491));
#286960=CARTESIAN_POINT('Ctrl Pts',(1.44672500392886,-0.572866002357884,
7.06254081203293));
#286961=CARTESIAN_POINT('Ctrl Pts',(1.4610122504768,-0.53537964254208,7.06550665087176));
#286962=CARTESIAN_POINT('Ctrl Pts',(1.50820098166086,-0.395551934121399,
7.07657829489497));
#286963=CARTESIAN_POINT('Ctrl Pts',(1.53191714611827,-0.290440505160677,
7.08494381894474));
#286964=CARTESIAN_POINT('Ctrl Pts',(1.5499660541996,-0.13871442806981,7.0967654060606));
#286965=CARTESIAN_POINT('Ctrl Pts',(1.5533512935746,-0.0934706506448398,
7.10025472282028));
#286966=CARTESIAN_POINT('Ctrl Pts',(1.55530273950125,-0.0304469370594353,
7.10501849250146));
#286967=CARTESIAN_POINT('Ctrl Pts',(1.55554854580069,-0.0127440085792736,
7.10634592338557));
#286968=CARTESIAN_POINT('Ctrl Pts',(1.55544961069072,0.0182822335078583,
7.10864957770304));
#286969=CARTESIAN_POINT('Ctrl Pts',(1.55523598122924,0.0316038878512167,
7.10963131904691));
#286970=CARTESIAN_POINT('Ctrl Pts',(1.55465690701263,0.0516470650495497,
7.11109573057003));
#286971=CARTESIAN_POINT('Ctrl Pts',(1.55441896580523,0.0583712354638141,
7.1115848688986));
#286972=CARTESIAN_POINT('Ctrl Pts',(1.55390753036541,0.0705819334814889,
7.11246896045836));
#286973=CARTESIAN_POINT('Ctrl Pts',(1.55364860129789,0.0760687070226881,
7.11286467031391));
#286974=CARTESIAN_POINT('Ctrl Pts',(1.55299481536975,0.0885213367051223,
7.11375930351815));
#286975=CARTESIAN_POINT('Ctrl Pts',(1.5525821546926,0.0954860279716213,
7.1142572415791));
#286976=CARTESIAN_POINT('Ctrl Pts',(1.55116111292197,0.117015326536737,
7.11578962725523));
#286977=CARTESIAN_POINT('Ctrl Pts',(1.54999450654879,0.131569202084861,
7.11681583215761));
#286978=CARTESIAN_POINT('Ctrl Pts',(1.53974108027983,0.240249081211163,
7.12442100428678));
#286979=CARTESIAN_POINT('Ctrl Pts',(1.52229140561027,0.333400992599896,
7.13062182459849));
#286980=CARTESIAN_POINT('Ctrl Pts',(1.46738249672422,0.527015586073728,
7.14386785359154));
#286981=CARTESIAN_POINT('Ctrl Pts',(1.42780875150913,0.626350462337095,
7.15089630805442));
#286982=CARTESIAN_POINT('Ctrl Pts',(1.36970155750898,0.737461390088812,
7.15958611006952));
#286983=CARTESIAN_POINT('Ctrl Pts',(1.36071510038732,0.753913802449323,
7.16089490724103));
#286984=CARTESIAN_POINT('Ctrl Pts',(1.34598909408515,0.779752862347507,
7.16298811388938));
#286985=CARTESIAN_POINT('Ctrl Pts',(1.3404433191501,0.789248290915252,7.16376558695342));
#286986=CARTESIAN_POINT('Ctrl Pts',(1.32977000644003,0.807086024440945,
7.16524227182624));
#286987=CARTESIAN_POINT('Ctrl Pts',(1.32466343817452,0.815440303385207,
7.1659406936499));
#286988=CARTESIAN_POINT('Ctrl Pts',(1.31287620534347,0.834321131196367,
7.16753505349304));
#286989=CARTESIAN_POINT('Ctrl Pts',(1.30614724688797,0.844816567760487,
7.16843274181945));
#286990=CARTESIAN_POINT('Ctrl Pts',(1.2882195287874,0.872052945351897,7.17079300903609));
#286991=CARTESIAN_POINT('Ctrl Pts',(1.27682083104916,0.888658758411981,
7.1722629524625));
#286992=CARTESIAN_POINT('Ctrl Pts',(1.17454986339862,1.0316178025739,7.18519621331196));
#286993=CARTESIAN_POINT('Ctrl Pts',(1.06552141325516,1.14387302927968,7.19741501249752));
#286994=CARTESIAN_POINT('Ctrl Pts',(0.91678408692183,1.25700729940031,7.21176019804354));
#286995=CARTESIAN_POINT('Ctrl Pts',(0.891297579510339,1.27520558687315,
7.21414430629795));
#286996=CARTESIAN_POINT('Ctrl Pts',(0.848418544825087,1.30390866680067,
7.21801628748301));
#286997=CARTESIAN_POINT('Ctrl Pts',(0.831339228286008,1.31486388221512,
7.2195238040548));
#286998=CARTESIAN_POINT('Ctrl Pts',(0.807285267109387,1.32963670194696,
7.22159416573021));
#286999=CARTESIAN_POINT('Ctrl Pts',(0.800489201953259,1.33373921981135,
7.22217337559145));
#287000=CARTESIAN_POINT('Ctrl Pts',(0.788844012330722,1.34064788634173,
7.22315573553395));
#287001=CARTESIAN_POINT('Ctrl Pts',(0.784010655969847,1.34348015489775,
7.22356051666608));
#287002=CARTESIAN_POINT('Ctrl Pts',(0.773845011574412,1.34936351149828,
7.2244055706674));
#287003=CARTESIAN_POINT('Ctrl Pts',(0.768509819067769,1.35240920197694,
7.22484550841922));
#287004=CARTESIAN_POINT('Ctrl Pts',(0.753981903448509,1.3605889897133,7.22603421809655));
#287005=CARTESIAN_POINT('Ctrl Pts',(0.744754662762928,1.36566160448789,
7.22677922900553));
#287006=CARTESIAN_POINT('Ctrl Pts',(0.698107372090106,1.39069222419757,
7.23049932084285));
#287007=CARTESIAN_POINT('Ctrl Pts',(0.659930055083606,1.40920964891525,
7.23339576843256));
#287008=CARTESIAN_POINT('Ctrl Pts',(0.545944016999929,1.45884685987556,
7.24175640378814));
#287009=CARTESIAN_POINT('Ctrl Pts',(0.468378955896553,1.48556777449472,
7.24709229992554));
#287010=CARTESIAN_POINT('Ctrl Pts',(0.334221626280769,1.52022527930509,
7.25624034812825));
#287011=CARTESIAN_POINT('Ctrl Pts',(0.278647292390724,1.5313862766584,7.26000631870906));
#287012=CARTESIAN_POINT('Ctrl Pts',(0.186483670670424,1.54471197640523,
7.26633022502652));
#287013=CARTESIAN_POINT('Ctrl Pts',(0.150206402729706,1.54866036859675,
7.26883858345569));
#287014=CARTESIAN_POINT('Ctrl Pts',(0.0997294027288756,1.55236403055502,
7.2723735322636));
#287015=CARTESIAN_POINT('Ctrl Pts',(0.0856196713792035,1.5532061311441,
7.27336642884897));
#287016=CARTESIAN_POINT('Ctrl Pts',(0.0614677129091435,1.5543174858183,
7.27507514200355));
#287017=CARTESIAN_POINT('Ctrl Pts',(0.0514305857802329,1.55468196512904,
7.27578794969664));
#287018=CARTESIAN_POINT('Ctrl Pts',(0.0322759468910776,1.55519183815218,
7.27715372660993));
#287019=CARTESIAN_POINT('Ctrl Pts',(0.023159276908928,1.55535431061846,
7.27780613172199));
#287020=CARTESIAN_POINT('Ctrl Pts',(-0.000553231564165983,1.55556837799962,
7.27950946372619));
#287021=CARTESIAN_POINT('Ctrl Pts',(-0.0151489966573689,1.55549470125027,
7.28056425039159));
#287022=CARTESIAN_POINT('Ctrl Pts',(-0.0667810235600491,1.55450731797242,
7.28431912917103));
#287023=CARTESIAN_POINT('Ctrl Pts',(-0.103780676694103,1.55247603922006,
7.28705326288367));
#287024=CARTESIAN_POINT('Ctrl Pts',(-0.261313325322442,1.53817114189868,
7.29888731682209));
#287025=CARTESIAN_POINT('Ctrl Pts',(-0.380251889264255,1.5131607554368,
7.30835074828367));
#287026=CARTESIAN_POINT('Ctrl Pts',(-0.531991375132014,1.46221852397795,
7.32070051715428));
#287027=CARTESIAN_POINT('Ctrl Pts',(-0.568445691944159,1.44843630701681,
7.32368542879435));
#287028=CARTESIAN_POINT('Ctrl Pts',(-0.626082748846818,1.42413381267385,
7.32839824742832));
#287029=CARTESIAN_POINT('Ctrl Pts',(-0.647609502019456,1.41447474822365,
7.33015681355987));
#287030=CARTESIAN_POINT('Ctrl Pts',(-0.676495098052812,1.400715969086,7.33250666972219));
#287031=CARTESIAN_POINT('Ctrl Pts',(-0.684051391025945,1.39704135468515,
7.3331204407238));
#287032=CARTESIAN_POINT('Ctrl Pts',(-0.696671307009299,1.39077736394873,
7.33414348733103));
#287033=CARTESIAN_POINT('Ctrl Pts',(-0.701751099595855,1.3882211583261,
7.33455472875851));
#287034=CARTESIAN_POINT('Ctrl Pts',(-0.712140880833589,1.38292130492553,
7.33539454117485));
#287035=CARTESIAN_POINT('Ctrl Pts',(-0.717449253388401,1.38017482291993,
7.33582293299826));
#287036=CARTESIAN_POINT('Ctrl Pts',(-0.731390111351289,1.37285984033884,
7.33694651467597));
#287037=CARTESIAN_POINT('Ctrl Pts',(-0.739995802063121,1.36824042553676,
7.33763861543021));
#287038=CARTESIAN_POINT('Ctrl Pts',(-0.777589174214755,1.34760237597381,
7.3406580269201));
#287039=CARTESIAN_POINT('Ctrl Pts',(-0.806106843720715,1.33074010629666,
7.34293806361482));
#287040=CARTESIAN_POINT('Ctrl Pts',(-0.908793134003266,1.26550887248818,
7.3511919498657));
#287041=CARTESIAN_POINT('Ctrl Pts',(-0.979336279307801,1.21174277756471,
7.35695674714405));
#287042=CARTESIAN_POINT('Ctrl Pts',(-1.09996902735297,1.10234735628645,
7.36769784063798));
#287043=CARTESIAN_POINT('Ctrl Pts',(-1.15135916420681,1.04855705397842,
7.37263716354117));
#287044=CARTESIAN_POINT('Ctrl Pts',(-1.21584980242207,0.970573639225771,
7.37957716228632));
#287045=CARTESIAN_POINT('Ctrl Pts',(-1.23245212984931,0.949402723122586,
7.38144054469549));
#287046=CARTESIAN_POINT('Ctrl Pts',(-1.2560153264828,0.917695294021819,
7.3842086761662));
#287047=CARTESIAN_POINT('Ctrl Pts',(-1.26341079399149,0.907486805436926,
7.38509656130911));
#287048=CARTESIAN_POINT('Ctrl Pts',(-1.27633744167304,0.889178920574204,
7.38668370151301));
#287049=CARTESIAN_POINT('Ctrl Pts',(-1.28191769549825,0.88111487998841,
7.38738103280793));
#287050=CARTESIAN_POINT('Ctrl Pts',(-1.29354818165743,0.863963270014136,
7.38886084856189));
#287051=CARTESIAN_POINT('Ctrl Pts',(-1.29957971122609,0.854863727807574,
7.38964398898473));
#287052=CARTESIAN_POINT('Ctrl Pts',(-1.31550366685818,0.830281820279892,
7.39175485965898));
#287053=CARTESIAN_POINT('Ctrl Pts',(-1.3252181205689,0.814686858752893,
7.39308906109718));
#287054=CARTESIAN_POINT('Ctrl Pts',(-1.38112082003019,0.721297830649551,
7.40105319270122));
#287055=CARTESIAN_POINT('Ctrl Pts',(-1.42071875397584,0.639779763202748,
7.4079164272815));
#287056=CARTESIAN_POINT('Ctrl Pts',(-1.47619111437831,0.494629401103293,
7.41991277673608));
#287057=CARTESIAN_POINT('Ctrl Pts',(-1.4955541711107,0.432569230404838,
7.42497258904737));
#287058=CARTESIAN_POINT('Ctrl Pts',(-1.51945786923799,0.334815686785833,
7.43272222755207));
#287059=CARTESIAN_POINT('Ctrl Pts',(-1.52673963748886,0.299866931441088,
7.4354498277595));
#287060=CARTESIAN_POINT('Ctrl Pts',(-1.53659501046379,0.242796113886426,
7.43980635398641));
#287061=CARTESIAN_POINT('Ctrl Pts',(-1.53990737905204,0.220815704077361,
7.44146099457647));
#287062=CARTESIAN_POINT('Ctrl Pts',(-1.54379780838238,0.190620313889035,
7.4436958183619));
#287063=CARTESIAN_POINT('Ctrl Pts',(-1.54478331648398,0.182461750367341,
7.4442958443289));
#287064=CARTESIAN_POINT('Ctrl Pts',(-1.54633739006574,0.168679766933739,
7.44530260772742));
#287065=CARTESIAN_POINT('Ctrl Pts',(-1.54694003935443,0.163060438509517,
7.44571117722064));
#287066=CARTESIAN_POINT('Ctrl Pts',(-1.54812309547542,0.151431755106252,
7.44655255939499));
#287067=CARTESIAN_POINT('Ctrl Pts',(-1.54869916490068,0.145422127491667,
7.44698513435231));
#287068=CARTESIAN_POINT('Ctrl Pts',(-1.55014029299135,0.129407013327003,
7.44813229750346));
#287069=CARTESIAN_POINT('Ctrl Pts',(-1.55094348823809,0.119396035769288,
7.44884355931561));
#287070=CARTESIAN_POINT('Ctrl Pts',(-1.55419254797389,0.0733043232473564,
7.45209444553764));
#287071=CARTESIAN_POINT('Ctrl Pts',(-1.55547689677781,0.03714985694327,
7.45457737297868));
#287072=CARTESIAN_POINT('Ctrl Pts',(-1.5555513709279,-0.0810240234271968,
7.46257013240316));
#287073=CARTESIAN_POINT('Ctrl Pts',(-1.54911823340247,-0.162909520585166,
7.46792058479099));
#287074=CARTESIAN_POINT('Ctrl Pts',(-1.52192293400986,-0.334197663141845,
7.47935317486277));
#287075=CARTESIAN_POINT('Ctrl Pts',(-1.49965905356957,-0.423032999341945,
7.48543149064005));
#287076=CARTESIAN_POINT('Ctrl Pts',(-1.46371375611712,-0.526744266357612,
7.49304283651953));
#287077=CARTESIAN_POINT('Ctrl Pts',(-1.45739341552974,-0.543987007957729,
7.49432552451019));
#287078=CARTESIAN_POINT('Ctrl Pts',(-1.44683212535322,-0.571293437162566,
7.49638670543128));
#287079=CARTESIAN_POINT('Ctrl Pts',(-1.44278777097378,-0.581431704756804,
7.49715863115549));
#287080=CARTESIAN_POINT('Ctrl Pts',(-1.43490777296516,-0.600596460508967,
7.49863096473053));
#287081=CARTESIAN_POINT('Ctrl Pts',(-1.43109278785405,-0.609630912723666,
7.49933064529748));
#287082=CARTESIAN_POINT('Ctrl Pts',(-1.42217806111985,-0.630197428803772,
7.50093663195371));
#287083=CARTESIAN_POINT('Ctrl Pts',(-1.41702307255711,-0.641704629294601,
7.5018447855074));
#287084=CARTESIAN_POINT('Ctrl Pts',(-1.40042535175481,-0.677579342446644,
7.50470699906612));
#287085=CARTESIAN_POINT('Ctrl Pts',(-1.38849017358543,-0.70171205067251,
7.5066777683561));
#287086=CARTESIAN_POINT('Ctrl Pts',(-1.34103754593463,-0.791704899204001,
7.51420521668325));
#287087=CARTESIAN_POINT('Ctrl Pts',(-1.30141481402088,-0.855274793738121,
7.51989834770173));
#287088=CARTESIAN_POINT('Ctrl Pts',(-1.20475689529122,-0.987993235384248,
7.53256831975693));
#287089=CARTESIAN_POINT('Ctrl Pts',(-1.1460051573368,-1.05557690613899,
7.5395589441975));
#287090=CARTESIAN_POINT('Ctrl Pts',(-1.05880874894783,-1.13996738602274,
7.54878307542085));
#287091=CARTESIAN_POINT('Ctrl Pts',(-1.03516251649051,-1.16148203738401,
7.55118395917232));
#287092=CARTESIAN_POINT('Ctrl Pts',(-1.00353337876584,-1.18852603655466,
7.55425033113436));
#287093=CARTESIAN_POINT('Ctrl Pts',(-0.996140091383027,-1.19472938896165,
7.55495719813143));
#287094=CARTESIAN_POINT('Ctrl Pts',(-0.984094901973606,-1.20464637581517,
7.55609230597254));
#287095=CARTESIAN_POINT('Ctrl Pts',(-0.979478727972305,-1.20840270254495,
7.55652346566215));
#287096=CARTESIAN_POINT('Ctrl Pts',(-0.970396769641774,-1.21570674330437,
7.55736403231715));
#287097=CARTESIAN_POINT('Ctrl Pts',(-0.965932861434693,-1.21925652966422,
7.55777357082743));
#287098=CARTESIAN_POINT('Ctrl Pts',(-0.954778355079439,-1.22802710076918,
7.55878826695374));
#287099=CARTESIAN_POINT('Ctrl Pts',(-0.948064229904457,-1.23321794189664,
7.55939135704702));
#287100=CARTESIAN_POINT('Ctrl Pts',(-0.922011138562466,-1.25302163480796,
7.56170362067648));
#287101=CARTESIAN_POINT('Ctrl Pts',(-0.902372933958467,-1.26723755121632,
7.56338784598552));
#287102=CARTESIAN_POINT('Ctrl Pts',(-0.849001025717572,-1.30400276616839,
7.56783471311015));
#287103=CARTESIAN_POINT('Ctrl Pts',(-0.814702932386624,-1.32570191464811,
7.57055815280981));
#287104=CARTESIAN_POINT('Ctrl Pts',(-0.662687990100577,-1.41374545896751,
7.58223612868556));
#287105=CARTESIAN_POINT('Ctrl Pts',(-0.537469250331609,-1.46593227017965,
7.59092905023762));
#287106=CARTESIAN_POINT('Ctrl Pts',(-0.381882709023447,-1.50812056240722,
7.60199460211515));
#287107=CARTESIAN_POINT('Ctrl Pts',(-0.356515026886978,-1.51431797641573,
7.60380447243743));
#287108=CARTESIAN_POINT('Ctrl Pts',(-0.318827794595403,-1.52252566310758,
7.60650810347402));
#287109=CARTESIAN_POINT('Ctrl Pts',(-0.306619877987969,-1.52503107895591,
7.60738613661701));
#287110=CARTESIAN_POINT('Ctrl Pts',(-0.284769565861887,-1.52924242853323,
7.60896236440718));
#287111=CARTESIAN_POINT('Ctrl Pts',(-0.275138572552282,-1.53100452930566,
7.60965873409149));
#287112=CARTESIAN_POINT('Ctrl Pts',(-0.2546539793997,-1.53455289357511,
7.61114361740713));
#287113=CARTESIAN_POINT('Ctrl Pts',(-0.243796832459268,-1.53631517774726,
7.61193285029291));
#287114=CARTESIAN_POINT('Ctrl Pts',(-0.214373890643901,-1.5407712401609,
7.61407815630462));
#287115=CARTESIAN_POINT('Ctrl Pts',(-0.195777108267731,-1.5432444544636,
7.61544107303951));
#287116=CARTESIAN_POINT('Ctrl Pts',(-0.154413535732602,-1.5479857973929,
7.61848928410685));
#287117=CARTESIAN_POINT('Ctrl Pts',(-0.131632635095191,-1.55008913241173,
7.62017931283));
#287118=CARTESIAN_POINT('Ctrl Pts',(-0.0590287607748288,-1.55518059515145,
7.62560235588266));
#287119=CARTESIAN_POINT('Ctrl Pts',(-0.00910832029281636,-1.55627351729704,
7.62938727075242));
#287120=CARTESIAN_POINT('Ctrl Pts',(0.0929951525243039,-1.55359616997825,
7.63722483980242));
#287121=CARTESIAN_POINT('Ctrl Pts',(0.145112248932143,-1.54959711217791,
7.64127699848221));
#287122=CARTESIAN_POINT('Ctrl Pts',(0.212169227030735,-1.54103879626259,
7.64651840754183));
#287123=CARTESIAN_POINT('Ctrl Pts',(0.227381658070818,-1.53886774617074,
7.64770919577214));
#287124=CARTESIAN_POINT('Ctrl Pts',(0.307615593882776,-1.52620138516531,
7.65399313510563));
#287125=CARTESIAN_POINT('Ctrl Pts',(0.371961783305136,-1.51180835518359,
7.65904759351741));
#287126=CARTESIAN_POINT('Ctrl Pts',(0.446058225091606,-1.49021476074776,
7.66475716154708));
#287127=CARTESIAN_POINT('Ctrl Pts',(0.456873985479725,-1.48693448223988,
7.66558766799229));
#287128=CARTESIAN_POINT('Ctrl Pts',(0.473734796253627,-1.48161946890251,
7.66687677917958));
#287129=CARTESIAN_POINT('Ctrl Pts',(0.479804450955065,-1.47966502984727,
7.66733970255103));
#287130=CARTESIAN_POINT('Ctrl Pts',(0.490590236162439,-1.47611864114055,
7.6681600769714));
#287131=CARTESIAN_POINT('Ctrl Pts',(0.49531081325639,-1.47454135985071,
7.66851833917315));
#287132=CARTESIAN_POINT('Ctrl Pts',(0.506773444915998,-1.47065010491476,
7.66938645968036));
#287133=CARTESIAN_POINT('Ctrl Pts',(0.513507283768295,-1.46831240898391,
7.66989492897863));
#287134=CARTESIAN_POINT('Ctrl Pts',(0.534747093206801,-1.460774878972,7.67149465106212));
#287135=CARTESIAN_POINT('Ctrl Pts',(0.549192535884902,-1.45540554701198,
7.67257658656303));
#287136=CARTESIAN_POINT('Ctrl Pts',(0.583559429438671,-1.44204688353981,
7.6751415364512));
#287137=CARTESIAN_POINT('Ctrl Pts',(0.603400397423282,-1.43385804113288,
7.67661497406404));
#287138=CARTESIAN_POINT('Ctrl Pts',(0.68054152992792,-1.40013504638731,
7.68233851202091));
#287139=CARTESIAN_POINT('Ctrl Pts',(0.736448527313433,-1.37155374683397,
7.68647688210462));
#287140=CARTESIAN_POINT('Ctrl Pts',(0.884582049499695,-1.28414682087576,
7.69780258632168));
#287141=CARTESIAN_POINT('Ctrl Pts',(0.972560631730535,-1.21886864259515,
7.70496338385475));
#287142=CARTESIAN_POINT('Ctrl Pts',(1.06788731059356,-1.13119744487014,
7.71389284280486));
#287143=CARTESIAN_POINT('Ctrl Pts',(1.08253394429636,-1.1171889554314,7.71530105289325));
#287144=CARTESIAN_POINT('Ctrl Pts',(1.1057674805973,-1.09408174472268,7.71759771759689));
#287145=CARTESIAN_POINT('Ctrl Pts',(1.1145259252083,-1.08515829771355,7.71847857854332));
#287146=CARTESIAN_POINT('Ctrl Pts',(1.1299521531551,-1.06905768187899,7.72005792593536));
#287147=CARTESIAN_POINT('Ctrl Pts',(1.13666158080587,-1.06192120155306,
7.72075455908065));
#287148=CARTESIAN_POINT('Ctrl Pts',(1.15074467697954,-1.04665533360013,
7.72223792615393));
#287149=CARTESIAN_POINT('Ctrl Pts',(1.15810056914642,-1.03851035587509,
7.72302536078774));
#287150=CARTESIAN_POINT('Ctrl Pts',(1.177719257509,-1.01631946203229,7.72516049224144));
#287151=CARTESIAN_POINT('Ctrl Pts',(1.18981634614515,-1.00213018353396,
7.72651492173042));
#287152=CARTESIAN_POINT('Ctrl Pts',(1.26926309661583,-0.905476410857493,
7.73567349159042));
#287153=CARTESIAN_POINT('Ctrl Pts',(1.32823469294344,-0.816517360817221,
7.7438092111462));
#287154=CARTESIAN_POINT('Ctrl Pts',(1.42178126464292,-0.638083298918485,
7.75941790586602));
#287155=CARTESIAN_POINT('Ctrl Pts',(1.45810601545017,-0.550038393187028,
7.76682888831033));
#287156=CARTESIAN_POINT('Ctrl Pts',(1.49046192045692,-0.44532577921856,
7.7749836965357));
#287157=CARTESIAN_POINT('Ctrl Pts',(1.49456084870292,-0.431369558442356,
7.77605728670087));
#287158=CARTESIAN_POINT('Ctrl Pts',(1.50033272054773,-0.410646448948991,
7.77762983851331));
#287159=CARTESIAN_POINT('Ctrl Pts',(1.5021567811821,-0.403922997776245,
7.77813670561533));
#287160=CARTESIAN_POINT('Ctrl Pts',(1.50533814549645,-0.391876875812767,
7.77903860995055));
#287161=CARTESIAN_POINT('Ctrl Pts',(1.50671249092974,-0.386559039042714,
7.77943458006285));
#287162=CARTESIAN_POINT('Ctrl Pts',(1.50970996293511,-0.374701841867542,
7.78031263245902));
#287163=CARTESIAN_POINT('Ctrl Pts',(1.51131880057658,-0.368159109667949,
7.78079390475368));
#287164=CARTESIAN_POINT('Ctrl Pts',(1.51599291411936,-0.348603578420759,
7.78222332123121));
#287165=CARTESIAN_POINT('Ctrl Pts',(1.51893309825835,-0.335561089913032,
7.78316473841743));
#287166=CARTESIAN_POINT('Ctrl Pts',(1.53845080418241,-0.243462269281697,
7.7897393407578));
#287167=CARTESIAN_POINT('Ctrl Pts',(1.54901867961024,-0.163246841870398,
7.79509104627263));
#287168=CARTESIAN_POINT('Ctrl Pts',(1.55950571733998,0.0340502686216471,
7.80811324795337));
#287169=CARTESIAN_POINT('Ctrl Pts',(1.55255264310236,0.150977429643399,
7.81573728681553));
#287170=CARTESIAN_POINT('Ctrl Pts',(1.52920179332225,0.285505201450163,
7.82515788400288));
#287171=CARTESIAN_POINT('Ctrl Pts',(1.52544855874996,0.304922906700598,
7.82653279637999));
#287172=CARTESIAN_POINT('Ctrl Pts',(1.51874938263034,0.336353045303748,
7.82878594711245));
#287173=CARTESIAN_POINT('Ctrl Pts',(1.51602850376104,0.348411564697607,
7.82965706579577));
#287174=CARTESIAN_POINT('Ctrl Pts',(1.51089786303221,0.369950757964319,
7.83122571118637));
#287175=CARTESIAN_POINT('Ctrl Pts',(1.50854181984313,0.379443652777201,
7.83192148216959));
#287176=CARTESIAN_POINT('Ctrl Pts',(1.5033309345747,0.399623193459529,7.83341029611257));
#287177=CARTESIAN_POINT('Ctrl Pts',(1.50045132583116,0.410302818299376,
7.83420410507415));
#287178=CARTESIAN_POINT('Ctrl Pts',(1.49230236339194,0.439291328708979,
7.83637534902949));
#287179=CARTESIAN_POINT('Ctrl Pts',(1.48681029719465,0.457535021158104,
7.83775991389872));
#287180=CARTESIAN_POINT('Ctrl Pts',(1.44877234586852,0.575964455032252,
7.8468707477336));
#287181=CARTESIAN_POINT('Ctrl Pts',(1.40646200060367,0.672705693894223,
7.85491989568598));
#287182=CARTESIAN_POINT('Ctrl Pts',(1.30778304293573,0.847587322118531,
7.87047604210372));
#287183=CARTESIAN_POINT('Ctrl Pts',(1.25328731124673,0.926269299289943,
7.87792447945845));
#287184=CARTESIAN_POINT('Ctrl Pts',(1.18260211194869,1.01056544755285,7.88610926774412));
#287185=CARTESIAN_POINT('Ctrl Pts',(1.17313508720526,1.02154020292545,7.88717895359027));
#287186=CARTESIAN_POINT('Ctrl Pts',(1.15889869909463,1.03758491031854,7.88874692947949));
#287187=CARTESIAN_POINT('Ctrl Pts',(1.15424681022674,1.0427573768373,7.88925306132998));
#287188=CARTESIAN_POINT('Ctrl Pts',(1.14586027631459,1.05195752860724,7.89015420499997));
#287189=CARTESIAN_POINT('Ctrl Pts',(1.14213884291817,1.05599681874827,7.89055014246653));
#287190=CARTESIAN_POINT('Ctrl Pts',(1.1337985691925,1.06495378605565,7.89142878577568));
#287191=CARTESIAN_POINT('Ctrl Pts',(1.12916905785518,1.06986120840961,7.89191067504753));
#287192=CARTESIAN_POINT('Ctrl Pts',(1.11524012903284,1.0844351604403,7.8933438311839));
#287193=CARTESIAN_POINT('Ctrl Pts',(1.10584716269768,1.09401199589192,7.89428831866406));
#287194=CARTESIAN_POINT('Ctrl Pts',(1.03599564171551,1.16341182818986,7.9011641271682));
#287195=CARTESIAN_POINT('Ctrl Pts',(0.970836239312873,1.21831653324784,
7.90678287780732));
#287196=CARTESIAN_POINT('Ctrl Pts',(0.810435518104754,1.33238994065278,
7.91974692427541));
#287197=CARTESIAN_POINT('Ctrl Pts',(0.712662931901051,1.38714695490054,
7.92706141074413));
#287198=CARTESIAN_POINT('Ctrl Pts',(0.591346288453293,1.43885212137053,
7.93615545534466));
#287199=CARTESIAN_POINT('Ctrl Pts',(0.572668214387081,1.44638753890662,
7.93755507885279));
#287200=CARTESIAN_POINT('Ctrl Pts',(0.542199911901414,1.45799688965956,
7.93984052878458));
#287201=CARTESIAN_POINT('Ctrl Pts',(0.53049737390352,1.46229552242961,7.94071888509545));
#287202=CARTESIAN_POINT('Ctrl Pts',(0.509513904668546,1.46971823876505,
7.94229546886922));
#287203=CARTESIAN_POINT('Ctrl Pts',(0.500252654652554,1.47289626040478,
7.94299186813151));
#287204=CARTESIAN_POINT('Ctrl Pts',(0.480527921212848,1.47945736257899,
7.94447657556078));
#287205=CARTESIAN_POINT('Ctrl Pts',(0.470057377665715,1.48281732555132,
7.94526560084619));
#287206=CARTESIAN_POINT('Ctrl Pts',(0.441642575568518,1.49160434402932,
7.94740973175514));
#287207=CARTESIAN_POINT('Ctrl Pts',(0.423634920188506,1.49681831932147,
7.94877166813593));
#287208=CARTESIAN_POINT('Ctrl Pts',(0.302521331243627,1.52952525422715,
7.95795630718059));
#287209=CARTESIAN_POINT('Ctrl Pts',(0.196935323411867,1.54666569120924,
7.96611192945075));
#287210=CARTESIAN_POINT('Ctrl Pts',(-0.00390681945205614,1.55836388938543,
7.98169933301478));
#287211=CARTESIAN_POINT('Ctrl Pts',(-0.0985739899200065,1.55524903061796,
7.98906823861353));
#287212=CARTESIAN_POINT('Ctrl Pts',(-0.206875574613135,1.54175100192689,
7.99718983681705));
#287213=CARTESIAN_POINT('Ctrl Pts',(-0.221346353541598,1.53974007158688,
7.99826825123573));
#287214=CARTESIAN_POINT('Ctrl Pts',(-0.242685096764264,1.5364676670645,
7.99984645460042));
#287215=CARTESIAN_POINT('Ctrl Pts',(-0.249575844972282,1.53536342628076,
8.00035422795687));
#287216=CARTESIAN_POINT('Ctrl Pts',(-0.261876878809404,1.53330718474823,
8.00125707217658));
#287217=CARTESIAN_POINT('Ctrl Pts',(-0.267289795028401,1.53237286287216,
8.00165308482519));
#287218=CARTESIAN_POINT('Ctrl Pts',(-0.279320346272054,1.53023058430116,
8.00253041906046));
#287219=CARTESIAN_POINT('Ctrl Pts',(-0.28593520371646,1.52900835862683,
8.00301093869851));
#287220=CARTESIAN_POINT('Ctrl Pts',(-0.305618946486915,1.52523918910693,
8.00443580022308));
#287221=CARTESIAN_POINT('Ctrl Pts',(-0.31866369107744,1.52256724238022,
8.00537347865366));
#287222=CARTESIAN_POINT('Ctrl Pts',(-0.348955226882635,1.51595626523493,
8.00753893098474));
#287223=CARTESIAN_POINT('Ctrl Pts',(-0.366172609857623,1.51188982013678,
8.00876066864415));
#287224=CARTESIAN_POINT('Ctrl Pts',(-0.427210254618112,1.49636986165555,
8.01307169110106));
#287225=CARTESIAN_POINT('Ctrl Pts',(-0.470597868001205,1.48329687655853,
8.0160991524277));
#287226=CARTESIAN_POINT('Ctrl Pts',(-0.614607642109122,1.43294894634925,
8.02620787291912));
#287227=CARTESIAN_POINT('Ctrl Pts',(-0.711921568214003,1.38717418581404,
8.03316094890744));
#287228=CARTESIAN_POINT('Ctrl Pts',(-0.838274930346336,1.31091624865259,
8.0431425903796));
#287229=CARTESIAN_POINT('Ctrl Pts',(-0.871972577936714,1.28874731296504,
8.04590556222786));
#287230=CARTESIAN_POINT('Ctrl Pts',(-0.917029715459742,1.25652853007427,
8.04976740445225));
#287231=CARTESIAN_POINT('Ctrl Pts',(-0.929162140221522,1.24758371870021,
8.05082470820076));
#287232=CARTESIAN_POINT('Ctrl Pts',(-0.94848931411271,1.23289616757936,
8.05253853125497));
#287233=CARTESIAN_POINT('Ctrl Pts',(-0.955766624526113,1.22726325287917,
8.05319074679607));
#287234=CARTESIAN_POINT('Ctrl Pts',(-0.970413826315627,1.21571647106866,
8.05451784000496));
#287235=CARTESIAN_POINT('Ctrl Pts',(-0.97778065784544,1.20979936775441,
8.05519282822235));
#287236=CARTESIAN_POINT('Ctrl Pts',(-0.985345748986534,1.20360878678822,
8.05589395168651));
#287237=CARTESIAN_POINT('Ctrl Pts',(-0.985598456674946,1.20340186092564,
8.05591738159988));
#287238=CARTESIAN_POINT('Ctrl Pts',(-0.986078891436294,1.20300821135571,
8.05596194298151));
#287239=CARTESIAN_POINT('Ctrl Pts',(-0.986306630725689,1.20282150251473,
8.05598307384691));
#287240=CARTESIAN_POINT('Ctrl Pts',(-0.986741923097343,1.20246442745936,
8.05602347702826));
#287241=CARTESIAN_POINT('Ctrl Pts',(-0.986949485137246,1.20229407213467,
8.05604274890235));
#287242=CARTESIAN_POINT('Ctrl Pts',(-0.987348100502012,1.20196673813331,
8.05607977190504));
#287243=CARTESIAN_POINT('Ctrl Pts',(-0.987539160547177,1.20180976761274,
8.05609752270271));
#287244=CARTESIAN_POINT('Ctrl Pts',(-0.98790765202604,1.20150687631958,
8.05613176839118));
#287245=CARTESIAN_POINT('Ctrl Pts',(-0.988085088591989,1.20136096177498,
8.05614826302903));
#287246=CARTESIAN_POINT('Ctrl Pts',(-0.988428630944044,1.20107832293102,
8.05618020790503));
#287247=CARTESIAN_POINT('Ctrl Pts',(-0.988594740713639,1.2009416034587,
8.05619565794715));
#287248=CARTESIAN_POINT('Ctrl Pts',(-0.988917493974861,1.20067584355609,
8.05622568541747));
#287249=CARTESIAN_POINT('Ctrl Pts',(-0.989074140596858,1.2005468069139,
8.05624026269183));
#287250=CARTESIAN_POINT('Ctrl Pts',(-0.998454038716651,1.19281709461721,
8.0571133559649));
#287251=CARTESIAN_POINT('Ctrl Pts',(-1.00758916450935,1.18511060639413,
8.05797615331686));
#287252=CARTESIAN_POINT('Ctrl Pts',(-1.02801729112677,1.16747029511556,
8.05993446047416));
#287253=CARTESIAN_POINT('Ctrl Pts',(-1.03925669487236,1.15747653699761,
8.0610323816227));
#287254=CARTESIAN_POINT('Ctrl Pts',(-1.06987351089627,1.12944748090326,
8.06408110609895));
#287255=CARTESIAN_POINT('Ctrl Pts',(-1.0889373863849,1.11107882622648,8.06604538081485));
#287256=CARTESIAN_POINT('Ctrl Pts',(-1.15188035877378,1.04725480346682,
8.07276042185629));
#287257=CARTESIAN_POINT('Ctrl Pts',(-1.19345259803146,0.999620106691458,
8.07759476834797));
#287258=CARTESIAN_POINT('Ctrl Pts',(-1.29219645310379,0.871509226434835,
8.09009538011309));
#287259=CARTESIAN_POINT('Ctrl Pts',(-1.34482501263367,0.787875389821688,
8.09781153203347));
#287260=CARTESIAN_POINT('Ctrl Pts',(-1.39839427240826,0.681537055315809,
8.10675293324725));
#287261=CARTESIAN_POINT('Ctrl Pts',(-1.40724282557082,0.663073927503623,
8.10827520824093));
#287262=CARTESIAN_POINT('Ctrl Pts',(-1.419116621202,0.63698923790651,8.1103788183201));
#287263=CARTESIAN_POINT('Ctrl Pts',(-1.42244962090517,0.629511205367611,
8.11097655834293));
#287264=CARTESIAN_POINT('Ctrl Pts',(-1.42795877747326,0.616883478913417,
8.11197657550083));
#287265=CARTESIAN_POINT('Ctrl Pts',(-1.43016646545815,0.61174780908894,
8.11238069557206));
#287266=CARTESIAN_POINT('Ctrl Pts',(-1.43469800364895,0.601047625838393,
8.11321717362903));
#287267=CARTESIAN_POINT('Ctrl Pts',(-1.43701725409301,0.595481338882939,
8.11364926039198));
#287268=CARTESIAN_POINT('Ctrl Pts',(-1.44310041794644,0.58063899370963,
8.11479367197184));
#287269=CARTESIAN_POINT('Ctrl Pts',(-1.44680733610097,0.571339656755301,
8.11550269843994));
#287270=CARTESIAN_POINT('Ctrl Pts',(-1.46482332166732,0.524843930637855,
8.11901123415298));
#287271=CARTESIAN_POINT('Ctrl Pts',(-1.47779032283321,0.487139524542371,
8.1217407347615));
#287272=CARTESIAN_POINT('Ctrl Pts',(-1.53312829995789,0.303577830989263,
8.1346691234551));
#287273=CARTESIAN_POINT('Ctrl Pts',(-1.55543186361473,0.152555481804566,
8.14431660589831));
#287274=CARTESIAN_POINT('Ctrl Pts',(-1.55549984414273,0.000696327469871839,
8.15470034727716));
#287275=CARTESIAN_POINT('',(-1.55550041530219,0.000134622242225962,9.55740376032212));
#287276=CARTESIAN_POINT('Ctrl Pts',(-1.55549984491818,0.000694593054951367,
8.15470046587205));
#287277=CARTESIAN_POINT('Ctrl Pts',(-1.55550789932647,-0.0173427753760322,
8.15593381561504));
#287278=CARTESIAN_POINT('Ctrl Pts',(-1.55520221524335,-0.0353784498513321,
8.15717529386514));
#287279=CARTESIAN_POINT('Ctrl Pts',(-1.55407751783141,-0.0681180456271037,
8.15944677560594));
#287280=CARTESIAN_POINT('Ctrl Pts',(-1.55336320788016,-0.0828234183071387,
8.16047359035147));
#287281=CARTESIAN_POINT('Ctrl Pts',(-1.55183252403885,-0.107191674461253,
8.16218719584306));
#287282=CARTESIAN_POINT('Ctrl Pts',(-1.55113432076261,-0.116861238739419,
8.16287032808959));
#287283=CARTESIAN_POINT('Ctrl Pts',(-1.54958746702436,-0.135815496798352,
8.16421594324766));
#287284=CARTESIAN_POINT('Ctrl Pts',(-1.54874563751119,-0.145100346403286,
8.16487818631273));
#287285=CARTESIAN_POINT('Ctrl Pts',(-1.54677937881439,-0.164814536897871,
8.16629115273489));
#287286=CARTESIAN_POINT('Ctrl Pts',(-1.54563281818133,-0.175241147263789,
8.16704253907163));
#287287=CARTESIAN_POINT('Ctrl Pts',(-1.54242831844991,-0.201897928479157,
8.1689744158036));
#287288=CARTESIAN_POINT('Ctrl Pts',(-1.54021966572537,-0.218108308930377,
8.17015957596642));
#287289=CARTESIAN_POINT('Ctrl Pts',(-1.52994400754783,-0.285555100941246,
8.17513580191733));
#287290=CARTESIAN_POINT('Ctrl Pts',(-1.51957346751206,-0.336401149508222,
8.17899776991617));
#287291=CARTESIAN_POINT('Ctrl Pts',(-1.48985770269308,-0.452202683826596,
8.18805121703722));
#287292=CARTESIAN_POINT('Ctrl Pts',(-1.46876949574899,-0.516602353441209,
8.19328085267065));
#287293=CARTESIAN_POINT('Ctrl Pts',(-1.41043894159779,-0.661926396868684,
8.20542274563435));
#287294=CARTESIAN_POINT('Ctrl Pts',(-1.37030552364181,-0.741451667115688,
8.2123306731396));
#287295=CARTESIAN_POINT('Ctrl Pts',(-1.31681441785143,-0.828098144743771,
8.21988540359756));
#287296=CARTESIAN_POINT('Ctrl Pts',(-1.30989947395352,-0.838993531187833,
8.22083570997917));
#287297=CARTESIAN_POINT('Ctrl Pts',(-1.29921975718629,-0.855366829972393,
8.22226287435499));
#287298=CARTESIAN_POINT('Ctrl Pts',(-1.29555435560631,-0.860908419824876,
8.2227457374602));
#287299=CARTESIAN_POINT('Ctrl Pts',(-1.28879133369826,-0.870992175824483,
8.2236238340034));
#287300=CARTESIAN_POINT('Ctrl Pts',(-1.2857050757125,-0.875541508126171,
8.22401976053202));
#287301=CARTESIAN_POINT('Ctrl Pts',(-1.27859092378134,-0.885909461752462,
8.22492162905039));
#287302=CARTESIAN_POINT('Ctrl Pts',(-1.27454737289478,-0.891717065127561,
8.22542651381292));
#287303=CARTESIAN_POINT('Ctrl Pts',(-1.26173412767695,-0.909855030229361,
8.22700310585555));
#287304=CARTESIAN_POINT('Ctrl Pts',(-1.25282375534327,-0.922085607569688,
8.22806587248533));
#287305=CARTESIAN_POINT('Ctrl Pts',(-1.19475916485722,-0.999390457200208,
8.23479492143033));
#287306=CARTESIAN_POINT('Ctrl Pts',(-1.14072354820114,-1.06065267076033,
8.24018524836666));
#287307=CARTESIAN_POINT('Ctrl Pts',(-1.02428064791024,-1.17341960409298,
8.25086293022408));
#287308=CARTESIAN_POINT('Ctrl Pts',(-0.962176487646554,-1.22485911072379,
8.25613659489299));
#287309=CARTESIAN_POINT('Ctrl Pts',(-0.85938465009403,-1.29733822138711,
8.26461426825687));
#287310=CARTESIAN_POINT('Ctrl Pts',(-0.821280375199611,-1.32178907331104,
8.26770735680118));
#287311=CARTESIAN_POINT('Ctrl Pts',(-0.768991019466856,-1.35220761261962,
8.27192362055029));
#287312=CARTESIAN_POINT('Ctrl Pts',(-0.755703274372199,-1.35967832514947,
8.27299262245724));
#287313=CARTESIAN_POINT('Ctrl Pts',(-0.73329318486691,-1.37184787549385,
8.27479271996333));
#287314=CARTESIAN_POINT('Ctrl Pts',(-0.724230075700085,-1.37665401491575,
8.27551996227547));
#287315=CARTESIAN_POINT('Ctrl Pts',(-0.706257365825941,-1.3859582917455,
8.27696101693094));
#287316=CARTESIAN_POINT('Ctrl Pts',(-0.697350690679561,-1.39046102386508,
8.27767462457068));
#287317=CARTESIAN_POINT('Ctrl Pts',(-0.677576600253739,-1.40021995392109,
8.27925808608104));
#287318=CARTESIAN_POINT('Ctrl Pts',(-0.666690180041657,-1.40543593135386,
8.28012928626409));
#287319=CARTESIAN_POINT('Ctrl Pts',(-0.629052693515328,-1.42293337402991,
8.28314005458366));
#287320=CARTESIAN_POINT('Ctrl Pts',(-0.602015903255887,-1.43458123279422,
8.28530088053537));
#287321=CARTESIAN_POINT('Ctrl Pts',(-0.465104128100968,-1.48901298903855,
8.2962403884792));
#287322=CARTESIAN_POINT('Ctrl Pts',(-0.350959888586336,-1.51996699525761,
8.30539361817135));
#287323=CARTESIAN_POINT('Ctrl Pts',(-0.186788787898854,-1.54499634215574,
8.31825302904556));
#287324=CARTESIAN_POINT('Ctrl Pts',(-0.138821582300288,-1.55004287622289,
8.32196849289158));
#287325=CARTESIAN_POINT('Ctrl Pts',(-0.0723439043108329,-1.55392551594971,
8.32700493941629));
#287326=CARTESIAN_POINT('Ctrl Pts',(-0.0539746445923887,-1.55467197642273,
8.32838467067837));
#287327=CARTESIAN_POINT('Ctrl Pts',(-0.0218890474583254,-1.55540640586726,
8.33076924654886));
#287328=CARTESIAN_POINT('Ctrl Pts',(-0.0081783201653691,-1.55553893141146,
8.33178012429151));
#287329=CARTESIAN_POINT('Ctrl Pts',(0.0123379068037048,-1.5554659538887,
8.33327895178847));
#287330=CARTESIAN_POINT('Ctrl Pts',(0.0191427772446983,-1.55539709283925,
8.33377381204244));
#287331=CARTESIAN_POINT('Ctrl Pts',(0.0314373418294043,-1.55519197984305,
8.33466352279674));
#287332=CARTESIAN_POINT('Ctrl Pts',(0.0369269454464578,-1.55507131791174,
8.3350591872781));
#287333=CARTESIAN_POINT('Ctrl Pts',(0.0493066609723958,-1.5547336165818,
8.33594789664946));
#287334=CARTESIAN_POINT('Ctrl Pts',(0.056196084585162,-1.55449984568892,
8.33644001693328));
#287335=CARTESIAN_POINT('Ctrl Pts',(0.0772349659554132,-1.55364590321822,
8.33793598121373));
#287336=CARTESIAN_POINT('Ctrl Pts',(0.0913781826362051,-1.55287826224807,
8.33893213609745));
#287337=CARTESIAN_POINT('Ctrl Pts',(0.206080142448297,-1.54508006660263,
8.34694835371305));
#287338=CARTESIAN_POINT('Ctrl Pts',(0.305763377152901,-1.52848167420207,
8.35353398011342));
#287339=CARTESIAN_POINT('Ctrl Pts',(0.499790012124531,-1.47641521859007,
8.36675914983694));
#287340=CARTESIAN_POINT('Ctrl Pts',(0.593688804644002,-1.44122234889674,
8.37337290950411));
#287341=CARTESIAN_POINT('Ctrl Pts',(0.70089965393884,-1.38877388193005,
8.3816376002143));
#287342=CARTESIAN_POINT('Ctrl Pts',(0.718087195331355,-1.37996519616769,
8.38298509626837));
#287343=CARTESIAN_POINT('Ctrl Pts',(0.744902065041766,-1.3655858560405,
8.38512576287522));
#287344=CARTESIAN_POINT('Ctrl Pts',(0.754641652658585,-1.36022784167536,
8.385911434107));
#287345=CARTESIAN_POINT('Ctrl Pts',(0.772834740893855,-1.34996378790021,
8.38739490066712));
#287346=CARTESIAN_POINT('Ctrl Pts',(0.781301096684744,-1.34508154165039,
8.3880918155283));
#287347=CARTESIAN_POINT('Ctrl Pts',(0.800297376091972,-1.33388720388864,
8.38967072826186));
#287348=CARTESIAN_POINT('Ctrl Pts',(0.810799595851049,-1.3275296464506,
8.39055434606303));
#287349=CARTESIAN_POINT('Ctrl Pts',(0.83777279452743,-1.31076185302639,
8.39285224675202));
#287350=CARTESIAN_POINT('Ctrl Pts',(0.854124928356442,-1.30016554084484,
8.39427326989057));
#287351=CARTESIAN_POINT('Ctrl Pts',(0.986580949639623,-1.21075577806206,
8.40602053909226));
#287352=CARTESIAN_POINT('Ctrl Pts',(1.0917106366282,-1.11688086927927,8.41694725144853));
#287353=CARTESIAN_POINT('Ctrl Pts',(1.21001101499556,-0.978370159168645,
8.43102144626592));
#287354=CARTESIAN_POINT('Ctrl Pts',(1.23591920897715,-0.945430590600515,
8.43423753821548));
#287355=CARTESIAN_POINT('Ctrl Pts',(1.27497556301943,-0.891420528739818,
8.43926596791238));
#287356=CARTESIAN_POINT('Ctrl Pts',(1.28900356018931,-0.871012769643257,
8.44111366988778));
#287357=CARTESIAN_POINT('Ctrl Pts',(1.30721427303261,-0.843115791546194,
8.44356148666245));
#287358=CARTESIAN_POINT('Ctrl Pts',(1.31183024314161,-0.835915555375306,
8.44418646337852));
#287359=CARTESIAN_POINT('Ctrl Pts',(1.31943202967484,-0.823839817605614,
8.44522286413904));
#287360=CARTESIAN_POINT('Ctrl Pts',(1.32245072723011,-0.818985350292293,
8.4456363638395));
#287361=CARTESIAN_POINT('Ctrl Pts',(1.32854745899736,-0.809059385910118,
8.44647531519638));
#287362=CARTESIAN_POINT('Ctrl Pts',(1.33162335783473,-0.803986739181109,
8.44690063258554));
#287363=CARTESIAN_POINT('Ctrl Pts',(1.33958195959829,-0.790690763075715,
8.44800685852535));
#287364=CARTESIAN_POINT('Ctrl Pts',(1.34441807327124,-0.78243962434958,
8.44868484839293));
#287365=CARTESIAN_POINT('Ctrl Pts',(1.36466579533613,-0.747151906283429,
8.45155076805521));
#287366=CARTESIAN_POINT('Ctrl Pts',(1.37934146314878,-0.719698658256215,
8.45369714682017));
#287367=CARTESIAN_POINT('Ctrl Pts',(1.43321319824275,-0.611212154762289,
8.461933278924));
#287368=CARTESIAN_POINT('Ctrl Pts',(1.46617350063791,-0.527274455043451,
8.46779373993058));
#287369=CARTESIAN_POINT('Ctrl Pts',(1.51300475933065,-0.368849314355551,
8.47868795308771));
#287370=CARTESIAN_POINT('Ctrl Pts',(1.52906075300844,-0.295304345720388,
8.48368357691161));
#287371=CARTESIAN_POINT('Ctrl Pts',(1.54356074658807,-0.194231487423029,
8.49068590181256));
#287372=CARTESIAN_POINT('Ctrl Pts',(1.54669217211062,-0.167477834887401,
8.49255144384527));
#287373=CARTESIAN_POINT('Ctrl Pts',(1.55026778747953,-0.128097949607766,
8.49532217538646));
#287374=CARTESIAN_POINT('Ctrl Pts',(1.55125536968243,-0.115525144391394,
8.49621045429779));
#287375=CARTESIAN_POINT('Ctrl Pts',(1.5527389743589,-0.093156364518863,
8.49779803313694));
#287376=CARTESIAN_POINT('Ctrl Pts',(1.55329543336722,-0.0833649769455995,
8.49849540534467));
#287377=CARTESIAN_POINT('Ctrl Pts',(1.55427543747475,-0.0626675819157516,
8.49997503075666));
#287378=CARTESIAN_POINT('Ctrl Pts',(1.55467685939939,-0.0517611144316235,
8.50075793747042));
#287379=CARTESIAN_POINT('Ctrl Pts',(1.55544559298367,-0.0225002465624098,
8.50286748907059));
#287380=CARTESIAN_POINT('Ctrl Pts',(1.55560278968477,-0.00414258205714366,
8.50420059104922));
#287381=CARTESIAN_POINT('Ctrl Pts',(1.55463357602343,0.101926799566723,
8.51196198292895));
#287382=CARTESIAN_POINT('Ctrl Pts',(1.54641432805462,0.189400200672458,
8.51860848978389));
#287383=CARTESIAN_POINT('Ctrl Pts',(1.51909684984382,0.341084462446118,
8.53049728121093));
#287384=CARTESIAN_POINT('Ctrl Pts',(1.50314530908757,0.405645059236957,
8.53567384546174));
#287385=CARTESIAN_POINT('Ctrl Pts',(1.4721060671133,0.503802815110005,8.54360586213524));
#287386=CARTESIAN_POINT('Ctrl Pts',(1.45987363367625,0.538221958689364,
8.54639856521226));
#287387=CARTESIAN_POINT('Ctrl Pts',(1.43813562604342,0.593174403285674,
8.55084575647337));
#287388=CARTESIAN_POINT('Ctrl Pts',(1.42937433132269,0.61398624621075,8.55252717964612));
#287389=CARTESIAN_POINT('Ctrl Pts',(1.41679015050072,0.642148150083101,
8.55479173543142));
#287390=CARTESIAN_POINT('Ctrl Pts',(1.41335763392529,0.64966821068319,8.5553953764301));
#287391=CARTESIAN_POINT('Ctrl Pts',(1.40747384319376,0.662291228272542,
8.55640641090681));
#287392=CARTESIAN_POINT('Ctrl Pts',(1.40505439815322,0.667408744921052,
8.55681567153365));
#287393=CARTESIAN_POINT('Ctrl Pts',(1.40000407879043,0.677941793140445,
8.55765658133414));
#287394=CARTESIAN_POINT('Ctrl Pts',(1.3973696222168,0.683355425621348,8.55808800858732));
#287395=CARTESIAN_POINT('Ctrl Pts',(1.39029055462063,0.697690305206675,
8.55922870305827));
#287396=CARTESIAN_POINT('Ctrl Pts',(1.38579142696881,0.706584547595514,
8.55993470965056));
#287397=CARTESIAN_POINT('Ctrl Pts',(1.36497523401698,0.746771931834281,
8.5631195439091));
#287398=CARTESIAN_POINT('Ctrl Pts',(1.34768023294315,0.777550098557509,
8.56554445887448));
#287399=CARTESIAN_POINT('Ctrl Pts',(1.27824321606583,0.891830634970399,
8.57459670166496));
#287400=CARTESIAN_POINT('Ctrl Pts',(1.21926362112187,0.970910193946696,
8.58097414490483));
#287401=CARTESIAN_POINT('Ctrl Pts',(1.11869031000628,1.08201518316962,8.59089288868535));
#287402=CARTESIAN_POINT('Ctrl Pts',(1.08231164326513,1.11840321165451,8.59432511128414));
#287403=CARTESIAN_POINT('Ctrl Pts',(1.02691804581631,1.16857315893815,8.59941148175886));
#287404=CARTESIAN_POINT('Ctrl Pts',(1.00928724422376,1.18383405482935,8.60101126459226));
#287405=CARTESIAN_POINT('Ctrl Pts',(0.976648320505758,1.21082650637596,
8.60394529911898));
#287406=CARTESIAN_POINT('Ctrl Pts',(0.961754856679362,1.22268978533247,
8.6052741872532));
#287407=CARTESIAN_POINT('Ctrl Pts',(0.937873092328922,1.24100628676697,
8.60739203540446));
#287408=CARTESIAN_POINT('Ctrl Pts',(0.929026930832726,1.24764237325617,
8.60817376911543));
#287409=CARTESIAN_POINT('Ctrl Pts',(0.912224438010216,1.25996924476657,
8.60965392979712));
#287410=CARTESIAN_POINT('Ctrl Pts',(0.904283681356347,1.26568042517313,
8.61035151946417));
#287411=CARTESIAN_POINT('Ctrl Pts',(0.88618340533644,1.27844128805939,8.61193761119209));
#287412=CARTESIAN_POINT('Ctrl Pts',(0.875992734348781,1.28544539669486,
8.61282779399249));
#287413=CARTESIAN_POINT('Ctrl Pts',(0.849278497968918,1.30334105688226,
8.61515472024469));
#287414=CARTESIAN_POINT('Ctrl Pts',(0.832629135382617,1.31403977634249,
8.6165984913052));
#287415=CARTESIAN_POINT('Ctrl Pts',(0.697553084560162,1.39724047358835,
8.62826538245604));
#287416=CARTESIAN_POINT('Ctrl Pts',(0.570125491654899,1.45389208150353,
8.6390735936983));
#287417=CARTESIAN_POINT('Ctrl Pts',(0.381753700185515,1.5090221115347,8.65424259549516));
#287418=CARTESIAN_POINT('Ctrl Pts',(0.325734187225226,1.52209797177998,
8.65864752384775));
#287419=CARTESIAN_POINT('Ctrl Pts',(0.255152161441555,1.53449619624826,
8.66397636768922));
#287420=CARTESIAN_POINT('Ctrl Pts',(0.241156642648422,1.53675785767554,
8.6650222409215));
#287421=CARTESIAN_POINT('Ctrl Pts',(0.220309776059693,1.5398348621197,8.66656226798937));
#287422=CARTESIAN_POINT('Ctrl Pts',(0.213481236270425,1.5407964066184,8.66706388033754));
#287423=CARTESIAN_POINT('Ctrl Pts',(0.201204049630122,1.54244200254902,
8.66796038657841));
#287424=CARTESIAN_POINT('Ctrl Pts',(0.195757964186956,1.54314264505527,
8.6683561615325));
#287425=CARTESIAN_POINT('Ctrl Pts',(0.1835565293768,1.54464673160189,8.66923860614164));
#287426=CARTESIAN_POINT('Ctrl Pts',(0.176799509071621,1.54543471656513,
8.66972441757734));
#287427=CARTESIAN_POINT('Ctrl Pts',(0.156421548857741,1.54767573531601,
8.67118147184432));
#287428=CARTESIAN_POINT('Ctrl Pts',(0.142785931209658,1.54899325183235,
8.67214559580656));
#287429=CARTESIAN_POINT('Ctrl Pts',(0.0240229169080802,1.55888683988535,
8.68046273685936));
#287430=CARTESIAN_POINT('Ctrl Pts',(-0.0817228579438755,1.55693077959304,
8.68733513725257));
#287431=CARTESIAN_POINT('Ctrl Pts',(-0.268925198803245,1.53432641936511,
8.69975312058207));
#287432=CARTESIAN_POINT('Ctrl Pts',(-0.350442402690428,1.51778336001912,
8.70524861461504));
#287433=CARTESIAN_POINT('Ctrl Pts',(-0.456504556424705,1.48725604946076,
8.71281404820483));
#287434=CARTESIAN_POINT('Ctrl Pts',(-0.482559388059072,1.47900752154215,
8.71470617284041));
#287435=CARTESIAN_POINT('Ctrl Pts',(-0.520367358752097,1.46593276970139,
8.71750888924652));
#287436=CARTESIAN_POINT('Ctrl Pts',(-0.532301083738477,1.46164175251112,
8.71840199064116));
#287437=CARTESIAN_POINT('Ctrl Pts',(-0.55337589662852,1.45377154672822,
8.71999495598603));
#287438=CARTESIAN_POINT('Ctrl Pts',(-0.562538185983711,1.45025079703295,
8.72069284375275));
#287439=CARTESIAN_POINT('Ctrl Pts',(-0.581781212988799,1.44264658080963,
8.72217020973442));
#287440=CARTESIAN_POINT('Ctrl Pts',(-0.591853629546439,1.43854364097082,
8.72295031184206));
#287441=CARTESIAN_POINT('Ctrl Pts',(-0.618645656081329,1.42730105697286,
8.72504404333851));
#287442=CARTESIAN_POINT('Ctrl Pts',(-0.635284050530813,1.41997354839179,
8.72636396175765));
#287443=CARTESIAN_POINT('Ctrl Pts',(-0.724744393648343,1.37868841794125,
8.73357123115145));
#287444=CARTESIAN_POINT('Ctrl Pts',(-0.794968748179386,1.33942413747065,
8.73963931795514));
#287445=CARTESIAN_POINT('Ctrl Pts',(-0.937779908103882,1.24437575792694,
8.75283722603123));
#287446=CARTESIAN_POINT('Ctrl Pts',(-1.00912732119861,1.18725063529203,
8.75997645945678));
#287447=CARTESIAN_POINT('Ctrl Pts',(-1.10295736605274,1.0975224650092,8.76989314995933));
#287448=CARTESIAN_POINT('Ctrl Pts',(-1.12985742006599,1.0698099378153,8.77280589558643));
#287449=CARTESIAN_POINT('Ctrl Pts',(-1.16233838856556,1.0337543563618,8.77638399635461));
#287450=CARTESIAN_POINT('Ctrl Pts',(-1.16890568760591,1.02632261301053,
8.77711076706121));
#287451=CARTESIAN_POINT('Ctrl Pts',(-1.17933783730091,1.0142872522371,8.77826992712943));
#287452=CARTESIAN_POINT('Ctrl Pts',(-1.18324773225751,1.0097233145516,8.77870545473933));
#287453=CARTESIAN_POINT('Ctrl Pts',(-1.19075037221299,1.00086221388954,
8.77954309742359));
#287454=CARTESIAN_POINT('Ctrl Pts',(-1.19434649017885,0.996568152637631,
8.7799454396193));
#287455=CARTESIAN_POINT('Ctrl Pts',(-1.20233871083706,0.98691938397058,
8.78084176798652));
#287456=CARTESIAN_POINT('Ctrl Pts',(-1.20672245168547,0.981554468899952,
8.78133488193624));
#287457=CARTESIAN_POINT('Ctrl Pts',(-1.22188528180436,0.962742749985558,
8.78304642720241));
#287458=CARTESIAN_POINT('Ctrl Pts',(-1.23247710915692,0.949145659971507,
8.78425260627023));
#287459=CARTESIAN_POINT('Ctrl Pts',(-1.30389110065943,0.854257197454036,
8.79248184156941));
#287460=CARTESIAN_POINT('Ctrl Pts',(-1.35686107882212,0.767346663813942,
8.79909480062707));
#287461=CARTESIAN_POINT('Ctrl Pts',(-1.43592233579858,0.603466613057719,
8.81108054674577));
#287462=CARTESIAN_POINT('Ctrl Pts',(-1.46518769883072,0.528458079462683,
8.81640542802211));
#287463=CARTESIAN_POINT('Ctrl Pts',(-1.49658769105761,0.424943899054878,
8.82381653768517));
#287464=CARTESIAN_POINT('Ctrl Pts',(-1.5039378269491,0.398149324621662,
8.82573942539005));
#287465=CARTESIAN_POINT('Ctrl Pts',(-1.51361151957026,0.358780277640172,
8.82857911276239));
#287466=CARTESIAN_POINT('Ctrl Pts',(-1.5165040808245,0.346350220762187,
8.82947773903295));
#287467=CARTESIAN_POINT('Ctrl Pts',(-1.52135229534149,0.324289964423222,
8.83107690729861));
#287468=CARTESIAN_POINT('Ctrl Pts',(-1.52337028038935,0.314674066788449,
8.83177541749129));
#287469=CARTESIAN_POINT('Ctrl Pts',(-1.52742165169151,0.294415915114111,
8.8332503521401));
#287470=CARTESIAN_POINT('Ctrl Pts',(-1.5294352057216,0.283770283209744,
8.83402736751941));
#287471=CARTESIAN_POINT('Ctrl Pts',(-1.5344949024693,0.255399838837611,
8.83610370420844));
#287472=CARTESIAN_POINT('Ctrl Pts',(-1.53734504865251,0.237642240322826,
8.83740913182853));
#287473=CARTESIAN_POINT('Ctrl Pts',(-1.55034894906355,0.146555351651667,
8.844137688748));
#287474=CARTESIAN_POINT('Ctrl Pts',(-1.55556494302191,0.0726289945413549,
8.84971241101516));
#287475=CARTESIAN_POINT('Ctrl Pts',(-1.55545559872507,-0.0508161200096765,
8.8591839896776));
#287476=CARTESIAN_POINT('Ctrl Pts',(-1.55305489340057,-0.100222515723241,
8.86301643856976));
#287477=CARTESIAN_POINT('Ctrl Pts',(-1.54079505185045,-0.227252872359269,
8.87291270117633));
#287478=CARTESIAN_POINT('Ctrl Pts',(-1.52742644059319,-0.304407879625256,
8.87896817315404));
#287479=CARTESIAN_POINT('Ctrl Pts',(-1.50463960339592,-0.394797945060312,
8.88591181063912));
#287480=CARTESIAN_POINT('Ctrl Pts',(-1.50075795258871,-0.409305955730549,
8.88702133829879));
#287481=CARTESIAN_POINT('Ctrl Pts',(-1.49473726770902,-0.430570444029356,
8.88863806432052));
#287482=CARTESIAN_POINT('Ctrl Pts',(-1.49276135315609,-0.437371643462518,
8.88915371062199));
#287483=CARTESIAN_POINT('Ctrl Pts',(-1.48916679969669,-0.4494361014576,
8.89006554240398));
#287484=CARTESIAN_POINT('Ctrl Pts',(-1.48756658044811,-0.454704562127828,
8.89046274207021));
#287485=CARTESIAN_POINT('Ctrl Pts',(-1.48400217523509,-0.466219546884688,
8.8913286712128));
#287486=CARTESIAN_POINT('Ctrl Pts',(-1.48202649345555,-0.472462272430623,
8.89179673404072));
#287487=CARTESIAN_POINT('Ctrl Pts',(-1.47618525454244,-0.490522092497547,
8.89314728161087));
#287488=CARTESIAN_POINT('Ctrl Pts',(-1.47221725523811,-0.502305890862283,
8.89402409831666));
#287489=CARTESIAN_POINT('Ctrl Pts',(-1.44026567050328,-0.593560001747837,
8.90078925802264));
#287490=CARTESIAN_POINT('Ctrl Pts',(-1.40600423576108,-0.67069733572262,
8.9063642692095));
#287491=CARTESIAN_POINT('Ctrl Pts',(-1.31084544323477,-0.845205587778962,
8.91946061275635));
#287492=CARTESIAN_POINT('Ctrl Pts',(-1.24511116240763,-0.93935236463195,
8.92694386450749));
#287493=CARTESIAN_POINT('Ctrl Pts',(-1.15648847941476,-1.04043885966709,
8.93621673542934));
#287494=CARTESIAN_POINT('Ctrl Pts',(-1.14304362355007,-1.05519184816699,
8.9376040974822));
#287495=CARTESIAN_POINT('Ctrl Pts',(-1.1207818101676,-1.07869481768303,
8.93987352530442));
#287496=CARTESIAN_POINT('Ctrl Pts',(-1.1121371096373,-1.08760535543687,
8.94074829579854));
#287497=CARTESIAN_POINT('Ctrl Pts',(-1.09648909755583,-1.10335292430509,
8.94232093749023));
#287498=CARTESIAN_POINT('Ctrl Pts',(-1.08952609157742,-1.11022921255347,
8.94301701640312));
#287499=CARTESIAN_POINT('Ctrl Pts',(-1.07457941684572,-1.1247137155052,
8.94450371394265));
#287500=CARTESIAN_POINT('Ctrl Pts',(-1.06657882820045,-1.13230360618835,
8.94529507362878));
#287501=CARTESIAN_POINT('Ctrl Pts',(-1.04465267493276,-1.15266563746746,
8.9474524260925));
#287502=CARTESIAN_POINT('Ctrl Pts',(-1.03057440483791,-1.16526976308204,
8.94882539481354));
#287503=CARTESIAN_POINT('Ctrl Pts',(-0.936382059385998,-1.24655694697754,
8.95793631250069));
#287504=CARTESIAN_POINT('Ctrl Pts',(-0.849700825360943,-1.30717863360615,
8.96599879509881));
#287505=CARTESIAN_POINT('Ctrl Pts',(-0.674056926382212,-1.4051230872358,
8.98157838686325));
#287506=CARTESIAN_POINT('Ctrl Pts',(-0.586419684209652,-1.44389706417766,
8.98903648189428));
#287507=CARTESIAN_POINT('Ctrl Pts',(-0.482044933432753,-1.47899378079796,
8.99722908585923));
#287508=CARTESIAN_POINT('Ctrl Pts',(-0.468255611205701,-1.48341721845791,
8.99829784352748));
#287509=CARTESIAN_POINT('Ctrl Pts',(-0.447755222496817,-1.48967911608659,
8.99986473128859));
#287510=CARTESIAN_POINT('Ctrl Pts',(-0.441090837923369,-1.49166601015651,
9.00037068809168));
#287511=CARTESIAN_POINT('Ctrl Pts',(-0.429139527054664,-1.49514202683466,
9.00127165087781));
#287512=CARTESIAN_POINT('Ctrl Pts',(-0.423857813767576,-1.49664791139053,
9.00166758078572));
#287513=CARTESIAN_POINT('Ctrl Pts',(-0.412068493232733,-1.49994178134671,
9.00254636574887));
#287514=CARTESIAN_POINT('Ctrl Pts',(-0.405557120928173,-1.50171542469041,
9.00302840265932));
#287515=CARTESIAN_POINT('Ctrl Pts',(-0.386059649779417,-1.50689030643539,
9.00446245463701));
#287516=CARTESIAN_POINT('Ctrl Pts',(-0.373040440789776,-1.51016598763882,
9.00540767773905));
#287517=CARTESIAN_POINT('Ctrl Pts',(-0.276239289390641,-1.53319320803928,
9.01235569803947));
#287518=CARTESIAN_POINT('Ctrl Pts',(-0.190977073683469,-1.54613115934851,
9.01803824575437));
#287519=CARTESIAN_POINT('Ctrl Pts',(0.00526735481943303,-1.55941752721037,
9.03099179324028));
#287520=CARTESIAN_POINT('Ctrl Pts',(0.116075057310498,-1.55509929444758,
9.03823470341701));
#287521=CARTESIAN_POINT('Ctrl Pts',(0.245472384173217,-1.5361418286467,
9.04725229260812));
#287522=CARTESIAN_POINT('Ctrl Pts',(0.265402162241918,-1.53282420298211,
9.04865620854486));
#287523=CARTESIAN_POINT('Ctrl Pts',(0.297534359347984,-1.52682986439947,
9.05094726526467));
#287524=CARTESIAN_POINT('Ctrl Pts',(0.309779460582336,-1.52439260017255,
9.05182687428356));
#287525=CARTESIAN_POINT('Ctrl Pts',(0.331574715545322,-1.51978102559053,
9.05340483923315));
#287526=CARTESIAN_POINT('Ctrl Pts',(0.341136281786932,-1.51766339712417,
9.05410135441048));
#287527=CARTESIAN_POINT('Ctrl Pts',(0.36137980920108,-1.51297903717607,
9.05558538630136));
#287528=CARTESIAN_POINT('Ctrl Pts',(0.372055801783793,-1.51038915592122,
9.05637361189284));
#287529=CARTESIAN_POINT('Ctrl Pts',(0.400824203664722,-1.50308673584154,
9.05851321757652));
#287530=CARTESIAN_POINT('Ctrl Pts',(0.418860021404101,-1.49816087374273,
9.05987137903083));
#287531=CARTESIAN_POINT('Ctrl Pts',(0.458661291428838,-1.48651565897887,
9.06290725528484));
#287532=CARTESIAN_POINT('Ctrl Pts',(0.480376406638293,-1.47964096791976,
9.06458964514343));
#287533=CARTESIAN_POINT('Ctrl Pts',(0.548845831861736,-1.45629847076299,
9.0699788135836));
#287534=CARTESIAN_POINT('Ctrl Pts',(0.594964248751368,-1.43807290661367,
9.07373676694237));
#287535=CARTESIAN_POINT('Ctrl Pts',(0.680172577348673,-1.39959844174086,
9.08090911479182));
#287536=CARTESIAN_POINT('Ctrl Pts',(0.719429430918415,-1.37983026599528,
9.08431073520318));
#287537=CARTESIAN_POINT('Ctrl Pts',(0.831416159786573,-1.31735875548053,
9.09425416416553));
#287538=CARTESIAN_POINT('Ctrl Pts',(0.901583456898515,-1.27036881126108,
9.10079992945036));
#287539=CARTESIAN_POINT('Ctrl Pts',(0.979362171192709,-1.20857585190162,
9.10819715770035));
#287540=CARTESIAN_POINT('Ctrl Pts',(0.990987156479298,-1.19906228034851,
9.10930655468245));
#287541=CARTESIAN_POINT('Ctrl Pts',(1.00786813627616,-1.18483410405858,
9.11092098686409));
#287542=CARTESIAN_POINT('Ctrl Pts',(1.01323234630829,-1.18025008021331,
9.11143452175219));
#287543=CARTESIAN_POINT('Ctrl Pts',(1.02271934901546,-1.17203054240051,
9.11234339823121));
#287544=CARTESIAN_POINT('Ctrl Pts',(1.02685427425019,-1.16840950088539,
9.11273973804126));
#287545=CARTESIAN_POINT('Ctrl Pts',(1.03595766139387,-1.1603518164743,9.11361275820906));
#287546=CARTESIAN_POINT('Ctrl Pts',(1.04091690355532,-1.15590510789968,
9.11408868597484));
#287547=CARTESIAN_POINT('Ctrl Pts',(1.05546030235224,-1.14269525292822,
9.11548592291274));
#287548=CARTESIAN_POINT('Ctrl Pts',(1.06496375016334,-1.13384352128698,
9.11640094770386));
#287549=CARTESIAN_POINT('Ctrl Pts',(1.12892734049978,-1.07275252073659,
9.12258270795883));
#287550=CARTESIAN_POINT('Ctrl Pts',(1.17964167411803,-1.01672196453946,
9.12760259375878));
#287551=CARTESIAN_POINT('Ctrl Pts',(1.30247235737939,-0.859390027855182,
9.14077559040882));
#287552=CARTESIAN_POINT('Ctrl Pts',(1.36685990545847,-0.752778764298437,
9.14884941363933));
#287553=CARTESIAN_POINT('Ctrl Pts',(1.42572013302073,-0.622305849264656,
9.15873592958155));
#287554=CARTESIAN_POINT('Ctrl Pts',(1.4332271386558,-0.604815990782045,
9.16006023968811));
#287555=CARTESIAN_POINT('Ctrl Pts',(1.44499532662816,-0.575948112668915,
9.16224714112165));
#287556=CARTESIAN_POINT('Ctrl Pts',(1.44944759382522,-0.564649785544136,
9.16310330671459));
#287557=CARTESIAN_POINT('Ctrl Pts',(1.45723963980532,-0.544176617881382,
9.16465579956939));
#287558=CARTESIAN_POINT('Ctrl Pts',(1.46062622350875,-0.535020173938064,
9.16535052078373));
#287559=CARTESIAN_POINT('Ctrl Pts',(1.46771504655266,-0.515284779554326,
9.16684903180084));
#287560=CARTESIAN_POINT('Ctrl Pts',(1.47138956619141,-0.504696536779223,
9.16765369625496));
#287561=CARTESIAN_POINT('Ctrl Pts',(1.48122184527803,-0.475344178389458,
9.16988678856115));
#287562=CARTESIAN_POINT('Ctrl Pts',(1.4871369784435,-0.456501679747827,
9.17132304912216));
#287563=CARTESIAN_POINT('Ctrl Pts',(1.52144092028485,-0.339475245154242,
9.18026432157958));
#287564=CARTESIAN_POINT('Ctrl Pts',(1.54044887664108,-0.238821746275747,
9.18806984095129));
#287565=CARTESIAN_POINT('Ctrl Pts',(1.55805036066665,-0.0398255174791783,
9.20354201709145));
#287566=CARTESIAN_POINT('Ctrl Pts',(1.55748067516752,0.0580012572155893,
9.21116058399213));
#287567=CARTESIAN_POINT('Ctrl Pts',(1.54631385281266,0.169409241380123,
9.2194888158955));
#287568=CARTESIAN_POINT('Ctrl Pts',(1.54468575206923,0.183662703703547,
9.2205473994175));
#287569=CARTESIAN_POINT('Ctrl Pts',(1.54197921662684,0.204764119960254,
9.2221023531579));
#287570=CARTESIAN_POINT('Ctrl Pts',(1.54105188629223,0.211630191640074,
9.22260638542932));
#287571=CARTESIAN_POINT('Ctrl Pts',(1.53930733016324,0.223927109390988,
9.22350536639301));
#287572=CARTESIAN_POINT('Ctrl Pts',(1.53850719155381,0.229360047427546,
9.2239012200487));
#287573=CARTESIAN_POINT('Ctrl Pts',(1.53665607893202,0.241483343524967,
9.22478159245966));
#287574=CARTESIAN_POINT('Ctrl Pts',(1.53559017230701,0.248171185720242,
9.22526527555621));
#287575=CARTESIAN_POINT('Ctrl Pts',(1.53226172003992,0.26821201339908,9.22670933491812));
#287576=CARTESIAN_POINT('Ctrl Pts',(1.52986836143609,0.281543055646231,
9.22766277792094));
#287577=CARTESIAN_POINT('Ctrl Pts',(1.523872505236,0.312602016824603,9.2298710710745));
#287578=CARTESIAN_POINT('Ctrl Pts',(1.5201342272213,0.330302025422514,9.23111954816163));
#287579=CARTESIAN_POINT('Ctrl Pts',(1.5055854065519,0.393697133375123,9.23556833773222));
#287580=CARTESIAN_POINT('Ctrl Pts',(1.49301542596418,0.438965203867435,
9.23870256483593));
#287581=CARTESIAN_POINT('Ctrl Pts',(1.44320280133831,0.591248144581873,
9.24930896669776));
#287582=CARTESIAN_POINT('Ctrl Pts',(1.39634062154498,0.694723156850064,
9.25665074390169));
#287583=CARTESIAN_POINT('Ctrl Pts',(1.32130906296903,0.821512875097195,
9.26667267481212));
#287584=CARTESIAN_POINT('Ctrl Pts',(1.30300006271734,0.850253840643107,
9.26901771711631));
#287585=CARTESIAN_POINT('Ctrl Pts',(1.27578285860249,0.89003262793136,9.2723840879517));
#287586=CARTESIAN_POINT('Ctrl Pts',(1.26764401822494,0.901586712954113,
9.27337684839587));
#287587=CARTESIAN_POINT('Ctrl Pts',(1.25351259275861,0.921078337115501,
9.27507834237803));
#287588=CARTESIAN_POINT('Ctrl Pts',(1.24759914577311,0.929072379543192,
9.27578400964369));
#287589=CARTESIAN_POINT('Ctrl Pts',(1.23540005641152,0.945237118723911,
9.27722735330804));
#287590=CARTESIAN_POINT('Ctrl Pts',(1.22910903178765,0.953403109143462,
9.27796521689099));
#287591=CARTESIAN_POINT('Ctrl Pts',(1.21316389620452,0.973680381061063,
9.2798198185778));
#287592=CARTESIAN_POINT('Ctrl Pts',(1.20340938401956,0.985710883445157,
9.28094051350126));
#287593=CARTESIAN_POINT('Ctrl Pts',(1.16302603929184,1.03402375681874,9.28552640879167));
#287594=CARTESIAN_POINT('Ctrl Pts',(1.13092613215031,1.06903690548297,9.28905070695363));
#287595=CARTESIAN_POINT('Ctrl Pts',(1.03489264340217,1.16461346403174,9.29927157467036));
#287596=CARTESIAN_POINT('Ctrl Pts',(0.967355057445862,1.22128967359131,
9.30609817576178));
#287597=CARTESIAN_POINT('Ctrl Pts',(0.837087772050156,1.31299241714589,
9.31844614138079));
#287598=CARTESIAN_POINT('Ctrl Pts',(0.776019212408873,1.34998566256816,
9.32395163925735));
#287599=CARTESIAN_POINT('Ctrl Pts',(0.699170476427338,1.38959343072602,
9.33039078529338));
#287600=CARTESIAN_POINT('Ctrl Pts',(0.685617845643648,1.39633000139551,
9.33150868630128));
#287601=CARTESIAN_POINT('Ctrl Pts',(0.665586009007611,1.40592517429502,
9.33313304221567));
#287602=CARTESIAN_POINT('Ctrl Pts',(0.659182656701938,1.40893880684659,
9.33364814072776));
#287603=CARTESIAN_POINT('Ctrl Pts',(0.64776885286771,1.41421567834306,9.33455867012328));
#287604=CARTESIAN_POINT('Ctrl Pts',(0.642766716140116,1.41649617840138,
9.33495511449354));
#287605=CARTESIAN_POINT('Ctrl Pts',(0.631692865473461,1.4214740624084,9.33582703408055));
#287606=CARTESIAN_POINT('Ctrl Pts',(0.625615862558263,1.42415911444394,
9.33630176960807));
#287607=CARTESIAN_POINT('Ctrl Pts',(0.607687486877178,1.43194365122322,
9.33769188091329));
#287608=CARTESIAN_POINT('Ctrl Pts',(0.595789301424893,1.43693487631924,
9.33860106833154));
#287609=CARTESIAN_POINT('Ctrl Pts',(0.502918919003025,1.47454157886878,
9.34560492749991));
#287610=CARTESIAN_POINT('Ctrl Pts',(0.419381089387667,1.50044135749048,
9.35136624647298));
#287611=CARTESIAN_POINT('Ctrl Pts',(0.226487766854592,1.54286231940791,
9.36437252715744));
#287612=CARTESIAN_POINT('Ctrl Pts',(0.116678221269466,1.55502524433712,
9.37159029038982));
#287613=CARTESIAN_POINT('Ctrl Pts',(-0.0137123308395208,1.55557102222298,
9.38058093610173));
#287614=CARTESIAN_POINT('Ctrl Pts',(-0.0339343744951911,1.55526127293766,
9.38198623677536));
#287615=CARTESIAN_POINT('Ctrl Pts',(-0.0666273556906808,1.55412260523556,
9.3842791019133));
#287616=CARTESIAN_POINT('Ctrl Pts',(-0.0791048237691668,1.55353747534766,
9.38515911467119));
#287617=CARTESIAN_POINT('Ctrl Pts',(-0.101350456054294,1.55222558118922,
9.38673752505595));
#287618=CARTESIAN_POINT('Ctrl Pts',(-0.111121464161474,1.5515566963633,
9.38743407788133));
#287619=CARTESIAN_POINT('Ctrl Pts',(-0.131834230012033,1.54994212576025,
9.38891789371985));
#287620=CARTESIAN_POINT('Ctrl Pts',(-0.142773543295223,1.54897274388154,
9.3897058629668));
#287621=CARTESIAN_POINT('Ctrl Pts',(-0.172289361347515,1.54604189602942,
9.39184401902448));
#287622=CARTESIAN_POINT('Ctrl Pts',(-0.190841759719558,1.54386156589375,
9.3932009714092));
#287623=CARTESIAN_POINT('Ctrl Pts',(-0.314803920101082,1.52702471841547,
9.40235893958102));
#287624=CARTESIAN_POINT('Ctrl Pts',(-0.418489423159696,1.501920196554,9.4104911160021));
#287625=CARTESIAN_POINT('Ctrl Pts',(-0.608357177766115,1.4347507566862,
9.42609442251736));
#287626=CARTESIAN_POINT('Ctrl Pts',(-0.6948480687262,1.39491844748509,9.43350368512298));
#287627=CARTESIAN_POINT('Ctrl Pts',(-0.789771283779657,1.34016910635176,
9.44165728796694));
#287628=CARTESIAN_POINT('Ctrl Pts',(-0.802271966389811,1.33272339468468,
9.44273120997891));
#287629=CARTESIAN_POINT('Ctrl Pts',(-0.820485633861986,1.32152572022651,
9.44429416106357));
#287630=CARTESIAN_POINT('Ctrl Pts',(-0.82628086758431,1.31791002620485,
9.44479119336549));
#287631=CARTESIAN_POINT('Ctrl Pts',(-0.836615876545272,1.31136695837279,
9.44567684195061));
#287632=CARTESIAN_POINT('Ctrl Pts',(-0.8411644329706,1.30845398242295,9.44606634853175));
#287633=CARTESIAN_POINT('Ctrl Pts',(-0.850097735729817,1.30266709905092,
9.44683077419142));
#287634=CARTESIAN_POINT('Ctrl Pts',(-0.854483163905904,1.29979469763431,
9.44720579083778));
#287635=CARTESIAN_POINT('Ctrl Pts',(-0.867930352825474,1.29088948377031,
9.44835523725316));
#287636=CARTESIAN_POINT('Ctrl Pts',(-0.876943623113277,1.28478350555915,
9.44912500378277));
#287637=CARTESIAN_POINT('Ctrl Pts',(-0.93143150457099,1.24703046789405,
9.45377927582328));
#287638=CARTESIAN_POINT('Ctrl Pts',(-0.975258198709604,1.21306330787374,
9.45752690921468));
#287639=CARTESIAN_POINT('Ctrl Pts',(-1.10046609302112,1.10484048345856,
9.46855628744581));
#287640=CARTESIAN_POINT('Ctrl Pts',(-1.17587112179077,1.02421962032387,
9.47566566622093));
#287641=CARTESIAN_POINT('Ctrl Pts',(-1.27067079520889,0.898456128274266,
9.48625767730017));
#287642=CARTESIAN_POINT('Ctrl Pts',(-1.29745878035107,0.859318154727518,
9.4894909768463));
#287643=CARTESIAN_POINT('Ctrl Pts',(-1.3307928331916,0.805495984516705,
9.49389829471147));
#287644=CARTESIAN_POINT('Ctrl Pts',(-1.33896116278301,0.791843619551476,
9.49501292822677));
#287645=CARTESIAN_POINT('Ctrl Pts',(-1.35211810995498,0.769067569125502,
9.49686843918668));
#287646=CARTESIAN_POINT('Ctrl Pts',(-1.35722733700829,0.760014641526437,
9.49760492812731));
#287647=CARTESIAN_POINT('Ctrl Pts',(-1.3670733164703,0.742152827294967,
9.49905642597725));
#287648=CARTESIAN_POINT('Ctrl Pts',(-1.37181661075697,0.733348109364659,
9.49977115720044));
#287649=CARTESIAN_POINT('Ctrl Pts',(-1.38294757765584,0.71220038588984,
9.50148637954612));
#287650=CARTESIAN_POINT('Ctrl Pts',(-1.38925527638184,0.699816508779698,
9.50248962237845));
#287651=CARTESIAN_POINT('Ctrl Pts',(-1.41078930501414,0.65610007401676,
9.50602815580005));
#287652=CARTESIAN_POINT('Ctrl Pts',(-1.42512726145782,0.624344218053379,
9.50859348032644));
#287653=CARTESIAN_POINT('Ctrl Pts',(-1.45851085004043,0.543250538412328,
9.51513643617743));
#287654=CARTESIAN_POINT('Ctrl Pts',(-1.47612825565984,0.493375546600439,
9.51915435051762));
#287655=CARTESIAN_POINT('Ctrl Pts',(-1.52306954352178,0.335262319226742,
9.53183527623317));
#287656=CARTESIAN_POINT('Ctrl Pts',(-1.54326198076776,0.224688153151286,
9.54064684326322));
#287657=CARTESIAN_POINT('Ctrl Pts',(-1.55302328018702,0.090558628642934,
9.55077008522699));
#287658=CARTESIAN_POINT('Ctrl Pts',(-1.5541665917424,0.0681800065310494,
9.55243931009175));
#287659=CARTESIAN_POINT('Ctrl Pts',(-1.55507076579162,0.0374735963420742,
9.55469598994108));
#287660=CARTESIAN_POINT('Ctrl Pts',(-1.55524883532423,0.0291620558589066,
9.55530343709561));
#287661=CARTESIAN_POINT('Ctrl Pts',(-1.55541955031962,0.0164266618512413,
9.55622861817319));
#287662=CARTESIAN_POINT('Ctrl Pts',(-1.55545997167684,0.0120037731757019,
9.55654889399728));
#287663=CARTESIAN_POINT('Ctrl Pts',(-1.55549362403694,0.00509865374687671,
9.55704724459287));
#287664=CARTESIAN_POINT('Ctrl Pts',(-1.55549977947085,0.00261661648208582,
9.55722603653157));
#287665=CARTESIAN_POINT('Ctrl Pts',(-1.55549999418008,0.00013455773656679,
9.55740449471797));
#287666=CARTESIAN_POINT('Ctrl Pts',(-1.55549999416998,0.000134674404654651,
9.55740448632962));
#287667=CARTESIAN_POINT('Ctrl Pts',(-1.55550028275703,-0.00319852879888876,
9.55764414118653));
#287668=CARTESIAN_POINT('Ctrl Pts',(-1.55548985752322,-0.00653175413623187,
9.55788319559715));
#287669=CARTESIAN_POINT('Ctrl Pts',(-1.55542442647104,-0.0168486752841418,
9.55862131983953));
#287670=CARTESIAN_POINT('Ctrl Pts',(-1.55533310121566,-0.0238321943166356,
9.55911841508268));
#287671=CARTESIAN_POINT('Ctrl Pts',(-1.55484660076764,-0.0483852383419172,
9.56085794921163));
#287672=CARTESIAN_POINT('Ctrl Pts',(-1.55420071026617,-0.065949245704217,
9.56208759395479));
#287673=CARTESIAN_POINT('Ctrl Pts',(-1.54805448062489,-0.180281405398427,
9.57001808780353));
#287674=CARTESIAN_POINT('Ctrl Pts',(-1.5338168189047,-0.276378287126682,
9.57634799938035));
#287675=CARTESIAN_POINT('Ctrl Pts',(-1.48751312522304,-0.465165108089252,
9.58914636655361));
#287676=CARTESIAN_POINT('Ctrl Pts',(-1.45546675969386,-0.557392943394599,
9.59559222354331));
#287677=CARTESIAN_POINT('Ctrl Pts',(-1.4067695810451,-0.664058094325602,
9.60370561485795));
#287678=CARTESIAN_POINT('Ctrl Pts',(-1.39818644981023,-0.681944569926769,
9.6050890059814));
#287679=CARTESIAN_POINT('Ctrl Pts',(-1.38421426204623,-0.709688073390144,
9.60727367126598));
#287680=CARTESIAN_POINT('Ctrl Pts',(-1.37905631298897,-0.719659612948166,
9.60806690705878));
#287681=CARTESIAN_POINT('Ctrl Pts',(-1.36921291790003,-0.738194762983717,
9.60955694979241));
#287682=CARTESIAN_POINT('Ctrl Pts',(-1.36455389470005,-0.746771841414218,
9.61025279463671));
#287683=CARTESIAN_POINT('Ctrl Pts',(-1.35393055336266,-0.765897607857494,
9.61181902503619));
#287684=CARTESIAN_POINT('Ctrl Pts',(-1.34792312654067,-0.776421482549624,
9.61269092195181));
#287685=CARTESIAN_POINT('Ctrl Pts',(-1.32991218075718,-0.807134119624555,
9.61526591720306));
#287686=CARTESIAN_POINT('Ctrl Pts',(-1.31757413248082,-0.827121629256503,
9.61698098357961));
#287687=CARTESIAN_POINT('Ctrl Pts',(-1.22124045786773,-0.975553332951358,
9.63002451022965));
#287688=CARTESIAN_POINT('Ctrl Pts',(-1.11910905297119,-1.09119547725724,
9.64207494651825));
#287689=CARTESIAN_POINT('Ctrl Pts',(-0.966342264906726,-1.21979727589253,
9.65740266118593));
#287690=CARTESIAN_POINT('Ctrl Pts',(-0.92961465222333,-1.24801453638141,
9.66091330023262));
#287691=CARTESIAN_POINT('Ctrl Pts',(-0.883131909495307,-1.28053391111836,
9.66510097441098));
#287692=CARTESIAN_POINT('Ctrl Pts',(-0.874524204746792,-1.28642780527455,
9.66586617488866));
#287693=CARTESIAN_POINT('Ctrl Pts',(-0.861533629118204,-1.29513209601409,
9.66700494227328));
#287694=CARTESIAN_POINT('Ctrl Pts',(-0.857195108438537,-1.2980076611573,
9.66738261280559));
#287695=CARTESIAN_POINT('Ctrl Pts',(-0.848450635142817,-1.30374052026392,
9.66813839148692));
#287696=CARTESIAN_POINT('Ctrl Pts',(-0.84404467001667,-1.30659726805992,
9.66851642975427));
#287697=CARTESIAN_POINT('Ctrl Pts',(-0.833789058088379,-1.31317329521972,
9.66939007640199));
#287698=CARTESIAN_POINT('Ctrl Pts',(-0.827928917189494,-1.31687585201734,
9.6698845932109));
#287699=CARTESIAN_POINT('Ctrl Pts',(-0.809227138278142,-1.32851782860721,
9.67144858787554));
#287700=CARTESIAN_POINT('Ctrl Pts',(-0.796294097619465,-1.33630982063883,
9.67250907340737));
#287701=CARTESIAN_POINT('Ctrl Pts',(-0.711245429827733,-1.38587724385318,
9.67936076999321));
#287702=CARTESIAN_POINT('Ctrl Pts',(-0.635975539747113,-1.42199319855628,
9.68486316652766));
#287703=CARTESIAN_POINT('Ctrl Pts',(-0.484166678993637,-1.48035397093751,
9.69557424374132));
#287704=CARTESIAN_POINT('Ctrl Pts',(-0.408106357669183,-1.50310128049723,
9.70076991348448));
#287705=CARTESIAN_POINT('Ctrl Pts',(-0.28680767924149,-1.52948827046994,
9.70913966347121));
#287706=CARTESIAN_POINT('Ctrl Pts',(-0.242580871023528,-1.53712293636007,
9.71220667406262));
#287707=CARTESIAN_POINT('Ctrl Pts',(-0.183013920608756,-1.54477090919968,
9.71639277502204));
#287708=CARTESIAN_POINT('Ctrl Pts',(-0.167911679392819,-1.54648533660861,
9.71745871552899));
#287709=CARTESIAN_POINT('Ctrl Pts',(-0.142587194684603,-1.54898489195791,
9.7192551076888));
#287710=CARTESIAN_POINT('Ctrl Pts',(-0.132377717971789,-1.54989078140122,
9.7199817411418));
#287711=CARTESIAN_POINT('Ctrl Pts',(-0.112203871375268,-1.55148003079474,
9.72142271268743));
#287712=CARTESIAN_POINT('Ctrl Pts',(-0.102240387568914,-1.55216844745509,
9.72213685589999));
#287713=CARTESIAN_POINT('Ctrl Pts',(-0.0801930284376602,-1.55347858851698,
9.72372290994633));
#287714=CARTESIAN_POINT('Ctrl Pts',(-0.0681072447501606,-1.55405535121208,
9.72459618306495));
#287715=CARTESIAN_POINT('Ctrl Pts',(-0.0261057610140671,-1.55556887977297,
9.72764507763219));
#287716=CARTESIAN_POINT('Ctrl Pts',(0.00382758342683263,-1.55578313791769,
9.72984280232344));
#287717=CARTESIAN_POINT('Ctrl Pts',(0.151206225656134,-1.55258499732075,
9.74079278736408));
#287718=CARTESIAN_POINT('Ctrl Pts',(0.267982377506082,-1.53673682528635,
9.74991476694166));
#287719=CARTESIAN_POINT('Ctrl Pts',(0.428458664110106,-1.49610035093421,
9.76273301789542));
#287720=CARTESIAN_POINT('Ctrl Pts',(0.474509705273616,-1.48213839622278,
9.76643971178456));
#287721=CARTESIAN_POINT('Ctrl Pts',(0.537143204565791,-1.45992957982976,
9.77146562513602));
#287722=CARTESIAN_POINT('Ctrl Pts',(0.554334921684502,-1.45348892721974,
9.77284336640256));
#287723=CARTESIAN_POINT('Ctrl Pts',(0.584147358572455,-1.44171414628763,
9.7752248709841));
#287724=CARTESIAN_POINT('Ctrl Pts',(0.596818888367281,-1.4365149023813,
9.77623464742721));
#287725=CARTESIAN_POINT('Ctrl Pts',(0.615678977299141,-1.42848378201638,
9.77773217667228));
#287726=CARTESIAN_POINT('Ctrl Pts',(0.621919909112617,-1.42577773509687,
9.77822682300302));
#287727=CARTESIAN_POINT('Ctrl Pts',(0.63316646840462,-1.42081336738367,
9.77911632509012));
#287728=CARTESIAN_POINT('Ctrl Pts',(0.638178053092129,-1.41856941199675,
9.77951199264671));
#287729=CARTESIAN_POINT('Ctrl Pts',(0.649457053639494,-1.41344732629456,
9.78040092670502));
#287730=CARTESIAN_POINT('Ctrl Pts',(0.655717318166121,-1.41055400896892,
9.78089326634564));
#287731=CARTESIAN_POINT('Ctrl Pts',(0.674789019925197,-1.40158519680976,
9.78239057054935));
#287732=CARTESIAN_POINT('Ctrl Pts',(0.687537243998021,-1.39537588506913,
9.78338782621608));
#287733=CARTESIAN_POINT('Ctrl Pts',(0.790024926813116,-1.34371124855323,
9.79139032860938));
#287734=CARTESIAN_POINT('Ctrl Pts',(0.875259958601092,-1.28981599892396,
9.79796311152944));
#287735=CARTESIAN_POINT('Ctrl Pts',(1.03232468202175,-1.16771266684552,
9.81105993526825));
#287736=CARTESIAN_POINT('Ctrl Pts',(1.1040417640007,-1.10015245984276,9.81755717733517));
#287737=CARTESIAN_POINT('Ctrl Pts',(1.1823535400239,-1.01095805281637,9.8257637803017));
#287738=CARTESIAN_POINT('Ctrl Pts',(1.19550440325007,-0.995371906852973,
9.82718493865666));
#287739=CARTESIAN_POINT('Ctrl Pts',(1.215486898086,-0.970721634816739,9.82941587123197));
#287740=CARTESIAN_POINT('Ctrl Pts',(1.22253247013869,-0.961833269833098,
9.83021702244878));
#287741=CARTESIAN_POINT('Ctrl Pts',(1.23545379987884,-0.9451609681197,9.83171424143816));
#287742=CARTESIAN_POINT('Ctrl Pts',(1.24135480810615,-0.937397236895416,
9.83240926335743));
#287743=CARTESIAN_POINT('Ctrl Pts',(1.2543339186761,-0.919983630970535,
9.83396365329924));
#287744=CARTESIAN_POINT('Ctrl Pts',(1.26137437478862,-0.910306614591972,
9.83482442937653));
#287745=CARTESIAN_POINT('Ctrl Pts',(1.27897485068468,-0.885518724345106,
9.8370222560162));
#287746=CARTESIAN_POINT('Ctrl Pts',(1.28937891783265,-0.870299966685399,
9.8383650979098));
#287747=CARTESIAN_POINT('Ctrl Pts',(1.3704516946631,-0.74706356939018,9.84919143650503));
#287748=CARTESIAN_POINT('Ctrl Pts',(1.4276817383381,-0.630835247412634,
9.85917718260273));
#287749=CARTESIAN_POINT('Ctrl Pts',(1.49216082625455,-0.444598579366025,
9.87444765146964));
#287750=CARTESIAN_POINT('Ctrl Pts',(1.5101842585719,-0.378889464329262,
9.8796949560682));
#287751=CARTESIAN_POINT('Ctrl Pts',(1.52691694778779,-0.297218614441416,
9.88590578026204));
#287752=CARTESIAN_POINT('Ctrl Pts',(1.5297662692152,-0.282186956512261,
9.88703608545995));
#287753=CARTESIAN_POINT('Ctrl Pts',(1.53361398350782,-0.260113269747403,
9.88867490303611));
#287754=CARTESIAN_POINT('Ctrl Pts',(1.53478649749467,-0.253103093448858,
9.88919227078725));
#287755=CARTESIAN_POINT('Ctrl Pts',(1.53669795941808,-0.241172923148172,
9.89006722415167));
#287756=CARTESIAN_POINT('Ctrl Pts',(1.53746140704036,-0.236257109770576,
9.89042614754676));
#287757=CARTESIAN_POINT('Ctrl Pts',(1.53915161729373,-0.225018621974873,
9.89124301996263));
#287758=CARTESIAN_POINT('Ctrl Pts',(1.54006301989316,-0.218693804004924,
9.8917001071892));
#287759=CARTESIAN_POINT('Ctrl Pts',(1.54248670461875,-0.201107243806639,
9.89296421256612));
#287760=CARTESIAN_POINT('Ctrl Pts',(1.54391464499911,-0.189833996497205,
9.89376672873699));
#287761=CARTESIAN_POINT('Ctrl Pts',(1.55378472154521,-0.104413676074503,
9.89979568497269));
#287762=CARTESIAN_POINT('Ctrl Pts',(1.55700586552081,-0.0297502730893351,
9.90477226802757));
#287763=CARTESIAN_POINT('Ctrl Pts',(1.55233898235879,0.131985944113632,
9.91546073616916));
#287764=CARTESIAN_POINT('Ctrl Pts',(1.54250761532666,0.218737898493034,
9.9211420544111));
#287765=CARTESIAN_POINT('Ctrl Pts',(1.5156306293346,0.353513332928016,9.93037052954646));
#287766=CARTESIAN_POINT('Ctrl Pts',(1.50341463739465,0.402307690465278,
9.93379561904323));
#287767=CARTESIAN_POINT('Ctrl Pts',(1.48429066455844,0.465521597197536,
9.93839436636857));
#287768=CARTESIAN_POINT('Ctrl Pts',(1.47949313175148,0.480550908392065,
9.93949988649892));
#287769=CARTESIAN_POINT('Ctrl Pts',(1.47116544608461,0.505331538667625,
9.94134429503418));
#287770=CARTESIAN_POINT('Ctrl Pts',(1.46776480940656,0.515125410530437,
9.94207890347509));
#287771=CARTESIAN_POINT('Ctrl Pts',(1.46092442894339,0.534207977393643,
9.94352170547116));
#287772=CARTESIAN_POINT('Ctrl Pts',(1.45749335683181,0.543499270120955,
9.94422958146824));
#287773=CARTESIAN_POINT('Ctrl Pts',(1.44902953093396,0.565762547329572,
9.94593906895808));
#287774=CARTESIAN_POINT('Ctrl Pts',(1.4439110803823,0.578700794932979,9.94694350416619));
#287775=CARTESIAN_POINT('Ctrl Pts',(1.42630147643978,0.621525146083746,
9.95030579230358));
#287776=CARTESIAN_POINT('Ctrl Pts',(1.41305126254654,0.651087744507704,
9.95268881102911));
#287777=CARTESIAN_POINT('Ctrl Pts',(1.34866117365497,0.783508821890407,
9.96365567864379));
#287778=CARTESIAN_POINT('Ctrl Pts',(1.28715315627535,0.880909658696088,
9.97258013580306));
#287779=CARTESIAN_POINT('Ctrl Pts',(1.18593295854578,1.00766496968798,9.98513811393158));
#287780=CARTESIAN_POINT('Ctrl Pts',(1.15468543650378,1.04332535705893,9.98878890275042));
#287781=CARTESIAN_POINT('Ctrl Pts',(1.10925603859308,1.09062467435328,9.99374758269093));
#287782=CARTESIAN_POINT('Ctrl Pts',(1.09642565374744,1.10352253732243,9.99511255768981));
#287783=CARTESIAN_POINT('Ctrl Pts',(1.07361146293197,1.12566587766457,9.99747433841182));
#287784=CARTESIAN_POINT('Ctrl Pts',(1.06372729469394,1.13501080060207,9.9984770299408));
#287785=CARTESIAN_POINT('Ctrl Pts',(1.04873150021597,1.14882048434801,9.9999661922508));
#287786=CARTESIAN_POINT('Ctrl Pts',(1.04371148565885,1.153383112477,10.0004594481348));
#287787=CARTESIAN_POINT('Ctrl Pts',(1.03457401949868,1.16157952864541,10.0013475609652));
#287788=CARTESIAN_POINT('Ctrl Pts',(1.03046704893257,1.16522447050142,10.0017432159499));
#287789=CARTESIAN_POINT('Ctrl Pts',(1.02114409405221,1.17341076103271,10.0026334939973));
#287790=CARTESIAN_POINT('Ctrl Pts',(1.01591704021907,1.1779391525821,10.0031271760292));
#287791=CARTESIAN_POINT('Ctrl Pts',(0.999805033205883,1.19171055702188,
10.0046328970824));
#287792=CARTESIAN_POINT('Ctrl Pts',(0.988822490618536,1.20083898842838,
10.0056371002573));
#287793=CARTESIAN_POINT('Ctrl Pts',(0.900689036249659,1.27206426212623,
10.0135364493857));
#287794=CARTESIAN_POINT('Ctrl Pts',(0.817882172923474,1.32682430962124,
10.0200134381943));
#287795=CARTESIAN_POINT('Ctrl Pts',(0.640431825087845,1.42120215557,10.0332436049806));
#287796=CARTESIAN_POINT('Ctrl Pts',(0.545971357085858,1.46009587175521,
10.039974704033));
#287797=CARTESIAN_POINT('Ctrl Pts',(0.430043180694643,1.49499509881758,
10.0483599537802));
#287798=CARTESIAN_POINT('Ctrl Pts',(0.411593542487943,1.50017938344392,
10.0496972668633));
#287799=CARTESIAN_POINT('Ctrl Pts',(0.382328657470157,1.50782224269089,
10.051825445954));
#287800=CARTESIAN_POINT('Ctrl Pts',(0.371574417018773,1.510508377687,10.0526089625023));
#287801=CARTESIAN_POINT('Ctrl Pts',(0.351281845404221,1.51534712632508,
10.0540906072181));
#287802=CARTESIAN_POINT('Ctrl Pts',(0.341750091707609,1.51752519418082,
10.0547878784527));
#287803=CARTESIAN_POINT('Ctrl Pts',(0.320158435165672,1.52224528924209,
10.0563706590364));
#287804=CARTESIAN_POINT('Ctrl Pts',(0.308087711444384,1.52473410470632,
10.0572578211574));
#287805=CARTESIAN_POINT('Ctrl Pts',(0.276699017408507,1.53081807765217,
10.0595713809875));
#287806=CARTESIAN_POINT('Ctrl Pts',(0.257340775937371,1.53419098966539,
10.0610046732927));
#287807=CARTESIAN_POINT('Ctrl Pts',(0.121106731183515,1.55527706552206,
10.0711407283076));
#287808=CARTESIAN_POINT('Ctrl Pts',(0.00262974571132385,1.5599795374538,
10.080252988605));
#287809=CARTESIAN_POINT('Ctrl Pts',(-0.195502670443402,1.54526418999826,
10.0956585921149));
#287810=CARTESIAN_POINT('Ctrl Pts',(-0.275220110826221,1.53307515730967,
10.1018899876751));
#287811=CARTESIAN_POINT('Ctrl Pts',(-0.366109826532087,1.51185573010769,
10.1088132266375));
#287812=CARTESIAN_POINT('Ctrl Pts',(-0.378541194094416,1.50879115398084,
10.1097559589325));
#287813=CARTESIAN_POINT('Ctrl Pts',(-0.397344710575575,1.50390867454509,
10.1111741372148));
#287814=CARTESIAN_POINT('Ctrl Pts',(-0.403745052507108,1.50220306793325,
10.1116554787919));
#287815=CARTESIAN_POINT('Ctrl Pts',(-0.415439262475882,1.49900657525242,
10.1125321810081));
#287816=CARTESIAN_POINT('Ctrl Pts',(-0.420736229318641,1.49752847075871,
10.1129282189027));
#287817=CARTESIAN_POINT('Ctrl Pts',(-0.432856925525221,1.49407683358175,
10.1138320753268));
#287818=CARTESIAN_POINT('Ctrl Pts',(-0.43967510077126,1.49208462013105,
10.114338817767));
#287819=CARTESIAN_POINT('Ctrl Pts',(-0.461109158996897,1.48566208631213,
10.1159271972903));
#287820=CARTESIAN_POINT('Ctrl Pts',(-0.475674120412569,1.48106301966805,
10.1169997046496));
#287821=CARTESIAN_POINT('Ctrl Pts',(-0.563831049768818,1.45179165246312,
10.123463092541));
#287822=CARTESIAN_POINT('Ctrl Pts',(-0.635568541283272,1.42185098505046,
10.1286057260794));
#287823=CARTESIAN_POINT('Ctrl Pts',(-0.778950850787198,1.34897684784595,
10.1392071448373));
#287824=CARTESIAN_POINT('Ctrl Pts',(-0.849975172472318,1.30539045520361,
10.1446482553512));
#287825=CARTESIAN_POINT('Ctrl Pts',(-0.954387770436467,1.22916535658077,
10.1533563840111));
#287826=CARTESIAN_POINT('Ctrl Pts',(-0.990375298541162,1.20035811270532,
10.1565039690023));
#287827=CARTESIAN_POINT('Ctrl Pts',(-1.03656408924026,1.15989237962767,
10.1607832418634));
#287828=CARTESIAN_POINT('Ctrl Pts',(-1.04794889928893,1.14961668330011,
10.1618585899196));
#287829=CARTESIAN_POINT('Ctrl Pts',(-1.06670656595603,1.1321762167919,10.1636664099232));
#287830=CARTESIAN_POINT('Ctrl Pts',(-1.07416384505524,1.12510351013287,
10.1643949561803));
#287831=CARTESIAN_POINT('Ctrl Pts',(-1.08871355923758,1.11102761985242,
10.1658363195881));
#287832=CARTESIAN_POINT('Ctrl Pts',(-1.09580986223409,1.10402913161156,
10.1665489121025));
#287833=CARTESIAN_POINT('Ctrl Pts',(-1.11289300223572,1.08685449654158,
10.1682882549027));
#287834=CARTESIAN_POINT('Ctrl Pts',(-1.12280795345046,1.0766084736797,10.1693180804695));
#287835=CARTESIAN_POINT('Ctrl Pts',(-1.15640672191953,1.04091881975398,
10.1728797906328));
#287836=CARTESIAN_POINT('Ctrl Pts',(-1.17937615148186,1.01482019878623,
10.1754412064161));
#287837=CARTESIAN_POINT('Ctrl Pts',(-1.28899456197786,0.881516246348095,
10.1883249848979));
#287838=CARTESIAN_POINT('Ctrl Pts',(-1.36199198907029,0.763900554405123,
10.1991542943032));
#287839=CARTESIAN_POINT('Ctrl Pts',(-1.4309878576702,0.61055382567494,10.2120521911623));
#287840=CARTESIAN_POINT('Ctrl Pts',(-1.44263400513142,0.58250286191313,
10.214362459187));
#287841=CARTESIAN_POINT('Ctrl Pts',(-1.46052457114569,0.535576671132989,
10.2181288594078));
#287842=CARTESIAN_POINT('Ctrl Pts',(-1.46724161869346,0.516891209679864,
10.2196034149299));
#287843=CARTESIAN_POINT('Ctrl Pts',(-1.47612025574444,0.490623292072964,
10.2216366663696));
#287844=CARTESIAN_POINT('Ctrl Pts',(-1.4785844581269,0.483146180167272,
10.2222109891023));
#287845=CARTESIAN_POINT('Ctrl Pts',(-1.48270149809656,0.470327307820379,
10.2231876683119));
#287846=CARTESIAN_POINT('Ctrl Pts',(-1.48438247181777,0.464994828593312,
10.2235916089882));
#287847=CARTESIAN_POINT('Ctrl Pts',(-1.48785803909051,0.453758500868902,
10.2244377245585));
#287848=CARTESIAN_POINT('Ctrl Pts',(-1.48964630277208,0.447852897469462,
10.2248795401082));
#287849=CARTESIAN_POINT('Ctrl Pts',(-1.4944269536241,0.43171968122671,10.2260790576758));
#287850=CARTESIAN_POINT('Ctrl Pts',(-1.49734952991703,0.421471475563612,
10.2268328806923));
#287851=CARTESIAN_POINT('Ctrl Pts',(-1.5118473082501,0.368578921152341,
10.2306856283154));
#287852=CARTESIAN_POINT('Ctrl Pts',(-1.52170810815697,0.325481136059841,
10.2336990399143));
#287853=CARTESIAN_POINT('Ctrl Pts',(-1.54679324570656,0.18941422676566,
10.2429895469406));
#287854=CARTESIAN_POINT('Ctrl Pts',(-1.55542223528351,0.0954485765964083,
10.2490946175472));
#287855=CARTESIAN_POINT('Ctrl Pts',(-1.55555778339162,-0.0698115119313443,
10.2600558083044));
#287856=CARTESIAN_POINT('Ctrl Pts',(-1.55074307203602,-0.140810644178326,
10.2648357607052));
#287857=CARTESIAN_POINT('Ctrl Pts',(-1.53866980533155,-0.228896468480794,
10.2710059133485));
#287858=CARTESIAN_POINT('Ctrl Pts',(-1.53594418862713,-0.246523359982548,
10.2722524768428));
#287859=CARTESIAN_POINT('Ctrl Pts',(-1.53108222236097,-0.274743801026789,
10.2742692838235));
#287860=CARTESIAN_POINT('Ctrl Pts',(-1.52913747026924,-0.285369084247679,
10.2750334554457));
#287861=CARTESIAN_POINT('Ctrl Pts',(-1.52521148618826,-0.305625325018494,
10.2764999494272));
#287862=CARTESIAN_POINT('Ctrl Pts',(-1.52324928150381,-0.315259472701574,
10.2772016334052));
#287863=CARTESIAN_POINT('Ctrl Pts',(-1.51851787066576,-0.337413905063551,
10.2788252310613));
#287864=CARTESIAN_POINT('Ctrl Pts',(-1.51568494839313,-0.349919684767954,
10.2797491400094));
#287865=CARTESIAN_POINT('Ctrl Pts',(-1.50614370277902,-0.38974714783133,
10.2827160883936));
#287866=CARTESIAN_POINT('Ctrl Pts',(-1.49884901282413,-0.416921022803087,
10.2847776408498));
#287867=CARTESIAN_POINT('Ctrl Pts',(-1.47968117304966,-0.48129832678765,
10.2897543422745));
#287868=CARTESIAN_POINT('Ctrl Pts',(-1.46713648761081,-0.518280359918293,
10.2926888874893));
#287869=CARTESIAN_POINT('Ctrl Pts',(-1.42833735818726,-0.619918213160373,
10.3009612327957));
#287870=CARTESIAN_POINT('Ctrl Pts',(-1.39910567361655,-0.683336087076675,
10.3063673298517));
#287871=CARTESIAN_POINT('Ctrl Pts',(-1.36023814559239,-0.754628106988403,
10.3126634426789));
#287872=CARTESIAN_POINT('Ctrl Pts',(-1.35464563125508,-0.764621872736702,
10.3135511450327));
#287873=CARTESIAN_POINT('Ctrl Pts',(-1.31372492335823,-0.835888412696872,
10.3199151809774));
#287874=CARTESIAN_POINT('Ctrl Pts',(-1.27435988941164,-0.894757989023516,
10.3253566874165));
#287875=CARTESIAN_POINT('Ctrl Pts',(-1.22419529206447,-0.959715834888923,
10.3314287263364));
#287876=CARTESIAN_POINT('Ctrl Pts',(-1.21717276664652,-0.968606768963859,
10.3322613007936));
#287877=CARTESIAN_POINT('Ctrl Pts',(-1.20604325932987,-0.982385177079956,
10.3335528757858));
#287878=CARTESIAN_POINT('Ctrl Pts',(-1.20200244626771,-0.987325226353898,
10.3340162217376));
#287879=CARTESIAN_POINT('Ctrl Pts',(-1.194757449722,-0.996072106540608,
10.3348368982606));
#287880=CARTESIAN_POINT('Ctrl Pts',(-1.19156536120063,-0.999888491878426,
10.3351950448079));
#287881=CARTESIAN_POINT('Ctrl Pts',(-1.18376258670696,-1.00912687038524,
10.3360622932033));
#287882=CARTESIAN_POINT('Ctrl Pts',(-1.17913292166726,-1.01453263157986,
10.336570013035));
#287883=CARTESIAN_POINT('Ctrl Pts',(-1.16439966563491,-1.03149860840886,
10.3381650227622));
#287884=CARTESIAN_POINT('Ctrl Pts',(-1.15416156682199,-1.04294155382191,
10.3392430712287));
#287885=CARTESIAN_POINT('Ctrl Pts',(-1.12928139194888,-1.06993451257986,
10.3417970393092));
#287886=CARTESIAN_POINT('Ctrl Pts',(-1.11448492323738,-1.08533855444128,
10.3432634902233));
#287887=CARTESIAN_POINT('Ctrl Pts',(-1.05538592764409,-1.14438069470012,
10.3489436974122));
#287888=CARTESIAN_POINT('Ctrl Pts',(-1.0087976994095,-1.18565383025421,
10.3530474331675));
#287889=CARTESIAN_POINT('Ctrl Pts',(-0.873212322475403,-1.29197727348091,
10.364393838861));
#287890=CARTESIAN_POINT('Ctrl Pts',(-0.779605273994225,-1.35052475871853,
10.3716071232752));
#287891=CARTESIAN_POINT('Ctrl Pts',(-0.662415596436684,-1.40754932852141,
10.3805932530735));
#287892=CARTESIAN_POINT('Ctrl Pts',(-0.644053977505205,-1.41604517734656,
10.3819990632949));
#287893=CARTESIAN_POINT('Ctrl Pts',(-0.61409390588095,-1.42920432766385,
10.3842926099728));
#287894=CARTESIAN_POINT('Ctrl Pts',(-0.602595412565447,-1.43409033467969,
10.3851727873525));
#287895=CARTESIAN_POINT('Ctrl Pts',(-0.581979842104226,-1.44255871369994,
10.3867513972379));
#287896=CARTESIAN_POINT('Ctrl Pts',(-0.572885326888024,-1.44619451434073,
10.3874479834532));
#287897=CARTESIAN_POINT('Ctrl Pts',(-0.553522629852327,-1.45372402325419,
10.3889317681512));
#287898=CARTESIAN_POINT('Ctrl Pts',(-0.543246382123762,-1.45759534659028,
10.3897196719726));
#287899=CARTESIAN_POINT('Ctrl Pts',(-0.515386205198999,-1.46775544187331,
10.3918573921451));
#287900=CARTESIAN_POINT('Ctrl Pts',(-0.497729115683304,-1.4738367103225,
10.3932139686503));
#287901=CARTESIAN_POINT('Ctrl Pts',(-0.458334857396247,-1.48661582965281,
10.3962457433056));
#287902=CARTESIAN_POINT('Ctrl Pts',(-0.436551981836944,-1.49315763917231,
10.3979255965166));
#287903=CARTESIAN_POINT('Ctrl Pts',(-0.366971135532644,-1.51240140275147,
10.403303589534));
#287904=CARTESIAN_POINT('Ctrl Pts',(-0.318710678453787,-1.52330183641062,
10.4070526584185));
#287905=CARTESIAN_POINT('Ctrl Pts',(-0.230601105354797,-1.53883243756245,
10.4139156864411));
#287906=CARTESIAN_POINT('Ctrl Pts',(-0.190932980983744,-1.54425597800546,
10.4170117432303));
#287907=CARTESIAN_POINT('Ctrl Pts',(-0.0629510142981618,-1.55674722084487,
10.4269803588373));
#287908=CARTESIAN_POINT('Ctrl Pts',(0.0257810817923055,-1.55780710454275,
10.4338694696636));
#287909=CARTESIAN_POINT('Ctrl Pts',(0.127536771487344,-1.55032106198754,
10.4414656322018));
#287910=CARTESIAN_POINT('Ctrl Pts',(0.140932970232763,-1.5491607252896,
10.4424593313239));
#287911=CARTESIAN_POINT('Ctrl Pts',(0.161112251171879,-1.54714892033522,
10.4439449990884));
#287912=CARTESIAN_POINT('Ctrl Pts',(0.167907121701986,-1.54642624857865,
10.4444433426678));
#287913=CARTESIAN_POINT('Ctrl Pts',(0.180240509369209,-1.54503227469975,
10.4453441393797));
#287914=CARTESIAN_POINT('Ctrl Pts',(0.185780590031195,-1.54437590878461,
10.4457473914912));
#287915=CARTESIAN_POINT('Ctrl Pts',(0.197331351165391,-1.54294436485019,
10.4465851282527));
#287916=CARTESIAN_POINT('Ctrl Pts',(0.203341199504102,-1.54216384833866,
10.4470193163872));
#287917=CARTESIAN_POINT('Ctrl Pts',(0.21939040513181,-1.53998403944075,
10.448174675313));
#287918=CARTESIAN_POINT('Ctrl Pts',(0.229421117952308,-1.53852167895274,
10.4488924417808));
#287919=CARTESIAN_POINT('Ctrl Pts',(0.280510396077361,-1.53056268096855,
10.4525294553288));
#287920=CARTESIAN_POINT('Ctrl Pts',(0.321314980448829,-1.52251949090368,
10.455372461685));
#287921=CARTESIAN_POINT('Ctrl Pts',(0.467373679116573,-1.48759398349703,
10.4654843255016));
#287922=CARTESIAN_POINT('Ctrl Pts',(0.570063614919924,-1.4513455813214,
10.472489895161));
#287923=CARTESIAN_POINT('Ctrl Pts',(0.72348968866107,-1.37836824980115,
10.4838139316509));
#287924=CARTESIAN_POINT('Ctrl Pts',(0.777224774687447,-1.34879822267972,
10.4879584466551));
#287925=CARTESIAN_POINT('Ctrl Pts',(0.843654765564453,-1.30695215884026,
10.4934122914425));
#287926=CARTESIAN_POINT('Ctrl Pts',(0.858083750356122,-1.29752439095823,
10.4946178069833));
#287927=CARTESIAN_POINT('Ctrl Pts',(0.881193362177257,-1.28187071438337,
10.4965845935519));
#287928=CARTESIAN_POINT('Ctrl Pts',(0.889972003179118,-1.27579155556228,
10.497340344943));
#287929=CARTESIAN_POINT('Ctrl Pts',(0.906749213119442,-1.26391600854525,
10.4988018365269));
#287930=CARTESIAN_POINT('Ctrl Pts',(0.91475654647108,-1.25813284853416,
10.4995070456327));
#287931=CARTESIAN_POINT('Ctrl Pts',(0.933267382592734,-1.2444935818224,
10.5011556291431));
#287932=CARTESIAN_POINT('Ctrl Pts',(0.943727532569405,-1.23658020658337,
10.5021011980458));
#287933=CARTESIAN_POINT('Ctrl Pts',(0.977643529692664,-1.21024089886292,
10.5052141879077));
#287934=CARTESIAN_POINT('Ctrl Pts',(1.00066829970582,-1.19127353389988,
10.5074027681746));
#287935=CARTESIAN_POINT('Ctrl Pts',(1.05500848846734,-1.14382177209762,
10.5127577380176));
#287936=CARTESIAN_POINT('Ctrl Pts',(1.08573282367552,-1.11469943753933,
10.51594775182));
#287937=CARTESIAN_POINT('Ctrl Pts',(1.16078419878238,-1.0375117210223,10.5241592268994));
#287938=CARTESIAN_POINT('Ctrl Pts',(1.20333872351954,-0.98783879239174,
10.5292267054032));
#287939=CARTESIAN_POINT('Ctrl Pts',(1.25148938714117,-0.92388904017262,
10.5354332311974));
#287940=CARTESIAN_POINT('Ctrl Pts',(1.2601706465525,-0.912012385686716,
10.5365732070718));
#287941=CARTESIAN_POINT('Ctrl Pts',(1.30698159082118,-0.846026533774559,
10.5428325413802));
#287942=CARTESIAN_POINT('Ctrl Pts',(1.3418005616862,-0.789642386365013,
10.5479132722681));
#287943=CARTESIAN_POINT('Ctrl Pts',(1.37823881746493,-0.721225245647919,
10.5536477762503));
#287944=CARTESIAN_POINT('Ctrl Pts',(1.38344510682597,-0.711187562539177,
10.5544786739812));
#287945=CARTESIAN_POINT('Ctrl Pts',(1.3914163810047,-0.695400161104967,
10.5557682950819));
#287946=CARTESIAN_POINT('Ctrl Pts',(1.39425611027449,-0.689688938764902,
10.556231341307));
#287947=CARTESIAN_POINT('Ctrl Pts',(1.39924754260943,-0.679493413981871,
10.557051565937));
#287948=CARTESIAN_POINT('Ctrl Pts',(1.40141290371434,-0.675016192103785,
10.5574095589381));
#287949=CARTESIAN_POINT('Ctrl Pts',(1.40662502700094,-0.664106123636475,
10.5582766773427));
#287950=CARTESIAN_POINT('Ctrl Pts',(1.40964916408628,-0.657662641111094,
10.5587844182476));
#287951=CARTESIAN_POINT('Ctrl Pts',(1.41906740637651,-0.637231876266187,
10.5603812663252));
#287952=CARTESIAN_POINT('Ctrl Pts',(1.4252986042657,-0.623169883307742,
10.5614610829948));
#287953=CARTESIAN_POINT('Ctrl Pts',(1.43970296880999,-0.5893165438916,10.5640203863862));
#287954=CARTESIAN_POINT('Ctrl Pts',(1.44767825100385,-0.569443946417325,
10.5654903335902));
#287955=CARTESIAN_POINT('Ctrl Pts',(1.47730900861638,-0.490960225240623,
10.5711935793446));
#287956=CARTESIAN_POINT('Ctrl Pts',(1.49583688236512,-0.431227383744786,
10.5753157532356));
#287957=CARTESIAN_POINT('Ctrl Pts',(1.53686570831554,-0.26394852550015,
10.5866559109783));
#287958=CARTESIAN_POINT('Ctrl Pts',(1.55165267317818,-0.154904759903231,
10.5938458883134));
#287959=CARTESIAN_POINT('Ctrl Pts',(1.55543111817508,-0.0249825338918657,
10.6028071309361));
#287960=CARTESIAN_POINT('Ctrl Pts',(1.55562449791537,-0.00473785627870441,
10.6042137983517));
#287961=CARTESIAN_POINT('Ctrl Pts',(1.55529823443904,0.0279940667465249,
10.6065079895558));
#287962=CARTESIAN_POINT('Ctrl Pts',(1.5550233035138,0.0404817879896868,
10.6073879277963));
#287963=CARTESIAN_POINT('Ctrl Pts',(1.55426484255743,0.0627438938977422,
10.6089656125016));
#287964=CARTESIAN_POINT('Ctrl Pts',(1.55383940084023,0.072519689933121,
10.609661507439));
#287965=CARTESIAN_POINT('Ctrl Pts',(1.55274178298795,0.0932383780253285,
10.611143270734));
#287966=CARTESIAN_POINT('Ctrl Pts',(1.55204609293042,0.104179430716684,
10.6119298388837));
#287967=CARTESIAN_POINT('Ctrl Pts',(1.54985664885033,0.133684113697593,
10.6140624736075));
#287968=CARTESIAN_POINT('Ctrl Pts',(1.54814510913308,0.152229232863489,
10.6154152635268));
#287969=CARTESIAN_POINT('Ctrl Pts',(1.53430153034745,0.277588079512021,
10.624647245127));
#287970=CARTESIAN_POINT('Ctrl Pts',(1.51145983887872,0.382905877595805,
10.6328654629736));
#287971=CARTESIAN_POINT('Ctrl Pts',(1.44869778326232,0.574159241408667,
10.6484632636017));
#287972=CARTESIAN_POINT('Ctrl Pts',(1.41143287498937,0.660488014155566,
10.6557775164042));
#287973=CARTESIAN_POINT('Ctrl Pts',(1.35959387539875,0.755844274568032,
10.6638557143908));
#287974=CARTESIAN_POINT('Ctrl Pts',(1.35239435741742,0.768651817858647,
10.6649403832672));
#287975=CARTESIAN_POINT('Ctrl Pts',(1.34150285625015,0.787400278453324,
10.666525625232));
#287976=CARTESIAN_POINT('Ctrl Pts',(1.3379507952754,0.793420938917952,10.667034294153));
#287977=CARTESIAN_POINT('Ctrl Pts',(1.33153668505157,0.804127133513199,
10.6679378426498));
#287978=CARTESIAN_POINT('Ctrl Pts',(1.32869029290779,0.808821673148615,
10.6683336747954));
#287979=CARTESIAN_POINT('Ctrl Pts',(1.32231089122076,0.819218622424716,
10.6692095155771));
#287980=CARTESIAN_POINT('Ctrl Pts',(1.31876579616933,0.824913343140161,
10.6696887336866));
#287981=CARTESIAN_POINT('Ctrl Pts',(1.30812217912994,0.841766900617,10.6711060364384));
#287982=CARTESIAN_POINT('Ctrl Pts',(1.30091784767906,0.852858683873841,
10.6720375599177));
#287983=CARTESIAN_POINT('Ctrl Pts',(1.24708471021245,0.933470422840288,
10.6788090708455));
#287984=CARTESIAN_POINT('Ctrl Pts',(1.19504641977618,0.999227379502725,
10.6843451181547));
#287985=CARTESIAN_POINT('Ctrl Pts',(1.06033010348591,1.14378589566827,10.6973622566328));
#287986=CARTESIAN_POINT('Ctrl Pts',(0.973797002134742,1.21830287971126,
10.70480712362));
#287987=CARTESIAN_POINT('Ctrl Pts',(0.863392823299522,1.29403800647458,
10.7140413685535));
#287988=CARTESIAN_POINT('Ctrl Pts',(0.846657264207012,1.30504901972728,
10.7154337115358));
#287989=CARTESIAN_POINT('Ctrl Pts',(0.819192654105145,1.32236847232441,
10.7177098923828));
#287990=CARTESIAN_POINT('Ctrl Pts',(0.808592003837131,1.32887694557807,
10.7185863683123));
#287991=CARTESIAN_POINT('Ctrl Pts',(0.789508591017037,1.34028069101927,
10.7201611970957));
#287992=CARTESIAN_POINT('Ctrl Pts',(0.781055409056963,1.34522436269302,
10.7208577439249));
#287993=CARTESIAN_POINT('Ctrl Pts',(0.762989615306636,1.35556209231758,
10.7223445026011));
#287994=CARTESIAN_POINT('Ctrl Pts',(0.753365263535971,1.36093442432579,
10.7231354474182));
#287995=CARTESIAN_POINT('Ctrl Pts',(0.727126487152051,1.37521734410045,
10.725289284484));
#287996=CARTESIAN_POINT('Ctrl Pts',(0.710406330958108,1.38392863212785,
10.7266591039591));
#287997=CARTESIAN_POINT('Ctrl Pts',(0.598033178483485,1.43990261176447,
10.7358518109454));
#287998=CARTESIAN_POINT('Ctrl Pts',(0.497911531314452,1.4775110747223,10.7440068925978));
#287999=CARTESIAN_POINT('Ctrl Pts',(0.303732709501313,1.52845716939883,
10.7595594139434));
#288000=CARTESIAN_POINT('Ctrl Pts',(0.210727454962227,1.54403105497301,
10.766893875974));
#288001=CARTESIAN_POINT('Ctrl Pts',(0.102257955602408,1.55220440760566,
10.7749886226034));
#288002=CARTESIAN_POINT('Ctrl Pts',(0.0876222453373523,1.55309935159465,
10.7760709706367));
#288003=CARTESIAN_POINT('Ctrl Pts',(0.065988560427154,1.55411540216812,
10.777654221212));
#288004=CARTESIAN_POINT('Ctrl Pts',(0.0589994227280295,1.55439642515554,
10.7781631591538));
#288005=CARTESIAN_POINT('Ctrl Pts',(0.0465016608314698,1.55481452404732,
10.7790683765666));
#288006=CARTESIAN_POINT('Ctrl Pts',(0.0409939780867431,1.55496948688485,
10.7794655952343));
#288007=CARTESIAN_POINT('Ctrl Pts',(0.0287296902881134,1.55524934234485,
10.7803463327242));
#288008=CARTESIAN_POINT('Ctrl Pts',(0.021972984108787,1.5553594775743,10.7808290399741));
#288009=CARTESIAN_POINT('Ctrl Pts',(0.00183837887307059,1.55555643990433,
10.7822605704648));
#288010=CARTESIAN_POINT('Ctrl Pts',(-0.0115405695724038,1.55551472639249,
10.7832027000114));
#288011=CARTESIAN_POINT('Ctrl Pts',(-0.105004327787419,1.55401731784783,
10.7897313233805));
#288012=CARTESIAN_POINT('Ctrl Pts',(-0.184883658543911,1.54655013284623,
10.7950427095603));
#288013=CARTESIAN_POINT('Ctrl Pts',(-0.378791620122958,1.51317616014496,
10.8080208358642));
#288014=CARTESIAN_POINT('Ctrl Pts',(-0.491138215690739,1.48052858247418,
10.8156400709515));
#288015=CARTESIAN_POINT('Ctrl Pts',(-0.616971025614448,1.42804609339886,
10.8250491812092));
#288016=CARTESIAN_POINT('Ctrl Pts',(-0.635019229594381,1.42011246379444,
10.8264200351323));
#288017=CARTESIAN_POINT('Ctrl Pts',(-0.664129891990716,1.40665010383958,
10.8286690417006));
#288018=CARTESIAN_POINT('Ctrl Pts',(-0.675286132463599,1.40132853097771,
10.8295401717767));
#288019=CARTESIAN_POINT('Ctrl Pts',(-0.695176004726446,1.39154831177086,
10.8311105631656));
#288020=CARTESIAN_POINT('Ctrl Pts',(-0.703933229263837,1.38713891959598,
10.8318080888403));
#288021=CARTESIAN_POINT('Ctrl Pts',(-0.722528085320177,1.37755470478362,
10.8333026094493));
#288022=CARTESIAN_POINT('Ctrl Pts',(-0.732353054938445,1.37235665547291,
10.834100389834));
#288023=CARTESIAN_POINT('Ctrl Pts',(-0.759011369935997,1.35788487633202,
10.8362878065772));
#288024=CARTESIAN_POINT('Ctrl Pts',(-0.775729385831765,1.34840404024374,
10.8376847073528));
#288025=CARTESIAN_POINT('Ctrl Pts',(-0.884120205623191,1.28425238790448,
10.8469119916551));
#288026=CARTESIAN_POINT('Ctrl Pts',(-0.970116626577675,1.22058925946963,
10.8550736498355));
#288027=CARTESIAN_POINT('Ctrl Pts',(-1.11814176333428,1.08541708142775,
10.8706064911498));
#288028=CARTESIAN_POINT('Ctrl Pts',(-1.18152566837724,1.01605679648136,
10.877914564296));
#288029=CARTESIAN_POINT('Ctrl Pts',(-1.24718670033915,0.929689277409492,
10.8859893736599));
#288030=CARTESIAN_POINT('Ctrl Pts',(-1.25592686137185,0.917847797149138,
10.887075885683));
#288031=CARTESIAN_POINT('Ctrl Pts',(-1.26857492652024,0.90019270812393,
10.8886636851969));
#288032=CARTESIAN_POINT('Ctrl Pts',(-1.27261343873815,0.894474312974158,
10.8891730878587));
#288033=CARTESIAN_POINT('Ctrl Pts',(-1.27974155920761,0.884235132607003,
10.8900762801216));
#288034=CARTESIAN_POINT('Ctrl Pts',(-1.28284608766674,0.879725040581249,
10.8904710478317));
#288035=CARTESIAN_POINT('Ctrl Pts',(-1.28966666001197,0.869703590339324,
10.8913414147905));
#288036=CARTESIAN_POINT('Ctrl Pts',(-1.29337126089165,0.864184711090659,
10.8918162547678));
#288037=CARTESIAN_POINT('Ctrl Pts',(-1.30426245419627,0.847732782968532,
10.8932190837928));
#288038=CARTESIAN_POINT('Ctrl Pts',(-1.31134683726718,0.83673228875342,
10.8941405972442));
#288039=CARTESIAN_POINT('Ctrl Pts',(-1.32748481873895,0.810965021560096,
10.8962644244732));
#288040=CARTESIAN_POINT('Ctrl Pts',(-1.33643240870579,0.796133584521806,
10.897460928771));
#288041=CARTESIAN_POINT('Ctrl Pts',(-1.36717162117044,0.743201379100567,
10.9016518571564));
#288042=CARTESIAN_POINT('Ctrl Pts',(-1.38759791565763,0.704328854631468,
10.9045872443426));
#288043=CARTESIAN_POINT('Ctrl Pts',(-1.44674496977784,0.579176165227472,
10.9137592018545));
#288044=CARTESIAN_POINT('Ctrl Pts',(-1.47926045143141,0.490208645686127,
10.9198894954674));
#288045=CARTESIAN_POINT('Ctrl Pts',(-1.51713017197339,0.34745190869074,
10.9297753778846));
#288046=CARTESIAN_POINT('Ctrl Pts',(-1.52811721567657,0.295404126428148,
10.9333866034349));
#288047=CARTESIAN_POINT('Ctrl Pts',(-1.53898230851263,0.226679073591335,
10.9382242821866));
#288048=CARTESIAN_POINT('Ctrl Pts',(-1.54128963861159,0.210419015548702,
10.9393737170175));
#288049=CARTESIAN_POINT('Ctrl Pts',(-1.54464334864976,0.183756376528848,
10.9412679995453));
#288050=CARTESIAN_POINT('Ctrl Pts',(-1.54584310037909,0.173374103442078,
10.9420079601729));
#288051=CARTESIAN_POINT('Ctrl Pts',(-1.54790969399638,0.153758950593175,
10.9434107491675));
#288052=CARTESIAN_POINT('Ctrl Pts',(-1.5487987750049,0.144528832042801,
10.9440728406153));
#288053=CARTESIAN_POINT('Ctrl Pts',(-1.55043998935338,0.125730648752053,
10.9454255599085));
#288054=CARTESIAN_POINT('Ctrl Pts',(-1.55118619971787,0.116162484060061,
10.9461163453934));
#288055=CARTESIAN_POINT('Ctrl Pts',(-1.5529198429744,0.0909219514400552,
10.9479448513701));
#288056=CARTESIAN_POINT('Ctrl Pts',(-1.55375854692078,0.07524084056863,
10.9490871787748));
#288057=CARTESIAN_POINT('Ctrl Pts',(-1.55513259868893,0.0393758202818612,
10.951715075679));
#288058=CARTESIAN_POINT('Ctrl Pts',(-1.55551263031814,0.0191893168875632,
10.9532051992225));
#288059=CARTESIAN_POINT('Ctrl Pts',(-1.55549967992335,-0.00099787692791932,
10.9547066646399));
#288060=CARTESIAN_POINT('Origin',(0.,0.,11.5));
#288061=CARTESIAN_POINT('',(-1.77820247099329,-0.00119341782894063,11.2217971285233));
#288062=CARTESIAN_POINT('Ctrl Pts',(1.55548765964693,0.00619602180104882,
11.4445));
#288063=CARTESIAN_POINT('Ctrl Pts',(1.56189352721799,-0.123480106596799,
11.4386107220588));
#288064=CARTESIAN_POINT('Ctrl Pts',(1.55157339318347,-0.253519976424599,
11.4332143653576));
#288065=CARTESIAN_POINT('Ctrl Pts',(1.49808469247915,-0.514160788411113,
11.4219950121858));
#288066=CARTESIAN_POINT('Ctrl Pts',(1.45350109175637,-0.643696036901404,
11.4161770675377));
#288067=CARTESIAN_POINT('Ctrl Pts',(1.30062304090847,-0.954321027644617,
11.400518906268));
#288068=CARTESIAN_POINT('Ctrl Pts',(1.17170724031108,-1.12368519948027,
11.3901617831135));
#288069=CARTESIAN_POINT('Ctrl Pts',(0.818804091578115,-1.43526580982338,
11.3682667882953));
#288070=CARTESIAN_POINT('Ctrl Pts',(0.621216082080241,-1.52501365559612,
11.3603867470286));
#288071=CARTESIAN_POINT('Ctrl Pts',(0.297108732731849,-1.63725103150195,
11.3469229737146));
#288072=CARTESIAN_POINT('Ctrl Pts',(0.107153340206811,-1.66829909150744,
11.3391230935286));
#288073=CARTESIAN_POINT('Ctrl Pts',(-0.292185223557251,-1.66621697631177,
11.321282124971));
#288074=CARTESIAN_POINT('Ctrl Pts',(-0.513310674133649,-1.62663919683985,
11.3104914809886));
#288075=CARTESIAN_POINT('Ctrl Pts',(-0.909998958031018,-1.45783368293536,
11.2926989463642));
#288076=CARTESIAN_POINT('Ctrl Pts',(-1.07580669034446,-1.34902596933128,
11.2857428355586));
#288077=CARTESIAN_POINT('Ctrl Pts',(-1.38700387291632,-1.05970778369804,
11.2694906051745));
#288078=CARTESIAN_POINT('Ctrl Pts',(-1.52291358407573,-0.872095507221723,
11.2599567992504));
#288079=CARTESIAN_POINT('Ctrl Pts',(-1.67153574440031,-0.550985528579673,
11.2444623587404));
#288080=CARTESIAN_POINT('Ctrl Pts',(-1.71193945495828,-0.431707929094432,
11.2389214746226));
#288081=CARTESIAN_POINT('Ctrl Pts',(-1.76131183138801,-0.207703856787064,
11.2295264907753));
#288082=CARTESIAN_POINT('Ctrl Pts',(-1.77428940940823,-0.104637895751818,
11.2256410604156));
#288083=CARTESIAN_POINT('Ctrl Pts',(-1.77813136846619,-0.00118827202808551,
11.2218682344905));
#288084=CARTESIAN_POINT('Ctrl Pts',(1.88253627798795,-0.516855496602614,
11.0478006140998));
#288085=CARTESIAN_POINT('Ctrl Pts',(1.89215033473946,-0.445574378263489,
11.0574016965198));
#288086=CARTESIAN_POINT('Ctrl Pts',(1.89787331411876,-0.373989233771073,
11.0669290501123));
#288087=CARTESIAN_POINT('Ctrl Pts',(1.89965572803299,-0.302473084920835,
11.0764143241982));
#288088=CARTESIAN_POINT('Ctrl Pts',(1.90139260519551,-0.232784016237714,
11.085657270412));
#288089=CARTESIAN_POINT('Ctrl Pts',(1.89938758197532,-0.163160762632793,
11.0948603968831));
#288090=CARTESIAN_POINT('Ctrl Pts',(1.89358682684666,-0.0939572062035731,
11.1040835916621));
#288091=CARTESIAN_POINT('Ctrl Pts',(1.88970231824742,-0.0476146518145124,
11.1102599564003));
#288092=CARTESIAN_POINT('Ctrl Pts',(1.88411554699461,-0.00146048069795877,
11.1164459542092));
#288093=CARTESIAN_POINT('Ctrl Pts',(1.87680793341714,0.0443978253500607,
11.1226670018792));
#288094=CARTESIAN_POINT('Ctrl Pts',(1.87053965133728,0.0837338951853796,
11.1280032558032));
#288095=CARTESIAN_POINT('Ctrl Pts',(1.86300522066158,0.122852251027833,
11.1333654053092));
#288096=CARTESIAN_POINT('Ctrl Pts',(1.85419110486612,0.161684829253256,
11.1387728141424));
#288097=CARTESIAN_POINT('Ctrl Pts',(1.85167893706529,0.172752751992759,
11.1403140144933));
#288098=CARTESIAN_POINT('Ctrl Pts',(1.8490632515539,0.1837951725869,11.1418585963554));
#288099=CARTESIAN_POINT('Ctrl Pts',(1.84634658998489,0.194800202160708,
11.1434055776474));
#288100=CARTESIAN_POINT('Ctrl Pts',(1.83039930705503,0.259401668264169,
11.1524866308905));
#288101=CARTESIAN_POINT('Ctrl Pts',(1.81095282151477,0.322816933304556,
11.1616636095605));
#288102=CARTESIAN_POINT('Ctrl Pts',(1.78801592867889,0.384801885349895,
11.1710458036959));
#288103=CARTESIAN_POINT('Ctrl Pts',(1.78062238327084,0.404782296857351,
11.1740700877114));
#288104=CARTESIAN_POINT('Ctrl Pts',(1.77286582172294,0.424614204120316,
11.1771157990191));
#288105=CARTESIAN_POINT('Ctrl Pts',(1.76474545843319,0.444289698912254,
11.1801868585978));
#288106=CARTESIAN_POINT('Ctrl Pts',(1.7378154418074,0.509540646802293,11.1903715858769));
#288107=CARTESIAN_POINT('Ctrl Pts',(1.70688632143051,0.573079490905792,
11.2008347187143));
#288108=CARTESIAN_POINT('Ctrl Pts',(1.6721221343155,0.634644923633791,11.211490393886));
#288109=CARTESIAN_POINT('Ctrl Pts',(1.64170347058988,0.68851467727079,11.2208141096613));
#288110=CARTESIAN_POINT('Ctrl Pts',(1.60834675830549,0.740872069419597,
11.2302849609928));
#288111=CARTESIAN_POINT('Ctrl Pts',(1.57215673141411,0.791480601409065,
11.2398527531659));
#288112=CARTESIAN_POINT('Ctrl Pts',(1.56528883456199,0.801084743969782,
11.2416684636086));
#288113=CARTESIAN_POINT('Ctrl Pts',(1.55831824486087,0.810626492044188,
11.2434878520796));
#288114=CARTESIAN_POINT('Ctrl Pts',(1.55125593009187,0.820090787420387,
11.2453080440553));
#288115=CARTESIAN_POINT('Ctrl Pts',(1.51205106392477,0.872629713498644,
11.2554124340665));
#288116=CARTESIAN_POINT('Ctrl Pts',(1.46995007963234,0.922884649798819,
11.2655582196712));
#288117=CARTESIAN_POINT('Ctrl Pts',(1.42516007265191,0.970612748098785,
11.2757116426035));
#288118=CARTESIAN_POINT('Ctrl Pts',(1.38066083958641,1.01803099857933,11.2857991501512));
#288119=CARTESIAN_POINT('Ctrl Pts',(1.33350635764439,1.06295444981336,11.2958939340275));
#288120=CARTESIAN_POINT('Ctrl Pts',(1.28391228682921,1.10509953210788,11.3059882715471));
#288121=CARTESIAN_POINT('Ctrl Pts',(1.2353687359176,1.14635188172166,11.3158687870855));
#288122=CARTESIAN_POINT('Ctrl Pts',(1.1844874395772,1.18494157633475,11.3257487414933));
#288123=CARTESIAN_POINT('Ctrl Pts',(1.13149317507234,1.22056969483562,11.33564811858));
#288124=CARTESIAN_POINT('Ctrl Pts',(1.11732550639015,1.23009463840087,11.3382946520498));
#288125=CARTESIAN_POINT('Ctrl Pts',(1.10300696040088,1.23940775844044,11.3409427327555));
#288126=CARTESIAN_POINT('Ctrl Pts',(1.08854214729938,1.24850303160568,11.3435930975827));
#288127=CARTESIAN_POINT('Ctrl Pts',(1.07955957366795,1.25415114889081,11.3452389603424));
#288128=CARTESIAN_POINT('Ctrl Pts',(1.07052139471689,1.25971465974848,11.3468855538523));
#288129=CARTESIAN_POINT('Ctrl Pts',(1.06143947727963,1.26518597414758,11.3485311649603));
#288130=CARTESIAN_POINT('Ctrl Pts',(1.00838526914422,1.29714797500361,11.3581443986012));
#288131=CARTESIAN_POINT('Ctrl Pts',(0.953742835520967,1.32602619339434,
11.367739831609));
#288132=CARTESIAN_POINT('Ctrl Pts',(0.897756806662159,1.35164031465119,
11.3773790263593));
#288133=CARTESIAN_POINT('Ctrl Pts',(0.842732813096956,1.37681429594516,
11.3868525861157));
#288134=CARTESIAN_POINT('Ctrl Pts',(0.786411165378941,1.39883566986307,
11.3963686518532));
#288135=CARTESIAN_POINT('Ctrl Pts',(0.729015815333678,1.41751519939103,
11.4060070892532));
#288136=CARTESIAN_POINT('Ctrl Pts',(0.67740328957587,1.43431268730852,11.4146744133165));
#288137=CARTESIAN_POINT('Ctrl Pts',(0.624923262383356,1.44840784882227,
11.423441002047));
#288138=CARTESIAN_POINT('Ctrl Pts',(0.571728575041354,1.45964595495108,
11.4323776356138));
#288139=CARTESIAN_POINT('Ctrl Pts',(0.567493011438373,1.4605407757624,11.4330892044143));
#288140=CARTESIAN_POINT('Ctrl Pts',(0.563252938966541,1.46141746636715,
11.4338018512908));
#288141=CARTESIAN_POINT('Ctrl Pts',(0.559008446750899,1.46227594031182,
11.4345156119738));
#288142=CARTESIAN_POINT('Ctrl Pts',(0.539367340846575,1.46624847149031,
11.4378184921425));
#288143=CARTESIAN_POINT('Ctrl Pts',(0.519630929867375,1.46983109384515,
11.4411453373854));
#288144=CARTESIAN_POINT('Ctrl Pts',(0.499806597877791,1.47301514408981,
11.4445));
#288145=CARTESIAN_POINT('',(-1.77834184724224,2.15144321225382E-15,11.2216581527578));
#288146=CARTESIAN_POINT('Ctrl Pts',(-1.77834184724224,-1.00752649088661E-15,
11.2216581527578));
#288147=CARTESIAN_POINT('Ctrl Pts',(-1.78056295809976,0.0630691399806642,
11.2194370419002));
#288148=CARTESIAN_POINT('Ctrl Pts',(-1.77938367163897,0.126382693101961,
11.2172615074937));
#288149=CARTESIAN_POINT('Ctrl Pts',(-1.77483216597492,0.189679055828712,
11.2150609641785));
#288150=CARTESIAN_POINT('Ctrl Pts',(-1.77329020973932,0.211122557913883,
11.2143154654937));
#288151=CARTESIAN_POINT('Ctrl Pts',(-1.77136105248992,0.232563838797864,
11.2135672537069));
#288152=CARTESIAN_POINT('Ctrl Pts',(-1.76904537453388,0.253991980379479,
11.2128140938177));
#288153=CARTESIAN_POINT('Ctrl Pts',(-1.76778031481698,0.265698219000541,
11.2124026409929));
#288154=CARTESIAN_POINT('Ctrl Pts',(-1.76639964595072,0.277402475295627,
11.2119896471974));
#288155=CARTESIAN_POINT('Ctrl Pts',(-1.7649042554453,0.289096769776087,
11.2115750020803));
#288156=CARTESIAN_POINT('Ctrl Pts',(-1.75618642716702,0.357272173289313,
11.2091577037803));
#288157=CARTESIAN_POINT('Ctrl Pts',(-1.74360249041908,0.424868383240363,
11.2066900058409));
#288158=CARTESIAN_POINT('Ctrl Pts',(-1.72729798068798,0.491522522760096,
11.2041289844565));
#288159=CARTESIAN_POINT('Ctrl Pts',(-1.71073794549437,0.55922127080288,
11.2015278265586));
#288160=CARTESIAN_POINT('Ctrl Pts',(-1.69033976331967,0.625947692112791,
11.1988302994765));
#288161=CARTESIAN_POINT('Ctrl Pts',(-1.6662481511712,0.691324926366082,
11.1960285326268));
#288162=CARTESIAN_POINT('Ctrl Pts',(-1.64236384340929,0.756139600199675,
11.1932508745232));
#288163=CARTESIAN_POINT('Ctrl Pts',(-1.61484988904239,0.819627995860444,
11.190370919865));
#288164=CARTESIAN_POINT('Ctrl Pts',(-1.58383624360157,0.881431640782451,
11.1874164891188));
#288165=CARTESIAN_POINT('Ctrl Pts',(-1.57286497683827,0.903295058182947,
11.1863713411722));
#288166=CARTESIAN_POINT('Ctrl Pts',(-1.56145560535928,0.924947732110167,
11.1853171870002));
#288167=CARTESIAN_POINT('Ctrl Pts',(-1.54961330849835,0.946374080476353,
11.1842562664096));
#288168=CARTESIAN_POINT('Ctrl Pts',(-1.54442636420112,0.955758854120637,
11.183791581554));
#288169=CARTESIAN_POINT('Ctrl Pts',(-1.53915787421691,0.96509736723114,
11.1833257442496));
#288170=CARTESIAN_POINT('Ctrl Pts',(-1.53381281501924,0.974381028115582,
11.1828593506641));
#288171=CARTESIAN_POINT('Ctrl Pts',(-1.49862875205757,1.0354910920071,11.1797892964942));
#288172=CARTESIAN_POINT('Ctrl Pts',(-1.46007853363983,1.09431741490311,
11.1766883201831));
#288173=CARTESIAN_POINT('Ctrl Pts',(-1.41837534558482,1.15057225854762,
11.1736360868923));
#288174=CARTESIAN_POINT('Ctrl Pts',(-1.37739382382525,1.20585362206971,
11.1706366719588));
#288175=CARTESIAN_POINT('Ctrl Pts',(-1.33336846171864,1.25865313843171,
11.167684930948));
#288176=CARTESIAN_POINT('Ctrl Pts',(-1.28644306758958,1.30871872921028,
11.1648758956585));
#288177=CARTESIAN_POINT('Ctrl Pts',(-1.26448173990596,1.33214968520263,
11.1635612525828));
#288178=CARTESIAN_POINT('Ctrl Pts',(-1.24188429129087,1.35498200658024,
11.1622780911309));
#288179=CARTESIAN_POINT('Ctrl Pts',(-1.21866009817821,1.37718997272362,
11.1610370705579));
#288180=CARTESIAN_POINT('Ctrl Pts',(-1.19068199257409,1.40394383319137,
11.1595420173399));
#288181=CARTESIAN_POINT('Ctrl Pts',(-1.16179384164629,1.42979214773977,
11.1581081113835));
#288182=CARTESIAN_POINT('Ctrl Pts',(-1.13203488986082,1.45471464743626,
11.1567155137289));
#288183=CARTESIAN_POINT('Ctrl Pts',(-1.12095836559293,1.46399100483939,
11.1561971775379));
#288184=CARTESIAN_POINT('Ctrl Pts',(-1.10976120370782,1.4731390256401,11.1556845718294));
#288185=CARTESIAN_POINT('Ctrl Pts',(-1.09844545044964,1.48215740611027,
11.1551767065377));
#288186=CARTESIAN_POINT('Ctrl Pts',(-1.08935715413905,1.48940055750147,
11.1547688123258));
#288187=CARTESIAN_POINT('Ctrl Pts',(-1.08019232237532,1.49655999164064,
11.154363979494));
#288188=CARTESIAN_POINT('Ctrl Pts',(-1.07096364146446,1.50362643251721,
11.1539621970547));
#288189=CARTESIAN_POINT('Ctrl Pts',(-1.01566987992673,1.54596510480667,
11.151554912351));
#288190=CARTESIAN_POINT('Ctrl Pts',(-0.957983446118207,1.58505012644099,
11.1492506572737));
#288191=CARTESIAN_POINT('Ctrl Pts',(-0.898228259814544,1.62079450667842,
11.1469514740276));
#288192=CARTESIAN_POINT('Ctrl Pts',(-0.837698849525372,1.65700201251613,
11.1446225011863));
#288193=CARTESIAN_POINT('Ctrl Pts',(-0.77504614367348,1.68978066505551,
11.1422983166927));
#288194=CARTESIAN_POINT('Ctrl Pts',(-0.710615248214486,1.71900501942652,
11.1399053013869));
#288195=CARTESIAN_POINT('Ctrl Pts',(-0.663013188082911,1.7405962058312,
11.1381373225676));
#288196=CARTESIAN_POINT('Ctrl Pts',(-0.614440761775559,1.76024657859127,
11.13633235624));
#288197=CARTESIAN_POINT('Ctrl Pts',(-0.565041756987997,1.77789819268943,
11.1344721468956));
#288198=CARTESIAN_POINT('Ctrl Pts',(-0.539651494217822,1.78697082729406,
11.1335160303854));
#288199=CARTESIAN_POINT('Ctrl Pts',(-0.514042933361847,1.79551535443774,
11.1325454839384));
#288200=CARTESIAN_POINT('Ctrl Pts',(-0.488235989627093,1.80352350105029,
11.1315590990326));
#288201=CARTESIAN_POINT('Ctrl Pts',(-0.47619036643152,1.80726137553791,
11.1310986950025));
#288202=CARTESIAN_POINT('Ctrl Pts',(-0.464101526274562,1.81088238877124,
11.1306348508758));
#288203=CARTESIAN_POINT('Ctrl Pts',(-0.451971511660108,1.81438568346352,
11.1301674792352));
#288204=CARTESIAN_POINT('Ctrl Pts',(-0.439847524072741,1.8178872374776,
11.129700339817));
#288205=CARTESIAN_POINT('Ctrl Pts',(-0.42768949408131,1.82126909162395,
11.1292299487222));
#288206=CARTESIAN_POINT('Ctrl Pts',(-0.415506737858453,1.82452903864206,
11.1287565465568));
#288207=CARTESIAN_POINT('Ctrl Pts',(-0.345947596059538,1.84314215974059,
11.1260535910234));
#288208=CARTESIAN_POINT('Ctrl Pts',(-0.275513093522433,1.85780178702206,
11.1232467369454));
#288209=CARTESIAN_POINT('Ctrl Pts',(-0.204614971902161,1.86847733419749,
11.1203524705051));
#288210=CARTESIAN_POINT('Ctrl Pts',(-0.133643475840232,1.87916392979416,
11.1174552087078));
#288211=CARTESIAN_POINT('Ctrl Pts',(-0.062207810260123,1.88585898842662,
11.1144706362429));
#288212=CARTESIAN_POINT('Ctrl Pts',(0.00931113847733771,1.88852707827048,
11.1114499681871));
#288213=CARTESIAN_POINT('Ctrl Pts',(0.0795509949153351,1.89114745022651,
11.1084833237617));
#288214=CARTESIAN_POINT('Ctrl Pts',(0.149871221863444,1.88988478521395,
11.1054822960035));
#288215=CARTESIAN_POINT('Ctrl Pts',(0.219944637317926,1.88468617466707,
11.1025233544346));
#288216=CARTESIAN_POINT('Ctrl Pts',(0.236268910205453,1.88347510857798,
11.1018340406725));
#288217=CARTESIAN_POINT('Ctrl Pts',(0.252579930614474,1.88205030856834,
11.1011471163361));
#288218=CARTESIAN_POINT('Ctrl Pts',(0.268873815199358,1.88041083505751,
11.1004637310381));
#288219=CARTESIAN_POINT('Ctrl Pts',(0.280585025716745,1.87923246538617,
11.0999725486533));
#288220=CARTESIAN_POINT('Ctrl Pts',(0.292287207949923,1.87794312096384,
11.099483204848));
#288221=CARTESIAN_POINT('Ctrl Pts',(0.303964922251466,1.87654437070336,
11.0989967256268));
#288222=CARTESIAN_POINT('Ctrl Pts',(0.375560982981668,1.86796863353342,
11.096014121757));
#288223=CARTESIAN_POINT('Ctrl Pts',(0.446366604285884,1.85527278904176,
11.0931327739186));
#288224=CARTESIAN_POINT('Ctrl Pts',(0.516098884532556,1.83847386708897,
11.0904596839593));
#288225=CARTESIAN_POINT('Ctrl Pts',(0.580751365491678,1.82289869906285,
11.0879813210392));
#288226=CARTESIAN_POINT('Ctrl Pts',(0.644489094069816,1.80379415961865,
11.0856817204922));
#288227=CARTESIAN_POINT('Ctrl Pts',(0.707133361048688,1.78130683067211,
11.0834688587693));
#288228=CARTESIAN_POINT('Ctrl Pts',(0.710628984808413,1.78005201127443,
11.0833453784831));
#288229=CARTESIAN_POINT('Ctrl Pts',(0.714121210943649,1.77878664733593,
11.0832221682817));
#288230=CARTESIAN_POINT('Ctrl Pts',(0.717610010741306,1.77751076026119,
11.083099212176));
#288231=CARTESIAN_POINT('Ctrl Pts',(0.784961797480596,1.75287957499815,
11.0807255266982));
#288232=CARTESIAN_POINT('Ctrl Pts',(0.851033618181087,1.72432966301448,
11.0784459483291));
#288233=CARTESIAN_POINT('Ctrl Pts',(0.915548362106642,1.69201720649116,
11.0761624209881));
#288234=CARTESIAN_POINT('Ctrl Pts',(0.930611525754063,1.6844727633012,11.075629253778));
#288235=CARTESIAN_POINT('Ctrl Pts',(0.945589580933063,1.676723154374,11.0750959642276));
#288236=CARTESIAN_POINT('Ctrl Pts',(0.960478600724483,1.66877030534791,
11.0745614851519));
#288237=CARTESIAN_POINT('Ctrl Pts',(0.975313302129192,1.66084647004704,
11.0740289559722));
#288238=CARTESIAN_POINT('Ctrl Pts',(0.99006444646142,1.65271797506666,11.0734950656497));
#288239=CARTESIAN_POINT('Ctrl Pts',(1.00470002911071,1.64440308869426,11.0729598689694));
#288240=CARTESIAN_POINT('Ctrl Pts',(1.06778798265132,1.60856104688918,11.0706528570719));
#288241=CARTESIAN_POINT('Ctrl Pts',(1.1288150742056,1.56921363248008,11.0683159018116));
#288242=CARTESIAN_POINT('Ctrl Pts',(1.18750283687179,1.52663356862106,11.065892184903));
#288243=CARTESIAN_POINT('Ctrl Pts',(1.24701567400671,1.48345488382351,11.0634343936516));
#288244=CARTESIAN_POINT('Ctrl Pts',(1.30412236127524,1.43695192355179,11.0608872144625));
#288245=CARTESIAN_POINT('Ctrl Pts',(1.35852490178442,1.38740391488404,11.0582277343097));
#288246=CARTESIAN_POINT('Ctrl Pts',(1.41273774521384,1.33802867595212,11.0555775275405));
#288247=CARTESIAN_POINT('Ctrl Pts',(1.46426503880922,1.28562996588739,11.0528158459264));
#288248=CARTESIAN_POINT('Ctrl Pts',(1.51281069067292,1.23047674230504,11.0499566160806));
#288249=CARTESIAN_POINT('Ctrl Pts',(1.52933742321749,1.21170054834898,11.048983228658));
#288250=CARTESIAN_POINT('Ctrl Pts',(1.54551859234449,1.19260502119365,11.0479988450508));
#288251=CARTESIAN_POINT('Ctrl Pts',(1.56134249951545,1.17320041606,11.0470049623625));
#288252=CARTESIAN_POINT('',(-0.999999999999999,-1.22464679914735E-16,12.));
#288253=CARTESIAN_POINT('',(-1.5,1.83697019872103E-16,11.5));
#288254=CARTESIAN_POINT('Origin',(0.,0.,12.));
#288255=CARTESIAN_POINT('Ctrl Pts',(-1.77829916038566,-0.00120041539116822,
11.2217004344528));
#288256=CARTESIAN_POINT('Ctrl Pts',(-1.77831352623488,-0.000800286888638816,
11.2216863387078));
#288257=CARTESIAN_POINT('Ctrl Pts',(-1.77832775518455,-0.000400148401643428,
11.2216722448155));
#288258=CARTESIAN_POINT('Ctrl Pts',(-1.77834184724224,-1.00752649088661E-15,
11.2216581527578));
#288259=CARTESIAN_POINT('Ctrl Pts',(1.13606312113376,-1.59291779518177,
-0.231572864370215));
#288260=CARTESIAN_POINT('Ctrl Pts',(1.66580317288383,-1.21512918566376,
-0.194523783755237));
#288261=CARTESIAN_POINT('Ctrl Pts',(2.30944881815147,0.10371475579539,-0.120437486311781));
#288262=CARTESIAN_POINT('Ctrl Pts',(1.16339684166879,2.00012929542641,-0.00931397203984471));
#288263=CARTESIAN_POINT('Ctrl Pts',(-1.04791166066631,2.06049852367029,
0.101797678445592));
#288264=CARTESIAN_POINT('Ctrl Pts',(-2.29995991841951,0.238642905340929,
0.212909328931029));
#288265=CARTESIAN_POINT('Ctrl Pts',(-1.44800670770165,-1.8030882775837,
0.324020979416465));
#288266=CARTESIAN_POINT('Ctrl Pts',(0.728891101841514,-2.19434009684312,
0.435132629901903));
#288267=CARTESIAN_POINT('Ctrl Pts',(2.2388411747295,-0.578378966553796,
0.546244280387339));
#288268=CARTESIAN_POINT('Ctrl Pts',(1.70047933315151,1.56697230991268,0.657355930872777));
#288269=CARTESIAN_POINT('Ctrl Pts',(-0.39369797820196,2.27855944506382,
0.768467581358213));
#288270=CARTESIAN_POINT('Ctrl Pts',(-2.12766415432316,0.905518297538944,
0.879579231843651));
#288271=CARTESIAN_POINT('Ctrl Pts',(-1.91500281753321,-1.29602787974305,
0.990690882329087));
#288272=CARTESIAN_POINT('Ctrl Pts',(0.0497274383191288,-2.31180100517801,
1.10180253281452));
#288273=CARTESIAN_POINT('Ctrl Pts',(1.9689597322423,-1.21248020017453,1.21291418329996));
#288274=CARTESIAN_POINT('Ctrl Pts',(2.08676085490371,0.996162330620904,
1.3240258337854));
#288275=CARTESIAN_POINT('Ctrl Pts',(0.295351476789991,2.29339794652186,
1.43513748427083));
#288276=CARTESIAN_POINT('Ctrl Pts',(-1.76627935167926,1.49236927838366,
1.54624913475627));
#288277=CARTESIAN_POINT('Ctrl Pts',(-2.21191375477208,-0.674052009334876,
1.65736078524171));
#288278=CARTESIAN_POINT('Ctrl Pts',(-0.633833682165421,-2.22377223890773,
1.76847243572715));
#288279=CARTESIAN_POINT('Ctrl Pts',(1.52415068530889,-1.73892872941285,
1.87958408621258));
#288280=CARTESIAN_POINT('Ctrl Pts',(2.28766582187352,0.336887910617784,
1.99069573669802));
#288281=CARTESIAN_POINT('Ctrl Pts',(0.95815978745069,2.1044804921888,2.10180738718346));
#288282=CARTESIAN_POINT('Ctrl Pts',(-1.24798158492499,1.9466510557791,2.21291903766889));
#288283=CARTESIAN_POINT('Ctrl Pts',(-2.31232513160447,0.00780017457708053,
2.32403068815433));
#288284=CARTESIAN_POINT('Ctrl Pts',(-1.26108632768448,-1.93818720060691,
2.43514233863977));
#288285=CARTESIAN_POINT('Ctrl Pts',(0.943940037394818,-2.1108968623253,
2.54625398912521));
#288286=CARTESIAN_POINT('Ctrl Pts',(2.2853409313939,-0.352314039762323,
2.65736563961064));
#288287=CARTESIAN_POINT('Ctrl Pts',(1.53584774180008,1.72860639494661,2.76847729009608));
#288288=CARTESIAN_POINT('Ctrl Pts',(-0.618816515269055,2.22799786267397,
2.87958894058151));
#288289=CARTESIAN_POINT('Ctrl Pts',(-2.20731588525495,0.688959315172647,
2.99070059106696));
#288290=CARTESIAN_POINT('Ctrl Pts',(-1.77630750418927,-1.48041886159491,
3.10181224155239));
#288291=CARTESIAN_POINT('Ctrl Pts',(0.279872333686937,-2.29533871839889,
3.21292389203783));
#288292=CARTESIAN_POINT('Ctrl Pts',(2.07999260576339,-1.01021736039841,
3.32403554252326));
#288293=CARTESIAN_POINT('Ctrl Pts',(1.97709518223906,1.19916762616646,3.4351471930087));
#288294=CARTESIAN_POINT('Ctrl Pts',(0.065322521730458,2.31141543722719,
3.54625884349413));
#288295=CARTESIAN_POINT('Ctrl Pts',(-1.90621473334059,1.3089131925695,3.65737049397958));
#288296=CARTESIAN_POINT('Ctrl Pts',(-2.13372638028968,-0.89113415900399,
3.76848214446501));
#288297=CARTESIAN_POINT('Ctrl Pts',(-0.409058462753209,-2.27586896137283,
3.87959379495045));
#288298=CARTESIAN_POINT('Ctrl Pts',(1.68986342616582,-1.57837573352984,
3.99070544543588));
#288299=CARTESIAN_POINT('Ctrl Pts',(2.24270289429889,0.563198085217235,
4.10181709592132));
#288300=CARTESIAN_POINT('Ctrl Pts',(0.743658484580136,2.18949318647061,
4.21292874640676));
#288301=CARTESIAN_POINT('Ctrl Pts',(-1.43577067829371,1.8125868019604,4.3240403968922));
#288302=CARTESIAN_POINT('Ctrl Pts',(-2.30159084080806,-0.222683535084021,
4.43515204737763));
#288303=CARTESIAN_POINT('Ctrl Pts',(-1.06164962419783,-2.05421723065739,
4.54626369786307));
#288304=CARTESIAN_POINT('Ctrl Pts',(1.14961140180695,-2.00631552357163,
4.65737534834851));
#288305=CARTESIAN_POINT('Ctrl Pts',(2.30907501534183,-0.122804433198633,
4.76848699883394));
#288306=CARTESIAN_POINT('Ctrl Pts',(1.35592986167235,1.87306234960673,4.87959864931938));
#288307=CARTESIAN_POINT('Ctrl Pts',(-0.837776683225523,2.15523515754841,
4.99071029980481));
#288308=CARTESIAN_POINT('Ctrl Pts',(-2.26498826620913,0.465549685021973,
5.10182195029026));
#288309=CARTESIAN_POINT('Ctrl Pts',(-1.61992673679233,-1.65007445974853,
5.21293360077568));
#288310=CARTESIAN_POINT('Ctrl Pts',(0.507231044863186,-2.25601973005913,
5.32404525126113));
#288311=CARTESIAN_POINT('Ctrl Pts',(2.17031522767223,-0.797897341656895,
5.43515690174656));
#288312=CARTESIAN_POINT('Ctrl Pts',(1.8477441385157,1.39023377669727,5.546268552232));
#288313=CARTESIAN_POINT('Ctrl Pts',(-0.165356899058651,2.30641831661622,
5.65738020271744));
#288314=CARTESIAN_POINT('Ctrl Pts',(-2.02717032910705,1.1124247444556,5.76849185320287));
#288315=CARTESIAN_POINT('Ctrl Pts',(-2.03429398882154,-1.09934358702528,
5.87960350368832));
#288316=CARTESIAN_POINT('Ctrl Pts',(-0.180210330756775,-2.30530531426481,
5.99071515417374));
#288317=CARTESIAN_POINT('Ctrl Pts',(1.83875057129879,-1.40210723264573,
6.1018268046592));
#288318=CARTESIAN_POINT('Ctrl Pts',(2.17540987993784,0.783900637554235,
6.21293845514461));
#288319=CARTESIAN_POINT('Ctrl Pts',(0.52175273974583,2.25270558081982,6.32405010563007));
#288320=CARTESIAN_POINT('Ctrl Pts',(-1.6092641245679,1.66047503223259,6.43516175611548));
#288321=CARTESIAN_POINT('Ctrl Pts',(-2.26794012696886,-0.450950036892674,
6.54627340660095));
#288322=CARTESIAN_POINT('Ctrl Pts',(-0.851642313493321,-2.14979387969097,
6.65738505708636));
#288323=CARTESIAN_POINT('Ctrl Pts',(1.34383634341701,-1.88175775205015,
6.76849670757181));
#288324=CARTESIAN_POINT('Ctrl Pts',(2.30981815768343,0.107927909851316,
6.87960835805725));
#288325=CARTESIAN_POINT('Ctrl Pts',(1.16251129221972,1.99886864269526,6.99072000854268));
#288326=CARTESIAN_POINT('Ctrl Pts',(-1.04839529676982,2.06101325978297,
7.10183165902812));
#288327=CARTESIAN_POINT('Ctrl Pts',(-2.3001086673767,0.237504681104215,
7.21294330951356));
#288328=CARTESIAN_POINT('Ctrl Pts',(-1.4474167224631,-1.8033006368383,7.32405495999898));
#288329=CARTESIAN_POINT('Ctrl Pts',(0.729539370371449,-2.19423805964062,
7.43516661048443));
#288330=CARTESIAN_POINT('Ctrl Pts',(2.23902850798198,-0.577632838161553,
7.54627826096985));
#288331=CARTESIAN_POINT('Ctrl Pts',(1.6999955211303,1.56745768153964,7.65738991145531));
#288332=CARTESIAN_POINT('Ctrl Pts',(-0.394389898323185,2.27845670651103,
7.76850156194073));
#288333=CARTESIAN_POINT('Ctrl Pts',(-2.12794184489071,0.904860132820632,
7.87961321242619));
#288334=CARTESIAN_POINT('Ctrl Pts',(-1.91460658872055,-1.2966070976552,
7.9907248629116));
#288335=CARTESIAN_POINT('Ctrl Pts',(0.0504321150938301,-2.31178825964159,
8.10183651339705));
#288336=CARTESIAN_POINT('Ctrl Pts',(1.9693296896238,-1.21187826459962,8.21294816388248));
#288337=CARTESIAN_POINT('Ctrl Pts',(2.08645679780942,0.996798066908651,
8.32405981436793));
#288338=CARTESIAN_POINT('Ctrl Pts',(0.294652019720973,2.29348829184849,
8.43517146485335));
#288339=CARTESIAN_POINT('Ctrl Pts',(-1.76673448864124,1.49183028428665,
8.54628311533881));
#288340=CARTESIAN_POINT('Ctrl Pts',(-2.21170804328929,-0.674726528470968,
8.65739476582423));
#288341=CARTESIAN_POINT('Ctrl Pts',(-0.633155389578567,-2.22396551725186,
8.76850641630968));
#288342=CARTESIAN_POINT('Ctrl Pts',(1.52468100466622,-1.73846373396192,
8.87961806679511));
#288343=CARTESIAN_POINT('Ctrl Pts',(2.28756296574735,0.33758562562678,8.99072971728054));
#288344=CARTESIAN_POINT('Ctrl Pts',(0.95751784602998,2.10477267467037,9.10184136776598));
#288345=CARTESIAN_POINT('Ctrl Pts',(-1.24857524943225,1.94627026738047,
9.21295301825142));
#288346=CARTESIAN_POINT('Ctrl Pts',(-2.31232744890977,0.00709498814131274,
9.32406466873686));
#288347=CARTESIAN_POINT('Ctrl Pts',(-1.26049501691729,-1.93857192891019,
9.43517631922229));
#288348=CARTESIAN_POINT('Ctrl Pts',(0.944583669006363,-2.11060852082977,
9.54628796970774));
#288349=CARTESIAN_POINT('Ctrl Pts',(2.28544860209947,-0.351617607164512,
9.65739962019316));
#288350=CARTESIAN_POINT('Ctrl Pts',(1.53531982431326,1.72907596712165,9.76851127067861));
#288351=CARTESIAN_POINT('Ctrl Pts',(-0.619494893047472,2.22780672033099,
9.87962292116403));
#288352=CARTESIAN_POINT('Ctrl Pts',(-2.20752811597315,0.688290399046372,
9.99073457164949));
#288353=CARTESIAN_POINT('Ctrl Pts',(-1.77585170267646,-1.48096889598351,
10.1018462221348));
#288354=CARTESIAN_POINT('Ctrl Pts',(0.280564466394787,-2.29523742190791,
10.2129578726204));
#288355=CARTESIAN_POINT('Ctrl Pts',(2.08031577474111,-1.00961302481287,
10.3240695231057));
#288356=CARTESIAN_POINT('Ctrl Pts',(1.97670051092818,1.19982795629719,10.4351811735912));
#288357=CARTESIAN_POINT('Ctrl Pts',(0.0646723860625978,2.31132606558188,
10.5462928240767));
#288358=CARTESIAN_POINT('Ctrl Pts',(-1.9067183409908,1.3085396174507,10.6574044745621));
#288359=CARTESIAN_POINT('Ctrl Pts',(-2.133255506411,-0.892181039348481,
10.7685161250475));
#288360=CARTESIAN_POINT('Ctrl Pts',(-0.408743935798804,-2.27523656122952,
10.8796277755329));
#288361=CARTESIAN_POINT('Ctrl Pts',(1.69107508575937,-1.57932721877126,
10.9907394260185));
#288362=CARTESIAN_POINT('Ctrl Pts',(2.24113370804431,0.567126268774148,
11.1018629835556));
#288363=CARTESIAN_POINT('Ctrl Pts',(1.24429396241602,1.64413287865399,11.1759493242644));
#288364=CARTESIAN_POINT('Ctrl Pts',(0.628071129403783,1.85298493614821,
11.2129984481446));
#288365=CARTESIAN_POINT('Ctrl Pts',(1.05790538596218,-1.48332982874757,
-0.1538593861323));
#288366=CARTESIAN_POINT('Ctrl Pts',(1.55120091107965,-1.13153194240705,
-0.116810305517322));
#288367=CARTESIAN_POINT('Ctrl Pts',(2.1505656665346,0.0965794916837141,
-0.0427240080738664));
#288368=CARTESIAN_POINT('Ctrl Pts',(1.08335862851045,1.86252639918517,0.0683995061980696));
#288369=CARTESIAN_POINT('Ctrl Pts',(-0.975818481569167,1.91874240560023,
0.179511156683506));
#288370=CARTESIAN_POINT('Ctrl Pts',(-2.14172957464275,0.222224989250477,
0.290622807168943));
#288371=CARTESIAN_POINT('Ctrl Pts',(-1.34838818943279,-1.67904121235574,
0.40173445765438));
#288372=CARTESIAN_POINT('Ctrl Pts',(0.678745580305889,-2.04337607998962,
0.512846108139817));
#288373=CARTESIAN_POINT('Ctrl Pts',(2.08481561719611,-0.538588228472594,
0.623957758625255));
#288374=CARTESIAN_POINT('Ctrl Pts',(1.58349145553025,1.45916931504287,0.73506940911069));
#288375=CARTESIAN_POINT('Ctrl Pts',(-0.366612738178346,2.12180138966432,
0.846181059596129));
#288376=CARTESIAN_POINT('Ctrl Pts',(-1.98128724232402,0.843221354723422,
0.957292710081565));
#288377=CARTESIAN_POINT('Ctrl Pts',(-1.78325636763855,-1.20686504898516,
1.068404360567));
#288378=CARTESIAN_POINT('Ctrl Pts',(0.0463063397176581,-2.15275603014899,
1.17951601105244));
#288379=CARTESIAN_POINT('Ctrl Pts',(1.83350120845665,-1.12906519917399,
1.29062766153788));
#288380=CARTESIAN_POINT('Ctrl Pts',(1.94319796721729,0.927629350211451,
1.40173931202331));
#288381=CARTESIAN_POINT('Ctrl Pts',(0.275032181078265,2.13561904672937,
1.51285096250875));
#288382=CARTESIAN_POINT('Ctrl Pts',(-1.64476463014706,1.38969874831511,
1.62396261299419));
#288383=CARTESIAN_POINT('Ctrl Pts',(-2.05974072296436,-0.627679252876699,
1.73507426347962));
#288384=CARTESIAN_POINT('Ctrl Pts',(-0.590227825983685,-2.07078337896038,
1.84618591396506));
#288385=CARTESIAN_POINT('Ctrl Pts',(1.41929368977058,-1.61929564865578,
1.9572975644505));
#288386=CARTESIAN_POINT('Ctrl Pts',(2.13028127506361,0.313711032845113,
2.06840921493594));
#288387=CARTESIAN_POINT('Ctrl Pts',(0.892241268024662,1.95969854660631,
2.17952086542137));
#288388=CARTESIAN_POINT('Ctrl Pts',(-1.16212419513821,1.81272730202038,
2.29063251590681));
#288389=CARTESIAN_POINT('Ctrl Pts',(-2.1532440982494,0.00726354596238041,
2.40174416639224));
#288390=CARTESIAN_POINT('Ctrl Pts',(-1.17432737090281,-1.80484573469715,
2.51285581687768));
#288391=CARTESIAN_POINT('Ctrl Pts',(0.878999794121258,-1.96567348972298,
2.62396746736312));
#288392=CARTESIAN_POINT('Ctrl Pts',(2.12811633007561,-0.32807589057435,
2.73507911784855));
#288393=CARTESIAN_POINT('Ctrl Pts',(1.43018602385987,1.60968345983953,2.846190768334));
#288394=CARTESIAN_POINT('Ctrl Pts',(-0.576243795126606,2.07471829248604,
2.95730241881943));
#288395=CARTESIAN_POINT('Ctrl Pts',(-2.05545917307893,0.641560980786489,
3.06841406930487));
#288396=CARTESIAN_POINT('Ctrl Pts',(-1.65410287584327,-1.37857048435678,
3.1795257197903));
#288397=CARTESIAN_POINT('Ctrl Pts',(0.260617956591843,-2.13742629932249,
3.29063737027575));
#288398=CARTESIAN_POINT('Ctrl Pts',(1.93689535331683,-0.940717436097568,
3.40174902076117));
#288399=CARTESIAN_POINT('Ctrl Pts',(1.84107696389546,1.11666849032732,3.51286067124662));
#288400=CARTESIAN_POINT('Ctrl Pts',(0.0608285281669042,2.15239698811669,
3.62397232173205));
#288401=CARTESIAN_POINT('Ctrl Pts',(-1.77507287727901,1.21886389093795,
3.7350839722175));
#288402=CARTESIAN_POINT('Ctrl Pts',(-1.98693240532736,-0.829826801775225,
3.84619562270292));
#288403=CARTESIAN_POINT('Ctrl Pts',(-0.380916467465418,-2.11929600318132,
3.95730727318837));
#288404=CARTESIAN_POINT('Ctrl Pts',(1.57360589110334,-1.46978821731913,
4.06841892367379));
#288405=CARTESIAN_POINT('Ctrl Pts',(2.08841166204214,0.524451746237755,
4.17953057415924));
#288406=CARTESIAN_POINT('Ctrl Pts',(0.692497011406068,2.0388626225127,4.29064222464467));
#288407=CARTESIAN_POINT('Ctrl Pts',(-1.3369939621468,1.68788626674563,4.40175387513011));
#288408=CARTESIAN_POINT('Ctrl Pts',(-2.14324829446283,-0.207363575797973,
4.51286552561555));
#288409=CARTESIAN_POINT('Ctrl Pts',(-0.988611314415993,-1.91289324670622,
4.62397717610099));
#288410=CARTESIAN_POINT('Ctrl Pts',(1.07052158556242,-1.86828703338926,
4.73508882658642));
#288411=CARTESIAN_POINT('Ctrl Pts',(2.15021758023707,-0.114355856540079,
4.84620047707186));
#288412=CARTESIAN_POINT('Ctrl Pts',(1.26264595423057,1.74420127810718,4.95731212755729));
#288413=CARTESIAN_POINT('Ctrl Pts',(-0.780140160287336,2.00696144322516,
5.06842377804273));
#288414=CARTESIAN_POINT('Ctrl Pts',(-2.10916386720878,0.43352126308458,
5.17953542852817));
#288415=CARTESIAN_POINT('Ctrl Pts',(-1.50848063618725,-1.53655428623061,
5.2906470790136));
#288416=CARTESIAN_POINT('Ctrl Pts',(0.47233507038983,-2.10081233944524,
5.40175872949904));
#288417=CARTESIAN_POINT('Ctrl Pts',(2.02100404975636,-0.74300439780258,
5.51287037998448));
#288418=CARTESIAN_POINT('Ctrl Pts',(1.72062488399853,1.29458986279462,5.62398203046992));
#288419=CARTESIAN_POINT('Ctrl Pts',(-0.153980840382875,2.14774365441516,
5.73509368095535));
#288420=CARTESIAN_POINT('Ctrl Pts',(-1.88770709085676,1.03589325869737,
5.84620533144079));
#288421=CARTESIAN_POINT('Ctrl Pts',(-1.89434066414993,-1.02371204566203,
5.95731698192623));
#288422=CARTESIAN_POINT('Ctrl Pts',(-0.167812400532235,-2.14670722328713,
6.06842863241166));
#288423=CARTESIAN_POINT('Ctrl Pts',(1.71225004723043,-1.30564646058762,
6.17954028289711));
#288424=CARTESIAN_POINT('Ctrl Pts',(2.02574820522723,0.729970624959828,
6.29065193338253));
#288425=CARTESIAN_POINT('Ctrl Pts',(0.485857716221588,2.09772619373299,
6.40176358386798));
#288426=CARTESIAN_POINT('Ctrl Pts',(-1.49855157970193,1.54623933052372,
6.51287523435341));
#288427=CARTESIAN_POINT('Ctrl Pts',(-2.11191264880221,-0.419926026955724,
6.62398688483885));
#288428=CARTESIAN_POINT('Ctrl Pts',(-0.793051876781918,-2.00189450896349,
6.73509853532428));
#288429=CARTESIAN_POINT('Ctrl Pts',(1.25138443375736,-1.75229846294388,
6.84621018580972));
#288430=CARTESIAN_POINT('Ctrl Pts',(2.15090959661459,0.100502793377733,
6.95732183629516));
#288431=CARTESIAN_POINT('Ctrl Pts',(1.08253400220732,1.86135247558067,7.06843348678059));
#288432=CARTESIAN_POINT('Ctrl Pts',(-0.976268844959389,1.91922172941229,
7.17954513726604));
#288433=CARTESIAN_POINT('Ctrl Pts',(-2.14186809011785,0.221165071427202,
7.29065678775147));
#288434=CARTESIAN_POINT('Ctrl Pts',(-1.34783879340901,-1.67923896193057,
7.40176843823691));
#288435=CARTESIAN_POINT('Ctrl Pts',(0.679349249905414,-2.0432810626406,
7.51288008872234));
#288436=CARTESIAN_POINT('Ctrl Pts',(2.08499006248272,-0.537893431475763,
7.62399173920778));
#288437=CARTESIAN_POINT('Ctrl Pts',(1.58304092832492,1.45962129455775,7.73510338969322));
#288438=CARTESIAN_POINT('Ctrl Pts',(-0.367257056270613,2.1217057192158,
7.84621504017865));
#288439=CARTESIAN_POINT('Ctrl Pts',(-1.98154582861344,0.842608469763599,
7.9573266906641));
#288440=CARTESIAN_POINT('Ctrl Pts',(-1.78288739817974,-1.20740441844228,
8.06843834114951));
#288441=CARTESIAN_POINT('Ctrl Pts',(0.0469625368439069,-2.15274416146725,
8.17954999163497));
#288442=CARTESIAN_POINT('Ctrl Pts',(1.83384571387996,-1.12850467496116,
8.29066164212039));
#288443=CARTESIAN_POINT('Ctrl Pts',(1.9429148283391,0.928221349749457,8.40177329260585));
#288444=CARTESIAN_POINT('Ctrl Pts',(0.274380844557604,2.1357031765685,8.51288494309127));
#288445=CARTESIAN_POINT('Ctrl Pts',(-1.6451884550512,1.38919683539529,8.62399659357671));
#288446=CARTESIAN_POINT('Ctrl Pts',(-2.05954916381456,-0.62830736711941,
8.73510824406215));
#288447=CARTESIAN_POINT('Ctrl Pts',(-0.5895961978923,-2.07096336033418,
8.84621989454758));
#288448=CARTESIAN_POINT('Ctrl Pts',(1.4197875247468,-1.61886264349714,8.95733154503303));
#288449=CARTESIAN_POINT('Ctrl Pts',(2.13018549513042,0.314360747154248,
9.06844319551845));
#288450=CARTESIAN_POINT('Ctrl Pts',(0.891643490248224,1.95997062780954,
9.17955484600391));
#288451=CARTESIAN_POINT('Ctrl Pts',(-1.16267701730804,1.81237271072142,
9.29066649648932));
#288452=CARTESIAN_POINT('Ctrl Pts',(-2.15324625613104,0.00660687423822486,
9.40177814697478));
#288453=CARTESIAN_POINT('Ctrl Pts',(-1.1737767405428,-1.80520399484714,
9.5128897974602));
#288454=CARTESIAN_POINT('Ctrl Pts',(0.879599145808469,-1.96540498525748,
9.62400144794565));
#288455=CARTESIAN_POINT('Ctrl Pts',(2.12821659335958,-0.327427370450354,
9.73511309843108));
#288456=CARTESIAN_POINT('Ctrl Pts',(1.42969442551268,1.61012072685739,9.84622474891651));
#288457=CARTESIAN_POINT('Ctrl Pts',(-0.576875502548628,2.07454030016294,
9.95733639940195));
#288458=CARTESIAN_POINT('Ctrl Pts',(-2.0556568029603,0.640938084083322,
10.0684480498874));
#288459=CARTESIAN_POINT('Ctrl Pts',(-1.6536784321074,-1.37908267802925,
10.1795597003728));
#288460=CARTESIAN_POINT('Ctrl Pts',(0.26126247264541,-2.13733197172626,
10.2906713508583));
#288461=CARTESIAN_POINT('Ctrl Pts',(1.93719628923821,-0.940154676987634,
10.4017830013437));
#288462=CARTESIAN_POINT('Ctrl Pts',(1.84070944478698,1.11728339172568,10.5128946518291));
#288463=CARTESIAN_POINT('Ctrl Pts',(0.0602231198829427,2.15231376497251,
10.6240063023145));
#288464=CARTESIAN_POINT('Ctrl Pts',(-1.77554183823342,1.2185160166668,10.7351179528));
#288465=CARTESIAN_POINT('Ctrl Pts',(-1.98649392615918,-0.83080165989208,
10.8462296032854));
#288466=CARTESIAN_POINT('Ctrl Pts',(-0.380623579022067,-2.118707110271,
10.9573412537709));
#288467=CARTESIAN_POINT('Ctrl Pts',(1.57473419215115,-1.47067424322988,
11.0684529042563));
#288468=CARTESIAN_POINT('Ctrl Pts',(2.08695043109518,0.528109682548335,
11.1795764617936));
#288469=CARTESIAN_POINT('Ctrl Pts',(1.15869026999699,1.53102146809392,11.2536628025023));
#288470=CARTESIAN_POINT('Ctrl Pts',(0.584861719567571,1.72550513047344,
11.2907119263826));
#288471=CARTESIAN_POINT('Ctrl Pts',(0.979747650790608,-1.37374186231338,
-0.0761459078943855));
#288472=CARTESIAN_POINT('Ctrl Pts',(1.43659864927549,-1.04793469915035,
-0.0390968272794079));
#288473=CARTESIAN_POINT('Ctrl Pts',(1.99168251491774,0.0894442275720395,
0.0349894701640479));
#288474=CARTESIAN_POINT('Ctrl Pts',(1.00332041535211,1.72492350294394,0.146112984435984));
#288475=CARTESIAN_POINT('Ctrl Pts',(-0.903725302472021,1.77698628753017,
0.25722463492142));
#288476=CARTESIAN_POINT('Ctrl Pts',(-1.98349923086599,0.205807073160022,
0.368336285406858));
#288477=CARTESIAN_POINT('Ctrl Pts',(-1.24876967116393,-1.55499414712776,
0.479447935892295));
#288478=CARTESIAN_POINT('Ctrl Pts',(0.62860005877027,-1.89241206313614,
0.590559586377731));
#288479=CARTESIAN_POINT('Ctrl Pts',(1.93079005966273,-0.498797490391393,
0.701671236863168));
#288480=CARTESIAN_POINT('Ctrl Pts',(1.46650357790899,1.35136632017308,0.812782887348605));
#288481=CARTESIAN_POINT('Ctrl Pts',(-0.339527498154739,1.96504333426481,
0.923894537834042));
#288482=CARTESIAN_POINT('Ctrl Pts',(-1.83491033032488,0.780924411907904,
1.03500618831948));
#288483=CARTESIAN_POINT('Ctrl Pts',(-1.6515099177439,-1.11770221822726,
1.14611783880492));
#288484=CARTESIAN_POINT('Ctrl Pts',(0.0428852411161929,-1.99371105511996,
1.25722948929036));
#288485=CARTESIAN_POINT('Ctrl Pts',(1.69804268467099,-1.04565019817345,
1.36834113977579));
#288486=CARTESIAN_POINT('Ctrl Pts',(1.79963507953087,0.859096369801998,
1.47945279026123));
#288487=CARTESIAN_POINT('Ctrl Pts',(0.254712885366533,1.97784014693687,
1.59056444074667));
#288488=CARTESIAN_POINT('Ctrl Pts',(-1.52324990861485,1.28702821824656,
1.7016760912321));
#288489=CARTESIAN_POINT('Ctrl Pts',(-1.90756769115663,-0.581306496418522,
1.81278774171754));
#288490=CARTESIAN_POINT('Ctrl Pts',(-0.546621969801947,-1.91779451901304,
1.92389939220298));
#288491=CARTESIAN_POINT('Ctrl Pts',(1.31443669423229,-1.49966256789871,
2.03501104268841));
#288492=CARTESIAN_POINT('Ctrl Pts',(1.9728967282537,0.290534155072444,2.14612269317385));
#288493=CARTESIAN_POINT('Ctrl Pts',(0.826322748598632,1.81491660102383,
2.25723434365928));
#288494=CARTESIAN_POINT('Ctrl Pts',(-1.07626680535143,1.67880354826165,
2.36834599414473));
#288495=CARTESIAN_POINT('Ctrl Pts',(-1.99416306489432,0.00672691734768011,
2.47945764463016));
#288496=CARTESIAN_POINT('Ctrl Pts',(-1.08756841412115,-1.6715042687874,
2.5905692951156));
#288497=CARTESIAN_POINT('Ctrl Pts',(0.814059550847701,-1.82045011712066,
2.70168094560104));
#288498=CARTESIAN_POINT('Ctrl Pts',(1.97089172875732,-0.303837741386377,
2.81279259608647));
#288499=CARTESIAN_POINT('Ctrl Pts',(1.32452430591967,1.49076052473245,2.92390424657191));
#288500=CARTESIAN_POINT('Ctrl Pts',(-0.533671074984155,1.92143872229811,
3.03501589705734));
#288501=CARTESIAN_POINT('Ctrl Pts',(-1.90360246090293,0.594162646400333,
3.14612754754278));
#288502=CARTESIAN_POINT('Ctrl Pts',(-1.53189824749729,-1.27672210711867,
3.25723919802822));
#288503=CARTESIAN_POINT('Ctrl Pts',(0.241363579496748,-1.9795138802461,
3.36835084851366));
#288504=CARTESIAN_POINT('Ctrl Pts',(1.79379810087027,-0.871217511796724,
3.47946249899909));
#288505=CARTESIAN_POINT('Ctrl Pts',(1.70505874555187,1.03416935448819,3.59057414948453));
#288506=CARTESIAN_POINT('Ctrl Pts',(0.0563345346033484,1.9933785390062,
3.70168579996997));
#288507=CARTESIAN_POINT('Ctrl Pts',(-1.64393102121742,1.12881458930639,
3.8127974504554));
#288508=CARTESIAN_POINT('Ctrl Pts',(-1.84013843036505,-0.768519444546461,
3.92390910094084));
#288509=CARTESIAN_POINT('Ctrl Pts',(-0.352774472177625,-1.96272304498979,
4.03502075142628));
#288510=CARTESIAN_POINT('Ctrl Pts',(1.45734835604085,-1.36120070110842,
4.14613240191171));
#288511=CARTESIAN_POINT('Ctrl Pts',(1.9341204297854,0.485705407258275,4.25724405239715));
#288512=CARTESIAN_POINT('Ctrl Pts',(0.641335538231996,1.88823205855479,
4.36835570288259));
#288513=CARTESIAN_POINT('Ctrl Pts',(-1.2382172459999,1.56318573153086,4.47946735336802));
#288514=CARTESIAN_POINT('Ctrl Pts',(-1.9849057481176,-0.192043616511923,
4.59057900385346));
#288515=CARTESIAN_POINT('Ctrl Pts',(-0.915573004634159,-1.77156926275505,
4.7016906543389));
#288516=CARTESIAN_POINT('Ctrl Pts',(0.991431769317905,-1.73025854320689,
4.81280230482433));
#288517=CARTESIAN_POINT('Ctrl Pts',(1.99136014513231,-0.105907279881526,
4.92391395530977));
#288518=CARTESIAN_POINT('Ctrl Pts',(1.16936204678881,1.61534020660762,5.03502560579521));
#288519=CARTESIAN_POINT('Ctrl Pts',(-0.722503637349151,1.85868772890191,
5.14613725628065));
#288520=CARTESIAN_POINT('Ctrl Pts',(-1.95333946820844,0.40149284114719,
5.25724890676608));
#288521=CARTESIAN_POINT('Ctrl Pts',(-1.39703453558216,-1.42303411271269,
5.36836055725152));
#288522=CARTESIAN_POINT('Ctrl Pts',(0.437439095916471,-1.94560494883135,
5.47947220773696));
#288523=CARTESIAN_POINT('Ctrl Pts',(1.87169287184049,-0.68811145394827,
5.5905838582224));
#288524=CARTESIAN_POINT('Ctrl Pts',(1.59350562948136,1.19894594889198,5.70169550870783));
#288525=CARTESIAN_POINT('Ctrl Pts',(-0.142604781707098,1.98906899221409,
5.81280715919328));
#288526=CARTESIAN_POINT('Ctrl Pts',(-1.74824385260649,0.959361772939144,
5.9239188096787));
#288527=CARTESIAN_POINT('Ctrl Pts',(-1.75438733947832,-0.948080504298782,
6.03503046016415));
#288528=CARTESIAN_POINT('Ctrl Pts',(-0.155414470307694,-1.98810913230945,
6.14614211064957));
#288529=CARTESIAN_POINT('Ctrl Pts',(1.58574952316206,-1.20918568852951,
6.25725376113503));
#288530=CARTESIAN_POINT('Ctrl Pts',(1.87608653051662,0.67604061236542,6.36836541162044));
#288531=CARTESIAN_POINT('Ctrl Pts',(0.449962692697341,1.94274680664615,
6.4794770621059));
#288532=CARTESIAN_POINT('Ctrl Pts',(-1.38783903483595,1.43200362881485,
6.59058871259132));
#288533=CARTESIAN_POINT('Ctrl Pts',(-1.95588517063554,-0.388902017018772,
6.70170036307677));
#288534=CARTESIAN_POINT('Ctrl Pts',(-0.734461440070516,-1.85399513823601,
6.8128120135622));
#288535=CARTESIAN_POINT('Ctrl Pts',(1.1589325240977,-1.62283917383761,6.92392366404763));
#288536=CARTESIAN_POINT('Ctrl Pts',(1.99200103554574,0.0930776769041453,
7.03503531453308));
#288537=CARTESIAN_POINT('Ctrl Pts',(1.00255671219492,1.72383630846607,7.14614696501851));
#288538=CARTESIAN_POINT('Ctrl Pts',(-0.904142393148962,1.77743019904159,
7.25725861550395));
#288539=CARTESIAN_POINT('Ctrl Pts',(-1.98362751285899,0.20482546175019,
7.36837026598938));
#288540=CARTESIAN_POINT('Ctrl Pts',(-1.24826086435494,-1.55517728702285,
7.47948191647483));
#288541=CARTESIAN_POINT('Ctrl Pts',(0.629159129439381,-1.89232406564059,
7.59059356696026));
#288542=CARTESIAN_POINT('Ctrl Pts',(1.93095161698345,-0.498154024789975,
7.7017052174457));
#288543=CARTESIAN_POINT('Ctrl Pts',(1.46608633551955,1.35178490757587,7.81281686793113));
#288544=CARTESIAN_POINT('Ctrl Pts',(-0.34012421421804,1.96495473192057,
7.92392851841657));
#288545=CARTESIAN_POINT('Ctrl Pts',(-1.83514981233618,0.780356806706567,
8.03504016890202));
#288546=CARTESIAN_POINT('Ctrl Pts',(-1.65116820763892,-1.11820173922936,
8.14615181938743));
#288547=CARTESIAN_POINT('Ctrl Pts',(0.0434929585939797,-1.9937000632929,
8.25726346987289));
#288548=CARTESIAN_POINT('Ctrl Pts',(1.69836173813612,-1.0451310853227,8.36837512035831));
#288549=CARTESIAN_POINT('Ctrl Pts',(1.79937285886876,0.859644632590266,
8.47948677084376));
#288550=CARTESIAN_POINT('Ctrl Pts',(0.254109669394238,1.97791806128852,
8.59059842132919));
#288551=CARTESIAN_POINT('Ctrl Pts',(-1.52364242146117,1.28656338650393,
8.70171007181462));
#288552=CARTESIAN_POINT('Ctrl Pts',(-1.90739028433983,-0.581888205767853,
8.81282172230007));
#288553=CARTESIAN_POINT('Ctrl Pts',(-0.546037006206034,-1.91796120341649,
8.92393337278549));
#288554=CARTESIAN_POINT('Ctrl Pts',(1.31489404482737,-1.49926155303236,
9.03504502327096));
#288555=CARTESIAN_POINT('Ctrl Pts',(1.97280802451347,0.29113586868172,9.14615667375636));
#288556=CARTESIAN_POINT('Ctrl Pts',(0.825769134466469,1.81516858094871,
9.25726832424182));
#288557=CARTESIAN_POINT('Ctrl Pts',(-1.07677878518382,1.67847515406237,
9.36837997472725));
#288558=CARTESIAN_POINT('Ctrl Pts',(-1.99416506335232,0.00611876033513456,
9.47949162521268));
#288559=CARTESIAN_POINT('Ctrl Pts',(-1.08705846416831,-1.67183606078409,
9.59060327569813));
#288560=CARTESIAN_POINT('Ctrl Pts',(0.814614622610574,-1.82020144968518,
9.70171492618355));
#288561=CARTESIAN_POINT('Ctrl Pts',(1.97098458461971,-0.303237133736198,
9.81282657666901));
#288562=CARTESIAN_POINT('Ctrl Pts',(1.32406902671211,1.49116548659312,9.92393822715443));
#288563=CARTESIAN_POINT('Ctrl Pts',(-0.534256112049782,1.92127387999488,
10.0350498776399));
#288564=CARTESIAN_POINT('Ctrl Pts',(-1.90378548994746,0.593585769120274,
10.1461615281253));
#288565=CARTESIAN_POINT('Ctrl Pts',(-1.53150516153833,-1.277196460075,10.2572731786108));
#288566=CARTESIAN_POINT('Ctrl Pts',(0.241960478896032,-1.97942652154461,
10.3683848290962));
#288567=CARTESIAN_POINT('Ctrl Pts',(1.79407680373531,-0.870696329162404,
10.4794964795816));
#288568=CARTESIAN_POINT('Ctrl Pts',(1.70471837864578,1.03473882715419,10.5906081300671));
#288569=CARTESIAN_POINT('Ctrl Pts',(0.0557738537032858,1.99330146436314,
10.7017197805525));
#288570=CARTESIAN_POINT('Ctrl Pts',(-1.64436533547605,1.12849241588291,
10.812831431038));
#288571=CARTESIAN_POINT('Ctrl Pts',(-1.83973234590736,-0.769422280435679,
10.9239430815234));
#288572=CARTESIAN_POINT('Ctrl Pts',(-0.35250322224533,-1.96217765931249,
11.0350547320088));
#288573=CARTESIAN_POINT('Ctrl Pts',(1.45839329854295,-1.36202126768849,
11.1461663824943));
#288574=CARTESIAN_POINT('Ctrl Pts',(1.93276715414607,0.489093096322522,
11.2572899400314));
#288575=CARTESIAN_POINT('Ctrl Pts',(1.07308657757797,1.41791005753384,11.3313762807402));
#288576=CARTESIAN_POINT('Ctrl Pts',(0.541652309731358,1.59802532479866,
11.3684254046204));
#288577=CARTESIAN_POINT('Ctrl Pts',(0.901589915619032,-1.26415389587918,
0.00156757034352902));
#288578=CARTESIAN_POINT('Ctrl Pts',(1.32199638747131,-0.964337455893649,
0.0386166509585065));
#288579=CARTESIAN_POINT('Ctrl Pts',(1.83279936330088,0.0823089634603651,
0.112702948401963));
#288580=CARTESIAN_POINT('Ctrl Pts',(0.923282202193781,1.58732060670271,
0.223826462673898));
#288581=CARTESIAN_POINT('Ctrl Pts',(-0.831632123374875,1.63523016946011,
0.334938113159335));
#288582=CARTESIAN_POINT('Ctrl Pts',(-1.82526888708922,0.189389157069568,
0.446049763644772));
#288583=CARTESIAN_POINT('Ctrl Pts',(-1.14915115289507,-1.4309470818998,
0.557161414130209));
#288584=CARTESIAN_POINT('Ctrl Pts',(0.57845453723465,-1.74144804628265,
0.668273064615646));
#288585=CARTESIAN_POINT('Ctrl Pts',(1.77676450212934,-0.459006752310191,
0.779384715101083));
#288586=CARTESIAN_POINT('Ctrl Pts',(1.34951570028772,1.24356332530328,0.890496365586519));
#288587=CARTESIAN_POINT('Ctrl Pts',(-0.312442258131127,1.8082852788653,
1.00160801607196));
#288588=CARTESIAN_POINT('Ctrl Pts',(-1.68853341832575,0.718627469092382,
1.1127196665574));
#288589=CARTESIAN_POINT('Ctrl Pts',(-1.51976346784924,-1.02853938746936,
1.22383131704283));
#288590=CARTESIAN_POINT('Ctrl Pts',(0.0394641425147256,-1.83466608009094,
1.33494296752827));
#288591=CARTESIAN_POINT('Ctrl Pts',(1.56258416088533,-0.962235197172911,
1.44605461801371));
#288592=CARTESIAN_POINT('Ctrl Pts',(1.65607219184445,0.790563389392543,
1.55716626849914));
#288593=CARTESIAN_POINT('Ctrl Pts',(0.234393589654803,1.82006124714437,
1.66827791898458));
#288594=CARTESIAN_POINT('Ctrl Pts',(-1.40173518708264,1.184357688178,1.77938956947002));
#288595=CARTESIAN_POINT('Ctrl Pts',(-1.75539465934889,-0.534933739960341,
1.89050121995545));
#288596=CARTESIAN_POINT('Ctrl Pts',(-0.503016113620211,-1.7648056590657,
2.00161287044089));
#288597=CARTESIAN_POINT('Ctrl Pts',(1.20957969869399,-1.38002948714164,
2.11272452092633));
#288598=CARTESIAN_POINT('Ctrl Pts',(1.8155121814438,0.267357277299772,2.22383617141177));
#288599=CARTESIAN_POINT('Ctrl Pts',(0.760404229172604,1.67013465544135,
2.3349478218972));
#288600=CARTESIAN_POINT('Ctrl Pts',(-0.990409415564645,1.54487979450293,
2.44605947238264));
#288601=CARTESIAN_POINT('Ctrl Pts',(-1.83508203153925,0.00619028873297843,
2.55717112286807));
#288602=CARTESIAN_POINT('Ctrl Pts',(-1.00080945733949,-1.53816280287764,
2.66828277335352));
#288603=CARTESIAN_POINT('Ctrl Pts',(0.749119307574141,-1.67522674451834,
2.77939442383895));
#288604=CARTESIAN_POINT('Ctrl Pts',(1.81366712743903,-0.279599592198403,
2.89050607432439));
#288605=CARTESIAN_POINT('Ctrl Pts',(1.21886258797946,1.37183758962537,3.00161772480983));
#288606=CARTESIAN_POINT('Ctrl Pts',(-0.491098354841707,1.76815915211019,
3.11272937529526));
#288607=CARTESIAN_POINT('Ctrl Pts',(-1.75174574872692,0.546764312014174,
3.2238410257807));
#288608=CARTESIAN_POINT('Ctrl Pts',(-1.4096936191513,-1.17487372988056,
3.33495267626613));
#288609=CARTESIAN_POINT('Ctrl Pts',(0.222109202401656,-1.82160146116971,
3.44606432675158));
#288610=CARTESIAN_POINT('Ctrl Pts',(1.6507008484237,-0.80171758749588,3.557175977237));
#288611=CARTESIAN_POINT('Ctrl Pts',(1.56904052720829,0.951670218649055,
3.66828762772245));
#288612=CARTESIAN_POINT('Ctrl Pts',(0.0518405410397911,1.8343600898957,
3.77939927820788));
#288613=CARTESIAN_POINT('Ctrl Pts',(-1.51278916515584,1.03876528767484,
3.89051092869332));
#288614=CARTESIAN_POINT('Ctrl Pts',(-1.69334445540273,-0.707212087317697,
4.00162257917875));
#288615=CARTESIAN_POINT('Ctrl Pts',(-0.324632476889834,-1.80615008679826,
4.1127342296642));
#288616=CARTESIAN_POINT('Ctrl Pts',(1.34109082097837,-1.25261318489772,
4.22384588014963));
#288617=CARTESIAN_POINT('Ctrl Pts',(1.77982919752865,0.446959068278794,
4.33495753063507));
#288618=CARTESIAN_POINT('Ctrl Pts',(0.590174065057926,1.73760149459688,
4.44606918112051));
#288619=CARTESIAN_POINT('Ctrl Pts',(-1.13944052985299,1.43848519631609,
4.55718083160594));
#288620=CARTESIAN_POINT('Ctrl Pts',(-1.82656320177237,-0.176723657225873,
4.66829248209138));
#288621=CARTESIAN_POINT('Ctrl Pts',(-0.842534694852325,-1.63024527880388,
4.77940413257681));
#288622=CARTESIAN_POINT('Ctrl Pts',(0.912341953073382,-1.59223005302452,
4.89051578306226));
#288623=CARTESIAN_POINT('Ctrl Pts',(1.83250271002755,-0.0974587032229718,
5.00162743354769));
#288624=CARTESIAN_POINT('Ctrl Pts',(1.07607813934704,1.48647913510807,5.11273908403313));
#288625=CARTESIAN_POINT('Ctrl Pts',(-0.664867114410965,1.71041401457865,
5.22385073451856));
#288626=CARTESIAN_POINT('Ctrl Pts',(-1.7975150692081,0.369464419209799,
5.334962385004));
#288627=CARTESIAN_POINT('Ctrl Pts',(-1.28558843497708,-1.30951393919477,
5.44607403548944));
#288628=CARTESIAN_POINT('Ctrl Pts',(0.402543121443117,-1.79039755821746,
5.55718568597487));
#288629=CARTESIAN_POINT('Ctrl Pts',(1.72238169392461,-0.633218510093957,
5.66829733646031));
#288630=CARTESIAN_POINT('Ctrl Pts',(1.46638637496419,1.10330203498933,5.77940898694574));
#288631=CARTESIAN_POINT('Ctrl Pts',(-0.131228723031326,1.83039433001302,
5.89052063743119));
#288632=CARTESIAN_POINT('Ctrl Pts',(-1.60878061435619,0.882830287180914,
6.00163228791661));
#288633=CARTESIAN_POINT('Ctrl Pts',(-1.61443401480672,-0.872448962935536,
6.11274393840206));
#288634=CARTESIAN_POINT('Ctrl Pts',(-0.143016540083152,-1.82951104133176,
6.22385558888749));
#288635=CARTESIAN_POINT('Ctrl Pts',(1.4592489990937,-1.11272491647141,6.33496723937292));
#288636=CARTESIAN_POINT('Ctrl Pts',(1.726424855806,0.622110599771014,6.44607888985837));
#288637=CARTESIAN_POINT('Ctrl Pts',(0.414067669173098,1.78776741955932,
6.5571905403438));
#288638=CARTESIAN_POINT('Ctrl Pts',(-1.27712648996998,1.31776792710599,
6.66830219082924));
#288639=CARTESIAN_POINT('Ctrl Pts',(-1.79985769246887,-0.357878007081822,
6.77941384131468));
#288640=CARTESIAN_POINT('Ctrl Pts',(-0.675871003359114,-1.70609576750853,
6.89052549180013));
#288641=CARTESIAN_POINT('Ctrl Pts',(1.06648061443804,-1.49337988473134,
7.00163714228554));
#288642=CARTESIAN_POINT('Ctrl Pts',(1.8330924744769,0.0856525604305603,
7.112748792771));
#288643=CARTESIAN_POINT('Ctrl Pts',(0.922579422182522,1.58632014135147,
7.22386044325642));
#288644=CARTESIAN_POINT('Ctrl Pts',(-0.832015941338537,1.63563866867091,
7.33497209374186));
#288645=CARTESIAN_POINT('Ctrl Pts',(-1.82538693560014,0.188485852073177,
7.44608374422731));
#288646=CARTESIAN_POINT('Ctrl Pts',(-1.14868293530086,-1.43111561211513,
7.55719539471273));
#288647=CARTESIAN_POINT('Ctrl Pts',(0.57896900897335,-1.74136706864058,
7.66830704519818));
#288648=CARTESIAN_POINT('Ctrl Pts',(1.77691317148419,-0.458414618104187,
7.7794186956836));
#288649=CARTESIAN_POINT('Ctrl Pts',(1.34913174271418,1.24394852059397,7.89053034616905));
#288650=CARTESIAN_POINT('Ctrl Pts',(-0.31299137216547,1.80820374462534,
8.00164199665448));
#288651=CARTESIAN_POINT('Ctrl Pts',(-1.68875379605891,0.718105143649537,
8.11275364713992));
#288652=CARTESIAN_POINT('Ctrl Pts',(-1.51944901709812,-1.02899906001644,
8.22386529762534));
#288653=CARTESIAN_POINT('Ctrl Pts',(0.0400233803440546,-1.83465596511855,
8.3349769481108));
#288654=CARTESIAN_POINT('Ctrl Pts',(1.5628777623923,-0.961757495684236,
8.44608859859622));
#288655=CARTESIAN_POINT('Ctrl Pts',(1.65583088939842,0.791067915431072,
8.55720024908167));
#288656=CARTESIAN_POINT('Ctrl Pts',(0.233838494230872,1.82013294600853,
8.6683118995671));
#288657=CARTESIAN_POINT('Ctrl Pts',(-1.40209638787114,1.18392993761256,
8.77942355005254));
#288658=CARTESIAN_POINT('Ctrl Pts',(-1.7552314048651,-0.535469044416299,
8.89053520053798));
#288659=CARTESIAN_POINT('Ctrl Pts',(-0.502477814519769,-1.76495904649879,
9.00164685102341));
#288660=CARTESIAN_POINT('Ctrl Pts',(1.21000056490795,-1.37966046256758,
9.11275850150884));
#288661=CARTESIAN_POINT('Ctrl Pts',(1.81543055389654,0.26791099020919,9.2238701519943));
#288662=CARTESIAN_POINT('Ctrl Pts',(0.759894778684712,1.67036653408787,
9.3349818024797));
#288663=CARTESIAN_POINT('Ctrl Pts',(-0.990880553059603,1.54457759740332,
9.44609345296518));
#288664=CARTESIAN_POINT('Ctrl Pts',(-1.83508387057358,0.00563064643204322,
9.55720510345058));
#288665=CARTESIAN_POINT('Ctrl Pts',(-1.00034018779382,-1.53846812672104,
9.66831675393604));
#288666=CARTESIAN_POINT('Ctrl Pts',(0.749630099412679,-1.67499791411289,
9.77942840442146));
#288667=CARTESIAN_POINT('Ctrl Pts',(1.81375257587983,-0.27904689702204,
9.89054005490692));
#288668=CARTESIAN_POINT('Ctrl Pts',(1.21844362791154,1.37221024632886,10.0016517053923));
#288669=CARTESIAN_POINT('Ctrl Pts',(-0.491636721550935,1.76800745982683,
10.1127633558778));
#288670=CARTESIAN_POINT('Ctrl Pts',(-1.75191417693461,0.546233454157225,
10.2238750063632));
#288671=CARTESIAN_POINT('Ctrl Pts',(-1.40933189096927,-1.17531024212075,
10.3349866568486));
#288672=CARTESIAN_POINT('Ctrl Pts',(0.222658485146653,-1.82152107136295,
10.4460983073341));
#288673=CARTESIAN_POINT('Ctrl Pts',(1.65095731823241,-0.801237981337174,
10.5572099578195));
#288674=CARTESIAN_POINT('Ctrl Pts',(1.56872731250459,0.952194262582688,
10.6683216083049));
#288675=CARTESIAN_POINT('Ctrl Pts',(0.0513245875236328,1.83428916375378,
10.7794332587904));
#288676=CARTESIAN_POINT('Ctrl Pts',(-1.51318883271867,1.038468815099,10.8905449092758));
#288677=CARTESIAN_POINT('Ctrl Pts',(-1.69297076565553,-0.708042900979278,
11.0016565597613));
#288678=CARTESIAN_POINT('Ctrl Pts',(-0.324382865468596,-1.80564820835397,
11.1127682102467));
#288679=CARTESIAN_POINT('Ctrl Pts',(1.34205240493473,-1.25336829214711,
11.2238798607321));
#288680=CARTESIAN_POINT('Ctrl Pts',(1.77858387719695,0.450076510096708,
11.3350034182694));
#288681=CARTESIAN_POINT('Ctrl Pts',(0.987482885158952,1.30479864697375,
11.4090897589781));
#288682=CARTESIAN_POINT('Ctrl Pts',(0.498442899895145,1.47054551912389,
11.4461388828584));
#288683=CARTESIAN_POINT('Ctrl Pts',(0.863567639152675,1.75641488315944,
6.58110718698701E-16));
#288684=CARTESIAN_POINT('Ctrl Pts',(0.902605506355986,1.73244147111074,
1.41492757312224E-15));
#288685=CARTESIAN_POINT('Ctrl Pts',(0.940681517855526,1.70703362163956,
3.0153021400338E-15));
#288686=CARTESIAN_POINT('Ctrl Pts',(0.977705169885399,1.68018661523996,
1.89431803576667E-15));
#288687=CARTESIAN_POINT('Ctrl Pts',(1.0358643592122,1.63801357064694,2.65822224384553E-16));
#288688=CARTESIAN_POINT('Ctrl Pts',(1.09142895154027,1.59229038852923,3.29238884271004E-15));
#288689=CARTESIAN_POINT('Ctrl Pts',(1.14423757319707,1.54335784953327,4.25354196309513E-15));
#288690=CARTESIAN_POINT('Ctrl Pts',(1.18228615197471,1.50810198588135,5.04045922924434E-15));
#288691=CARTESIAN_POINT('Ctrl Pts',(1.21890323710713,1.47117925249246,2.90921159275611E-15));
#288692=CARTESIAN_POINT('Ctrl Pts',(1.25401379483509,1.43270976178997,3.57006091356027E-15));
#288693=CARTESIAN_POINT('Ctrl Pts',(1.26389181876557,1.42188673377951,3.51159535440953E-15));
#288694=CARTESIAN_POINT('Ctrl Pts',(1.27364380619492,1.41094858444086,1.87046246663327E-15));
#288695=CARTESIAN_POINT('Ctrl Pts',(1.28326720497828,1.3998998522991,2.22044604925031E-15));
#288696=CARTESIAN_POINT('Ctrl Pts',(1.3301037638391,1.34612627344776,4.69467974937994E-15));
#288697=CARTESIAN_POINT('Ctrl Pts',(1.37390887238432,1.28972344251136,1.71987005091003E-15));
#288698=CARTESIAN_POINT('Ctrl Pts',(1.41451968724013,1.23102458107283,2.50494069931051E-15));
#288699=CARTESIAN_POINT('Ctrl Pts',(1.45487033903532,1.17270175925579,3.28498198832941E-15));
#288700=CARTESIAN_POINT('Ctrl Pts',(1.49206780791658,1.11211115787746,4.00139226059959E-15));
#288701=CARTESIAN_POINT('Ctrl Pts',(1.525903395753,1.04956595044032,4.00374178255447E-15));
#288702=CARTESIAN_POINT('Ctrl Pts',(1.5305357317926,1.0410030603875,4.0040634490578E-15));
#288703=CARTESIAN_POINT('Ctrl Pts',(1.53510497437072,1.03240352730891,3.37876692969174E-15));
#288704=CARTESIAN_POINT('Ctrl Pts',(1.53961051084785,1.02376815184549,3.41393580072236E-15));
#288705=CARTESIAN_POINT('Ctrl Pts',(1.5453767175419,1.01271655786648,3.46566903485334E-15));
#288706=CARTESIAN_POINT('Ctrl Pts',(1.55103417937643,1.00161467257822,3.03674728701833E-15));
#288707=CARTESIAN_POINT('Ctrl Pts',(1.55658137030158,0.990465869694388,
3.02535774210355E-15));
#288708=CARTESIAN_POINT('Ctrl Pts',(1.58754193823296,0.928240993410824,
2.09404046666805E-15));
#288709=CARTESIAN_POINT('Ctrl Pts',(1.61507975241109,0.864539873642212,
1.89375059754463E-15));
#288710=CARTESIAN_POINT('Ctrl Pts',(1.63904156643728,0.799669212580803,
2.04003480774873E-15));
#288711=CARTESIAN_POINT('Ctrl Pts',(1.66267720699393,0.735681585189814,
2.18432776519006E-15));
#288712=CARTESIAN_POINT('Ctrl Pts',(1.68283372774119,0.670555047536874,
9.94305425112374E-16));
#288713=CARTESIAN_POINT('Ctrl Pts',(1.69931410754026,0.604578807305152,
9.43689570931383E-16));
#288714=CARTESIAN_POINT('Ctrl Pts',(1.71527610637215,0.540677812161158,
8.94665809636882E-16));
#288715=CARTESIAN_POINT('Ctrl Pts',(1.72778958794875,0.475978937320602,
1.95320499488021E-15));
#288716=CARTESIAN_POINT('Ctrl Pts',(1.73662725954747,0.410752997999464,
2.31759056390501E-15));
#288717=CARTESIAN_POINT('Ctrl Pts',(1.73865677872466,0.395774245595767,
2.40126956147422E-15));
#288718=CARTESIAN_POINT('Ctrl Pts',(1.74049224208592,0.380767759452602,
2.15272180223388E-15));
#288719=CARTESIAN_POINT('Ctrl Pts',(1.74213052178609,0.365736946962489,
1.98452365651747E-15));
#288720=CARTESIAN_POINT('Ctrl Pts',(1.74338539139703,0.354223827548557,
1.9006075599436E-15));
#288721=CARTESIAN_POINT('Ctrl Pts',(1.74452450777523,0.342696049837885,
3.20340688219071E-16));
#288722=CARTESIAN_POINT('Ctrl Pts',(1.74554535151306,0.331170337018761,
7.21644966006352E-16));
#288723=CARTESIAN_POINT('Ctrl Pts',(1.75129431083391,0.266262406759458,
2.83665743705786E-15));
#288724=CARTESIAN_POINT('Ctrl Pts',(1.75331011127704,0.201301920292928,
5.37283262797766E-16));
#288725=CARTESIAN_POINT('Ctrl Pts',(1.75142561531545,0.136549272921142,
-1.11022302462516E-15));
#288726=CARTESIAN_POINT('Ctrl Pts',(1.75088296778463,0.117903510379641,
-1.47891683923337E-15));
#288727=CARTESIAN_POINT('Ctrl Pts',(1.75001659332986,0.0992750230412608,
-4.137032525397E-16));
#288728=CARTESIAN_POINT('Ctrl Pts',(1.74882170147482,0.080670175218092,
-5.96744875736022E-16));
#288729=CARTESIAN_POINT('Ctrl Pts',(1.74456409946248,0.0143779520375277,
-1.14186309985328E-15));
#288730=CARTESIAN_POINT('Ctrl Pts',(1.73613918364975,-0.0516159836678278,
-1.20522593144347E-15));
#288731=CARTESIAN_POINT('Ctrl Pts',(1.72372245238697,-0.117006780976604,
-9.15933995315754E-16));
#288732=CARTESIAN_POINT('Ctrl Pts',(1.71175318101375,-0.180041099891606,
-6.3706722947246E-16));
#288733=CARTESIAN_POINT('Ctrl Pts',(1.69607374898919,-0.242515614155525,
-3.38441552534961E-15));
#288734=CARTESIAN_POINT('Ctrl Pts',(1.67680493801022,-0.304129401844208,
-1.66533453693773E-15));
#288735=CARTESIAN_POINT('Ctrl Pts',(1.67349552259788,-0.314711560692092,
-1.43194362083307E-15));
#288736=CARTESIAN_POINT('Ctrl Pts',(1.67008173945308,-0.32526302074398,
-9.20645452357687E-16));
#288737=CARTESIAN_POINT('Ctrl Pts',(1.66656691458475,-0.335775244456301,
-1.38777878078145E-15));
#288738=CARTESIAN_POINT('Ctrl Pts',(1.64602231395326,-0.397220535760641,
-3.28484698948248E-15));
#288739=CARTESIAN_POINT('Ctrl Pts',(1.62200575451327,-0.457403213326927,
-2.70920381044168E-15));
#288740=CARTESIAN_POINT('Ctrl Pts',(1.59470364320676,-0.516049647263231,
-3.10862446895044E-15));
#288741=CARTESIAN_POINT('Ctrl Pts',(1.56766036096921,-0.574140102150036,
-3.50425854568154E-15));
#288742=CARTESIAN_POINT('Ctrl Pts',(1.53739275011846,-0.630724091745741,
-3.35336214633415E-15));
#288743=CARTESIAN_POINT('Ctrl Pts',(1.50404316674669,-0.685503900933402,
-2.96984659087229E-15));
#288744=CARTESIAN_POINT('Ctrl Pts',(1.47096966581936,-0.739830218889776,
-2.58950594499927E-15));
#288745=CARTESIAN_POINT('Ctrl Pts',(1.43486430828708,-0.792382821984317,
-9.97104400078256E-17));
#288746=CARTESIAN_POINT('Ctrl Pts',(1.39583852741916,-0.842828743497356,
-2.02615701994091E-15));
#288747=CARTESIAN_POINT('Ctrl Pts',(1.38891448399703,-0.851778974428235,
-2.60911541074168E-15));
#288748=CARTESIAN_POINT('Ctrl Pts',(1.38189845475662,-0.860662765012676,
-2.92338460246606E-15));
#288749=CARTESIAN_POINT('Ctrl Pts',(1.3747909965488,-0.869478087839507,
-2.83106871279415E-15));
#288750=CARTESIAN_POINT('Ctrl Pts',(1.36801000346398,-0.877888498619476,
-2.65001119591314E-15));
#288751=CARTESIAN_POINT('Ctrl Pts',(1.36114891147745,-0.8862326313589,-1.96909756090429E-15));
#288752=CARTESIAN_POINT('Ctrl Pts',(1.35421355798306,-0.894502968665375,
-1.94289029309402E-15));
#288753=CARTESIAN_POINT('Ctrl Pts',(1.31434175760682,-0.942049678201485,
-1.45304958986999E-15));
#288754=CARTESIAN_POINT('Ctrl Pts',(1.2719676049916,-0.9872233030338,-1.28559172267538E-15));
#288755=CARTESIAN_POINT('Ctrl Pts',(1.22722986402212,-1.02975664628297,
-1.74860126378462E-15));
#288756=CARTESIAN_POINT('Ctrl Pts',(1.18329662428731,-1.07152512911637,
-2.16477509457826E-15));
#288757=CARTESIAN_POINT('Ctrl Pts',(1.13708333145971,-1.11074797100956,
-2.12946189812955E-15));
#288758=CARTESIAN_POINT('Ctrl Pts',(1.08869802628372,-1.14712822354084,
-2.33146835171283E-15));
#288759=CARTESIAN_POINT('Ctrl Pts',(1.04185702698958,-1.18234733349458,
-1.71822951363253E-15));
#288760=CARTESIAN_POINT('Ctrl Pts',(0.992979843245106,-1.21490270869377,
1.81230356841659E-15));
#288761=CARTESIAN_POINT('Ctrl Pts',(0.942151955843589,-1.24447758124097,
3.5527136788005E-15));
#288762=CARTESIAN_POINT('Ctrl Pts',(0.929425469399051,-1.25188265420018,
3.19009398667763E-15));
#288763=CARTESIAN_POINT('Ctrl Pts',(0.916576650434786,-1.25910062270965,
2.60075520077752E-15));
#288764=CARTESIAN_POINT('Ctrl Pts',(0.903606778650244,-1.26612599672281,
4.16333634234434E-16));
#288765=CARTESIAN_POINT('Ctrl Pts',(-0.684399482591588,1.39375527916939,
-0.23169217219233));
#288766=CARTESIAN_POINT('Ctrl Pts',(-1.14813007759954,1.16604830489444,
-0.194624624464132));
#288767=CARTESIAN_POINT('Ctrl Pts',(-1.82232784108757,0.215386159079778,
-0.120494936792213));
#288768=CARTESIAN_POINT('Ctrl Pts',(-1.16734347439351,-1.41806245612601,
-0.0093031091765735));
#288769=CARTESIAN_POINT('Ctrl Pts',(0.558471034725876,-1.74792270953766,
0.101883310654589));
#288770=CARTESIAN_POINT('Ctrl Pts',(1.77191842122005,-0.478866139559988,
0.213069730485752));
#288771=CARTESIAN_POINT('Ctrl Pts',(1.36262118629268,1.23002510036026,0.324256150316915));
#288772=CARTESIAN_POINT('Ctrl Pts',(-0.295111057128028,1.81154554732604,
0.435442570148077));
#288773=CARTESIAN_POINT('Ctrl Pts',(-1.68239591977648,0.733934265747275,
0.54662898997924));
#288774=CARTESIAN_POINT('Ctrl Pts',(-1.52859240585868,-1.01616207295397,
0.657815409810402));
#288775=CARTESIAN_POINT('Ctrl Pts',(0.025499203811463,-1.83532087192271,
0.769001829641565));
#288776=CARTESIAN_POINT('Ctrl Pts',(1.55621608150441,-0.973292876645946,
0.880188249472728));
#288777=CARTESIAN_POINT('Ctrl Pts',(1.66138010486741,0.780338174659502,
0.99137466930389));
#288778=CARTESIAN_POINT('Ctrl Pts',(0.244643362335791,1.81913270512971,
1.10256108913506));
#288779=CARTESIAN_POINT('Ctrl Pts',(-1.39619494321738,1.19152953216238,
1.21374750896622));
#288780=CARTESIAN_POINT('Ctrl Pts',(-1.75805935358985,-0.527569944496845,
1.32493392879738));
#288781=CARTESIAN_POINT('Ctrl Pts',(-0.509464470574177,-1.76339059445253,
1.43612034862854));
#288782=CARTESIAN_POINT('Ctrl Pts',(1.20582162646513,-1.38386993918644,
1.54730676845971));
#288783=CARTESIAN_POINT('Ctrl Pts',(1.81652298091137,0.263336133863676,
1.65849318829087));
#288784=CARTESIAN_POINT('Ctrl Pts',(0.763210382228217,1.66931461278863,
1.76967960812203));
#288785=CARTESIAN_POINT('Ctrl Pts',(-0.989235987808251,1.54612862738527,
1.88086602795319));
#288786=CARTESIAN_POINT('Ctrl Pts',(-1.83549930227322,0.00662166747232072,
1.99205244778436));
#288787=CARTESIAN_POINT('Ctrl Pts',(-1.00036561103327,-1.53895098784626,
2.10323886761552));
#288788=CARTESIAN_POINT('Ctrl Pts',(0.751146372438219,-1.67477779326081,
2.21442528744668));
#288789=CARTESIAN_POINT('Ctrl Pts',(1.81457569490279,-0.276435470852209,
2.32561170727784));
#288790=CARTESIAN_POINT('Ctrl Pts',(1.21577495550945,1.37513373000844,2.43679812710901));
#288791=CARTESIAN_POINT('Ctrl Pts',(-0.496728387120161,1.76702077853356,
2.54798454694017));
#288792=CARTESIAN_POINT('Ctrl Pts',(-1.75420697769208,0.54024013213266,
2.65917096677134));
#288793=CARTESIAN_POINT('Ctrl Pts',(-1.40475587210311,-1.18142391219023,
2.77035738660249));
#288794=CARTESIAN_POINT('Ctrl Pts',(0.231512555941918,-1.82085239862611,
2.88154380643366));
#288795=CARTESIAN_POINT('Ctrl Pts',(1.65570543891066,-0.79230109204954,
2.99273022626482));
#288796=CARTESIAN_POINT('Ctrl Pts',(1.56320030886811,0.96203238782093,3.10391664609599));
#288797=CARTESIAN_POINT('Ctrl Pts',(0.0387358782285723,1.83510246381186,
3.21510306592715));
#288798=CARTESIAN_POINT('Ctrl Pts',(-1.5212122973926,1.0271390690517,3.32628948575831));
#288799=CARTESIAN_POINT('Ctrl Pts',(-1.68766401250321,-0.721728274221359,
3.43747590558947));
#288800=CARTESIAN_POINT('Ctrl Pts',(-0.30814227474981,-1.80946120694338,
3.54866232542063));
#288801=CARTESIAN_POINT('Ctrl Pts',(1.35365115508378,-1.23964917265128,
3.6598487452518));
#288802=CARTESIAN_POINT('Ctrl Pts',(1.77544140021948,0.465735284578745,
3.77103516508296));
#288803=CARTESIAN_POINT('Ctrl Pts',(0.570850297216628,1.74448601573192,
3.88222158491412));
#288804=CARTESIAN_POINT('Ctrl Pts',(-1.15666444373811,1.42521187390071,
3.99340800474529));
#288805=CARTESIAN_POINT('Ctrl Pts',(-1.82462437363633,-0.199618175645153,
4.10459442457644));
#288806=CARTESIAN_POINT('Ctrl Pts',(-0.821149217997519,-1.64158931608911,
4.21578084440761));
#288807=CARTESIAN_POINT('Ctrl Pts',(0.934534245966791,-1.57979342448024,
4.32696726423877));
#288808=CARTESIAN_POINT('Ctrl Pts',(1.83414379690324,-0.0708382184779958,
4.43815368406993));
#288809=CARTESIAN_POINT('Ctrl Pts',(1.05359805760058,1.50300786888694,4.5493401039011));
#288810=CARTESIAN_POINT('Ctrl Pts',(-0.692089211636685,1.7000335420373,
4.66052652373226));
#288811=CARTESIAN_POINT('Ctrl Pts',(-1.80379273749893,0.339754736629052,
4.77171294356342));
#288812=CARTESIAN_POINT('Ctrl Pts',(-1.26314386028315,-1.33175414741037,
4.88289936339459));
#288813=CARTESIAN_POINT('Ctrl Pts',(0.43459959303458,-1.78331845575879,
4.99408578322575));
#288814=CARTESIAN_POINT('Ctrl Pts',(1.73423096451572,-0.601285691356955,
5.10527220305691));
#288815=CARTESIAN_POINT('Ctrl Pts',(1.44523153483113,1.13155085243458,5.21645862288808));
#288816=CARTESIAN_POINT('Ctrl Pts',(-0.167662680511327,1.82783772432881,
5.32764504271924));
#288817=CARTESIAN_POINT('Ctrl Pts',(-1.62697060664768,0.84974594204401,
5.4388314625504));
#288818=CARTESIAN_POINT('Ctrl Pts',(-1.59590287279599,-0.906749988429709,
5.55001788238156));
#288819=CARTESIAN_POINT('Ctrl Pts',(-0.102918871003275,-1.83262359116846,
5.66120430221273));
#288820=CARTESIAN_POINT('Ctrl Pts',(1.48434328164846,-1.07973447807358,
5.77239072204388));
#288821=CARTESIAN_POINT('Ctrl Pts',(1.7118825917383,0.66223826000852,5.88357714187506));
#288822=CARTESIAN_POINT('Ctrl Pts',(0.371263179685662,1.79757202145712,
5.99476356170621));
#288823=CARTESIAN_POINT('Ctrl Pts',(-1.30944941179655,1.28625182560081,
6.10594998153738));
#288824=CARTESIAN_POINT('Ctrl Pts',(-1.79064953307602,-0.40333084510164,
6.21713640136854));
#288825=CARTESIAN_POINT('Ctrl Pts',(-0.631536996732062,-1.72344496363371,
6.3283228211997));
#288826=CARTESIAN_POINT('Ctrl Pts',(1.10609082714422,-1.46480872574654,
6.43950924103086));
#288827=CARTESIAN_POINT('Ctrl Pts',(1.83049146684385,0.135655854011535,
6.55069566086203));
#288828=CARTESIAN_POINT('Ctrl Pts',(0.878082509091036,1.61185378621765,
6.66188208069318));
#288829=CARTESIAN_POINT('Ctrl Pts',(-0.878688121616026,1.61152372177596,
6.77306850052436));
#288830=CARTESIAN_POINT('Ctrl Pts',(-1.83054231202212,0.134968014034564,
6.88425492035551));
#288831=CARTESIAN_POINT('Ctrl Pts',(-1.10554032858663,-1.46522424999876,
6.99544134018668));
#288832=CARTESIAN_POINT('Ctrl Pts',(0.632184558464056,-1.72320753391902,
7.10662776001784));
#288833=CARTESIAN_POINT('Ctrl Pts',(1.79080096334203,-0.402657957339467,
7.217814179849));
#288834=CARTESIAN_POINT('Ctrl Pts',(1.30896599390356,1.28674377702811,7.32900059968016));
#288835=CARTESIAN_POINT('Ctrl Pts',(-0.371938613975646,1.79743238769886,
7.44018701951133));
#288836=CARTESIAN_POINT('Ctrl Pts',(-1.71213131531173,0.661594951646106,
7.55137343934249));
#288837=CARTESIAN_POINT('Ctrl Pts',(-1.48393745292332,-1.08029216267287,
7.66255985917366));
#288838=CARTESIAN_POINT('Ctrl Pts',(0.103607495311869,-1.83258478871351,
7.77374627900482));
#288839=CARTESIAN_POINT('Ctrl Pts',(1.59624348293943,-0.906150243659566,
7.88493269883597));
#288840=CARTESIAN_POINT('Ctrl Pts',(1.62665118897041,0.850357236913776,
7.99611911866715));
#288841=CARTESIAN_POINT('Ctrl Pts',(0.166975835438897,1.82790059665215,
8.10730553849828));
#288842=CARTESIAN_POINT('Ctrl Pts',(-1.44565662736788,1.13100770848327,
8.21849195832947));
#288843=CARTESIAN_POINT('Ctrl Pts',(-1.73400490139949,-0.601937308250454,
8.32967837816063));
#288844=CARTESIAN_POINT('Ctrl Pts',(-0.433929457718794,-1.78348163607784,
8.44086479799179));
#288845=CARTESIAN_POINT('Ctrl Pts',(1.26364419445534,-1.33127941123177,
8.55205121782296));
#288846=CARTESIAN_POINT('Ctrl Pts',(1.8036649433301,0.340432510995058,8.66323763765411));
#288847=CARTESIAN_POINT('Ctrl Pts',(0.691450352967021,1.70029348267665,
8.77442405748529));
#288848=CARTESIAN_POINT('Ctrl Pts',(-1.05416275630007,1.50261186116277,
8.88561047731643));
#288849=CARTESIAN_POINT('Ctrl Pts',(-1.83411705133878,-0.0715274186238769,
8.99679689714761));
#288850=CARTESIAN_POINT('Ctrl Pts',(-0.93394054821382,-1.58014447160157,
9.10798331697877));
#288851=CARTESIAN_POINT('Ctrl Pts',(0.821765999768745,-1.64128065142731,
9.21916973680992));
#288852=CARTESIAN_POINT('Ctrl Pts',(1.8246992696381,-0.198932519657866,
9.33035615664109));
#288853=CARTESIAN_POINT('Ctrl Pts',(1.15612879063603,1.42564637392063,9.44154257647225));
#288854=CARTESIAN_POINT('Ctrl Pts',(-0.571505712575411,1.74427144678546,
9.55272899630341));
#288855=CARTESIAN_POINT('Ctrl Pts',(-1.7756163895225,0.46506799577476,9.66391541613459));
#288856=CARTESIAN_POINT('Ctrl Pts',(-1.35318503866645,-1.24015752487752,
9.77510183596573));
#288857=CARTESIAN_POINT('Ctrl Pts',(0.308821787045722,-1.80934569414666,
9.88628825579692));
#288858=CARTESIAN_POINT('Ctrl Pts',(1.68793584191459,-0.721093294283745,
9.99747467562806));
#288859=CARTESIAN_POINT('Ctrl Pts',(1.52082480165556,1.0277091496512,10.1086610954593));
#288860=CARTESIAN_POINT('Ctrl Pts',(-0.0394227203814493,1.83509056147044,
10.2198475152904));
#288861=CARTESIAN_POINT('Ctrl Pts',(-1.56356686902893,0.961439630001686,
10.3310339351216));
#288862=CARTESIAN_POINT('Ctrl Pts',(-1.65539775368066,-0.792913103321646,
10.4422203549528));
#288863=CARTESIAN_POINT('Ctrl Pts',(-0.230847085212319,-1.82095846328463,
10.5534067747839));
#288864=CARTESIAN_POINT('Ctrl Pts',(1.4052354109789,-1.18085942306844,10.6645931946151));
#288865=CARTESIAN_POINT('Ctrl Pts',(1.75393587956343,0.540829674163776,
10.7757796144463));
#288866=CARTESIAN_POINT('Ctrl Pts',(0.496193799610693,1.76733979700505,
10.8869660342774));
#288867=CARTESIAN_POINT('Ctrl Pts',(-1.21653822386253,1.37442439623192,
10.9981524541086));
#288868=CARTESIAN_POINT('Ctrl Pts',(-1.81400015511254,-0.2766353780646,
11.1093388739397));
#288869=CARTESIAN_POINT('Ctrl Pts',(-0.751432125101304,-1.67598976072319,
11.2205252937709));
#288870=CARTESIAN_POINT('Ctrl Pts',(1.00302336056212,-1.53668295415482,
11.3317236110345));
#288871=CARTESIAN_POINT('Ctrl Pts',(1.55494787760704,-0.510025057698862,
11.4058597883545));
#288872=CARTESIAN_POINT('Ctrl Pts',(1.55271109992305,0.00668241897662998,
11.4429338257307));
#288873=CARTESIAN_POINT('Ctrl Pts',(-0.743729958480259,1.51457968960343,
-0.153977644258129));
#288874=CARTESIAN_POINT('Ctrl Pts',(-1.2476612806743,1.26713283607588,-0.116910096529931));
#288875=CARTESIAN_POINT('Ctrl Pts',(-1.98030513473999,0.234057948938039,
-0.0427804088580121));
#288876=CARTESIAN_POINT('Ctrl Pts',(-1.26854028360072,-1.54099405163692,
0.0684114187576278));
#288877=CARTESIAN_POINT('Ctrl Pts',(0.606884794676209,-1.89944983486631,
0.179597838588791));
#288878=CARTESIAN_POINT('Ctrl Pts',(1.9255257307534,-0.520378964554392,
0.290784258419953));
#288879=CARTESIAN_POINT('Ctrl Pts',(1.48074658745842,1.33665576916651,0.401970678251116));
#288880=CARTESIAN_POINT('Ctrl Pts',(-0.320694184971879,1.96858812574808,
0.513157098082277));
#288881=CARTESIAN_POINT('Ctrl Pts',(-1.82824253873584,0.797558903645778,
0.624343517913441));
#288882=CARTESIAN_POINT('Ctrl Pts',(-1.66110582409801,-1.10425299193025,
0.735529937744604));
#288883=CARTESIAN_POINT('Ctrl Pts',(0.027709725495631,-1.99442452923011,
0.846716357575766));
#288884=CARTESIAN_POINT('Ctrl Pts',(1.69112419153345,-1.05766747221376,
0.957902777406929));
#288885=CARTESIAN_POINT('Ctrl Pts',(1.80540486637151,0.84798555960686,1.06908919723809));
#288886=CARTESIAN_POINT('Ctrl Pts',(0.265851454217222,1.97683301298401,
1.18027561706925));
#288887=CARTESIAN_POINT('Ctrl Pts',(-1.51723084771687,1.29482302664448,
1.29146203690042));
#288888=CARTESIAN_POINT('Ctrl Pts',(-1.9104652228843,-0.57330489413916,
1.40264845673157));
#288889=CARTESIAN_POINT('Ctrl Pts',(-0.55362985973125,-1.91625862811955,
1.51383487656274));
#288890=CARTESIAN_POINT('Ctrl Pts',(1.31035410019542,-1.50383739116212,
1.6250212963939));
#288891=CARTESIAN_POINT('Ctrl Pts',(1.97399705221268,0.286164698960839,
1.73620771622506));
#288892=CARTESIAN_POINT('Ctrl Pts',(0.829372961734173,1.81402721544818,
1.84739413605623));
#288893=CARTESIAN_POINT('Ctrl Pts',(-1.07499268899777,1.68016225771552,
1.95858055588739));
#288894=CARTESIAN_POINT('Ctrl Pts',(-1.99461842767766,0.00719569871038447,
2.06976697571855));
#288895=CARTESIAN_POINT('Ctrl Pts',(-1.0870871373859,-1.67236238981361,
2.18095339554972));
#288896=CARTESIAN_POINT('Ctrl Pts',(0.816263124967095,-1.81996399811548,
2.29213981538088));
#288897=CARTESIAN_POINT('Ctrl Pts',(1.97188095630794,-0.300399615266935,
2.40332623521204));
#288898=CARTESIAN_POINT('Ctrl Pts',(1.32117028165843,1.49434384148169,2.5145126550432));
#288899=CARTESIAN_POINT('Ctrl Pts',(-0.539789687347405,1.92020351224723,
2.62569907487436));
#288900=CARTESIAN_POINT('Ctrl Pts',(-1.9062788851687,0.587073458207422,
2.73688549470553));
#288901=CARTESIAN_POINT('Ctrl Pts',(-1.52653392208601,-1.28384135217877,
2.84807191453669));
#288902=CARTESIAN_POINT('Ctrl Pts',(0.251582340428331,-1.97870178642002,
2.95925833436786));
#288903=CARTESIAN_POINT('Ctrl Pts',(1.79923826457862,-0.860985540290846,
3.07044475419901));
#288904=CARTESIAN_POINT('Ctrl Pts',(1.69871388039113,1.0454308135088,3.18163117403018));
#288905=CARTESIAN_POINT('Ctrl Pts',(0.0420938849888638,1.9941871873569,
3.29281759386134));
#288906=CARTESIAN_POINT('Ctrl Pts',(-1.65308593527184,1.11618158197113,
3.40400401369251));
#288907=CARTESIAN_POINT('Ctrl Pts',(-1.83396732153388,-0.784294776770008,
3.51519043352367));
#288908=CARTESIAN_POINT('Ctrl Pts',(-0.334855076654795,-1.96632309424865,
3.62637685335483));
#288909=CARTESIAN_POINT('Ctrl Pts',(1.47099894575461,-1.34711415066372,
3.737563273186));
#288910=CARTESIAN_POINT('Ctrl Pts',(1.92935411620901,0.506109797966104,
3.84874969301715));
#288911=CARTESIAN_POINT('Ctrl Pts',(0.620337213347576,1.89571521465329,
3.95993611284832));
#288912=CARTESIAN_POINT('Ctrl Pts',(-1.25693548957618,1.54876325123453,
4.07112253267948));
#288913=CARTESIAN_POINT('Ctrl Pts',(-1.98280075330865,-0.216923041674854,
4.18230895251065));
#288914=CARTESIAN_POINT('Ctrl Pts',(-0.89233450541905,-1.7838984174469,
4.2934953723418));
#288915=CARTESIAN_POINT('Ctrl Pts',(1.01554886236819,-1.71674545040129,
4.40468179217297));
#288916=CARTESIAN_POINT('Ctrl Pts',(1.99314541377542,-0.0769791717082739,
4.51586821200413));
#288917=CARTESIAN_POINT('Ctrl Pts',(1.14493429578145,1.63330336792476,4.6270546318353));
#288918=CARTESIAN_POINT('Ctrl Pts',(-0.752086308841275,1.84740916350018,
4.73824105166646));
#288919=CARTESIAN_POINT('Ctrl Pts',(-1.96016322614266,0.369208017530612,
4.84942747149762));
#288920=CARTESIAN_POINT('Ctrl Pts',(-1.37264558880974,-1.44720369017359,
4.96061389132878));
#288921=CARTESIAN_POINT('Ctrl Pts',(0.472274958565424,-1.93791403236648,
5.07180031115995));
#288922=CARTESIAN_POINT('Ctrl Pts',(1.88457115477419,-0.653411046680418,
5.18298673099111));
#288923=CARTESIAN_POINT('Ctrl Pts',(1.57051841319957,1.22964480527183,5.29417315082227));
#288924=CARTESIAN_POINT('Ctrl Pts',(-0.182197330049385,1.9862926688315,
5.40535957065344));
#288925=CARTESIAN_POINT('Ctrl Pts',(-1.76801241454587,0.923410274657261,
5.51654599048461));
#288926=CARTESIAN_POINT('Ctrl Pts',(-1.7342514240786,-0.985355992224259,
5.62773241031575));
#288927=CARTESIAN_POINT('Ctrl Pts',(-0.111840890598383,-1.99149342166151,
5.73891883014693));
#288928=CARTESIAN_POINT('Ctrl Pts',(1.61302075076181,-1.17333647814372,
5.85010524997808));
#288929=CARTESIAN_POINT('Ctrl Pts',(1.86028540532431,0.71964758324355,5.96129166980924));
#288930=CARTESIAN_POINT('Ctrl Pts',(0.403447922209576,1.9534032372748,6.07247808964042));
#288931=CARTESIAN_POINT('Ctrl Pts',(-1.42296536078566,1.39775677974926,
6.18366450947157));
#288932=CARTESIAN_POINT('Ctrl Pts',(-1.94588063954174,-0.438295528140028,
6.29485092930274));
#288933=CARTESIAN_POINT('Ctrl Pts',(-0.686284832623981,-1.87285011729214,
6.40603734913389));
#288934=CARTESIAN_POINT('Ctrl Pts',(1.20197765467668,-1.59179274749852,
6.51722376896506));
#288935=CARTESIAN_POINT('Ctrl Pts',(1.98917646383827,0.147415837150472,
6.62841018879622));
#288936=CARTESIAN_POINT('Ctrl Pts',(0.954203333929539,1.75158511949853,
6.7395966086274));
#288937=CARTESIAN_POINT('Ctrl Pts',(-0.954861446902296,1.75122644182599,
6.85078302845855));
#288938=CARTESIAN_POINT('Ctrl Pts',(-1.98923171677648,0.146668368441778,
6.96196944828972));
#288939=CARTESIAN_POINT('Ctrl Pts',(-1.20137943349188,-1.59224429347817,
7.07315586812087));
#288940=CARTESIAN_POINT('Ctrl Pts',(0.686988531373428,-1.87259210483547,
7.18434228795204));
#288941=CARTESIAN_POINT('Ctrl Pts',(1.946045197272,-0.437564307851112,7.29552870778319));
#288942=CARTESIAN_POINT('Ctrl Pts',(1.42244003547697,1.39829137836292,7.40671512761436));
#288943=CARTESIAN_POINT('Ctrl Pts',(-0.404181909784372,1.95325149868955,
7.51790154744553));
#288944=CARTESIAN_POINT('Ctrl Pts',(-1.86055569070241,0.718948506587575,
7.62908796727668));
#288945=CARTESIAN_POINT('Ctrl Pts',(-1.61257974081286,-1.17394250832697,
7.74027438710785));
#288946=CARTESIAN_POINT('Ctrl Pts',(0.11258921163228,-1.99145125542828,
7.85146080693901));
#288947=CARTESIAN_POINT('Ctrl Pts',(1.73462156165799,-0.984704255681033,
7.96264722677019));
#288948=CARTESIAN_POINT('Ctrl Pts',(1.76766530660397,0.924074562576307,
8.07383364660135));
#288949=CARTESIAN_POINT('Ctrl Pts',(0.181450942493336,1.98636099154596,
8.18502006643251));
#288950=CARTESIAN_POINT('Ctrl Pts',(-1.57098035693673,1.22905457626289,
8.29620648626366));
#288951=CARTESIAN_POINT('Ctrl Pts',(-1.88432549428448,-0.654119152132637,
8.40739290609483));
#288952=CARTESIAN_POINT('Ctrl Pts',(-0.471546729332007,-1.9380913587599,
8.51857932592599));
#288953=CARTESIAN_POINT('Ctrl Pts',(1.37318929686702,-1.44668779919563,
8.62976574575715));
#288954=CARTESIAN_POINT('Ctrl Pts',(1.96002435351886,0.369944548042224,
8.74095216558831));
#288955=CARTESIAN_POINT('Ctrl Pts',(0.751392067621162,1.84769163834976,
8.85213858541948));
#288956=CARTESIAN_POINT('Ctrl Pts',(-1.14554794811607,1.6328730303577,8.96332500525063));
#288957=CARTESIAN_POINT('Ctrl Pts',(-1.99311634964249,-0.0777281184986929,
9.07451142508181));
#288958=CARTESIAN_POINT('Ctrl Pts',(-1.01490369705703,-1.71712692973843,
9.18569784491295));
#288959=CARTESIAN_POINT('Ctrl Pts',(0.893004755898116,-1.78356299469757,
9.29688426474413));
#288960=CARTESIAN_POINT('Ctrl Pts',(1.98288214203219,-0.216177946285538,
9.40807068457528));
#288961=CARTESIAN_POINT('Ctrl Pts',(1.25635340079693,1.54923541798798,9.51925710440647));
#288962=CARTESIAN_POINT('Ctrl Pts',(-0.621049446553396,1.89548204476102,
9.6304435242376));
#288963=CARTESIAN_POINT('Ctrl Pts',(-1.92954427530524,0.505384662008117,
9.74162994406879));
#288964=CARTESIAN_POINT('Ctrl Pts',(-1.47049242178358,-1.34766657185882,
9.85281636389993));
#288965=CARTESIAN_POINT('Ctrl Pts',(0.335593495757164,-1.96619756766704,
9.96400278373111));
#288966=CARTESIAN_POINT('Ctrl Pts',(1.83426271579115,-0.783604750528571,
10.0751892035622));
#288967=CARTESIAN_POINT('Ctrl Pts',(1.65266484759463,1.11680108276175,10.1863756233934));
#288968=CARTESIAN_POINT('Ctrl Pts',(-0.0428402693722631,1.99417425320353,
10.2975620432246));
#288969=CARTESIAN_POINT('Ctrl Pts',(-1.69911221759054,1.04478666961406,
10.4087484630557));
#288970=CARTESIAN_POINT('Ctrl Pts',(-1.79890390616785,-0.861650606717026,
10.5199348828869));
#288971=CARTESIAN_POINT('Ctrl Pts',(-0.250859180153293,-1.97881704580591,
10.6311213027181));
#288972=CARTESIAN_POINT('Ctrl Pts',(1.52705503210616,-1.2832279275901,10.7423077225492));
#288973=CARTESIAN_POINT('Ctrl Pts',(1.90598428558895,0.587714107537896,
10.8534941423804));
#288974=CARTESIAN_POINT('Ctrl Pts',(0.539208756536806,1.92055018637627,
10.9646805622115));
#288975=CARTESIAN_POINT('Ctrl Pts',(-1.32199971761647,1.49357301567956,
11.0758669820427));
#288976=CARTESIAN_POINT('Ctrl Pts',(-1.97125552307022,-0.300616852401862,
11.1870534018739));
#288977=CARTESIAN_POINT('Ctrl Pts',(-0.816573649480457,-1.82128103083306,
11.2982398217051));
#288978=CARTESIAN_POINT('Ctrl Pts',(1.0899752867738,-1.66989774066344,11.4094381389687));
#288979=CARTESIAN_POINT('Ctrl Pts',(1.68974604725378,-0.554239044059365,
11.4835743162886));
#288980=CARTESIAN_POINT('Ctrl Pts',(1.68731536368905,0.00726171675233516,
11.5206483536649));
#288981=CARTESIAN_POINT('Ctrl Pts',(-0.80306043436893,1.63540410003748,
-0.0762631163239277));
#288982=CARTESIAN_POINT('Ctrl Pts',(-1.34719248374907,1.36821736725733,
-0.0391955685957298));
#288983=CARTESIAN_POINT('Ctrl Pts',(-2.1382824283924,0.252729738796303,
0.0349341190761892));
#288984=CARTESIAN_POINT('Ctrl Pts',(-1.36973709280792,-1.66392564714785,
0.146125946691829));
#288985=CARTESIAN_POINT('Ctrl Pts',(0.65529855462654,-2.05097696019496,
0.257312366522992));
#288986=CARTESIAN_POINT('Ctrl Pts',(2.07913304028677,-0.561891789548798,
0.368498786354154));
#288987=CARTESIAN_POINT('Ctrl Pts',(1.59887198862417,1.44328643797276,0.479685206185317));
#288988=CARTESIAN_POINT('Ctrl Pts',(-0.346277312815728,2.12563070417011,
0.59087162601648));
#288989=CARTESIAN_POINT('Ctrl Pts',(-1.9740891576952,0.861183541544282,
0.702058045847641));
#288990=CARTESIAN_POINT('Ctrl Pts',(-1.79361924233733,-1.19234391090653,
0.813244465678806));
#288991=CARTESIAN_POINT('Ctrl Pts',(0.0299202471797978,-2.15352818653751,
0.924430885509967));
#288992=CARTESIAN_POINT('Ctrl Pts',(1.82603230156248,-1.14204206778157,
1.03561730534113));
#288993=CARTESIAN_POINT('Ctrl Pts',(1.94942962787562,0.915632944554216,
1.14680372517229));
#288994=CARTESIAN_POINT('Ctrl Pts',(0.287059546098653,2.1345333208383,1.25799014500346));
#288995=CARTESIAN_POINT('Ctrl Pts',(-1.63826675221636,1.39811652112659,
1.36917656483462));
#288996=CARTESIAN_POINT('Ctrl Pts',(-2.06287109217876,-0.619039843781474,
1.48036298466578));
#288997=CARTESIAN_POINT('Ctrl Pts',(-0.597795248888325,-2.06912666178656,
1.59154940449694));
#288998=CARTESIAN_POINT('Ctrl Pts',(1.41488657392572,-1.6238048431378,1.70273582432811));
#288999=CARTESIAN_POINT('Ctrl Pts',(2.131471123514,0.308993264057997,1.81392224415927));
#289000=CARTESIAN_POINT('Ctrl Pts',(0.895535541240127,1.95873981810775,
1.92510866399043));
#289001=CARTESIAN_POINT('Ctrl Pts',(-1.16074939018729,1.81419588804578,
2.03629508382159));
#289002=CARTESIAN_POINT('Ctrl Pts',(-2.1537375530821,0.00776972994845119,
2.14748150365276));
#289003=CARTESIAN_POINT('Ctrl Pts',(-1.17380866373853,-1.80577379178097,
2.25866792348392));
#289004=CARTESIAN_POINT('Ctrl Pts',(0.881379877495971,-1.96515020297015,
2.36985434331508));
#289005=CARTESIAN_POINT('Ctrl Pts',(2.12918621771311,-0.32436375968166,
2.48104076314625));
#289006=CARTESIAN_POINT('Ctrl Pts',(1.42656560780741,1.61355395295493,2.59222718297741));
#289007=CARTESIAN_POINT('Ctrl Pts',(-0.582850987574644,2.07338624596089,
2.70341360280857));
#289008=CARTESIAN_POINT('Ctrl Pts',(-2.05835079264534,0.633906784282185,
2.81460002263973));
#289009=CARTESIAN_POINT('Ctrl Pts',(-1.64831197206892,-1.38625879216731,
2.92578644247089));
#289010=CARTESIAN_POINT('Ctrl Pts',(0.271652124914743,-2.13655117421392,
3.03697286230206));
#289011=CARTESIAN_POINT('Ctrl Pts',(1.94277109024656,-0.929669988532152,
3.14815928213322));
#289012=CARTESIAN_POINT('Ctrl Pts',(1.83422745191416,1.12882923919668,3.25934570196439));
#289013=CARTESIAN_POINT('Ctrl Pts',(0.0454518917491524,2.15327191090196,
3.37053212179554));
#289014=CARTESIAN_POINT('Ctrl Pts',(-1.78495957315107,1.20522409489056,
3.48171854162671));
#289015=CARTESIAN_POINT('Ctrl Pts',(-1.98027063056456,-0.84686127931866,
3.59290496145787));
#289016=CARTESIAN_POINT('Ctrl Pts',(-0.361567878559777,-2.12318498155391,
3.70409138128903));
#289017=CARTESIAN_POINT('Ctrl Pts',(1.58834673642544,-1.45457912867615,
3.8152778011202));
#289018=CARTESIAN_POINT('Ctrl Pts',(2.08326683219855,0.546484311353464,
3.92646422095136));
#289019=CARTESIAN_POINT('Ctrl Pts',(0.669824129478524,2.04694441357467,
4.03765064078252));
#289020=CARTESIAN_POINT('Ctrl Pts',(-1.35720653541426,1.67231462856835,
4.14883706061369));
#289021=CARTESIAN_POINT('Ctrl Pts',(-2.14097713298096,-0.234227907704556,
4.26002348044485));
#289022=CARTESIAN_POINT('Ctrl Pts',(-0.963519792840582,-1.92620751880469,
4.37120990027601));
#289023=CARTESIAN_POINT('Ctrl Pts',(1.09656347876959,-1.85369747632234,
4.48239632010718));
#289024=CARTESIAN_POINT('Ctrl Pts',(2.15214703064762,-0.0831201249385476,
4.59358273993833));
#289025=CARTESIAN_POINT('Ctrl Pts',(1.23627053396232,1.76359886696258,4.70476915976951));
#289026=CARTESIAN_POINT('Ctrl Pts',(-0.812083406045863,1.99478478496305,
4.81595557960066));
#289027=CARTESIAN_POINT('Ctrl Pts',(-2.1165337147864,0.39866129843217,4.92714199943183));
#289028=CARTESIAN_POINT('Ctrl Pts',(-1.48214731733634,-1.56265323293681,
5.03832841926298));
#289029=CARTESIAN_POINT('Ctrl Pts',(0.509950324096264,-2.09250960897417,
5.14951483909416));
#289030=CARTESIAN_POINT('Ctrl Pts',(2.03491134503264,-0.70553640200388,
5.2607012589253));
#289031=CARTESIAN_POINT('Ctrl Pts',(1.69580529156801,1.32773875810908,5.37188767875649));
#289032=CARTESIAN_POINT('Ctrl Pts',(-0.196731979587439,2.1447476133342,
5.48307409858763));
#289033=CARTESIAN_POINT('Ctrl Pts',(-1.90905422244406,0.997074607270514,
5.59426051841881));
#289034=CARTESIAN_POINT('Ctrl Pts',(-1.87259997536121,-1.06396199601881,
5.70544693824995));
#289035=CARTESIAN_POINT('Ctrl Pts',(-0.120762910193491,-2.15036325215456,
5.81663335808113));
#289036=CARTESIAN_POINT('Ctrl Pts',(1.74169821987516,-1.26693847821385,
5.92781977791228));
#289037=CARTESIAN_POINT('Ctrl Pts',(2.00868821891031,0.777056906478581,
6.03900619774346));
#289038=CARTESIAN_POINT('Ctrl Pts',(0.435632664733492,2.10923445309248,
6.15019261757461));
#289039=CARTESIAN_POINT('Ctrl Pts',(-1.53648130977477,1.50926173389771,
6.26137903740579));
#289040=CARTESIAN_POINT('Ctrl Pts',(-2.10111174600745,-0.473260211178417,
6.37256545723693));
#289041=CARTESIAN_POINT('Ctrl Pts',(-0.741032668515901,-2.02225527095057,
6.4837518770681));
#289042=CARTESIAN_POINT('Ctrl Pts',(1.29786448220914,-1.71877676925049,
6.59493829689926));
#289043=CARTESIAN_POINT('Ctrl Pts',(2.14786146083268,0.159175820289415,
6.70612471673043));
#289044=CARTESIAN_POINT('Ctrl Pts',(1.03032415876804,1.89131645277941,6.81731113656159));
#289045=CARTESIAN_POINT('Ctrl Pts',(-1.03103477218856,1.89092916187603,
6.92849755639275));
#289046=CARTESIAN_POINT('Ctrl Pts',(-2.14792112153084,0.158368722848993,
7.03968397622391));
#289047=CARTESIAN_POINT('Ctrl Pts',(-1.29721853839713,-1.71926433695757,
7.15087039605508));
#289048=CARTESIAN_POINT('Ctrl Pts',(0.741792504282802,-2.02197667575194,
7.26205681588624));
#289049=CARTESIAN_POINT('Ctrl Pts',(2.10128943120197,-0.472470658362756,
7.37324323571741));
#289050=CARTESIAN_POINT('Ctrl Pts',(1.53591407705037,1.50983897969773,7.48442965554857));
#289051=CARTESIAN_POINT('Ctrl Pts',(-0.436425205593098,2.10907060968025,
7.59561607537972));
#289052=CARTESIAN_POINT('Ctrl Pts',(-2.0089800660931,0.776302061529043,
7.7068024952109));
#289053=CARTESIAN_POINT('Ctrl Pts',(-1.74122202870239,-1.26759285398107,
7.81798891504205));
#289054=CARTESIAN_POINT('Ctrl Pts',(0.121570927952693,-2.15031772214305,
7.92917533487322));
#289055=CARTESIAN_POINT('Ctrl Pts',(1.87299964037655,-1.0632582677025,8.04036175470437));
#289056=CARTESIAN_POINT('Ctrl Pts',(1.90867942423754,0.997791888238837,
8.15154817453555));
#289057=CARTESIAN_POINT('Ctrl Pts',(0.195926049547773,2.14482138643978,
8.2627345943667));
#289058=CARTESIAN_POINT('Ctrl Pts',(-1.69630408650556,1.32710144404251,
8.37392101419787));
#289059=CARTESIAN_POINT('Ctrl Pts',(-2.03464608716948,-0.706300996014821,
8.48510743402903));
#289060=CARTESIAN_POINT('Ctrl Pts',(-0.50916400094522,-2.09270108144195,
8.59629385386019));
#289061=CARTESIAN_POINT('Ctrl Pts',(1.48273439927872,-1.5620961871595,8.70748027369137));
#289062=CARTESIAN_POINT('Ctrl Pts',(2.11638376370763,0.39945658508939,8.8186666935225));
#289063=CARTESIAN_POINT('Ctrl Pts',(0.811333782275305,1.99508979402288,
8.9298531133537));
#289064=CARTESIAN_POINT('Ctrl Pts',(-1.23693313993207,1.76313419955262,
9.04103953318483));
#289065=CARTESIAN_POINT('Ctrl Pts',(-2.1521156479462,-0.0839288183735102,
9.15222595301602));
#289066=CARTESIAN_POINT('Ctrl Pts',(-1.09586684590024,-1.85410938787528,
9.26341237284717));
#289067=CARTESIAN_POINT('Ctrl Pts',(0.964243512027486,-1.92584533796783,
9.37459879267833));
#289068=CARTESIAN_POINT('Ctrl Pts',(2.14106501442627,-0.233423372913213,
9.4857852125095));
#289069=CARTESIAN_POINT('Ctrl Pts',(1.35657801095782,1.67282446205533,9.59697163234066));
#289070=CARTESIAN_POINT('Ctrl Pts',(-0.670593180531384,2.04669264273658,
9.70815805217182));
#289071=CARTESIAN_POINT('Ctrl Pts',(-2.08347216108797,0.545701328241475,
9.81934447200298));
#289072=CARTESIAN_POINT('Ctrl Pts',(-1.58779980490072,-1.4551756188401,
9.93053089183414));
#289073=CARTESIAN_POINT('Ctrl Pts',(0.362365204468606,-2.12304944118742,
10.0417173116654));
#289074=CARTESIAN_POINT('Ctrl Pts',(1.98058958966769,-0.846116206773402,
10.1529037314965));
#289075=CARTESIAN_POINT('Ctrl Pts',(1.78450489353371,1.20589301587231,10.2640901513277));
#289076=CARTESIAN_POINT('Ctrl Pts',(-0.0462578183630766,2.1532579449366,
10.3752765711588));
#289077=CARTESIAN_POINT('Ctrl Pts',(-1.83465756615216,1.12813370922645,
10.48646299099));
#289078=CARTESIAN_POINT('Ctrl Pts',(-1.94241005865504,-0.930388110112408,
10.5976494108212));
#289079=CARTESIAN_POINT('Ctrl Pts',(-0.270871275094269,-2.13667562832719,
10.7088358306523));
#289080=CARTESIAN_POINT('Ctrl Pts',(1.64887465323342,-1.38559643211176,
10.8200222504835));
#289081=CARTESIAN_POINT('Ctrl Pts',(2.05803269161448,0.634598540912015,
10.9312086703146));
#289082=CARTESIAN_POINT('Ctrl Pts',(0.58222371346292,2.07376057574749,11.0423950901458));
#289083=CARTESIAN_POINT('Ctrl Pts',(-1.42746121137041,1.61272163512721,
11.153581509977));
#289084=CARTESIAN_POINT('Ctrl Pts',(-2.12851089102789,-0.324598326739125,
11.2647679298081));
#289085=CARTESIAN_POINT('Ctrl Pts',(-0.881715173859612,-1.96657230094293,
11.3759543496393));
#289086=CARTESIAN_POINT('Ctrl Pts',(1.17692721298547,-1.80311252717206,
11.487152666903));
#289087=CARTESIAN_POINT('Ctrl Pts',(1.82454421690053,-0.59845303041987,
11.5612888442229));
#289088=CARTESIAN_POINT('Ctrl Pts',(1.82191962745507,0.00784101452804033,
11.5983628815991));
#289089=CARTESIAN_POINT('Ctrl Pts',(-0.862390910257602,1.75622851047153,
0.00145141161027357));
#289090=CARTESIAN_POINT('Ctrl Pts',(-1.44672368682384,1.46930189843877,
0.0385189593384715));
#289091=CARTESIAN_POINT('Ctrl Pts',(-2.2962597220448,0.271401528654564,
0.11264864701039));
#289092=CARTESIAN_POINT('Ctrl Pts',(-1.47093390201513,-1.78685724265875,
0.22384047462603));
#289093=CARTESIAN_POINT('Ctrl Pts',(0.703712314576871,-2.20250408552361,
0.335026894457193));
#289094=CARTESIAN_POINT('Ctrl Pts',(2.23274034982012,-0.603404614543201,
0.446213314288355));
#289095=CARTESIAN_POINT('Ctrl Pts',(1.71699738978991,1.54991710677901,0.557399734119519));
#289096=CARTESIAN_POINT('Ctrl Pts',(-0.371860440659578,2.28267328259214,
0.668586153950681));
#289097=CARTESIAN_POINT('Ctrl Pts',(-2.11993577665456,0.924808179442785,
0.779772573781843));
#289098=CARTESIAN_POINT('Ctrl Pts',(-1.92613266057665,-1.2804348298828,
0.890958993613007));
#289099=CARTESIAN_POINT('Ctrl Pts',(0.0321307688639665,-2.31263184384491,
1.00214541344416));
#289100=CARTESIAN_POINT('Ctrl Pts',(1.9609404115915,-1.22641666334938,1.11333183327534));
#289101=CARTESIAN_POINT('Ctrl Pts',(2.09345438937972,0.983280329501573,
1.2245182531065));
#289102=CARTESIAN_POINT('Ctrl Pts',(0.308267637980082,2.29223362869261,
1.33570467293766));
#289103=CARTESIAN_POINT('Ctrl Pts',(-1.75930265671585,1.50141001560869,
1.44689109276882));
#289104=CARTESIAN_POINT('Ctrl Pts',(-2.21527696147322,-0.66477479342379,
1.55807751259999));
#289105=CARTESIAN_POINT('Ctrl Pts',(-0.6419606380454,-2.22199469545358,
1.66926393243115));
#289106=CARTESIAN_POINT('Ctrl Pts',(1.51941904765603,-1.74377229511349,
1.78045035226231));
#289107=CARTESIAN_POINT('Ctrl Pts',(2.2889451948153,0.331821829155158,1.89163677209348));
#289108=CARTESIAN_POINT('Ctrl Pts',(0.961698120746081,2.10345242076731,
2.00282319192464));
#289109=CARTESIAN_POINT('Ctrl Pts',(-1.24650609137681,1.94822951837603,
2.1140096117558));
#289110=CARTESIAN_POINT('Ctrl Pts',(-2.31285667848653,0.00834376118651563,
2.22519603158696));
#289111=CARTESIAN_POINT('Ctrl Pts',(-1.26053019009116,-1.93918519374832,
2.33638245141813));
#289112=CARTESIAN_POINT('Ctrl Pts',(0.946496630024849,-2.11033640782483,
2.44756887124929));
#289113=CARTESIAN_POINT('Ctrl Pts',(2.28649147911827,-0.348327904096385,
2.55875529108045));
#289114=CARTESIAN_POINT('Ctrl Pts',(1.53196093395638,1.73276406442818,2.66994171091161));
#289115=CARTESIAN_POINT('Ctrl Pts',(-0.625912287801888,2.22656897967456,
2.78112813074278));
#289116=CARTESIAN_POINT('Ctrl Pts',(-2.21042270012197,0.680740110356948,
2.89231455057394));
#289117=CARTESIAN_POINT('Ctrl Pts',(-1.77009002205183,-1.48867623215584,
3.0035009704051));
#289118=CARTESIAN_POINT('Ctrl Pts',(0.291721909401159,-2.29440056200783,
3.11468739023627));
#289119=CARTESIAN_POINT('Ctrl Pts',(2.0863039159145,-0.998354436773457,
3.22587381006743));
#289120=CARTESIAN_POINT('Ctrl Pts',(1.96974102343718,1.21222766488455,3.33706022989859));
#289121=CARTESIAN_POINT('Ctrl Pts',(0.0488098985094419,2.31235663444701,
3.44824664972975));
#289122=CARTESIAN_POINT('Ctrl Pts',(-1.9168332110303,1.29426660780999,3.55943306956092));
#289123=CARTESIAN_POINT('Ctrl Pts',(-2.12657393959523,-0.909427781867309,
3.67061948939208));
#289124=CARTESIAN_POINT('Ctrl Pts',(-0.38828068046476,-2.28004686885918,
3.78180590922325));
#289125=CARTESIAN_POINT('Ctrl Pts',(1.70569452709628,-1.56204410668859,
3.8929923290544));
#289126=CARTESIAN_POINT('Ctrl Pts',(2.23717954818808,0.586858824740825,
4.00417874888557));
#289127=CARTESIAN_POINT('Ctrl Pts',(0.719311045609473,2.19817361249604,
4.11536516871672));
#289128=CARTESIAN_POINT('Ctrl Pts',(-1.45747758125233,1.79586600590217,
4.2265515885479));
#289129=CARTESIAN_POINT('Ctrl Pts',(-2.29915351265328,-0.251532773734257,
4.33773800837905));
#289130=CARTESIAN_POINT('Ctrl Pts',(-1.03470508026212,-2.06851662016248,
4.44892442821022));
#289131=CARTESIAN_POINT('Ctrl Pts',(1.17757809517098,-1.9906495022434,4.56011084804138));
#289132=CARTESIAN_POINT('Ctrl Pts',(2.3111486475198,-0.0892610781688252,
4.67129726787255));
#289133=CARTESIAN_POINT('Ctrl Pts',(1.32760677214319,1.89389436600039,4.7824836877037));
#289134=CARTESIAN_POINT('Ctrl Pts',(-0.872080503250453,2.14216040642593,
4.89367010753487));
#289135=CARTESIAN_POINT('Ctrl Pts',(-2.27290420343013,0.428114579333728,
5.00485652736603));
#289136=CARTESIAN_POINT('Ctrl Pts',(-1.59164904586292,-1.67810277570002,
5.11604294719719));
#289137=CARTESIAN_POINT('Ctrl Pts',(0.547625689627108,-2.24710518558187,
5.22722936702836));
#289138=CARTESIAN_POINT('Ctrl Pts',(2.1852515352911,-0.757661757327341,
5.33841578685952));
#289139=CARTESIAN_POINT('Ctrl Pts',(1.82109216993646,1.42583271094635,5.44960220669068));
#289140=CARTESIAN_POINT('Ctrl Pts',(-0.211266629125497,2.3032025578369,
5.56078862652184));
#289141=CARTESIAN_POINT('Ctrl Pts',(-2.05009603034226,1.07073893988376,
5.67197504635302));
#289142=CARTESIAN_POINT('Ctrl Pts',(-2.01094852664382,-1.14256799981336,
5.78316146618415));
#289143=CARTESIAN_POINT('Ctrl Pts',(-0.129684929788602,-2.30923308264762,
5.89434788601535));
#289144=CARTESIAN_POINT('Ctrl Pts',(1.87037568898851,-1.36054047828399,
6.00553430584648));
#289145=CARTESIAN_POINT('Ctrl Pts',(2.15709103249631,0.834466229713613,
6.11672072567766));
#289146=CARTESIAN_POINT('Ctrl Pts',(0.467817407257409,2.26506566891016,
6.22790714550882));
#289147=CARTESIAN_POINT('Ctrl Pts',(-1.64999725876389,1.62076668804616,
6.33909356533998));
#289148=CARTESIAN_POINT('Ctrl Pts',(-2.25634285247318,-0.508224894216808,
6.45027998517114));
#289149=CARTESIAN_POINT('Ctrl Pts',(-0.795780504407822,-2.17166042460899,
6.5614664050023));
#289150=CARTESIAN_POINT('Ctrl Pts',(1.3937513097416,-1.84576079100247,6.67265282483347));
#289151=CARTESIAN_POINT('Ctrl Pts',(2.3065464578271,0.170935803428354,6.78383924466464));
#289152=CARTESIAN_POINT('Ctrl Pts',(1.10644498360655,2.03104778606029,6.89502566449579));
#289153=CARTESIAN_POINT('Ctrl Pts',(-1.10720809747483,2.03063188192607,
7.00621208432696));
#289154=CARTESIAN_POINT('Ctrl Pts',(-2.30661052628519,0.170069077256207,
7.11739850415812));
#289155=CARTESIAN_POINT('Ctrl Pts',(-1.39305764330237,-1.84628438043696,
7.22858492398928));
#289156=CARTESIAN_POINT('Ctrl Pts',(0.796596477192177,-2.1713612466684,
7.33977134382045));
#289157=CARTESIAN_POINT('Ctrl Pts',(2.25653366513194,-0.507377008874402,
7.4509577636516));
#289158=CARTESIAN_POINT('Ctrl Pts',(1.64938811862379,1.62138658103253,7.56214418348278));
#289159=CARTESIAN_POINT('Ctrl Pts',(-0.468668501401827,2.26488972067095,
7.67333060331392));
#289160=CARTESIAN_POINT('Ctrl Pts',(-2.15740444148378,0.833655616470511,
7.7845170231451));
#289161=CARTESIAN_POINT('Ctrl Pts',(-1.86986431659192,-1.36124319963517,
7.89570344297626));
#289162=CARTESIAN_POINT('Ctrl Pts',(0.130552644273102,-2.30918418885782,
8.00688986280742));
#289163=CARTESIAN_POINT('Ctrl Pts',(2.01137771909512,-1.14181227972396,
8.11807628263858));
#289164=CARTESIAN_POINT('Ctrl Pts',(2.0496935418711,1.07150921390136,8.22926270246975));
#289165=CARTESIAN_POINT('Ctrl Pts',(0.210401156602211,2.30328178133359,
8.34044912230091));
#289166=CARTESIAN_POINT('Ctrl Pts',(-1.82162781607441,1.42514831182212,
8.45163554213207));
#289167=CARTESIAN_POINT('Ctrl Pts',(-2.18496668005448,-0.758482839897003,
8.56282196196324));
#289168=CARTESIAN_POINT('Ctrl Pts',(-0.546781272558432,-2.24731080412402,
8.6740083817944));
#289169=CARTESIAN_POINT('Ctrl Pts',(1.5922795016904,-1.67750457512337,8.78519480162556));
#289170=CARTESIAN_POINT('Ctrl Pts',(2.2727431738964,0.428968622136553,8.89638122145672));
#289171=CARTESIAN_POINT('Ctrl Pts',(0.871275496929446,2.14248794969599,
9.00756764128788));
#289172=CARTESIAN_POINT('Ctrl Pts',(-1.32831833174806,1.89339536874755,
9.11875406111905));
#289173=CARTESIAN_POINT('Ctrl Pts',(-2.31111494624991,-0.0901295182483251,
9.22994048095021));
#289174=CARTESIAN_POINT('Ctrl Pts',(-1.17682999474345,-1.99109184601215,
9.34112690078138));
#289175=CARTESIAN_POINT('Ctrl Pts',(1.03548226815685,-2.06812768123808,
9.45231332061253));
#289176=CARTESIAN_POINT('Ctrl Pts',(2.29924788682036,-0.250668799540886,
9.5634997404437));
#289177=CARTESIAN_POINT('Ctrl Pts',(1.45680262111872,1.79641350612268,9.67468616027486));
#289178=CARTESIAN_POINT('Ctrl Pts',(-0.720136914509369,2.19790324071213,
9.78587258010602));
#289179=CARTESIAN_POINT('Ctrl Pts',(-2.23740004687071,0.586017994474835,
9.8970589999372));
#289180=CARTESIAN_POINT('Ctrl Pts',(-1.70510718801785,-1.5626846658214,
10.0082454197683));
#289181=CARTESIAN_POINT('Ctrl Pts',(0.389136913180049,-2.2799013147078,
10.1194318395995));
#289182=CARTESIAN_POINT('Ctrl Pts',(2.12691646354425,-0.908627663018235,
10.2306182594307));
#289183=CARTESIAN_POINT('Ctrl Pts',(1.91634493947277,1.29498494898287,10.3418046792618));
#289184=CARTESIAN_POINT('Ctrl Pts',(-0.0496753673538915,2.31234163666967,
10.452991099093));
#289185=CARTESIAN_POINT('Ctrl Pts',(-1.97020291471376,1.21148074883883,
10.5641775189242));
#289186=CARTESIAN_POINT('Ctrl Pts',(-2.08591621114224,-0.999125613507789,
10.6753639387553));
#289187=CARTESIAN_POINT('Ctrl Pts',(-0.290883370035243,-2.29453421084847,
10.7865503585865));
#289188=CARTESIAN_POINT('Ctrl Pts',(1.77069427436068,-1.48796493663344,
10.8977367784176));
#289189=CARTESIAN_POINT('Ctrl Pts',(2.21008109764,0.681482974286134,11.0089231982488));
#289190=CARTESIAN_POINT('Ctrl Pts',(0.625238670389037,2.22697096511872,
11.12010961808));
#289191=CARTESIAN_POINT('Ctrl Pts',(-1.53292270512435,1.73187025457486,
11.2312960379111));
#289192=CARTESIAN_POINT('Ctrl Pts',(-2.28576625898556,-0.348579801076388,
11.3424824577423));
#289193=CARTESIAN_POINT('Ctrl Pts',(-0.946856698238769,-2.11186357105279,
11.4536688775734));
#289194=CARTESIAN_POINT('Ctrl Pts',(1.26387913919714,-1.93632731368067,
11.5648671948371));
#289195=CARTESIAN_POINT('Ctrl Pts',(1.95934238654728,-0.642667016780374,
11.6390033721571));
#289196=CARTESIAN_POINT('Ctrl Pts',(1.95652389122108,0.0084203123037455,
11.6760774095333));
#289197=CARTESIAN_POINT('Ctrl Pts',(-0.905549614304899,-1.2679201530598,
4.74121610027911E-15));
#289198=CARTESIAN_POINT('Ctrl Pts',(-0.937460871048186,-1.25085822491965,
5.35356706249551E-15));
#289199=CARTESIAN_POINT('Ctrl Pts',(-0.968677330061126,-1.23263760516135,
2.06292740774959E-15));
#289200=CARTESIAN_POINT('Ctrl Pts',(-0.999128467894991,-1.21327242330634,
3.11035919242642E-15));
#289201=CARTESIAN_POINT('Ctrl Pts',(-1.04946899074794,-1.18125873025347,
4.97913816412496E-15));
#289202=CARTESIAN_POINT('Ctrl Pts',(-1.09771925513438,-1.14612002703508,
1.15989844385816E-15));
#289203=CARTESIAN_POINT('Ctrl Pts',(-1.14379931197614,-1.10818274058947,
1.43288159115684E-15));
#289204=CARTESIAN_POINT('Ctrl Pts',(-1.16971380115341,-1.08684758029691,
1.58640177539923E-15));
#289205=CARTESIAN_POINT('Ctrl Pts',(-1.19494165042771,-1.06462634929242,
8.09273529658737E-16));
#289206=CARTESIAN_POINT('Ctrl Pts',(-1.21946596262296,-1.04157045589269,
3.88231113923609E-15));
#289207=CARTESIAN_POINT('Ctrl Pts',(-1.23288807387334,-1.02895200756582,
5.583948728977E-15));
#289208=CARTESIAN_POINT('Ctrl Pts',(-1.24610308792281,-1.01607950194371,
4.60197854996867E-15));
#289209=CARTESIAN_POINT('Ctrl Pts',(-1.25908578368524,-1.0029839550804,
4.413136522885E-15));
#289210=CARTESIAN_POINT('Ctrl Pts',(-1.30295565515111,-0.958732748075211,
3.84808658795903E-15));
#289211=CARTESIAN_POINT('Ctrl Pts',(-1.34421879940214,-0.911899879065187,
3.37019496524957E-15));
#289212=CARTESIAN_POINT('Ctrl Pts',(-1.38278669882382,-0.862834134377072,
3.37924133120282E-15));
#289213=CARTESIAN_POINT('Ctrl Pts',(-1.41244324646807,-0.825105333564397,
3.38619747833354E-15));
#289214=CARTESIAN_POINT('Ctrl Pts',(-1.4405058985096,-0.786055062173812,
3.2670621097051E-15));
#289215=CARTESIAN_POINT('Ctrl Pts',(-1.46692433972057,-0.745823635123971,
2.87270207621759E-15));
#289216=CARTESIAN_POINT('Ctrl Pts',(-1.479951210132,-0.725985614308893,
2.71914094754812E-15));
#289217=CARTESIAN_POINT('Ctrl Pts',(-1.49257814628919,-0.705860181165346,
1.35885657295169E-15));
#289218=CARTESIAN_POINT('Ctrl Pts',(-1.50479813274716,-0.685463000140715,
2.90739654573713E-15));
#289219=CARTESIAN_POINT('Ctrl Pts',(-1.51107691151866,-0.674982678607109,
3.93652404230936E-15));
#289220=CARTESIAN_POINT('Ctrl Pts',(-1.51724344631134,-0.664438579506566,
8.43130975647999E-16));
#289221=CARTESIAN_POINT('Ctrl Pts',(-1.52329612440981,-0.653835068968427,
8.39606162372775E-16));
#289222=CARTESIAN_POINT('Ctrl Pts',(-1.55557337502278,-0.597289493365581,
9.14793561799881E-16));
#289223=CARTESIAN_POINT('Ctrl Pts',(-1.58462509497716,-0.539041271463454,
4.04685630789369E-15));
#289224=CARTESIAN_POINT('Ctrl Pts',(-1.61035605010574,-0.479448801937299,
2.52575738102223E-15));
#289225=CARTESIAN_POINT('Ctrl Pts',(-1.63646674525678,-0.418976860755161,
9.82209923274866E-16));
#289226=CARTESIAN_POINT('Ctrl Pts',(-1.65915866890572,-0.357119868309094,
2.21604429794495E-15));
#289227=CARTESIAN_POINT('Ctrl Pts',(-1.67829774581707,-0.294211317115571,
2.22044604925031E-15));
#289228=CARTESIAN_POINT('Ctrl Pts',(-1.69743682272842,-0.231302765922048,
2.22484780055568E-15));
#289229=CARTESIAN_POINT('Ctrl Pts',(-1.71302373935576,-0.167341670456775,
-3.16069756809386E-16));
#289230=CARTESIAN_POINT('Ctrl Pts',(-1.72487954070067,-0.102634681883507,
1.38777878078145E-16));
#289231=CARTESIAN_POINT('Ctrl Pts',(-1.72700542719079,-0.0910319475914678,
1.76532081056099E-16));
#289232=CARTESIAN_POINT('Ctrl Pts',(-1.7290114810898,-0.0794035343790092,
1.48190968167817E-15));
#289233=CARTESIAN_POINT('Ctrl Pts',(-1.73089565945358,-0.0677563287869379,
1.1518563880486E-15));
#289234=CARTESIAN_POINT('Ctrl Pts',(-1.74172479314054,-0.000815136349513676,
-1.09817221617784E-15));
#289235=CARTESIAN_POINT('Ctrl Pts',(-1.74848828324155,0.0664709664375185,
-1.01621691135569E-15));
#289236=CARTESIAN_POINT('Ctrl Pts',(-1.75106678679188,0.133744024403217,
1.40165656858926E-15));
#289237=CARTESIAN_POINT('Ctrl Pts',(-1.75197767455369,0.157509050901846,
1.84139826595573E-15));
#289238=CARTESIAN_POINT('Ctrl Pts',(-1.75236592486443,0.181272742264378,
1.30313374020808E-15));
#289239=CARTESIAN_POINT('Ctrl Pts',(-1.75222496230419,0.20502014676713,
1.36002320516582E-15));
#289240=CARTESIAN_POINT('Ctrl Pts',(-1.75183827977442,0.270163021817557,
1.65088958438666E-15));
#289241=CARTESIAN_POINT('Ctrl Pts',(-1.74747328053466,0.335182661606698,
-5.45003011681782E-16));
#289242=CARTESIAN_POINT('Ctrl Pts',(-1.73934992124973,0.399840282146608,
4.44089209850063E-16));
#289243=CARTESIAN_POINT('Ctrl Pts',(-1.73503446184581,0.43418904437749,
9.69535294288643E-16));
#289244=CARTESIAN_POINT('Ctrl Pts',(-1.72965742919137,0.468435827184092,
-8.92233996393924E-16));
#289245=CARTESIAN_POINT('Ctrl Pts',(-1.72324590502526,0.502545438383203,
-1.19348975147204E-15));
#289246=CARTESIAN_POINT('Ctrl Pts',(-1.71875224847293,0.526451903350239,
-1.42038410822672E-15));
#289247=CARTESIAN_POINT('Ctrl Pts',(-1.71375034317529,0.550290993458765,
7.97551584050136E-16));
#289248=CARTESIAN_POINT('Ctrl Pts',(-1.70824837476028,0.574050543226345,
-1.0547118733939E-15));
#289249=CARTESIAN_POINT('Ctrl Pts',(-1.70556019910987,0.585659087356795,
-1.90745213862594E-15));
#289250=CARTESIAN_POINT('Ctrl Pts',(-1.70275214211861,0.597250589985585,
1.78912282367783E-15));
#289251=CARTESIAN_POINT('Ctrl Pts',(-1.69982665236451,0.608817432227435,
1.52655665885959E-15));
#289252=CARTESIAN_POINT('Ctrl Pts',(-1.68329918195351,0.674163975531249,
9.89167680777905E-17));
#289253=CARTESIAN_POINT('Ctrl Pts',(-1.66308692883257,0.738494974736257,
-2.34765560940025E-15));
#289254=CARTESIAN_POINT('Ctrl Pts',(-1.63944765697508,0.801558514632328,
-1.83186799063151E-15));
#289255=CARTESIAN_POINT('Ctrl Pts',(-1.61503541916896,0.866684130265462,
-1.29921495111579E-15));
#289256=CARTESIAN_POINT('Ctrl Pts',(-1.58696831921506,0.930458915358801,
-9.17800768984529E-16));
#289257=CARTESIAN_POINT('Ctrl Pts',(-1.5554737368783,0.992609975972325,
2.77555756156289E-17));
#289258=CARTESIAN_POINT('Ctrl Pts',(-1.52397915454153,1.05476103658585,
9.73311920215787E-16));
#289259=CARTESIAN_POINT('Ctrl Pts',(-1.48905670384034,1.11528933690167,
-4.42442216625048E-16));
#289260=CARTESIAN_POINT('Ctrl Pts',(-1.45088203376166,1.17391247934434,
-9.99200722162641E-16));
#289261=CARTESIAN_POINT('Ctrl Pts',(-1.43586030613212,1.19698067814596,
-1.43460498315299E-15));
#289262=CARTESIAN_POINT('Ctrl Pts',(-1.42033446520901,1.21975369583959,
5.24609266153E-16));
#289263=CARTESIAN_POINT('Ctrl Pts',(-1.40431321996707,1.24221341255695,
-1.19348975147204E-15));
#289264=CARTESIAN_POINT('Ctrl Pts',(-1.39827097600966,1.25068385824148,
-1.7740599430818E-15));
#289265=CARTESIAN_POINT('Ctrl Pts',(-1.39215941512485,1.25910802930607,
4.60573495314624E-17));
#289266=CARTESIAN_POINT('Ctrl Pts',(-1.38598454691313,1.26747777400967,
1.66533453693773E-16));
#289267=CARTESIAN_POINT('Ctrl Pts',(-1.34312430180715,1.32557282918673,
5.82247531511251E-16));
#289268=CARTESIAN_POINT('Ctrl Pts',(-1.29714727100502,1.3811465117294,2.77899044665911E-15));
#289269=CARTESIAN_POINT('Ctrl Pts',(-1.24829449347749,1.43391808714855,
1.63757896132211E-15));
#289270=CARTESIAN_POINT('Ctrl Pts',(-1.19933005103827,1.48681028484563,
7.27406218455119E-16));
#289271=CARTESIAN_POINT('Ctrl Pts',(-1.14747626837413,1.53688856047857,
1.20355823038891E-15));
#289272=CARTESIAN_POINT('Ctrl Pts',(-1.09292624807967,1.58385401469232,
4.44089209850063E-16));
#289273=CARTESIAN_POINT('Ctrl Pts',(-1.03954323644595,1.6298147196589,-3.4956008221888E-17));
#289274=CARTESIAN_POINT('Ctrl Pts',(-0.983577546990472,1.67279522225456,
-1.08379257054093E-15));
#289275=CARTESIAN_POINT('Ctrl Pts',(-0.925170399959829,1.71248623000829,
-9.71445146547012E-16));
#289276=CARTESIAN_POINT('Ctrl Pts',(-0.904266808866141,1.72669141958458,
-5.96153040997855E-16));
#289277=CARTESIAN_POINT('Ctrl Pts',(-0.883050159679862,1.74047492563423,
-1.22518073453117E-15));
#289278=CARTESIAN_POINT('Ctrl Pts',(-0.861525859670579,1.75382131162752,
2.22044604925031E-16));
#289279=CARTESIAN_POINT('Origin',(-0.866025403784439,-1.5,-4.));
#289280=CARTESIAN_POINT('',(-0.866025403784439,-1.5,-4.));
#289281=CARTESIAN_POINT('',(0.866025403784439,-1.5,-4.));
#289282=CARTESIAN_POINT('',(-0.43301270189222,-1.5,-4.));
#289283=CARTESIAN_POINT('',(-0.866025403784439,-1.5,-2.));
#289284=CARTESIAN_POINT('',(-0.866025403784439,-1.5,-4.));
#289285=CARTESIAN_POINT('',(0.866025403784439,-1.5,-2.));
#289286=CARTESIAN_POINT('',(-0.866025403784439,-1.5,-2.));
#289287=CARTESIAN_POINT('',(0.866025403784439,-1.5,-4.));
#289288=CARTESIAN_POINT('Origin',(-1.73205080756888,2.12115047744981E-16,
-4.));
#289289=CARTESIAN_POINT('',(-1.73205080756888,2.12115047744981E-16,-4.));
#289290=CARTESIAN_POINT('',(-1.51554445662277,-0.375,-4.));
#289291=CARTESIAN_POINT('',(-1.73205080756888,2.77555756156289E-16,-2.));
#289292=CARTESIAN_POINT('',(-1.73205080756888,2.12115047744981E-16,-4.));
#289293=CARTESIAN_POINT('',(-1.73205080756888,2.12115047744981E-16,-2.));
#289294=CARTESIAN_POINT('Origin',(-0.866025403784438,1.5,-4.));
#289295=CARTESIAN_POINT('',(-0.866025403784438,1.5,-4.));
#289296=CARTESIAN_POINT('',(-1.08253175473055,1.125,-4.));
#289297=CARTESIAN_POINT('',(-0.866025403784438,1.5,-2.));
#289298=CARTESIAN_POINT('',(-0.866025403784438,1.5,-4.));
#289299=CARTESIAN_POINT('',(-0.866025403784438,1.5,-2.));
#289300=CARTESIAN_POINT('Origin',(0.866025403784439,1.5,-4.));
#289301=CARTESIAN_POINT('',(0.866025403784439,1.5,-4.));
#289302=CARTESIAN_POINT('',(0.43301270189222,1.5,-4.));
#289303=CARTESIAN_POINT('',(0.866025403784439,1.5,-2.));
#289304=CARTESIAN_POINT('',(0.866025403784439,1.5,-4.));
#289305=CARTESIAN_POINT('',(0.866025403784439,1.5,-2.));
#289306=CARTESIAN_POINT('Origin',(1.73205080756888,0.,-4.));
#289307=CARTESIAN_POINT('',(1.73205080756888,0.,-4.));
#289308=CARTESIAN_POINT('',(1.51554445662277,0.375,-4.));
#289309=CARTESIAN_POINT('',(1.73205080756888,0.,-2.));
#289310=CARTESIAN_POINT('',(1.73205080756888,0.,-4.));
#289311=CARTESIAN_POINT('',(1.73205080756888,0.,-2.));
#289312=CARTESIAN_POINT('Origin',(0.866025403784439,-1.5,-4.));
#289313=CARTESIAN_POINT('',(1.08253175473055,-1.125,-4.));
#289314=CARTESIAN_POINT('',(0.866025403784439,-1.5,-2.));
#289315=CARTESIAN_POINT('Origin',(0.,2.77555756156289E-16,-2.));
#289316=CARTESIAN_POINT('Origin',(0.,0.,0.));
#289317=CARTESIAN_POINT('',(-3.5,-4.28626379701574E-16,0.));
#289318=CARTESIAN_POINT('Origin',(0.,0.,0.));
#289319=CARTESIAN_POINT('Origin',(0.,0.,-4.));
#289320=CARTESIAN_POINT('',(-3.5,-4.28626379701574E-16,-4.));
#289321=CARTESIAN_POINT('',(-3.5,-4.28626379701574E-16,-4.));
#289322=CARTESIAN_POINT('Origin',(0.,0.,-4.));
#289323=CARTESIAN_POINT('Origin',(0.,0.,-4.));
#289324=CARTESIAN_POINT('Origin',(0.,0.,12.));
#289367=UNCERTAINTY_MEASURE_WITH_UNIT(LENGTH_MEASURE(0.01),#289388,
'DISTANCE_ACCURACY_VALUE',
'Maximum model space distance between geometric entities at asserted c
onnectivities');
#289368=UNCERTAINTY_MEASURE_WITH_UNIT(LENGTH_MEASURE(0.01),#289388,
'DISTANCE_ACCURACY_VALUE',
'Maximum model space distance between geometric entities at asserted c
onnectivities');
#289386=(
GEOMETRIC_REPRESENTATION_CONTEXT(3)
GLOBAL_UNCERTAINTY_ASSIGNED_CONTEXT((#289367))
GLOBAL_UNIT_ASSIGNED_CONTEXT((#289388,#289390,#289391))
REPRESENTATION_CONTEXT('','3D')
);
#289387=(
GEOMETRIC_REPRESENTATION_CONTEXT(3)
GLOBAL_UNCERTAINTY_ASSIGNED_CONTEXT((#289368))
GLOBAL_UNIT_ASSIGNED_CONTEXT((#289388,#289390,#289391))
REPRESENTATION_CONTEXT('','3D')
);
#289388=(
LENGTH_UNIT()
NAMED_UNIT(*)
SI_UNIT(.MILLI.,.METRE.)
);
#289390=(
NAMED_UNIT(*)
PLANE_ANGLE_UNIT()
SI_UNIT($,.RADIAN.)
);
#289391=(
NAMED_UNIT(*)
SI_UNIT($,.STERADIAN.)
SOLID_ANGLE_UNIT()
);
#289409=SHAPE_DEFINITION_REPRESENTATION(#289427,#289470);
#289427=PRODUCT_DEFINITION_SHAPE('',$,#289489);
#289470=SHAPE_REPRESENTATION('',(#17842),#289386);
#289471=PRODUCT_DEFINITION_CONTEXT('part definition',#289527,'design');
#289489=PRODUCT_DEFINITION('Socket head cap screw M4x12',
'Socket head cap screw M4x12',#289507,#289471);
#289507=PRODUCT_DEFINITION_FORMATION('',$,#289546);
#289527=APPLICATION_CONTEXT(
'Core Data for Automotive Mechanical Design Process');
#289528=PRODUCT_CONTEXT('part definition',#289527,'mechanical');
#289546=PRODUCT('Socket head cap screw M4x12',
'Socket head cap screw M4x12',$,(#289528));
#289553=PRESENTATION_STYLE_ASSIGNMENT((#289560));
#289560=SURFACE_STYLE_USAGE(.BOTH.,#289567);
#289567=SURFACE_SIDE_STYLE('',(#289574));
#289574=SURFACE_STYLE_FILL_AREA(#289581);
#289581=FILL_AREA_STYLE('Opaque(64,72,82)',(#289588));
#289588=FILL_AREA_STYLE_COLOUR('Opaque(64,72,82)',#289595);
#289595=COLOUR_RGB('Opaque(64,72,82)',0.250980392156863,0.282352941176471,
0.32156862745098);
ENDSEC;
END-ISO-10303-21;
